ISO-10303-21;
HEADER;
FILE_DESCRIPTION (('STEP AP214'),
    '1' );
FILE_NAME ('straight bevel gear(wobble in)_iso_ISO - Straight bevel gear 2M 49GT 48PT 20PA 5FW ---49O1H50MD20.0S1.step',
    '2026-10-08T08:02:49',
    ( '' ),
    ( '' ),
    'SwSTEP 2.0',
    'SolidWorks 2026',
    '' );
FILE_SCHEMA (( 'AUTOMOTIVE_DESIGN' ));
ENDSEC;

DATA;
#1=CARTESIAN_POINT ( 'NONE',  ( 0.6000166863083090663, -45.71468846346234471, -17.94410043432203139 ) ) ;
#8=CARTESIAN_POINT ( 'NONE',  ( -6.077587904424778920, 5.472951620448720078, -18.46192898789718129 ) ) ;
#17=CARTESIAN_POINT ( 'NONE',  ( 0.1152809850208375564, -22.68421566702489756, -37.84668601161344981 ) ) ;
#21=ORIENTED_EDGE ( 'NONE', *, *, #24258, .F. ) ;
#34=DIRECTION ( 'NONE',  ( 0.09722883295013594329, -0.9880289017988295175, -0.1197724645039638103 ) ) ;
#39=CARTESIAN_POINT ( 'NONE',  ( 0.5987334308729315158, 46.79309025446952575, 14.89864460301000015 ) ) ;
#46=FACE_OUTER_BOUND ( 'NONE', #12216, .T. ) ;
#47=EDGE_CURVE ( 'NONE', #13219, #36056, #34301, .T. ) ;
#54=CARTESIAN_POINT ( 'NONE',  ( 0.5997462898726536595, 5.235280152387709940, -48.82769165002913070 ) ) ;
#56=EDGE_CURVE ( 'NONE', #14922, #2416, #61883, .T. ) ;
#58=CARTESIAN_POINT ( 'NONE',  ( -6.078726893082806448, 15.42998809551244577, -11.51996131248123234 ) ) ;
#75=CARTESIAN_POINT ( 'NONE',  ( 0.2285344041767094769, -7.790448184841448409, -43.42591492847049750 ) ) ;
#76=( BOUNDED_SURFACE ( )  B_SPLINE_SURFACE ( 3, 1, ( 
 ( #47518, #33740 ),
 ( #24014, #29022 ),
 ( #42835, #9289 ),
 ( #58121, #38143 ) ),
 .UNSPECIFIED., .F., .F., .F. ) 
 B_SPLINE_SURFACE_WITH_KNOTS ( ( 4, 4 ),
 ( 2, 2 ),
 ( 0.000000000000000000, 1.000000000000000000 ),
 ( 0.000000000000000000, 1.000000000000000000 ),
 .UNSPECIFIED. ) 
 GEOMETRIC_REPRESENTATION_ITEM ( )  RATIONAL_B_SPLINE_SURFACE ( (
 ( 1.000000000000000000, 1.000000000000000000),
 ( 0.7211978278499970862, 0.9934217856018976445),
 ( 0.7211978278499970862, 0.9934217856018976445),
 ( 1.000000000000000000, 1.000000000000000000) ) ) 
 REPRESENTATION_ITEM ( '' )  SURFACE ( )  );
#83=CARTESIAN_POINT ( 'NONE',  ( 0.7044674535452954967, 36.84332507061608908, 32.47109669462702897 ) ) ;
#87=DIRECTION ( 'NONE',  ( 0.09722883295013592941, 0.4536333312076272772, -0.8858687006891176052 ) ) ;
#91=ORIENTED_EDGE ( 'NONE', *, *, #56070, .F. ) ;
#92=CARTESIAN_POINT ( 'NONE',  ( 0.8744876279028306332, 41.62483489565916983, 26.03311679935014666 ) ) ;
#93=CARTESIAN_POINT ( 'NONE',  ( -6.078075953587585900, 9.986729131371458124, -16.46391252114006321 ) ) ;
#94=CARTESIAN_POINT ( 'NONE',  ( 0.6008123274975389894, -34.97209513635705491, -34.47473151356003740 ) ) ;
#99=CARTESIAN_POINT ( 'NONE',  ( 4.553261556744875094, 35.06776520399859010, 26.45357082552112260 ) ) ;
#112=CARTESIAN_POINT ( 'NONE',  ( 0.6026112563231247332, 41.06109594249098649, 26.93561573281289512 ) ) ;
#113=CARTESIAN_POINT ( 'NONE',  ( 0.1139756605157203062, -35.12259180221513333, 26.70877692426205030 ) ) ;
#118=CARTESIAN_POINT ( 'NONE',  ( 0.6008122571543326185, 48.11686503207880605, -9.814369564573597771 ) ) ;
#119=CARTESIAN_POINT ( 'NONE',  ( 0.6016118706126977189, -30.88962476549868796, 38.17567467158400518 ) ) ;
#120=EDGE_CURVE ( 'NONE', #16502, #9752, #36523, .T. ) ;
#125=CARTESIAN_POINT ( 'NONE',  ( 0.1154773475650540671, -6.864599028446649598, 43.58693508638535974 ) ) ;
#131=CARTESIAN_POINT ( 'NONE',  ( 0.5987334308729319599, -47.34446294507543485, 13.04088704851432290 ) ) ;
#135=ORIENTED_EDGE ( 'NONE', *, *, #59672, .F. ) ;
#140=CARTESIAN_POINT ( 'NONE',  ( 2.648799415243708655, 41.83591888777168322, 25.57876764242928047 ) ) ;
#146=CARTESIAN_POINT ( 'NONE',  ( 0.1152809850208375703, 33.45438703243825529, 28.77063208853051890 ) ) ;
#155=CARTESIAN_POINT ( 'NONE',  ( 0.1156867017252034696, -40.85238086880038111, -16.67410521214435093 ) ) ;
#162=EDGE_LOOP ( 'NONE', ( #14150, #34103, #5570, #1627 ) ) ;
#164=ORIENTED_EDGE ( 'NONE', *, *, #58852, .T. ) ;
#170=CARTESIAN_POINT ( 'NONE',  ( 0.1139756605157203062, -27.19909892944385987, 34.74426912630842423 ) ) ;
#180=ORIENTED_EDGE ( 'NONE', *, *, #28573, .F. ) ;
#181=EDGE_CURVE ( 'NONE', #8116, #45706, #44738, .T. ) ;
#187=CARTESIAN_POINT ( 'NONE',  ( 4.975610109902397937, 39.54077024310177535, -28.79195887257430897 ) ) ;
#189=FACE_OUTER_BOUND ( 'NONE', #26362, .T. ) ;
#193=CARTESIAN_POINT ( 'NONE',  ( 0.7242486021783862693, -29.97000013935198481, -38.89486539404931875 ) ) ;
#196=EDGE_CURVE ( 'NONE', #14140, #9995, #46409, .T. ) ;
#208=CARTESIAN_POINT ( 'NONE',  ( 0.2940133293162999761, -22.17757316225551278, -38.13654150825487932 ) ) ;
#216=CARTESIAN_POINT ( 'NONE',  ( 50.15577769773999961, 12.80000000000000071, 3.000000000000000000 ) ) ;
#221=CARTESIAN_POINT ( 'NONE',  ( 4.975610109902397937, -48.11736577406863802, 8.784561349450592971 ) ) ;
#223=CARTESIAN_POINT ( 'NONE',  ( 0.8744876279028263033, -43.20725972823498040, 23.31271664041618052 ) ) ;
#224=B_SPLINE_CURVE_WITH_KNOTS ( 'NONE', 3,
 ( #5732, #1055, #14880, #20192 ),
 .UNSPECIFIED., .F., .F.,
 ( 4, 4 ),
 ( 0.000000000000000000, 0.005013413432710142441 ),
 .UNSPECIFIED. ) ;
#227=CARTESIAN_POINT ( 'NONE',  ( 0.6026777506516368677, -8.009456454756694654, -48.44992257926296020 ) ) ;
#237=CARTESIAN_POINT ( 'NONE',  ( 3.894904216938897878, -29.11014567165013744, -32.93514462472435866 ) ) ;
#245=ADVANCED_FACE ( 'NONE', ( #8464 ), #1616, .F. ) ;
#248=ORIENTED_EDGE ( 'NONE', *, *, #5501, .F. ) ;
#250=FACE_OUTER_BOUND ( 'NONE', #162, .T. ) ;
#251=B_SPLINE_CURVE_WITH_KNOTS ( 'NONE', 3,
 ( #19332, #43782, #824, #19959 ),
 .UNSPECIFIED., .F., .F.,
 ( 4, 4 ),
 ( 0.000000000000000000, 0.005013413432710153717 ),
 .UNSPECIFIED. ) ;
#257=EDGE_CURVE ( 'NONE', #37381, #21977, #57325, .T. ) ;
#259=CARTESIAN_POINT ( 'NONE',  ( 0.3676999524040323597, -7.853951980432424484, 43.40813312746703190 ) ) ;
#261=CARTESIAN_POINT ( 'NONE',  ( -6.077587904424778920, -16.13490349385120481, -10.51003856501195877 ) ) ;
#268=CARTESIAN_POINT ( 'NONE',  ( -6.077587904424778920, -19.21689618909966413, -1.227567615774088017 ) ) ;
#269=EDGE_CURVE ( 'NONE', #35355, #39250, #33541, .T. ) ;
#280=CARTESIAN_POINT ( 'NONE',  ( -6.077587904424778920, -12.94128980615176872, -14.25899854643104803 ) ) ;
#283=ORIENTED_EDGE ( 'NONE', *, *, #47533, .F. ) ;
#295=ORIENTED_EDGE ( 'NONE', *, *, #34419, .F. ) ;
#297=CARTESIAN_POINT ( 'NONE',  ( -6.078457390727109555, -6.654470124808820941, 18.06965794904637335 ) ) ;
#302=CARTESIAN_POINT ( 'NONE',  ( -6.078075953587585900, 5.473785299353540523, -18.46165888385214870 ) ) ;
#303=ORIENTED_EDGE ( 'NONE', *, *, #61917, .T. ) ;
#307=CARTESIAN_POINT ( 'NONE',  ( 0.2279481005628815338, -43.84759606547602573, 4.887924544401895055 ) ) ;
#318=CIRCLE ( 'NONE', #20387, 48.91267123290010943 ) ;
#324=ORIENTED_EDGE ( 'NONE', *, *, #24698, .T. ) ;
#326=CARTESIAN_POINT ( 'NONE',  ( 0.1152809850208376258, 25.42529477452768560, -36.06244123902498444 ) ) ;
#329=EDGE_CURVE ( 'NONE', #33849, #9438, #31034, .T. ) ;
#340=DIRECTION ( 'NONE',  ( 0.09722883295013598492, -0.9860961158916706770, -0.1347627703281412404 ) ) ;
#353=CARTESIAN_POINT ( 'NONE',  ( 2.879087469061463178, 18.80129513073439185, -39.78206855092381744 ) ) ;
#361=ORIENTED_EDGE ( 'NONE', *, *, #7612, .T. ) ;
#363=EDGE_CURVE ( 'NONE', #33629, #19850, #31166, .T. ) ;
#365=CARTESIAN_POINT ( 'NONE',  ( 0.5997462898726536595, -31.02483596213057737, 38.06587952047342327 ) ) ;
#377=CARTESIAN_POINT ( 'NONE',  ( 0.7044674535452954967, 27.40191655692298767, 40.75460332058619883 ) ) ;
#380=EDGE_LOOP ( 'NONE', ( #10073, #51406, #39218, #28392 ) ) ;
#382=EDGE_LOOP ( 'NONE', ( #16913, #17732, #52074, #3845 ) ) ;
#383=CARTESIAN_POINT ( 'NONE',  ( 2.706805983486680223, 34.55979480539205184, 27.24695756096361166 ) ) ;
#384=CARTESIAN_POINT ( 'NONE',  ( -6.077587904424778920, 9.987489566522585349, 16.46347695818028001 ) ) ;
#394=EDGE_LOOP ( 'NONE', ( #29612, #23490, #21931, #13933 ) ) ;
#395=CARTESIAN_POINT ( 'NONE',  ( 0.08486401232817714080, 0.000000000000000000, 44.12552607296456131 ) ) ;
#396=CARTESIAN_POINT ( 'NONE',  ( 0.8744876279028306332, 33.66006955981207227, 35.74003032466684004 ) ) ;
#398=CARTESIAN_POINT ( 'NONE',  ( -6.072942160501519027, 11.99473239968586391, 15.06421444845188518 ) ) ;
#399=CARTESIAN_POINT ( 'NONE',  ( 0.6016117650947691020, -35.51782622858503657, -33.91216705314681690 ) ) ;
#402=ORIENTED_EDGE ( 'NONE', *, *, #26650, .F. ) ;
#404=EDGE_CURVE ( 'NONE', #47983, #17365, #23744, .T. ) ;
#406=LINE ( 'NONE', #42444, #21829 ) ;
#407=CIRCLE ( 'NONE', #30421, 43.92652462719577500 ) ;
#413=CARTESIAN_POINT ( 'NONE',  ( 0.8753041380234524160, -48.57841546934886168, 7.160717726618433865 ) ) ;
#419=EDGE_CURVE ( 'NONE', #16304, #19741, #25964, .T. ) ;
#422=CARTESIAN_POINT ( 'NONE',  ( 0.1119899015040011631, -35.69472091171160599, 25.93931778647085196 ) ) ;
#423=CARTESIAN_POINT ( 'NONE',  ( 0.1157991065609915299, -35.41034345021505203, 26.32584172017128310 ) ) ;
#424=EDGE_CURVE ( 'NONE', #19414, #14922, #59166, .T. ) ;
#428=CARTESIAN_POINT ( 'NONE',  ( 0.6029442701453591180, 32.95047274681666494, -36.41169552382268648 ) ) ;
#434=CARTESIAN_POINT ( 'NONE',  ( 4.975610109902397937, -41.30423662854430944, -26.19941685746064053 ) ) ;
#438=EDGE_LOOP ( 'NONE', ( #51636, #8049, #36131, #12773 ) ) ;
#441=CARTESIAN_POINT ( 'NONE',  ( 0.8744876279028306332, -48.57046782678520458, 7.159588358747709158 ) ) ;
#450=VERTEX_POINT ( 'NONE', #35397 ) ;
#452=CARTESIAN_POINT ( 'NONE',  ( 0.8744876279028306332, 32.34273794994798834, -36.93639603806098393 ) ) ;
#462=VERTEX_POINT ( 'NONE', #56553 ) ;
#463=DIRECTION ( 'NONE',  ( -1.000000000000000000, -0.000000000000000000, -0.000000000000000000 ) ) ;
#464=CARTESIAN_POINT ( 'NONE',  ( 0.9268187852002115479, 44.04984738791743126, 1.834469408251422351 ) ) ;
#466=ORIENTED_EDGE ( 'NONE', *, *, #12676, .F. ) ;
#473=VERTEX_POINT ( 'NONE', #43416 ) ;
#474=DIRECTION ( 'NONE',  ( -1.000000000000000000, 0.000000000000000000, 0.000000000000000000 ) ) ;
#479=CARTESIAN_POINT ( 'NONE',  ( 0.6027444965799114707, 4.845435411165755824, -48.86778357531332517 ) ) ;
#481=ORIENTED_EDGE ( 'NONE', *, *, #49627, .F. ) ;
#483=CARTESIAN_POINT ( 'NONE',  ( 0.1129192098497447394, 10.29049805561828101, 42.90754522869457332 ) ) ;
#484=ORIENTED_EDGE ( 'NONE', *, *, #31844, .F. ) ;
#491=CARTESIAN_POINT ( 'NONE',  ( 0.8753041380234524160, 49.05142151719380195, 2.257515230415333196 ) ) ;
#494=AXIS2_PLACEMENT_3D ( 'NONE', #841, #54061, #35924 ) ;
#496=CARTESIAN_POINT ( 'NONE',  ( 0.1129192098497455998, -38.68182264534154058, 21.22895156665764915 ) ) ;
#515=ORIENTED_EDGE ( 'NONE', *, *, #31367, .T. ) ;
#517=CARTESIAN_POINT ( 'NONE',  ( 0.5980271706414711508, -47.67913160907373538, 11.77920421107846316 ) ) ;
#524=CARTESIAN_POINT ( 'NONE',  ( 0.1157991065609915993, 9.897904771235362276, -42.99969589052061281 ) ) ;
#526=EDGE_CURVE ( 'NONE', #5254, #21667, #31964, .T. ) ;
#527=CARTESIAN_POINT ( 'NONE',  ( 0.2279481005628749279, -22.21835642701406144, -38.11624489315645548 ) ) ;
#528=( BOUNDED_SURFACE ( )  B_SPLINE_SURFACE ( 3, 1, ( 
 ( #7956, #17065 ),
 ( #3239, #18301 ),
 ( #36177, #22999 ),
 ( #13289, #2627 ) ),
 .UNSPECIFIED., .F., .F., .F. ) 
 B_SPLINE_SURFACE_WITH_KNOTS ( ( 4, 4 ),
 ( 2, 2 ),
 ( 0.000000000000000000, 1.000000000000000000 ),
 ( 0.000000000000000000, 1.000000000000000000 ),
 .UNSPECIFIED. ) 
 GEOMETRIC_REPRESENTATION_ITEM ( )  RATIONAL_B_SPLINE_SURFACE ( (
 ( 1.000000000000000000, 1.000000000000000000),
 ( 0.9953485035131437453, 0.8621029689291515030),
 ( 0.9953485035131437453, 0.8621029689291515030),
 ( 1.000000000000000000, 1.000000000000000000) ) ) 
 REPRESENTATION_ITEM ( '' )  SURFACE ( )  );
#529=CARTESIAN_POINT ( 'NONE',  ( -6.078457390727109555, -11.01309887717693670, 15.79576412077085656 ) ) ;
#541=CARTESIAN_POINT ( 'NONE',  ( 0.3676999524040323597, -2.238562284876542741, 44.05609404179593724 ) ) ;
#542=ORIENTED_EDGE ( 'NONE', *, *, #53181, .F. ) ;
#545=CARTESIAN_POINT ( 'NONE',  ( 0.5997462898726536595, 22.24958391914503153, 43.77793560195857481 ) ) ;
#547=ORIENTED_EDGE ( 'NONE', *, *, #20916, .F. ) ;
#548=CARTESIAN_POINT ( 'NONE',  ( 4.975610109902397937, 48.90928568712960356, 0.5754830253899292369 ) ) ;
#558=CARTESIAN_POINT ( 'NONE',  ( -2.739355103387248747, 13.33354922980911361, -6.712974891005759837 ) ) ;
#563=CARTESIAN_POINT ( 'NONE',  ( -6.063463321072278589, 19.25669258467947387, 0.01559418547018328639 ) ) ;
#566=B_SPLINE_CURVE_WITH_KNOTS ( 'NONE', 3,
 ( #25141, #5401, #33641, #24529, #7175, #53940, #58323, #5699, #11936, #43670, #15144, #53329, #10440, #48640, #24846, #43986, #39270, #15449, #31012 ),
 .UNSPECIFIED., .F., .F.,
 ( 4, 3, 3, 3, 3, 3, 4 ),
 ( 1.517943542627326963E-18, 0.0002612768053151706790, 0.0003919133833142909797, 0.0005225499612322605366, 0.0006531865391693358501, 0.0008112755173415187732, 0.0009693688056799720310 ),
 .UNSPECIFIED. ) ;
#570=B_SPLINE_CURVE_WITH_KNOTS ( 'NONE', 3,
 ( #8385, #3987, #23127, #3374, #22510, #41628, #56005, #13125, #32224, #27508, #46636, #3679, #41946, #61013, #18121, #37242, #42257, #56310, #18429, #13424, #32531, #43726, #20817, #5753, #16120 ),
 .UNSPECIFIED., .F., .F.,
 ( 4, 3, 3, 3, 3, 3, 3, 3, 4 ),
 ( 5.553824967135426632E-18, 0.0005656085177311408327, 0.001131215744874501140, 0.001696821861372767651, 0.002262427090022497284, 0.002828031679238745058, 0.003393635864401604862, 0.003977030878808131623, 0.004561030005651157265 ),
 .UNSPECIFIED. ) ;
#571=CARTESIAN_POINT ( 'NONE',  ( -6.078075953587585900, -18.90195907099241879, 3.675747206441630333 ) ) ;
#578=CARTESIAN_POINT ( 'NONE',  ( 0.5997462898726536595, -20.35457962188166192, -44.69052157405179315 ) ) ;
#580=CARTESIAN_POINT ( 'NONE',  ( 0.1129192098497447394, -42.55567333040724520, 11.66046547873710537 ) ) ;
#586=CARTESIAN_POINT ( 'NONE',  ( 0.6016117650947689910, 37.16599190767838223, -32.09735346976265191 ) ) ;
#587=CARTESIAN_POINT ( 'NONE',  ( 5.901764892641288895, -22.68842833057508912, -43.39615982236257707 ) ) ;
#588=CARTESIAN_POINT ( 'NONE',  ( 0.1129192098497447394, 30.02178898772887550, 32.33641869102754640 ) ) ;
#590=DIRECTION ( 'NONE',  ( -0.1011922191286467598, 0.6101824289146680069, 0.7857719377985040721 ) ) ;
#597=CARTESIAN_POINT ( 'NONE',  ( 0.9268187852002115479, 24.40384675953001192, -36.71793289723704135 ) ) ;
#598=CARTESIAN_POINT ( 'NONE',  ( 2.706805983486680223, 40.34082766586489299, 17.58959171080285699 ) ) ;
#604=B_SPLINE_CURVE_WITH_KNOTS ( 'NONE', 3,
 ( #30557, #55279, #7044, #58741, #45007, #54663, #54345, #16471, #25555, #54046, #20559, #59060, #26479, #49364, #2663, #36214, #40928, #59992, #49668 ),
 .UNSPECIFIED., .F., .F.,
 ( 4, 3, 3, 3, 3, 3, 4 ),
 ( 1.301113191146877164E-18, 0.0002612768053151710043, 0.0003919133833142908713, 0.0005225499612322609703, 0.0006531865391693360669, 0.0008112755173415192068, 0.0009693688056799722478 ),
 .UNSPECIFIED. ) ;
#605=EDGE_CURVE ( 'NONE', #26948, #16981, #11334, .T. ) ;
#607=ORIENTED_EDGE ( 'NONE', *, *, #39326, .T. ) ;
#610=CARTESIAN_POINT ( 'NONE',  ( 0.1129192098497447394, -0.9297496242502409913, 44.11448008785053077 ) ) ;
#614=CARTESIAN_POINT ( 'NONE',  ( 0.2940133293163011974, 41.60821255532008678, 14.66278273484767780 ) ) ;
#616=CARTESIAN_POINT ( 'NONE',  ( 4.975610109902397937, -37.61482235126175766, 31.26618855282478648 ) ) ;
#622=ORIENTED_EDGE ( 'NONE', *, *, #59993, .F. ) ;
#628=EDGE_LOOP ( 'NONE', ( #53914, #15394, #25567, #1434 ) ) ;
#632=CARTESIAN_POINT ( 'NONE',  ( 0.8744876279028306332, 27.35388303025845147, -40.76904626731451486 ) ) ;
#637=ORIENTED_EDGE ( 'NONE', *, *, #3991, .T. ) ;
#643=CARTESIAN_POINT ( 'NONE',  ( 0.1135584504625007929, 24.88873145264492592, 36.43491592982444871 ) ) ;
#646=CARTESIAN_POINT ( 'NONE',  ( 0.08486401232817714080, 0.000000000000000000, 3.000000000000000000 ) ) ;
#647=CARTESIAN_POINT ( 'NONE',  ( 0.1129192098497447394, -22.45785791439742241, 37.98152716363431125 ) ) ;
#651=ORIENTED_EDGE ( 'NONE', *, *, #50283, .F. ) ;
#652=CARTESIAN_POINT ( 'NONE',  ( 0.1135584504625008623, -41.05968028581452955, 16.15718747065669447 ) ) ;
#653=CIRCLE ( 'NONE', #23655, 43.92652462719577500 ) ;
#656=EDGE_CURVE ( 'NONE', #2290, #7571, #45749, .T. ) ;
#667=CARTESIAN_POINT ( 'NONE',  ( 0.1129192098497455998, 39.54191224844618802, 19.58032082273768637 ) ) ;
#671=CARTESIAN_POINT ( 'NONE',  ( 0.6000166863083106206, -48.77118664543515791, 5.761495891223091803 ) ) ;
#672=ORIENTED_EDGE ( 'NONE', *, *, #404, .F. ) ;
#680=EDGE_CURVE ( 'NONE', #47950, #8264, #32312, .T. ) ;
#681=ORIENTED_EDGE ( 'NONE', *, *, #11907, .F. ) ;
#685=EDGE_CURVE ( 'NONE', #32705, #13041, #48717, .T. ) ;
#697=CARTESIAN_POINT ( 'NONE',  ( 0.5997462898726536595, 48.29911994996575686, -8.873930482211887849 ) ) ;
#705=CARTESIAN_POINT ( 'NONE',  ( -6.079354080745853928, -16.13884862108074003, -10.50383360654586795 ) ) ;
#710=EDGE_LOOP ( 'NONE', ( #19478, #17460, #53566, #59552 ) ) ;
#714=CARTESIAN_POINT ( 'NONE',  ( -6.078726893082806448, 9.985094725776210822, 16.46486940689163703 ) ) ;
#717=CARTESIAN_POINT ( 'NONE',  ( 0.1152809850208375564, 37.10017609937931127, -23.88560687704625352 ) ) ;
#719=CARTESIAN_POINT ( 'NONE',  ( 1.834102595619085507, -5.740732742422371082, 43.67197880148968636 ) ) ;
#725=CARTESIAN_POINT ( 'NONE',  ( 1.830465331921977024, -42.27910384509804231, -12.36339087523346336 ) ) ;
#726=CARTESIAN_POINT ( 'NONE',  ( 4.834790513006555379, -47.12142688710419947, 3.487186408506746105 ) ) ;
#737=B_SPLINE_CURVE_WITH_KNOTS ( 'NONE', 3,
 ( #57303, #14440, #48863, #33549 ),
 .UNSPECIFIED., .F., .F.,
 ( 4, 4 ),
 ( 0.000000000000000000, 0.005013413432710154584 ),
 .UNSPECIFIED. ) ;
#738=CARTESIAN_POINT ( 'NONE',  ( 0.1119898979215350476, 39.99500470998355439, 18.63762073066790492 ) ) ;
#741=AXIS2_PLACEMENT_3D ( 'NONE', #15685, #34479, #34171 ) ;
#746=CARTESIAN_POINT ( 'NONE',  ( 0.1129192098497455998, -27.13044910148877165, -34.79785222304216319 ) ) ;
#748=CARTESIAN_POINT ( 'NONE',  ( 0.6016117650947691020, 32.75634116857341382, -36.58651619780874853 ) ) ;
#752=CARTESIAN_POINT ( 'NONE',  ( 0.6029443449137434907, 22.75264314188179782, -43.51846467927736484 ) ) ;
#757=CARTESIAN_POINT ( 'NONE',  ( 0.8753041380234465318, -8.714053517584193997, 48.32394436680080219 ) ) ;
#759=VERTEX_POINT ( 'NONE', #26750 ) ;
#762=CARTESIAN_POINT ( 'NONE',  ( 2.359973842542475886, 43.81130819181431946, -4.324947300761510682 ) ) ;
#771=ORIENTED_EDGE ( 'NONE', *, *, #4210, .F. ) ;
#773=CARTESIAN_POINT ( 'NONE',  ( 5.901764892641288895, 47.37867283933450580, 12.37953260115202525 ) ) ;
#778=CARTESIAN_POINT ( 'NONE',  ( -6.079354080745853928, -12.94667982361303160, 14.25399722158711846 ) ) ;
#786=CARTESIAN_POINT ( 'NONE',  ( 0.1365634738349390531, 43.42681589074051374, -7.808603025828129596 ) ) ;
#793=CARTESIAN_POINT ( 'NONE',  ( 0.3676999524040366896, 40.09552319080398775, 18.39292264373822405 ) ) ;
#796=FACE_OUTER_BOUND ( 'NONE', #9055, .T. ) ;
#799=B_SPLINE_CURVE_WITH_KNOTS ( 'NONE', 3,
 ( #60694, #8701, #46635, #55683, #55382, #31593, #46951, #46327, #41627, #56004, #3986, #7773, #50681, #27507, #3073, #22200, #59050, #36206, #45602, #2653, #59358, #21785, #6716, #30545, #45301 ),
 .UNSPECIFIED., .F., .F.,
 ( 4, 3, 3, 3, 3, 3, 3, 3, 4 ),
 ( 3.469446951953613804E-18, 0.0005656085177311393148, 0.001131215744874498972, 0.001696821861372763965, 0.002262427090022496850, 0.002828031679238744624, 0.003393635864401604429, 0.003977030878808129888, 0.004561030005651157265 ),
 .UNSPECIFIED. ) ;
#802=CARTESIAN_POINT ( 'NONE',  ( 0.6021448801613057400, 4.975419407533241412, -48.85474736753931069 ) ) ;
#811=CARTESIAN_POINT ( 'NONE',  ( 0.1155031312995260795, 33.70714732405365766, -28.47402064700997926 ) ) ;
#815=EDGE_CURVE ( 'NONE', #12977, #53425, #47107, .T. ) ;
#820=CARTESIAN_POINT ( 'NONE',  ( 4.553261556744875094, 0.000000000000000000, 0.000000000000000000 ) ) ;
#821=CARTESIAN_POINT ( 'NONE',  ( 4.553261556744875094, -15.38244134641827898, 41.14510984366961566 ) ) ;
#824=CARTESIAN_POINT ( 'NONE',  ( 4.834790513006555379, 41.39428925248022040, 22.78381351324621917 ) ) ;
#837=ORIENTED_EDGE ( 'NONE', *, *, #10998, .T. ) ;
#839=VECTOR ( 'NONE', #31657, 1000.000000000000227 ) ;
#841=CARTESIAN_POINT ( 'NONE',  ( 0.08486401232817714080, 0.000000000000000000, 0.000000000000000000 ) ) ;
#846=EDGE_CURVE ( 'NONE', #28462, #53243, #29302, .T. ) ;
#855=VERTEX_POINT ( 'NONE', #32699 ) ;
#858=ORIENTED_EDGE ( 'NONE', *, *, #44639, .F. ) ;
#871=ORIENTED_EDGE ( 'NONE', *, *, #55780, .T. ) ;
#873=VERTEX_POINT ( 'NONE', #13279 ) ;
#877=CARTESIAN_POINT ( 'NONE',  ( 4.975610109902397937, 39.54077024310134902, 28.79195887257488451 ) ) ;
#880=DIRECTION ( 'NONE',  ( -0.1011922191286467598, 0.7056551247449875941, 0.7012923639317314439 ) ) ;
#885=VERTEX_POINT ( 'NONE', #22990 ) ;
#887=CARTESIAN_POINT ( 'NONE',  ( -6.078726893082806448, 7.797636468844645563, 17.60655862934219584 ) ) ;
#889=EDGE_CURVE ( 'NONE', #22076, #50810, #31522, .T. ) ;
#890=CARTESIAN_POINT ( 'NONE',  ( 0.7948878604505672518, -13.13616273002648072, 47.30898303735433075 ) ) ;
#891=CARTESIAN_POINT ( 'NONE',  ( 0.8744876279028263033, -45.83369275826233036, 17.59609782084381280 ) ) ;
#897=DIRECTION ( 'NONE',  ( 0.000000000000000000, 0.000000000000000000, 1.000000000000000000 ) ) ;
#900=CARTESIAN_POINT ( 'NONE',  ( 0.5980271706414711508, -48.61493274831085643, -6.974063142736467213 ) ) ;
#906=CARTESIAN_POINT ( 'NONE',  ( 0.8753041380234471980, -6.957149426673730375, -48.60798699522449340 ) ) ;
#911=B_SPLINE_CURVE_WITH_KNOTS ( 'NONE', 3,
 ( #35772, #40794, #49848, #40176, #59541, #54839 ),
 .UNSPECIFIED., .F., .F.,
 ( 4, 2, 4 ),
 ( 2.818925648462311528E-18, 0.0002447193893791703044, 0.0004894387787583377898 ),
 .UNSPECIFIED. ) ;
#912=ORIENTED_EDGE ( 'NONE', *, *, #39913, .F. ) ;
#916=CARTESIAN_POINT ( 'NONE',  ( 1.830465331921977468, -40.35099765304325814, -17.66841940532562560 ) ) ;
#917=CARTESIAN_POINT ( 'NONE',  ( 0.6026777506516367566, -47.54531535096658246, -12.28777354993009396 ) ) ;
#923=CARTESIAN_POINT ( 'NONE',  ( 0.5997462898726536595, 32.62638226927682439, 36.70246327105753892 ) ) ;
#926=ADVANCED_FACE ( 'NONE', ( #57380 ), #4353, .F. ) ;
#927=B_SPLINE_CURVE_WITH_KNOTS ( 'NONE', 3,
 ( #45392, #7755, #22796, #26879, #21564, #16557, #54745, #41611, #26252, #36605, #11883, #30962, #40699, #59768, #12486, #35995, #31270, #7436, #26567 ),
 .UNSPECIFIED., .F., .F.,
 ( 4, 3, 3, 3, 3, 3, 4 ),
 ( 0.000000000000000000, 0.0002612768053151720343, 0.0003919133833142897328, 0.0005225499612322591272, 0.0006531865391693329227, 0.0008112755173415183395, 0.0009693688056799717057 ),
 .UNSPECIFIED. ) ;
#930=CARTESIAN_POINT ( 'NONE',  ( 4.834790513006555379, -32.10612123254703221, -34.66678987626880826 ) ) ;
#931=CARTESIAN_POINT ( 'NONE',  ( 4.553261556744873317, 7.233533384970671776, 43.32684572631789166 ) ) ;
#938=CARTESIAN_POINT ( 'NONE',  ( 0.3676999524040366896, -13.34038000160327364, -42.04741186726791113 ) ) ;
#948=CARTESIAN_POINT ( 'NONE',  ( 0.9268187852002115479, -35.91688603071045094, -25.56817613295056191 ) ) ;
#950=CARTESIAN_POINT ( 'NONE',  ( 0.8753041380234530822, -45.17330286263802464, 19.24866323549142066 ) ) ;
#951=ORIENTED_EDGE ( 'NONE', *, *, #57190, .F. ) ;
#961=CARTESIAN_POINT ( 'NONE',  ( -2.601141883200665639, 8.168301201416211299, 12.49296934088654076 ) ) ;
#976=CARTESIAN_POINT ( 'NONE',  ( 0.8744876279028306332, 17.78802839418675674, 45.75954650373076049 ) ) ;
#980=CARTESIAN_POINT ( 'NONE',  ( 0.1145239942831223490, 39.61174555950172760, 19.43849516896738905 ) ) ;
#983=DIRECTION ( 'NONE',  ( -0.1011922191286467598, -0.9919158664526095404, -0.07657054699679781418 ) ) ;
#986=CARTESIAN_POINT ( 'NONE',  ( 0.5997462898726536595, -7.321308210775749004, 48.55872811583040516 ) ) ;
#988=VERTEX_POINT ( 'NONE', #20435 ) ;
#990=CARTESIAN_POINT ( 'NONE',  ( 3.894904216938898323, 26.94017379411146607, 34.73256927466309918 ) ) ;
#991=EDGE_CURVE ( 'NONE', #3830, #45554, #39257, .T. ) ;
#996=CARTESIAN_POINT ( 'NONE',  ( 0.7044674535453004927, 21.96536420256020250, -43.92408790469978896 ) ) ;
#1002=CARTESIAN_POINT ( 'NONE',  ( 0.5980271706414734822, -20.51809962909598184, -44.62125984832962899 ) ) ;
#1014=VECTOR ( 'NONE', #19095, 1000.000000000000000 ) ;
#1019=ORIENTED_EDGE ( 'NONE', *, *, #22432, .T. ) ;
#1025=CARTESIAN_POINT ( 'NONE',  ( 2.359973842542475886, -42.94220026048606087, -9.700687162299988842 ) ) ;
#1026=CARTESIAN_POINT ( 'NONE',  ( 4.975610109902397937, 0.000000000000000000, 0.000000000000000000 ) ) ;
#1027=CARTESIAN_POINT ( 'NONE',  ( 5.901764892641307547, -32.89013534638866787, -36.27989063291003191 ) ) ;
#1034=CARTESIAN_POINT ( 'NONE',  ( 3.240649175237396484, -42.05244175136726170, -12.91731629037221474 ) ) ;
#1036=CARTESIAN_POINT ( 'NONE',  ( 0.1119898979215350893, 15.76451811348070997, 41.21214962728306119 ) ) ;
#1041=CARTESIAN_POINT ( 'NONE',  ( -6.078457390727109555, -6.654470124808557152, -18.06965794904646216 ) ) ;
#1048=EDGE_CURVE ( 'NONE', #8147, #48887, #3112, .T. ) ;
#1055=CARTESIAN_POINT ( 'NONE',  ( 4.834790513006553603, -16.75039937818133140, 44.18159641293876660 ) ) ;
#1061=CARTESIAN_POINT ( 'NONE',  ( 0.6029443199889047422, 48.20183188216083892, 9.387281025851251570 ) ) ;
#1063=ORIENTED_EDGE ( 'NONE', *, *, #30338, .F. ) ;
#1066=CARTESIAN_POINT ( 'NONE',  ( 0.1368894036331276820, -43.83795633916983547, -5.009482002001066192 ) ) ;
#1067=CARTESIAN_POINT ( 'NONE',  ( 0.1135584504625008068, 41.73827531235328081, 14.31322556538019164 ) ) ;
#1068=ORIENTED_EDGE ( 'NONE', *, *, #6587, .F. ) ;
#1072=ORIENTED_EDGE ( 'NONE', *, *, #37861, .F. ) ;
#1073=ORIENTED_EDGE ( 'NONE', *, *, #49902, .F. ) ;
#1084=EDGE_LOOP ( 'NONE', ( #1474, #55394, #45983, #47094 ) ) ;
#1095=CARTESIAN_POINT ( 'NONE',  ( 0.5987334363312691865, 28.58958334901124587, -39.92741702642453561 ) ) ;
#1108=CARTESIAN_POINT ( 'NONE',  ( 0.1129192098497447394, -18.30288010335054949, -40.14917642626718930 ) ) ;
#1115=FACE_OUTER_BOUND ( 'NONE', #7002, .T. ) ;
#1119=CARTESIAN_POINT ( 'NONE',  ( 3.240649175237395596, 16.89562953456788819, -40.61776237101557285 ) ) ;
#1120=VERTEX_POINT ( 'NONE', #49868 ) ;
#1124=CARTESIAN_POINT ( 'NONE',  ( 0.6024113833632039894, 22.52083809065578990, 43.63890146183028662 ) ) ;
#1126=B_SPLINE_CURVE_WITH_KNOTS ( 'NONE', 3,
 ( #53200, #18468, #47908, #47595, #4636, #57262 ),
 .UNSPECIFIED., .F., .F.,
 ( 4, 2, 4 ),
 ( 4.878909776184769953E-19, 0.0002293801035737091010, 0.0004587602071474177140 ),
 .UNSPECIFIED. ) ;
#1127=CARTESIAN_POINT ( 'NONE',  ( 0.6024113833632039894, -20.07675414434353200, 44.81591025660922156 ) ) ;
#1131=ADVANCED_FACE ( 'NONE', ( #41422 ), #10810, .F. ) ;
#1134=LINE ( 'NONE', #20271, #18358 ) ;
#1136=ORIENTED_EDGE ( 'NONE', *, *, #51297, .F. ) ;
#1139=CARTESIAN_POINT ( 'NONE',  ( 0.5997462898726536595, -8.352924653000716404, 48.39194436975645175 ) ) ;
#1143=CARTESIAN_POINT ( 'NONE',  ( 0.1158516988532803799, 9.770552602771916284, -43.02880965898619081 ) ) ;
#1149=CARTESIAN_POINT ( 'NONE',  ( 0.6024113833632039894, 37.25118206351266537, 31.99830157948853326 ) ) ;
#1155=ADVANCED_FACE ( 'NONE', ( #26675 ), #57594, .F. ) ;
#1157=VERTEX_POINT ( 'NONE', #7237 ) ;
#1161=CARTESIAN_POINT ( 'NONE',  ( 2.648799415243708655, 26.90653288552096711, -40.99458441513923646 ) ) ;
#1176=CARTESIAN_POINT ( 'NONE',  ( 0.1129192098497447394, 33.91039995638862337, 28.23183597612653983 ) ) ;
#1185=ORIENTED_EDGE ( 'NONE', *, *, #43378, .T. ) ;
#1189=CARTESIAN_POINT ( 'NONE',  ( 0.7044674535452954967, -19.10600803152149751, -45.24116687167055773 ) ) ;
#1190=DIRECTION ( 'NONE',  ( 0.09722883295013597105, -0.9646010353641062407, 0.2451354658503108463 ) ) ;
#1194=EDGE_CURVE ( 'NONE', #21289, #10372, #9768, .T. ) ;
#1203=CARTESIAN_POINT ( 'NONE',  ( 2.879087469061463178, 11.47169626938654474, 42.47942868596894073 ) ) ;
#1206=CARTESIAN_POINT ( 'NONE',  ( -6.077587904424778920, 9.987489566522585349, 16.46347695818028001 ) ) ;
#1207=CARTESIAN_POINT ( 'NONE',  ( 0.7948884756798509921, -47.70571120116157005, 11.61308586860173797 ) ) ;
#1225=AXIS2_PLACEMENT_3D ( 'NONE', #21925, #31315, #55107 ) ;
#1226=ORIENTED_EDGE ( 'NONE', *, *, #1888, .F. ) ;
#1235=CARTESIAN_POINT ( 'NONE',  ( 0.1155031312995260795, 29.78923516837971874, -32.55062365938290014 ) ) ;
#1236=CARTESIAN_POINT ( 'NONE',  ( 0.1152339509894530906, 20.60693138425672544, 39.01662555090813811 ) ) ;
#1241=CARTESIAN_POINT ( 'NONE',  ( 0.1152339509894530906, -1.190938228105830055, 44.10809853748038023 ) ) ;
#1244=CARTESIAN_POINT ( 'NONE',  ( 2.359973842542475886, -36.16349720208508955, -25.10652036319019587 ) ) ;
#1246=CARTESIAN_POINT ( 'NONE',  ( 0.5980271706414734822, -45.25597162979979515, 19.07737599053966449 ) ) ;
#1257=CARTESIAN_POINT ( 'NONE',  ( 4.834790513006555379, -35.67803047646649617, 30.97850032271910692 ) ) ;
#1259=CARTESIAN_POINT ( 'NONE',  ( 0.8753041380234524160, -38.81339214172321306, 30.07754840949971609 ) ) ;
#1262=ORIENTED_EDGE ( 'NONE', *, *, #48309, .T. ) ;
#1275=( BOUNDED_SURFACE ( )  B_SPLINE_SURFACE ( 3, 1, ( 
 ( #32106, #12699 ),
 ( #40598, #7649 ),
 ( #17385, #59976 ),
 ( #31475, #44989 ) ),
 .UNSPECIFIED., .F., .F., .F. ) 
 B_SPLINE_SURFACE_WITH_KNOTS ( ( 4, 4 ),
 ( 2, 2 ),
 ( 0.000000000000000000, 1.000000000000000000 ),
 ( 0.000000000000000000, 1.000000000000000000 ),
 .UNSPECIFIED. ) 
 GEOMETRIC_REPRESENTATION_ITEM ( )  RATIONAL_B_SPLINE_SURFACE ( (
 ( 1.000000000000000000, 1.000000000000000000),
 ( 0.7211978278499970862, 0.9934217856018976445),
 ( 0.7211978278499970862, 0.9934217856018976445),
 ( 1.000000000000000000, 1.000000000000000000) ) ) 
 REPRESENTATION_ITEM ( '' )  SURFACE ( )  );
#1282=CARTESIAN_POINT ( 'NONE',  ( 4.553261556744875094, -9.994631851593741345, 42.77437199977043036 ) ) ;
#1284=ORIENTED_EDGE ( 'NONE', *, *, #49360, .T. ) ;
#1285=CARTESIAN_POINT ( 'NONE',  ( -4.915099999999999802, 0.000000000000000000, 3.000000000000000000 ) ) ;
#1286=CARTESIAN_POINT ( 'NONE',  ( 3.894904216938898323, 18.33300990194901559, -39.95028260740141945 ) ) ;
#1288=ORIENTED_EDGE ( 'NONE', *, *, #26094, .T. ) ;
#1289=CARTESIAN_POINT ( 'NONE',  ( 0.5987334363312689645, -14.55165115253731756, 46.90215725536444324 ) ) ;
#1290=CARTESIAN_POINT ( 'NONE',  ( 0.1139756605157203340, 4.632526725434476411, 43.88046166385626634 ) ) ;
#1292=ORIENTED_EDGE ( 'NONE', *, *, #1379, .F. ) ;
#1293=VERTEX_POINT ( 'NONE', #57019 ) ;
#1294=CARTESIAN_POINT ( 'NONE',  ( 0.5997462898726536595, 10.41743419021273631, 47.98988117339838055 ) ) ;
#1298=VERTEX_POINT ( 'NONE', #17914 ) ;
#1303=FACE_OUTER_BOUND ( 'NONE', #57037, .T. ) ;
#1309=VERTEX_POINT ( 'NONE', #38568 ) ;
#1310=CARTESIAN_POINT ( 'NONE',  ( 0.3676999524040323597, -17.09834788623527047, -40.66444494744902727 ) ) ;
#1319=CARTESIAN_POINT ( 'NONE',  ( 4.834790513006553603, 7.085748555637120916, 46.71596631057383320 ) ) ;
#1322=LINE ( 'NONE', #16078, #26277 ) ;
#1323=CARTESIAN_POINT ( 'NONE',  ( 2.185380717157383135, 8.390375351159853778, -43.22524036409571124 ) ) ;
#1324=CARTESIAN_POINT ( 'NONE',  ( 2.299652685299201860, -29.55407244308045023, -39.12593164241979338 ) ) ;
#1341=CARTESIAN_POINT ( 'NONE',  ( 0.1145239942831223490, -6.719625162407512953, -43.60954159792800056 ) ) ;
#1347=AXIS2_PLACEMENT_3D ( 'NONE', #12331, #7917, #59917 ) ;
#1349=CARTESIAN_POINT ( 'NONE',  ( -4.915099999999998914, 9.539392014169456147, -3.000000000000000000 ) ) ;
#1350=CARTESIAN_POINT ( 'NONE',  ( 0.2285344041767098378, 44.07067438182842523, 2.068049763982732880 ) ) ;
#1356=ORIENTED_EDGE ( 'NONE', *, *, #44945, .F. ) ;
#1359=CARTESIAN_POINT ( 'NONE',  ( 1.296416391601052265, 43.89588502411658766, -3.931749232300615571 ) ) ;
#1360=CARTESIAN_POINT ( 'NONE',  ( 0.1139756605157203201, 42.00001770421683744, 13.52603905585425714 ) ) ;
#1361=VERTEX_POINT ( 'NONE', #29753 ) ;
#1363=LINE ( 'NONE', #40872, #18313 ) ;
#1365=CARTESIAN_POINT ( 'NONE',  ( 2.648799415243708655, 48.37728179772441450, 8.009748382637324582 ) ) ;
#1366=VERTEX_POINT ( 'NONE', #39498 ) ;
#1367=ORIENTED_EDGE ( 'NONE', *, *, #20893, .F. ) ;
#1371=CARTESIAN_POINT ( 'NONE',  ( -6.079354080745853928, -12.94495173828262047, 14.25556662296156496 ) ) ;
#1376=CARTESIAN_POINT ( 'NONE',  ( 0.5980271706414711508, -13.30134363210393644, -47.27709276618382006 ) ) ;
#1379=EDGE_CURVE ( 'NONE', #46207, #45900, #10564, .T. ) ;
#1386=CARTESIAN_POINT ( 'NONE',  ( 0.6008123274975393224, -8.267100005214324199, 48.40671036811161088 ) ) ;
#1389=VECTOR ( 'NONE', #52131, 1000.000000000000114 ) ;
#1400=CARTESIAN_POINT ( 'NONE',  ( 0.1154773475650540393, 9.993826709811125752, 42.97751805002688741 ) ) ;
#1404=EDGE_CURVE ( 'NONE', #41574, #37380, #46122, .T. ) ;
#1406=CARTESIAN_POINT ( 'NONE',  ( 0.1129192098497455998, -42.55567333040708888, -11.66046547873770756 ) ) ;
#1409=CARTESIAN_POINT ( 'NONE',  ( -6.072942160501519027, -19.21577577016805094, -1.248248308487848401 ) ) ;
#1411=CARTESIAN_POINT ( 'NONE',  ( 1.296416391601052265, 21.36356421792644511, 38.54744476593347002 ) ) ;
#1417=CARTESIAN_POINT ( 'NONE',  ( 0.7948884756798506590, 33.64624544102139225, -35.75791957486759998 ) ) ;
#1420=CARTESIAN_POINT ( 'NONE',  ( 0.6000166863083106206, 37.05402083933981316, -32.23077754796219807 ) ) ;
#1421=CARTESIAN_POINT ( 'NONE',  ( 0.5987334308729317378, 48.96426922180645391, -3.750099484572206432 ) ) ;
#1422=CARTESIAN_POINT ( 'NONE',  ( 0.5980271706414734822, 5.412294693954527780, 48.81348490926923489 ) ) ;
#1434=ORIENTED_EDGE ( 'NONE', *, *, #19326, .F. ) ;
#1435=CARTESIAN_POINT ( 'NONE',  ( 4.694002226626921015, -4.034398983147713835, 45.40934261020424856 ) ) ;
#1437=B_SPLINE_CURVE_WITH_KNOTS ( 'NONE', 3,
 ( #47295, #47008, #4042, #17876 ),
 .UNSPECIFIED., .F., .F.,
 ( 4, 4 ),
 ( 0.000000000000000000, 0.005013413432710148512 ),
 .UNSPECIFIED. ) ;
#1442=ORIENTED_EDGE ( 'NONE', *, *, #24398, .F. ) ;
#1446=CARTESIAN_POINT ( 'NONE',  ( 0.5997462898726536595, 37.72933316221968170, 31.43324751403423534 ) ) ;
#1471=VECTOR ( 'NONE', #19350, 1000.000000000000114 ) ;
#1474=ORIENTED_EDGE ( 'NONE', *, *, #15088, .T. ) ;
#1478=CARTESIAN_POINT ( 'NONE',  ( 0.6016118706126978299, -30.34494265132144619, -38.61004416304056974 ) ) ;
#1498=CARTESIAN_POINT ( 'NONE',  ( 0.2285344041767113921, -38.80901244121420035, -20.98479744084123766 ) ) ;
#1501=CARTESIAN_POINT ( 'NONE',  ( 4.975610109902397937, 47.16372689271670993, -12.96272628450527264 ) ) ;
#1503=CARTESIAN_POINT ( 'NONE',  ( 3.390910168358336474, 11.69695288386326837, 42.39432072537923801 ) ) ;
#1505=ADVANCED_FACE ( 'NONE', ( #36831 ), #7660, .F. ) ;
#1506=CARTESIAN_POINT ( 'NONE',  ( 0.6008123274975391004, 37.67355407045358362, -31.50012499751496264 ) ) ;
#1507=CARTESIAN_POINT ( 'NONE',  ( 0.8744876279028263033, 11.79038800009220722, -47.65854384249244191 ) ) ;
#1508=B_SPLINE_CURVE_WITH_KNOTS ( 'NONE', 3,
 ( #20044, #10634, #5889, #33522 ),
 .UNSPECIFIED., .F., .F.,
 ( 4, 4 ),
 ( 0.000000000000000000, 0.004442905043737215703 ),
 .UNSPECIFIED. ) ;
#1509=CARTESIAN_POINT ( 'NONE',  ( 0.8744876279028306332, -29.90976330662902427, 38.93271258621624042 ) ) ;
#1511=CARTESIAN_POINT ( 'NONE',  ( 0.2285344041767106982, -17.16127025498933634, 40.64470412649936293 ) ) ;
#1516=DIRECTION ( 'NONE',  ( 0.000000000000000000, 0.000000000000000000, 1.000000000000000000 ) ) ;
#1517=CARTESIAN_POINT ( 'NONE',  ( -6.063463321072276813, 5.464110623310199699, -18.46520911269890064 ) ) ;
#1521=ORIENTED_EDGE ( 'NONE', *, *, #31367, .F. ) ;
#1525=( BOUNDED_SURFACE ( )  B_SPLINE_SURFACE ( 3, 1, ( 
 ( #60113, #36961 ),
 ( #55099, #54787 ),
 ( #22532, #12223 ),
 ( #13144, #41351 ) ),
 .UNSPECIFIED., .F., .F., .F. ) 
 B_SPLINE_SURFACE_WITH_KNOTS ( ( 4, 4 ),
 ( 2, 2 ),
 ( 0.000000000000000000, 1.000000000000000000 ),
 ( 0.000000000000000000, 1.000000000000000000 ),
 .UNSPECIFIED. ) 
 GEOMETRIC_REPRESENTATION_ITEM ( )  RATIONAL_B_SPLINE_SURFACE ( (
 ( 1.000000000000000000, 1.000000000000000000),
 ( 0.7211978278499968642, 0.9934217856018975334),
 ( 0.7211978278499968642, 0.9934217856018975334),
 ( 1.000000000000000000, 1.000000000000000000) ) ) 
 REPRESENTATION_ITEM ( '' )  SURFACE ( )  );
#1526=CARTESIAN_POINT ( 'NONE',  ( 0.6008122571543326185, -13.55447923524773302, 47.19990088047383381 ) ) ;
#1528=CARTESIAN_POINT ( 'NONE',  ( 0.5549461598389365813, -44.09588694354911098, 0.8777528858055476668 ) ) ;
#1535=VECTOR ( 'NONE', #49234, 1000.000000000000000 ) ;
#1539=ORIENTED_EDGE ( 'NONE', *, *, #10760, .T. ) ;
#1540=CARTESIAN_POINT ( 'NONE',  ( 0.1156495703730067853, 29.56366858242225604, -32.75564765318752336 ) ) ;
#1543=CIRCLE ( 'NONE', #53547, 43.92652462719577500 ) ;
#1546=CARTESIAN_POINT ( 'NONE',  ( -6.078726893082806448, 17.85000270430361269, -7.222980321520601876 ) ) ;
#1548=VERTEX_POINT ( 'NONE', #58345 ) ;
#1551=DIRECTION ( 'NONE',  ( 1.000000000000000000, 0.000000000000000000, 0.000000000000000000 ) ) ;
#1554=CARTESIAN_POINT ( 'NONE',  ( 0.1365634738349403299, -6.412693133886302022, -43.65478194188872862 ) ) ;
#1559=ORIENTED_EDGE ( 'NONE', *, *, #8314, .T. ) ;
#1562=ORIENTED_EDGE ( 'NONE', *, *, #45647, .T. ) ;
#1566=CARTESIAN_POINT ( 'NONE',  ( -2.739355103387248747, 14.24824591804147289, 4.453656386614430751 ) ) ;
#1569=CARTESIAN_POINT ( 'NONE',  ( 0.6253024248130448770, 49.04477337953059646, -2.460575454669923445 ) ) ;
#1570=ORIENTED_EDGE ( 'NONE', *, *, #59670, .T. ) ;
#1586=CARTESIAN_POINT ( 'NONE',  ( 0.8753041380234465318, -45.17330286263774752, -19.24866323549208147 ) ) ;
#1587=CARTESIAN_POINT ( 'NONE',  ( 0.6021448801613057400, -45.61590711508016938, 18.18598792189538926 ) ) ;
#1589=ORIENTED_EDGE ( 'NONE', *, *, #61644, .F. ) ;
#1590=DIRECTION ( 'NONE',  ( 0.09722883295013594329, -0.1662994675516162035, 0.9812701162958157308 ) ) ;
#1594=CARTESIAN_POINT ( 'NONE',  ( 0.1129192098497447394, 37.24220309526806005, 23.66368729500878842 ) ) ;
#1600=CARTESIAN_POINT ( 'NONE',  ( -6.077587904424778920, -8.912150607695380700, 17.06955163264944630 ) ) ;
#1603=CARTESIAN_POINT ( 'NONE',  ( 0.6021447746440204973, 11.18199449963166003, 47.81740413383703014 ) ) ;
#1607=ORIENTED_EDGE ( 'NONE', *, *, #26595, .F. ) ;
#1608=CARTESIAN_POINT ( 'NONE',  ( 0.5987334363312689645, -48.77819064245283442, 5.678998513875774812 ) ) ;
#1616=( BOUNDED_SURFACE ( )  B_SPLINE_SURFACE ( 3, 1, ( 
 ( #42949, #36707 ),
 ( #55774, #12899 ),
 ( #31999, #51076 ),
 ( #3455, #22593 ) ),
 .UNSPECIFIED., .F., .F., .F. ) 
 B_SPLINE_SURFACE_WITH_KNOTS ( ( 4, 4 ),
 ( 2, 2 ),
 ( 0.000000000000000000, 1.000000000000000000 ),
 ( 0.000000000000000000, 1.000000000000000000 ),
 .UNSPECIFIED. ) 
 GEOMETRIC_REPRESENTATION_ITEM ( )  RATIONAL_B_SPLINE_SURFACE ( (
 ( 1.000000000000000000, 1.000000000000000000),
 ( 0.9754377213608244057, 0.9999580625633939235),
 ( 0.9754377213608244057, 0.9999580625633939235),
 ( 1.000000000000000000, 1.000000000000000000) ) ) 
 REPRESENTATION_ITEM ( '' )  SURFACE ( )  );
#1619=EDGE_CURVE ( 'NONE', #27238, #20167, #55359, .T. ) ;
#1627=ORIENTED_EDGE ( 'NONE', *, *, #680, .F. ) ;
#1629=LINE ( 'NONE', #10754, #47485 ) ;
#1630=CARTESIAN_POINT ( 'NONE',  ( -2.739355103387248747, 12.36564479942413897, -8.362917890634330220 ) ) ;
#1632=CARTESIAN_POINT ( 'NONE',  ( 3.050102900204245682, -42.97776842906123562, -9.398758962546484241 ) ) ;
#1638=VERTEX_POINT ( 'NONE', #35205 ) ;
#1640=CARTESIAN_POINT ( 'NONE',  ( 4.553261556744875094, 42.43205150231973732, 11.36048287389764688 ) ) ;
#1645=CARTESIAN_POINT ( 'NONE',  ( 0.7044674535452954967, 16.16814117525538563, 46.37234017976575018 ) ) ;
#1650=CARTESIAN_POINT ( 'NONE',  ( 0.1129192098497455998, -6.563350895508677674, -43.63340707310831590 ) ) ;
#1653=CARTESIAN_POINT ( 'NONE',  ( 2.185380717157383135, 41.31325970390012969, -15.23267460774046178 ) ) ;
#1657=CARTESIAN_POINT ( 'NONE',  ( 0.8753041380234465318, 11.79227530596935303, -47.66634631457717575 ) ) ;
#1660=CARTESIAN_POINT ( 'NONE',  ( 0.6008123274975389894, 48.11686618743674870, 9.814363935516372095 ) ) ;
#1668=CARTESIAN_POINT ( 'NONE',  ( 0.8744876279028263033, -34.64280934553510605, -34.78829991575325664 ) ) ;
#1678=VECTOR ( 'NONE', #9467, 1000.000000000000000 ) ;
#1680=CARTESIAN_POINT ( 'NONE',  ( -6.078457390727109555, -18.27366031693668091, 6.071890122418351687 ) ) ;
#1681=CARTESIAN_POINT ( 'NONE',  ( 4.553261556744875094, -9.994631851593741345, 42.77437199977043036 ) ) ;
#1692=CARTESIAN_POINT ( 'NONE',  ( 0.1129192098497455998, -40.71518461128082578, -17.00663193740825463 ) ) ;
#1695=CARTESIAN_POINT ( 'NONE',  ( 0.6026777506516367566, -7.665548088515766523, 48.50552301686759904 ) ) ;
#1699=ORIENTED_EDGE ( 'NONE', *, *, #39716, .F. ) ;
#1706=CARTESIAN_POINT ( 'NONE',  ( -6.072942160501519915, 18.63017572808491806, 4.870391630012528950 ) ) ;
#1709=CARTESIAN_POINT ( 'NONE',  ( 1.830465331921977246, 41.40011171874475338, 15.04682044665391949 ) ) ;
#1713=VECTOR ( 'NONE', #21673, 1000.000000000000114 ) ;
#1716=CARTESIAN_POINT ( 'NONE',  ( 2.648799415243708655, 49.00436887187488111, 1.757638972832060720 ) ) ;
#1718=CARTESIAN_POINT ( 'NONE',  ( 3.727782113643637096, 22.20616388426432408, 37.94290528479822910 ) ) ;
#1719=CARTESIAN_POINT ( 'NONE',  ( 4.553261556744875094, -43.85016385001095784, 2.588956575693979190 ) ) ;
#1726=B_SPLINE_CURVE_WITH_KNOTS ( 'NONE', 3,
 ( #60754, #24102, #23798, #18803 ),
 .UNSPECIFIED., .F., .F.,
 ( 4, 4 ),
 ( 0.000000000000000000, 0.004444103432399266161 ),
 .UNSPECIFIED. ) ;
#1734=EDGE_CURVE ( 'NONE', #12769, #55806, #53791, .T. ) ;
#1740=VECTOR ( 'NONE', #39786, 1000.000000000000114 ) ;
#1743=CARTESIAN_POINT ( 'NONE',  ( 0.7948878604505665857, 48.35174766440331240, 8.532710301907952655 ) ) ;
#1744=VERTEX_POINT ( 'NONE', #56130 ) ;
#1745=ORIENTED_EDGE ( 'NONE', *, *, #28623, .F. ) ;
#1750=CARTESIAN_POINT ( 'NONE',  ( -2.739355103387247858, -7.962282735395077360, 12.62733624295506196 ) ) ;
#1756=ADVANCED_FACE ( 'NONE', ( #46456 ), #56058, .F. ) ;
#1760=CARTESIAN_POINT ( 'NONE',  ( 0.6026112563231247332, 37.27953482426413245, 31.96525110476507692 ) ) ;
#1761=EDGE_CURVE ( 'NONE', #41223, #46515, #2321, .T. ) ;
#1762=ORIENTED_EDGE ( 'NONE', *, *, #37756, .F. ) ;
#1769=ORIENTED_EDGE ( 'NONE', *, *, #21092, .F. ) ;
#1781=CARTESIAN_POINT ( 'NONE',  ( 0.1140933569871963732, 39.91767626351668241, -18.80236878175147552 ) ) ;
#1784=B_SPLINE_CURVE_WITH_KNOTS ( 'NONE', 3,
 ( #42064, #61118, #47351, #56421, #42363, #61418, #18535, #37663, #13856, #32960, #52032, #9128, #28234, #36356, #46671, #32258 ),
 .UNSPECIFIED., .F., .F.,
 ( 4, 3, 3, 3, 3, 4 ),
 ( 2.194378057379452319E-17, 0.0002612764279487688802, 0.0003919131003184762093, 0.0005225497727000617864, 0.0007837925190632418848, 0.001045051706266715867 ),
 .UNSPECIFIED. ) ;
#1791=CARTESIAN_POINT ( 'NONE',  ( 0.5980271706414711508, -42.44486003424485432, -24.70795619866254711 ) ) ;
#1793=CARTESIAN_POINT ( 'NONE',  ( 0.1152339509894530906, 43.35263776105328759, 8.215320420661617717 ) ) ;
#1797=B_SPLINE_CURVE_WITH_KNOTS ( 'NONE', 3,
 ( #16475, #31496, #50903, #12111 ),
 .UNSPECIFIED., .F., .F.,
 ( 4, 4 ),
 ( 2.093184199687144787E-17, 0.004559932413162186803 ),
 .UNSPECIFIED. ) ;
#1800=CARTESIAN_POINT ( 'NONE',  ( 1.112077966505211624, 30.40372978055294695, 31.91619558405531976 ) ) ;
#1801=CARTESIAN_POINT ( 'NONE',  ( 4.553261556744873317, -33.59363643963353496, -28.30206982864260112 ) ) ;
#1807=VECTOR ( 'NONE', #52222, 999.9999999999998863 ) ;
#1811=EDGE_CURVE ( 'NONE', #50189, #49082, #41196, .T. ) ;
#1813=CARTESIAN_POINT ( 'NONE',  ( 0.6029443199889047422, -19.87788362468473835, -44.90442499863340231 ) ) ;
#1814=CARTESIAN_POINT ( 'NONE',  ( 0.1155031312995260795, -42.72350491080801760, 11.02922303101952117 ) ) ;
#1820=CARTESIAN_POINT ( 'NONE',  ( 0.1156867017252034419, 20.51982528184129606, -39.06250859427608191 ) ) ;
#1823=CARTESIAN_POINT ( 'NONE',  ( 0.1152809850208375425, 29.50062020599969514, 32.81247765639037084 ) ) ;
#1830=CARTESIAN_POINT ( 'NONE',  ( 0.6253024248130502061, 27.52858932731207631, 40.66473898927478814 ) ) ;
#1834=VERTEX_POINT ( 'NONE', #25330 ) ;
#1842=CARTESIAN_POINT ( 'NONE',  ( 4.553261556744875094, -14.95853073564453339, -41.30111286702108941 ) ) ;
#1846=CARTESIAN_POINT ( 'NONE',  ( 1.834102595619085507, -44.02840226159792536, 1.302896445847945950 ) ) ;
#1847=CARTESIAN_POINT ( 'NONE',  ( 4.335381028904201628, 39.85754067141741785, 28.48040202122594167 ) ) ;
#1848=VERTEX_POINT ( 'NONE', #5579 ) ;
#1852=CARTESIAN_POINT ( 'NONE',  ( 0.6039202388192952409, -35.39742030260028827, 34.03801329058516245 ) ) ;
#1857=ADVANCED_FACE ( 'NONE', ( #25637 ), #54862, .F. ) ;
#1875=CARTESIAN_POINT ( 'NONE',  ( 0.8744876279028306332, -34.64280934553560343, 34.78829991575276637 ) ) ;
#1878=DIRECTION ( 'NONE',  ( 0.09722883295013597105, 0.9927043560032283720, 0.07130649069594115208 ) ) ;
#1880=ORIENTED_EDGE ( 'NONE', *, *, #27271, .F. ) ;
#1884=CARTESIAN_POINT ( 'NONE',  ( 0.8744876279028306332, 48.35212675551500183, 8.510105087371359289 ) ) ;
#1888=EDGE_CURVE ( 'NONE', #41892, #30382, #23864, .T. ) ;
#1892=ADVANCED_FACE ( 'NONE', ( #45389 ), #39356, .F. ) ;
#1905=( BOUNDED_SURFACE ( )  B_SPLINE_SURFACE ( 3, 1, ( 
 ( #18082, #61273 ),
 ( #3640, #8981 ),
 ( #14012, #28390 ),
 ( #9586, #42828 ) ),
 .UNSPECIFIED., .F., .F., .F. ) 
 B_SPLINE_SURFACE_WITH_KNOTS ( ( 4, 4 ),
 ( 2, 2 ),
 ( 0.000000000000000000, 1.000000000000000000 ),
 ( 0.000000000000000000, 1.000000000000000000 ),
 .UNSPECIFIED. ) 
 GEOMETRIC_REPRESENTATION_ITEM ( )  RATIONAL_B_SPLINE_SURFACE ( (
 ( 1.000000000000000000, 1.000000000000000000),
 ( 0.9953485035131437453, 0.8621029689291515030),
 ( 0.9953485035131437453, 0.8621029689291515030),
 ( 1.000000000000000000, 1.000000000000000000) ) ) 
 REPRESENTATION_ITEM ( '' )  SURFACE ( )  );
#1907=CARTESIAN_POINT ( 'NONE',  ( 0.1158516988532803660, 37.00677167196558059, 24.03000227323755666 ) ) ;
#1910=CARTESIAN_POINT ( 'NONE',  ( 1.834102595619085507, -2.713406789205373038, -43.96402129530440561 ) ) ;
#1912=CARTESIAN_POINT ( 'NONE',  ( 2.706805983486680223, -42.11943299225157489, 12.75654646567733153 ) ) ;
#1914=ORIENTED_EDGE ( 'NONE', *, *, #48852, .T. ) ;
#1915=CARTESIAN_POINT ( 'NONE',  ( 0.5980271706414734822, 48.33586592461342235, 8.700190122029439976 ) ) ;
#1916=CARTESIAN_POINT ( 'NONE',  ( 0.7242486021783884897, 44.58864233489314444, -20.56366789035821441 ) ) ;
#1920=CARTESIAN_POINT ( 'NONE',  ( 0.2940133293163006978, 3.434477758206464948, 43.98232499659869177 ) ) ;
#1921=CARTESIAN_POINT ( 'NONE',  ( 50.15577769773999961, 1.224646799147353256E-15, -10.00000000000000000 ) ) ;
#1922=ORIENTED_EDGE ( 'NONE', *, *, #59059, .F. ) ;
#1925=ORIENTED_EDGE ( 'NONE', *, *, #58983, .T. ) ;
#1933=AXIS2_PLACEMENT_3D ( 'NONE', #51157, #46486, #60861 ) ;
#1937=CARTESIAN_POINT ( 'NONE',  ( 0.1154773475650540254, 43.27575480954529752, -8.611194789937002270 ) ) ;
#1942=VERTEX_POINT ( 'NONE', #41308 ) ;
#1948=CARTESIAN_POINT ( 'NONE',  ( 2.533389852662419894, -42.95075564070678098, -9.627207363816017605 ) ) ;
#1958=CARTESIAN_POINT ( 'NONE',  ( 0.8753041380234465318, 49.05142151719384458, -2.257515230414630203 ) ) ;
#1961=CARTESIAN_POINT ( 'NONE',  ( 2.706805983486679779, -41.38491211916735324, -14.96880630539891399 ) ) ;
#1970=CARTESIAN_POINT ( 'NONE',  ( 0.5549461598389364703, 41.57286777559680502, -14.72801277768148509 ) ) ;
#1974=CARTESIAN_POINT ( 'NONE',  ( -6.057079549204054558, -17.34624894862984235, -8.362946760077846875 ) ) ;
#1977=CARTESIAN_POINT ( 'NONE',  ( 0.5997462898726536595, 48.97040376101519144, -3.667585803694250135 ) ) ;
#1980=VERTEX_POINT ( 'NONE', #40386 ) ;
#1984=CARTESIAN_POINT ( 'NONE',  ( 0.9268187852002115479, 3.245393988162387000, -43.96841765142595904 ) ) ;
#1986=VERTEX_POINT ( 'NONE', #16555 ) ;
#1991=CARTESIAN_POINT ( 'NONE',  ( -6.063463321072278589, -18.89860197674386200, -3.696389563355431562 ) ) ;
#1998=CARTESIAN_POINT ( 'NONE',  ( 0.2940133293163009753, -2.218054141563334802, 44.06042198394310816 ) ) ;
#2007=CARTESIAN_POINT ( 'NONE',  ( 0.6029442701453591180, -7.751548539172897989, 48.49184179223475155 ) ) ;
#2008=CARTESIAN_POINT ( 'NONE',  ( 0.5987334363312688534, -8.434467551029658949, 48.37791503984752239 ) ) ;
#2010=ORIENTED_EDGE ( 'NONE', *, *, #41099, .T. ) ;
#2012=CARTESIAN_POINT ( 'NONE',  ( 0.6024113833632039894, -35.42741226244881858, 34.00647481711914111 ) ) ;
#2013=( BOUNDED_SURFACE ( )  B_SPLINE_SURFACE ( 3, 1, ( 
 ( #46893, #3929 ),
 ( #36562, #18375 ),
 ( #60325, #31533 ),
 ( #32787, #51864 ) ),
 .UNSPECIFIED., .F., .F., .F. ) 
 B_SPLINE_SURFACE_WITH_KNOTS ( ( 4, 4 ),
 ( 2, 2 ),
 ( 0.000000000000000000, 1.000000000000000000 ),
 ( 0.000000000000000000, 1.000000000000000000 ),
 .UNSPECIFIED. ) 
 GEOMETRIC_REPRESENTATION_ITEM ( )  RATIONAL_B_SPLINE_SURFACE ( (
 ( 1.000000000000000000, 1.000000000000000000),
 ( 0.9953485035131437453, 0.8621029689291515030),
 ( 0.9953485035131437453, 0.8621029689291515030),
 ( 1.000000000000000000, 1.000000000000000000) ) ) 
 REPRESENTATION_ITEM ( '' )  SURFACE ( )  );
#2017=CARTESIAN_POINT ( 'NONE',  ( 0.8744876279028263033, 23.49358985382666631, -43.10917867646825385 ) ) ;
#2029=CARTESIAN_POINT ( 'NONE',  ( 2.706805983486680223, 21.80916877957961475, 38.22481223581831244 ) ) ;
#2033=CARTESIAN_POINT ( 'NONE',  ( -6.063463321072278589, -19.21812676738395353, 1.218218384457574688 ) ) ;
#2036=CARTESIAN_POINT ( 'NONE',  ( 0.3676999524040323597, 16.00695768809450215, -41.10629986868669761 ) ) ;
#2038=ADVANCED_FACE ( 'NONE', ( #56602 ), #56882, .F. ) ;
#2040=CARTESIAN_POINT ( 'NONE',  ( 4.553261556744875094, -3.993093339916522488, -43.74465420371214464 ) ) ;
#2043=CARTESIAN_POINT ( 'NONE',  ( -6.079354080745853928, 18.62591919961132447, 4.885497847478016631 ) ) ;
#2050=ORIENTED_EDGE ( 'NONE', *, *, #33871, .F. ) ;
#2053=CARTESIAN_POINT ( 'NONE',  ( 0.08486401232817714080, 0.000000000000000000, 44.12552607296456131 ) ) ;
#2056=EDGE_LOOP ( 'NONE', ( #10118, #29574, #481, #3544 ) ) ;
#2057=LINE ( 'NONE', #45626, #49516 ) ;
#2064=CARTESIAN_POINT ( 'NONE',  ( 0.6029442701453591180, 37.44910241782426397, 31.76649104414250147 ) ) ;
#2070=LINE ( 'NONE', #31847, #33940 ) ;
#2074=CARTESIAN_POINT ( 'NONE',  ( -6.079354080745853928, 15.43131048252518944, -11.51814273396845323 ) ) ;
#2083=DIRECTION ( 'NONE',  ( 0.09722883295013594329, 0.8382159563662527901, 0.5366009360187167232 ) ) ;
#2087=( BOUNDED_SURFACE ( )  B_SPLINE_SURFACE ( 3, 1, ( 
 ( #48643, #44593 ),
 ( #39275, #10756 ),
 ( #5094, #29846 ),
 ( #714, #19855 ) ),
 .UNSPECIFIED., .F., .F., .F. ) 
 B_SPLINE_SURFACE_WITH_KNOTS ( ( 4, 4 ),
 ( 2, 2 ),
 ( 0.000000000000000000, 1.000000000000000000 ),
 ( 0.000000000000000000, 1.000000000000000000 ),
 .UNSPECIFIED. ) 
 GEOMETRIC_REPRESENTATION_ITEM ( )  RATIONAL_B_SPLINE_SURFACE ( (
 ( 1.000000000000000000, 1.000000000000000000),
 ( 0.9754377213608244057, 0.9999580625633939235),
 ( 0.9754377213608244057, 0.9999580625633939235),
 ( 1.000000000000000000, 1.000000000000000000) ) ) 
 REPRESENTATION_ITEM ( '' )  SURFACE ( )  );
#2094=CARTESIAN_POINT ( 'NONE',  ( -2.601141883200665639, 5.573165628699342733, -13.84684990690925943 ) ) ;
#2098=CARTESIAN_POINT ( 'NONE',  ( 0.1129192098497447394, 14.78321943369649283, -41.57412910645673776 ) ) ;
#2102=CARTESIAN_POINT ( 'NONE',  ( 1.296416391601052487, 30.44260198708226639, 31.86777931284597187 ) ) ;
#2106=CARTESIAN_POINT ( 'NONE',  ( 0.7044674535453004927, 40.69315356317313359, -27.49308960256953682 ) ) ;
#2108=EDGE_CURVE ( 'NONE', #12977, #14660, #15667, .T. ) ;
#2111=ORIENTED_EDGE ( 'NONE', *, *, #18060, .T. ) ;
#2112=EDGE_CURVE ( 'NONE', #22007, #56473, #2202, .T. ) ;
#2114=CARTESIAN_POINT ( 'NONE',  ( 0.6016117650947691020, 44.39439963300118563, 20.99257810441308081 ) ) ;
#2117=CARTESIAN_POINT ( 'NONE',  ( 5.901764892641307547, 13.89173340560966352, 46.95754689533032433 ) ) ;
#2134=CARTESIAN_POINT ( 'NONE',  ( 3.678748215320120529, -21.50126778036843334, -44.00350324845027927 ) ) ;
#2135=CARTESIAN_POINT ( 'NONE',  ( 4.975610109902397937, -5.269241389991576874, 48.62802178077752302 ) ) ;
#2139=CARTESIAN_POINT ( 'NONE',  ( 0.6016118706126978299, 28.38023484439529298, -40.07634370749035213 ) ) ;
#2145=CARTESIAN_POINT ( 'NONE',  ( 4.975610109902397937, 34.73360008816180056, -34.43873447229760387 ) ) ;
#2151=CARTESIAN_POINT ( 'NONE',  ( 0.1158516988532803660, 20.45274844683495985, 39.09766284323509922 ) ) ;
#2153=ORIENTED_EDGE ( 'NONE', *, *, #33275, .F. ) ;
#2155=VECTOR ( 'NONE', #44445, 1000.000000000000114 ) ;
#2159=CARTESIAN_POINT ( 'NONE',  ( 0.1156867017252034557, -1.539136465540023035, 44.09732266493773523 ) ) ;
#2165=ORIENTED_EDGE ( 'NONE', *, *, #31844, .T. ) ;
#2167=CARTESIAN_POINT ( 'NONE',  ( -6.078075953587585900, -17.35139778253845932, 8.350099953848184597 ) ) ;
#2169=CARTESIAN_POINT ( 'NONE',  ( 0.6026112563231247332, -25.30784345655240486, -42.08389305283965598 ) ) ;
#2174=CARTESIAN_POINT ( 'NONE',  ( -6.072942160501519027, 16.78547611690390440, -9.436734277167554197 ) ) ;
#2175=VERTEX_POINT ( 'NONE', #39691 ) ;
#2178=CARTESIAN_POINT ( 'NONE',  ( 0.5980271706414711508, -35.76345691233170498, 33.66042769367994936 ) ) ;
#2189=DIRECTION ( 'NONE',  ( -1.000000000000000000, -0.000000000000000000, -0.000000000000000000 ) ) ;
#2193=ORIENTED_EDGE ( 'NONE', *, *, #58111, .F. ) ;
#2196=CARTESIAN_POINT ( 'NONE',  ( 0.1140933569871965397, -35.58732562960275914, 26.08624550633002315 ) ) ;
#2200=ADVANCED_FACE ( 'NONE', ( #26480 ), #20861, .F. ) ;
#2201=CARTESIAN_POINT ( 'NONE',  ( 0.1135584504625008900, -43.70468290122602895, -6.070646146707417756 ) ) ;
#2202=B_SPLINE_CURVE_WITH_KNOTS ( 'NONE', 3,
 ( #33752, #5506, #10545, #43465, #1127, #19963, #53132, #29640, #34988, #20265, #11168, #29037, #34666, #49063, #25254, #5808 ),
 .UNSPECIFIED., .F., .F.,
 ( 4, 3, 3, 3, 3, 4 ),
 ( 2.194378057379452319E-17, 0.0002612764279487765238, 0.0003919131003184808172, 0.0005225497727000681832, 0.0007837925190632486069, 0.001045051706266716300 ),
 .UNSPECIFIED. ) ;
#2205=CIRCLE ( 'NONE', #37265, 43.92652462719577500 ) ;
#2208=CARTESIAN_POINT ( 'NONE',  ( 0.1157506346131639274, 37.03045437084058733, 23.99345971076133566 ) ) ;
#2209=VERTEX_POINT ( 'NONE', #7997 ) ;
#2210=CARTESIAN_POINT ( 'NONE',  ( -2.739355103387247858, -2.641750642666087945, 14.69247155835226870 ) ) ;
#2213=ORIENTED_EDGE ( 'NONE', *, *, #10690, .F. ) ;
#2216=B_SPLINE_CURVE_WITH_KNOTS ( 'NONE', 3,
 ( #11329, #16334, #49530, #6585 ),
 .UNSPECIFIED., .F., .F.,
 ( 4, 4 ),
 ( 0.000000000000000000, 0.004444103432399266161 ),
 .UNSPECIFIED. ) ;
#2217=DIRECTION ( 'NONE',  ( 1.000000000000000000, 0.000000000000000000, 0.000000000000000000 ) ) ;
#2222=VERTEX_POINT ( 'NONE', #50589 ) ;
#2223=CARTESIAN_POINT ( 'NONE',  ( 0.6024113833632039894, 10.71508360385645631, 47.92419902787352015 ) ) ;
#2228=VERTEX_POINT ( 'NONE', #27108 ) ;
#2231=B_SPLINE_CURVE_WITH_KNOTS ( 'NONE', 3,
 ( #2235, #20754, #44274, #6605, #5685, #58947 ),
 .UNSPECIFIED., .F., .F.,
 ( 4, 2, 4 ),
 ( 2.504504451673693158E-17, 0.0002293755540694321588, 0.0004587511081388392724 ),
 .UNSPECIFIED. ) ;
#2233=ORIENTED_EDGE ( 'NONE', *, *, #57194, .T. ) ;
#2235=CARTESIAN_POINT ( 'NONE',  ( 0.1129192098497455998, 37.24220309526837980, -23.66368729500826618 ) ) ;
#2239=EDGE_CURVE ( 'NONE', #28569, #2327, #55116, .T. ) ;
#2242=CARTESIAN_POINT ( 'NONE',  ( 0.1129192098497447394, 4.719118110134695954, 43.87119455916095490 ) ) ;
#2246=ORIENTED_EDGE ( 'NONE', *, *, #15858, .T. ) ;
#2247=CIRCLE ( 'NONE', #57236, 48.91267123290010943 ) ;
#2251=EDGE_CURVE ( 'NONE', #24292, #47165, #45934, .T. ) ;
#2252=CARTESIAN_POINT ( 'NONE',  ( 3.559346040607745287, 13.24178938536624450, -41.92952772707547382 ) ) ;
#2259=ORIENTED_EDGE ( 'NONE', *, *, #36823, .F. ) ;
#2263=CARTESIAN_POINT ( 'NONE',  ( 0.6252788684277227338, -49.10165704764342820, 0.6867360113443859992 ) ) ;
#2264=( BOUNDED_SURFACE ( )  B_SPLINE_SURFACE ( 3, 1, ( 
 ( #50633, #49720 ),
 ( #17448, #26844 ),
 ( #50036, #40356 ),
 ( #11846, #11518 ) ),
 .UNSPECIFIED., .F., .F., .F. ) 
 B_SPLINE_SURFACE_WITH_KNOTS ( ( 4, 4 ),
 ( 2, 2 ),
 ( 0.000000000000000000, 1.000000000000000000 ),
 ( 0.000000000000000000, 1.000000000000000000 ),
 .UNSPECIFIED. ) 
 GEOMETRIC_REPRESENTATION_ITEM ( )  RATIONAL_B_SPLINE_SURFACE ( (
 ( 1.000000000000000000, 1.000000000000000000),
 ( 0.9754377213608244057, 0.9999580625633939235),
 ( 0.9754377213608244057, 0.9999580625633939235),
 ( 1.000000000000000000, 1.000000000000000000) ) ) 
 REPRESENTATION_ITEM ( '' )  SURFACE ( )  );
#2266=CARTESIAN_POINT ( 'NONE',  ( 3.727782113643637096, -14.54354975905613045, -41.48810596197220946 ) ) ;
#2268=CARTESIAN_POINT ( 'NONE',  ( 0.8744876279028306332, 44.61213666265828692, 20.49651952824657286 ) ) ;
#2274=CARTESIAN_POINT ( 'NONE',  ( 0.8744876279028306332, 44.61213666265828692, 20.49651952824657286 ) ) ;
#2278=( BOUNDED_SURFACE ( )  B_SPLINE_SURFACE ( 3, 1, ( 
 ( #43301, #18874 ),
 ( #43613, #38297 ),
 ( #52975, #10078 ),
 ( #19796, #33283 ) ),
 .UNSPECIFIED., .F., .F., .F. ) 
 B_SPLINE_SURFACE_WITH_KNOTS ( ( 4, 4 ),
 ( 2, 2 ),
 ( 0.000000000000000000, 1.000000000000000000 ),
 ( 0.000000000000000000, 1.000000000000000000 ),
 .UNSPECIFIED. ) 
 GEOMETRIC_REPRESENTATION_ITEM ( )  RATIONAL_B_SPLINE_SURFACE ( (
 ( 1.000000000000000000, 1.000000000000000000),
 ( 0.9754377213608244057, 0.9999580625633939235),
 ( 0.9754377213608244057, 0.9999580625633939235),
 ( 1.000000000000000000, 1.000000000000000000) ) ) 
 REPRESENTATION_ITEM ( '' )  SURFACE ( )  );
#2282=CARTESIAN_POINT ( 'NONE',  ( 0.3676999524040323597, 29.04098611012938136, 33.20499524279608750 ) ) ;
#2283=B_SPLINE_CURVE_WITH_KNOTS ( 'NONE', 3,
 ( #4332, #23466, #42597, #18788 ),
 .UNSPECIFIED., .F., .F.,
 ( 4, 4 ),
 ( 0.000000000000000000, 0.005013413432710145910 ),
 .UNSPECIFIED. ) ;
#2290=VERTEX_POINT ( 'NONE', #13330 ) ;
#2293=CARTESIAN_POINT ( 'NONE',  ( 4.226256110419178924, -29.84627472560808314, 32.24945170062143518 ) ) ;
#2298=ORIENTED_EDGE ( 'NONE', *, *, #43067, .F. ) ;
#2306=CARTESIAN_POINT ( 'NONE',  ( -6.079354080745853928, -16.13757513887051687, 10.50579001719862404 ) ) ;
#2310=VERTEX_POINT ( 'NONE', #13639 ) ;
#2316=CARTESIAN_POINT ( 'NONE',  ( 0.6021447746440204973, -48.67017425780974094, 6.538751930064458762 ) ) ;
#2318=EDGE_CURVE ( 'NONE', #7116, #10837, #26074, .T. ) ;
#2320=CARTESIAN_POINT ( 'NONE',  ( 4.390527457369401532, -43.82188413991281095, -3.134933341664180695 ) ) ;
#2321=B_SPLINE_CURVE_WITH_KNOTS ( 'NONE', 3,
 ( #57578, #22634, #46153, #3200 ),
 .UNSPECIFIED., .F., .F.,
 ( 4, 4 ),
 ( 0.000000000000000000, 0.002122961284640939757 ),
 .UNSPECIFIED. ) ;
#2325=CARTESIAN_POINT ( 'NONE',  ( 0.1149546198390366952, -31.50544959404307122, -30.89260770638230014 ) ) ;
#2327=VERTEX_POINT ( 'NONE', #23037 ) ;
#2336=DIRECTION ( 'NONE',  ( -1.000000000000000000, 0.000000000000000000, 0.000000000000000000 ) ) ;
#2342=CARTESIAN_POINT ( 'NONE',  ( 1.830465331921977246, -36.02667829546079759, 25.34668630953094492 ) ) ;
#2352=CARTESIAN_POINT ( 'NONE',  ( 4.694002226626920127, -40.92287315640982115, 20.08987864748135976 ) ) ;
#2358=PRODUCT_CONTEXT ( 'NONE', #36374, 'mechanical' ) ;
#2359=CARTESIAN_POINT ( 'NONE',  ( 2.299746137290200387, 23.81427056122728914, 42.86212611762045555 ) ) ;
#2365=VERTEX_POINT ( 'NONE', #42769 ) ;
#2367=CARTESIAN_POINT ( 'NONE',  ( -6.063463321072276813, 0.6016212027212631819, -19.24729862624639054 ) ) ;
#2370=VERTEX_POINT ( 'NONE', #61825 ) ;
#2371=CARTESIAN_POINT ( 'NONE',  ( 0.5997462898726536595, -47.36625756029525292, -12.96106765957508244 ) ) ;
#2378=CARTESIAN_POINT ( 'NONE',  ( 0.6016118706126977189, 37.16599942407935231, 32.09734477481374881 ) ) ;
#2382=CARTESIAN_POINT ( 'NONE',  ( -6.078457390727109555, 9.978433202401499003, -16.46892169702434572 ) ) ;
#2385=SHAPE_REPRESENTATION ( 'straight bevel gear(wobble in)_iso_ISO - Straight bevel gear 2M 49GT 48PT 20PA 5FW ---49O1H50MD20.0S1', ( #14677 ), #61711 ) ;
#2386=CARTESIAN_POINT ( 'NONE',  ( 0.2940135542859035889, 29.05872894121237238, -33.19383709384268855 ) ) ;
#2388=ADVANCED_FACE ( 'NONE', ( #57131 ), #18118, .F. ) ;
#2389=ORIENTED_EDGE ( 'NONE', *, *, #45161, .F. ) ;
#2392=B_SPLINE_CURVE_WITH_KNOTS ( 'NONE', 3,
 ( #32218, #26574, #61004, #55996 ),
 .UNSPECIFIED., .F., .F.,
 ( 4, 4 ),
 ( 0.000000000000000000, 0.004444103432399267029 ),
 .UNSPECIFIED. ) ;
#2398=CARTESIAN_POINT ( 'NONE',  ( 2.299746137290200387, -42.07681931141168974, 25.17583393496532551 ) ) ;
#2401=B_SPLINE_CURVE_WITH_KNOTS ( 'NONE', 3,
 ( #28633, #29248, #28030, #61819, #738, #47446 ),
 .UNSPECIFIED., .F., .F.,
 ( 4, 2, 4 ),
 ( 1.029992063861229212E-18, 0.0002293801035737083962, 0.0004587602071474157625 ),
 .UNSPECIFIED. ) ;
#2406=VERTEX_POINT ( 'NONE', #24878 ) ;
#2411=CARTESIAN_POINT ( 'NONE',  ( 0.1149546198390366675, -43.79613980524445793, 5.370726504180043825 ) ) ;
#2412=ORIENTED_EDGE ( 'NONE', *, *, #45028, .F. ) ;
#2413=CARTESIAN_POINT ( 'NONE',  ( 0.1139756605157202646, -27.82078886304557130, -34.24848794812498198 ) ) ;
#2416=VERTEX_POINT ( 'NONE', #20482 ) ;
#2417=EDGE_LOOP ( 'NONE', ( #36052, #5937, #36617, #30490 ) ) ;
#2423=CARTESIAN_POINT ( 'NONE',  ( 0.1365634738349400801, 33.18118851476105391, 29.08386749335686261 ) ) ;
#2424=ORIENTED_EDGE ( 'NONE', *, *, #32462, .F. ) ;
#2428=CARTESIAN_POINT ( 'NONE',  ( 0.7044674535453004927, -43.19749584530687514, -23.36191506502847304 ) ) ;
#2431=CARTESIAN_POINT ( 'NONE',  ( 0.1135584504625008206, -42.78871615279810214, 10.77394181024413378 ) ) ;
#2433=CARTESIAN_POINT ( 'NONE',  ( 4.834790513006553603, 33.61992680604592465, 33.20075093247886144 ) ) ;
#2437=ADVANCED_FACE ( 'NONE', ( #14568 ), #49139, .F. ) ;
#2445=CARTESIAN_POINT ( 'NONE',  ( 4.553261556744875094, 17.57396821678876364, 40.25785894628445760 ) ) ;
#2447=CARTESIAN_POINT ( 'NONE',  ( 0.5987334363312687424, 40.82324421486000432, 27.29515778019931460 ) ) ;
#2454=CARTESIAN_POINT ( 'NONE',  ( 0.1158516988532803244, -38.47034482238524333, -21.60959805455839700 ) ) ;
#2455=CARTESIAN_POINT ( 'NONE',  ( 0.8753041380234524160, 32.34805756193409110, -36.94240787824717387 ) ) ;
#2461=( BOUNDED_SURFACE ( )  B_SPLINE_SURFACE ( 3, 1, ( 
 ( #37914, #28466 ),
 ( #9057, #41990 ),
 ( #47593, #47283 ),
 ( #46993, #4634 ) ),
 .UNSPECIFIED., .F., .F., .F. ) 
 B_SPLINE_SURFACE_WITH_KNOTS ( ( 4, 4 ),
 ( 2, 2 ),
 ( 0.000000000000000000, 1.000000000000000000 ),
 ( 0.000000000000000000, 1.000000000000000000 ),
 .UNSPECIFIED. ) 
 GEOMETRIC_REPRESENTATION_ITEM ( )  RATIONAL_B_SPLINE_SURFACE ( (
 ( 1.000000000000000000, 1.000000000000000000),
 ( 0.7211978278499968642, 0.9934217856018975334),
 ( 0.7211978278499968642, 0.9934217856018975334),
 ( 1.000000000000000000, 1.000000000000000000) ) ) 
 REPRESENTATION_ITEM ( '' )  SURFACE ( )  );
#2465=EDGE_CURVE ( 'NONE', #56737, #40264, #39611, .T. ) ;
#2466=EDGE_LOOP ( 'NONE', ( #42337, #3518, #28965, #17680 ) ) ;
#2470=CARTESIAN_POINT ( 'NONE',  ( 0.8753041380234524160, -26.21158409634513475, -41.52217705074249210 ) ) ;
#2479=FACE_OUTER_BOUND ( 'NONE', #13500, .T. ) ;
#2511=ORIENTED_EDGE ( 'NONE', *, *, #55388, .F. ) ;
#2513=CARTESIAN_POINT ( 'NONE',  ( 0.8753041380234471980, -0.6841799139044226763, -49.09857661601188994 ) ) ;
#2515=CARTESIAN_POINT ( 'NONE',  ( 0.5980271706414711508, 4.018631420204758165, 48.94792992916254093 ) ) ;
#2521=CARTESIAN_POINT ( 'NONE',  ( 0.8753041380234524160, 5.600023814135298927, 48.78296896616787848 ) ) ;
#2524=EDGE_CURVE ( 'NONE', #40320, #18600, #32098, .T. ) ;
#2525=B_SPLINE_CURVE_WITH_KNOTS ( 'NONE', 3,
 ( #45898, #28000, #55877, #41193, #42428, #23005 ),
 .UNSPECIFIED., .F., .F.,
 ( 4, 2, 4 ),
 ( 0.000000000000000000, 0.0002447195606305742582, 0.0004894391212611485164 ),
 .UNSPECIFIED. ) ;
#2528=FACE_OUTER_BOUND ( 'NONE', #34304, .T. ) ;
#2531=CARTESIAN_POINT ( 'NONE',  ( 3.390910168358336918, -3.377210997459680453, -43.84850718567593475 ) ) ;
#2534=EDGE_LOOP ( 'NONE', ( #50849, #28925, #12291, #26740 ) ) ;
#2541=DIRECTION ( 'NONE',  ( 1.000000000000000000, 0.000000000000000000, 0.000000000000000000 ) ) ;
#2544=ORIENTED_EDGE ( 'NONE', *, *, #32151, .T. ) ;
#2546=EDGE_CURVE ( 'NONE', #35321, #42399, #32154, .T. ) ;
#2549=CARTESIAN_POINT ( 'NONE',  ( 0.1140933569871963871, 44.00767033400067874, 3.205448776352883833 ) ) ;
#2553=CARTESIAN_POINT ( 'NONE',  ( 0.6000166863083106206, -43.04473087057989744, -23.64264422580097502 ) ) ;
#2555=CARTESIAN_POINT ( 'NONE',  ( 0.5987334308729320709, 40.82324396785260490, -27.29515815141791535 ) ) ;
#2570=CARTESIAN_POINT ( 'NONE',  ( -6.078726893082806448, 9.979253153318998315, -16.46841060244408794 ) ) ;
#2578=CARTESIAN_POINT ( 'NONE',  ( 3.559346040607745287, 42.33240525468902149, 11.89107845801906649 ) ) ;
#2582=CARTESIAN_POINT ( 'NONE',  ( 0.7413678028165008316, -13.43842184872795897, -41.99874890976961694 ) ) ;
#2594=CARTESIAN_POINT ( 'NONE',  ( -6.072942160501519027, -17.34299816270043593, -8.368068894170846761 ) ) ;
#2604=CARTESIAN_POINT ( 'NONE',  ( 0.3676999524040366896, 3.413584541509296688, -43.98065510995495941 ) ) ;
#2609=CARTESIAN_POINT ( 'NONE',  ( 0.5997462898726536595, 37.05192695178169515, -32.22896739432000146 ) ) ;
#2613=EDGE_CURVE ( 'NONE', #25770, #53648, #44757, .T. ) ;
#2621=CARTESIAN_POINT ( 'NONE',  ( 4.553261556744875094, 0.000000000000000000, 0.000000000000000000 ) ) ;
#2622=CARTESIAN_POINT ( 'NONE',  ( 0.1155031312995260795, 15.39696621848024272, -41.35063559123108945 ) ) ;
#2624=AXIS2_PLACEMENT_3D ( 'NONE', #35525, #55211, #22033 ) ;
#2627=CARTESIAN_POINT ( 'NONE',  ( 0.6000166863083090663, -1.051715750664325322, 49.09905676984292455 ) ) ;
#2629=CARTESIAN_POINT ( 'NONE',  ( 0.5997462898726536595, -48.76843890605309184, 5.761162800240605897 ) ) ;
#2631=CARTESIAN_POINT ( 'NONE',  ( 0.6000166863083090663, -39.04292238714170793, 29.79049669240313847 ) ) ;
#2640=B_SPLINE_CURVE_WITH_KNOTS ( 'NONE', 3,
 ( #17185, #41314, #60370, #55675 ),
 .UNSPECIFIED., .F., .F.,
 ( 4, 4 ),
 ( 2.170598744017606518E-17, 0.004559932413162186803 ),
 .UNSPECIFIED. ) ;
#2647=DIRECTION ( 'NONE',  ( 1.000000000000000000, 0.000000000000000000, 0.000000000000000000 ) ) ;
#2648=CARTESIAN_POINT ( 'NONE',  ( -6.078075953587585900, 0.6118799989804611927, -19.24631853404654791 ) ) ;
#2649=CARTESIAN_POINT ( 'NONE',  ( -2.601141883200662974, -4.674544242619348644, -14.17547401652526418 ) ) ;
#2653=CARTESIAN_POINT ( 'NONE',  ( 1.296416391601053153, -32.42183002721205298, -29.85183933634123576 ) ) ;
#2655=CARTESIAN_POINT ( 'NONE',  ( 0.6008123274975391004, 41.39240128969535704, -26.42392224162195902 ) ) ;
#2663=CARTESIAN_POINT ( 'NONE',  ( 0.1149546198390366814, 44.05025956747236648, -2.553663458940844677 ) ) ;
#2664=CARTESIAN_POINT ( 'NONE',  ( 0.6039202388192952409, -47.45712035475593638, -12.62479467093234575 ) ) ;
#2669=CARTESIAN_POINT ( 'NONE',  ( 4.553261556744875094, 35.33793455049291765, -26.09156851415253087 ) ) ;
#2674=LINE ( 'NONE', #26806, #53327 ) ;
#2687=ORIENTED_EDGE ( 'NONE', *, *, #14205, .T. ) ;
#2692=CARTESIAN_POINT ( 'NONE',  ( 0.6029442701453591180, 49.01209361462912995, 3.059396128177434449 ) ) ;
#2698=ORIENTED_EDGE ( 'NONE', *, *, #34693, .T. ) ;
#2700=CARTESIAN_POINT ( 'NONE',  ( 0.6000166863083106206, -39.04292238714170793, 29.79049669240313847 ) ) ;
#2710=CARTESIAN_POINT ( 'NONE',  ( 0.1152339509894530906, 39.65706410057246245, -19.34579947632894914 ) ) ;
#2718=CARTESIAN_POINT ( 'NONE',  ( 0.7242486021783828276, 10.12618746694265326, 48.04655856310944984 ) ) ;
#2731=LINE ( 'NONE', #21549, #50799 ) ;
#2733=AXIS2_PLACEMENT_3D ( 'NONE', #54755, #9771, #40098 ) ;
#2740=CARTESIAN_POINT ( 'NONE',  ( 0.1129192098497455998, -42.80154921430131054, 10.72283417016679508 ) ) ;
#2752=CONICAL_SURFACE ( 'NONE', #47803, 43.92652462719577500, 1.486293639869522343 ) ;
#2756=CARTESIAN_POINT ( 'NONE',  ( 2.009741617377216460, 16.48880107124495709, 40.83654633849385363 ) ) ;
#2758=CARTESIAN_POINT ( 'NONE',  ( 3.678834586032787346, -33.87007428955444510, -35.37556271281655285 ) ) ;
#2771=CARTESIAN_POINT ( 'NONE',  ( 0.2279481005628808121, 43.97337838321706727, 3.584059240488700393 ) ) ;
#2773=CARTESIAN_POINT ( 'NONE',  ( 5.901764892641288895, 39.27045567455304820, 29.25444886769604480 ) ) ;
#2777=EDGE_LOOP ( 'NONE', ( #9549, #39429, #651, #25838 ) ) ;
#2779=VERTEX_POINT ( 'NONE', #47998 ) ;
#2782=B_SPLINE_CURVE_WITH_KNOTS ( 'NONE', 3,
 ( #46593, #12160, #3637, #22770, #41904, #31241 ),
 .UNSPECIFIED., .F., .F.,
 ( 4, 2, 4 ),
 ( 0.000000000000000000, 0.0002447195606305748545, 0.0004894391212611497090 ),
 .UNSPECIFIED. ) ;
#2792=CARTESIAN_POINT ( 'NONE',  ( 0.6021447746440204973, -25.67999315004615823, -41.85784383962067778 ) ) ;
#2796=CARTESIAN_POINT ( 'NONE',  ( 0.7413678028165009426, 5.162182772362567285, 43.79312686706632718 ) ) ;
#2805=ORIENTED_EDGE ( 'NONE', *, *, #14358, .T. ) ;
#2808=VECTOR ( 'NONE', #7267, 1000.000000000000341 ) ;
#2812=CARTESIAN_POINT ( 'NONE',  ( 0.2940133293163009753, 39.39157466687257170, 19.86314161562180303 ) ) ;
#2826=EDGE_CURVE ( 'NONE', #29313, #2228, #35102, .T. ) ;
#2829=CARTESIAN_POINT ( 'NONE',  ( 0.6008122571543325074, -49.10565090547250833, 0.4354303792607690515 ) ) ;
#2834=CARTESIAN_POINT ( 'NONE',  ( -6.072942160501519027, -16.14637491494731947, 10.49279464179969246 ) ) ;
#2838=CARTESIAN_POINT ( 'NONE',  ( -4.915099999999998914, 9.539392014169456147, 3.000000000000000000 ) ) ;
#2840=CARTESIAN_POINT ( 'NONE',  ( 1.834102595619085507, -42.25796167961109973, 12.42829109500596729 ) ) ;
#2843=CARTESIAN_POINT ( 'NONE',  ( 0.6029442701453591180, 44.20645327330244356, -21.38538552735501597 ) ) ;
#2854=CARTESIAN_POINT ( 'NONE',  ( 0.1156867017252034557, 44.02533442314084056, 2.951734440256478909 ) ) ;
#2856=CARTESIAN_POINT ( 'NONE',  ( -6.072942160501519027, -8.919639966878298409, 17.06587780192650072 ) ) ;
#2861=CARTESIAN_POINT ( 'NONE',  ( 2.079412931998606329, -0.01372856698588024484, 44.03669822926320165 ) ) ;
#2862=EDGE_LOOP ( 'NONE', ( #18275, #8560, #55564, #25530 ) ) ;
#2863=CARTESIAN_POINT ( 'NONE',  ( 0.1149546198390367369, 14.98162911076433090, 41.50298006421608932 ) ) ;
#2866=CARTESIAN_POINT ( 'NONE',  ( -6.078075953587585900, 3.078503442539340273, 19.00836633699512390 ) ) ;
#2868=ADVANCED_FACE ( 'NONE', ( #45471 ), #58897, .F. ) ;
#2879=CARTESIAN_POINT ( 'NONE',  ( 0.9268187852002115479, 8.841305801404754305, -43.19242577853983533 ) ) ;
#2886=CARTESIAN_POINT ( 'NONE',  ( 4.060580049360325461, 42.38076202783113899, 11.63351642022113630 ) ) ;
#2887=FACE_OUTER_BOUND ( 'NONE', #44367, .T. ) ;
#2892=EDGE_CURVE ( 'NONE', #53425, #45127, #11924, .T. ) ;
#2895=CARTESIAN_POINT ( 'NONE',  ( -6.077587904424778920, 19.09718056542704900, 2.468545289316316893 ) ) ;
#2898=CARTESIAN_POINT ( 'NONE',  ( 0.6000166863083090663, -20.35571918921453261, 44.69304395538859609 ) ) ;
#2913=CARTESIAN_POINT ( 'NONE',  ( 0.6008122571543326185, 16.55073813642506764, -46.23448515561519656 ) ) ;
#2918=ORIENTED_EDGE ( 'NONE', *, *, #34519, .T. ) ;
#2921=B_SPLINE_CURVE_WITH_KNOTS ( 'NONE', 3,
 ( #37702, #56766, #19207, #47388 ),
 .UNSPECIFIED., .F., .F.,
 ( 4, 4 ),
 ( 0.000000000000000000, 0.005013413432710141573 ),
 .UNSPECIFIED. ) ;
#2923=ORIENTED_EDGE ( 'NONE', *, *, #6537, .F. ) ;
#2930=( BOUNDED_SURFACE ( )  B_SPLINE_SURFACE ( 3, 1, ( 
 ( #53638, #48659 ),
 ( #44607, #48973 ),
 ( #11078, #16701 ),
 ( #15777, #1958 ) ),
 .UNSPECIFIED., .F., .F., .F. ) 
 B_SPLINE_SURFACE_WITH_KNOTS ( ( 4, 4 ),
 ( 2, 2 ),
 ( 0.000000000000000000, 1.000000000000000000 ),
 ( 0.000000000000000000, 1.000000000000000000 ),
 .UNSPECIFIED. ) 
 GEOMETRIC_REPRESENTATION_ITEM ( )  RATIONAL_B_SPLINE_SURFACE ( (
 ( 1.000000000000000000, 1.000000000000000000),
 ( 0.9953485035131437453, 0.8621029689291523912),
 ( 0.9953485035131437453, 0.8621029689291523912),
 ( 1.000000000000000000, 1.000000000000000000) ) ) 
 REPRESENTATION_ITEM ( '' )  SURFACE ( )  );
#2932=B_SPLINE_CURVE_WITH_KNOTS ( 'NONE', 3,
 ( #43118, #34948, #54012, #49028, #30218, #11135, #52793, #19301, #34025, #29605, #15523, #155, #29918, #6079, #20226, #33715, #25218, #38733, #48716 ),
 .UNSPECIFIED., .F., .F.,
 ( 4, 3, 3, 3, 3, 3, 4 ),
 ( 0.000000000000000000, 0.0002612768053151700827, 0.0003919133833142882692, 0.0005225499612322571756, 0.0006531865391693363922, 0.0008112755173415194237, 0.0009693688056799737657 ),
 .UNSPECIFIED. ) ;
#2934=CARTESIAN_POINT ( 'NONE',  ( 0.8753041380234530822, -42.34096624980190171, 24.86726573039578980 ) ) ;
#2936=ORIENTED_EDGE ( 'NONE', *, *, #59282, .T. ) ;
#2947=CARTESIAN_POINT ( 'NONE',  ( -2.739355103387248747, 5.401627249124187458, 13.91653656670854744 ) ) ;
#2957=B_SPLINE_CURVE_WITH_KNOTS ( 'NONE', 3,
 ( #35288, #39692, #54348, #30559 ),
 .UNSPECIFIED., .F., .F.,
 ( 4, 4 ),
 ( 0.000000000000000000, 0.004442905043737217438 ),
 .UNSPECIFIED. ) ;
#2959=ORIENTED_EDGE ( 'NONE', *, *, #19256, .F. ) ;
#2968=CARTESIAN_POINT ( 'NONE',  ( -6.072942160501519027, -18.27069728648816849, -6.081593784077838905 ) ) ;
#2969=CARTESIAN_POINT ( 'NONE',  ( 0.5980271706414734822, 48.96187791475881568, -3.844964746511586373 ) ) ;
#2970=EDGE_CURVE ( 'NONE', #7798, #11211, #32285, .T. ) ;
#2975=CARTESIAN_POINT ( 'NONE',  ( -6.077587904424778920, 15.42837212129410673, 11.52221137980054699 ) ) ;
#2982=CARTESIAN_POINT ( 'NONE',  ( 1.296416391601052487, 36.31792729719459345, -24.96628788810715704 ) ) ;
#2985=ORIENTED_EDGE ( 'NONE', *, *, #29421, .F. ) ;
#2991=ADVANCED_FACE ( 'NONE', ( #46390 ), #23123, .F. ) ;
#2992=VERTEX_POINT ( 'NONE', #51676 ) ;
#2993=CARTESIAN_POINT ( 'NONE',  ( 0.7242486021783833827, -47.28179493328054406, -13.24550226534200981 ) ) ;
#2996=ORIENTED_EDGE ( 'NONE', *, *, #58617, .T. ) ;
#2997=EDGE_CURVE ( 'NONE', #39074, #29160, #8897, .T. ) ;
#2998=EDGE_LOOP ( 'NONE', ( #11330, #45882, #7990, #51314 ) ) ;
#2999=FACE_OUTER_BOUND ( 'NONE', #60876, .T. ) ;
#3010=CARTESIAN_POINT ( 'NONE',  ( 0.5980271706414711508, -31.16543947089417443, 37.95740540958632891 ) ) ;
#3014=FACE_OUTER_BOUND ( 'NONE', #394, .T. ) ;
#3023=VECTOR ( 'NONE', #13591, 1000.000000000000227 ) ;
#3026=ADVANCED_FACE ( 'NONE', ( #24413 ), #48125, .F. ) ;
#3029=CARTESIAN_POINT ( 'NONE',  ( 0.6016117650947688800, -48.74769398499142170, -5.934086735979687610 ) ) ;
#3031=VECTOR ( 'NONE', #20456, 1000.000000000000000 ) ;
#3032=CARTESIAN_POINT ( 'NONE',  ( 0.1129192098497447394, -43.69739906996321110, 6.122834499276631703 ) ) ;
#3040=CARTESIAN_POINT ( 'NONE',  ( 4.553261556744873317, 43.59419396814051595, 5.393126930805304475 ) ) ;
#3048=CARTESIAN_POINT ( 'NONE',  ( 0.8744876279028306332, -48.79802643035336018, -5.394688766001929814 ) ) ;
#3053=DIRECTION ( 'NONE',  ( 0.09722883295013594329, 0.4670337431504633652, 0.8788777143619136423 ) ) ;
#3056=LINE ( 'NONE', #11881, #37628 ) ;
#3062=CARTESIAN_POINT ( 'NONE',  ( 0.8753041380234471980, 46.31375555491744223, 16.31485134079786548 ) ) ;
#3065=CARTESIAN_POINT ( 'NONE',  ( 0.5549461598389363592, 16.05292175970580715, 41.07945226562262064 ) ) ;
#3073=CARTESIAN_POINT ( 'NONE',  ( 2.185380717157383135, -32.61424324914600703, -29.58261212862606016 ) ) ;
#3077=CARTESIAN_POINT ( 'NONE',  ( 1.834102595619085507, -40.32172980854549849, 17.73008319507659536 ) ) ;
#3081=CARTESIAN_POINT ( 'NONE',  ( 0.3676999524040366896, -26.85386693986640338, 34.99743438737744583 ) ) ;
#3083=CARTESIAN_POINT ( 'NONE',  ( -6.077587904424778920, 12.01079512011132522, 15.05114022181178335 ) ) ;
#3087=VERTEX_POINT ( 'NONE', #10018 ) ;
#3090=EDGE_CURVE ( 'NONE', #18280, #1366, #7126, .T. ) ;
#3091=B_SPLINE_CURVE_WITH_KNOTS ( 'NONE', 3,
 ( #4425, #23566, #42692, #33298, #30412, #44252, #2208, #1907, #40174, #16330, #39863, #44557, #59539, #35143, #45178, #54514, #15729, #59222, #25108 ),
 .UNSPECIFIED., .F., .F.,
 ( 4, 3, 3, 3, 3, 3, 4 ),
 ( 3.469552829456483146E-18, 0.0002612768053151643365, 0.0003919133833142878897, 0.0005225499612322573924, 0.0006531865391693325975, 0.0008112755173415177974, 0.0009693688056799712720 ),
 .UNSPECIFIED. ) ;
#3093=CARTESIAN_POINT ( 'NONE',  ( 4.975610109902397937, 2.142807115709817189, -48.86571174967818365 ) ) ;
#3107=CARTESIAN_POINT ( 'NONE',  ( 0.8753041380234530822, 3.828530797421374032, -48.95386276695819561 ) ) ;
#3108=EDGE_CURVE ( 'NONE', #1361, #7783, #39466, .T. ) ;
#3110=CARTESIAN_POINT ( 'NONE',  ( 2.114184763582917181, 7.651710973661706259E-12, 44.03514965515166324 ) ) ;
#3112=B_SPLINE_CURVE_WITH_KNOTS ( 'NONE', 3,
 ( #34545, #30129, #48940, #10111, #6295, #25431 ),
 .UNSPECIFIED., .F., .F.,
 ( 4, 2, 4 ),
 ( 2.033052538357063276E-17, 0.0002293755540694316438, 0.0004587511081388429587 ),
 .UNSPECIFIED. ) ;
#3115=CARTESIAN_POINT ( 'NONE',  ( -6.078075953587585900, -17.34679059108042765, 8.359666885488888255 ) ) ;
#3116=CARTESIAN_POINT ( 'NONE',  ( 0.8753041380234524160, 23.49739456791611403, 43.11624724384818563 ) ) ;
#3124=EDGE_LOOP ( 'NONE', ( #40321, #51696, #41255, #17315 ) ) ;
#3125=EDGE_CURVE ( 'NONE', #34487, #8248, #16327, .T. ) ;
#3128=CARTESIAN_POINT ( 'NONE',  ( 3.050102900204245682, -43.36385787569175676, 7.416271254132083435 ) ) ;
#3139=CARTESIAN_POINT ( 'NONE',  ( -2.601141883200662974, 2.883136076038183671, -14.64523655788583589 ) ) ;
#3143=EDGE_CURVE ( 'NONE', #17913, #53301, #52153, .T. ) ;
#3144=LINE ( 'NONE', #11641, #21277 ) ;
#3145=CARTESIAN_POINT ( 'NONE',  ( -6.057079549204054558, -16.14367994231351489, 10.49822980410900541 ) ) ;
#3146=ORIENTED_EDGE ( 'NONE', *, *, #17564, .T. ) ;
#3150=CARTESIAN_POINT ( 'NONE',  ( -6.072942160501519027, -4.299083787220820518, 18.77024349547643567 ) ) ;
#3151=CARTESIAN_POINT ( 'NONE',  ( 0.2279481005628808954, -18.55039463836296321, 40.02981820885408126 ) ) ;
#3152=ORIENTED_EDGE ( 'NONE', *, *, #42797, .F. ) ;
#3157=CARTESIAN_POINT ( 'NONE',  ( 0.7242486021783807182, -45.19981481568854775, -19.18301861025617683 ) ) ;
#3159=CARTESIAN_POINT ( 'NONE',  ( 0.5997462898726536595, 37.05192695178125462, 32.22896739432052016 ) ) ;
#3169=CARTESIAN_POINT ( 'NONE',  ( 1.479689385636123067, -0.2368883799086275443, 44.06277033010017874 ) ) ;
#3172=CARTESIAN_POINT ( 'NONE',  ( 0.1158516988532803382, 15.28513351191913294, 41.39211099177720143 ) ) ;
#3174=CARTESIAN_POINT ( 'NONE',  ( 2.185380717157384023, -37.63955117804344752, 22.84915731887389256 ) ) ;
#3176=ORIENTED_EDGE ( 'NONE', *, *, #25244, .F. ) ;
#3180=CARTESIAN_POINT ( 'NONE',  ( 4.975610109902397937, 39.54077024310134902, 28.79195887257488451 ) ) ;
#3183=ORIENTED_EDGE ( 'NONE', *, *, #59745, .F. ) ;
#3185=CARTESIAN_POINT ( 'NONE',  ( 2.533389852662419894, 13.70698264761542617, -41.82785146803010434 ) ) ;
#3186=ORIENTED_EDGE ( 'NONE', *, *, #53361, .T. ) ;
#3189=CARTESIAN_POINT ( 'NONE',  ( 1.112077966505211846, 8.782297753024950637, -43.19608282362842999 ) ) ;
#3192=ORIENTED_EDGE ( 'NONE', *, *, #57942, .T. ) ;
#3199=( BOUNDED_SURFACE ( )  B_SPLINE_SURFACE ( 3, 1, ( 
 ( #20944, #2117 ),
 ( #49440, #40088 ),
 ( #11879, #7121 ),
 ( #34438, #53507 ) ),
 .UNSPECIFIED., .F., .F., .F. ) 
 B_SPLINE_SURFACE_WITH_KNOTS ( ( 4, 4 ),
 ( 2, 2 ),
 ( 0.000000000000000000, 1.000000000000000000 ),
 ( 0.000000000000000000, 1.000000000000000000 ),
 .UNSPECIFIED. ) 
 GEOMETRIC_REPRESENTATION_ITEM ( )  RATIONAL_B_SPLINE_SURFACE ( (
 ( 1.000000000000000000, 1.000000000000000000),
 ( 0.7211978278499968642, 0.9934217856018975334),
 ( 0.7211978278499968642, 0.9934217856018975334),
 ( 1.000000000000000000, 1.000000000000000000) ) ) 
 REPRESENTATION_ITEM ( '' )  SURFACE ( )  );
#3200=CARTESIAN_POINT ( 'NONE',  ( 2.881901169982995725, 1.330622528702777754E-16, 49.00591519830862808 ) ) ;
#3210=EDGE_CURVE ( 'NONE', #3847, #61531, #49162, .T. ) ;
#3211=CARTESIAN_POINT ( 'NONE',  ( 0.6029443449137434907, 16.91913962848288477, 46.10078363992560924 ) ) ;
#3212=CARTESIAN_POINT ( 'NONE',  ( 0.6021447746440204973, -47.43443576215717883, 12.70887260988444289 ) ) ;
#3214=VERTEX_POINT ( 'NONE', #23653 ) ;
#3215=VERTEX_POINT ( 'NONE', #19275 ) ;
#3216=CARTESIAN_POINT ( 'NONE',  ( 0.6024113833632039894, 17.16413907095168057, -46.01015321702263350 ) ) ;
#3217=CARTESIAN_POINT ( 'NONE',  ( 3.559346040607745287, 2.173097940776011594, -43.91705735681505018 ) ) ;
#3218=CARTESIAN_POINT ( 'NONE',  ( 0.7948878604505659196, 44.60603605348585887, 20.51828927794751323 ) ) ;
#3224=ORIENTED_EDGE ( 'NONE', *, *, #17264, .F. ) ;
#3225=ORIENTED_EDGE ( 'NONE', *, *, #17656, .T. ) ;
#3229=CARTESIAN_POINT ( 'NONE',  ( 0.6253024248130498730, 48.95676787329645663, 3.831332251033968017 ) ) ;
#3230=ORIENTED_EDGE ( 'NONE', *, *, #24745, .F. ) ;
#3234=CIRCLE ( 'NONE', #1225, 48.91267123290010943 ) ;
#3239=CARTESIAN_POINT ( 'NONE',  ( -6.078075953587585900, 0.6224930363970364589, -19.24597819459362569 ) ) ;
#3244=CARTESIAN_POINT ( 'NONE',  ( 4.975610109902397937, -4.123593823332411645, 48.73854102369035957 ) ) ;
#3245=CARTESIAN_POINT ( 'NONE',  ( 2.009741617377216460, -43.83235551399246077, -4.269506730058997945 ) ) ;
#3249=CARTESIAN_POINT ( 'NONE',  ( 0.8753041380234471980, -47.71532843791173661, 11.59248721953970218 ) ) ;
#3251=CARTESIAN_POINT ( 'NONE',  ( -6.063463321072276813, 3.057971819381750223, -19.01234495877183761 ) ) ;
#3255=ORIENTED_EDGE ( 'NONE', *, *, #52298, .F. ) ;
#3258=CARTESIAN_POINT ( 'NONE',  ( 0.5980271706414711508, -2.273683837878000435, 49.05995928093535241 ) ) ;
#3259=EDGE_CURVE ( 'NONE', #2365, #7116, #57347, .T. ) ;
#3260=PRODUCT ( 'straight bevel gear(wobble in)_iso_ISO - Straight bevel gear 2M 49GT 48PT 20PA 5FW ---49O1H50MD20.0S1', 'straight bevel gear(wobble in)_iso_ISO - Straight bevel gear 2M 49GT 48PT 20PA 5FW ---49O1H50MD20.0S1', '', ( #2358 ) ) ;
#3265=CARTESIAN_POINT ( 'NONE',  ( 0.6008122571543326185, 40.91731943791382520, -27.15377543696339302 ) ) ;
#3268=ORIENTED_EDGE ( 'NONE', *, *, #25474, .T. ) ;
#3278=CARTESIAN_POINT ( 'NONE',  ( 1.657374760986086493, 36.23257293270000190, -25.06174586753322231 ) ) ;
#3286=LINE ( 'NONE', #55602, #55514 ) ;
#3296=ORIENTED_EDGE ( 'NONE', *, *, #45161, .T. ) ;
#3297=EDGE_LOOP ( 'NONE', ( #57767, #51722, #50105, #38799 ) ) ;
#3300=CARTESIAN_POINT ( 'NONE',  ( 3.050102900204245682, 37.82667193297250208, 22.46259423248638498 ) ) ;
#3303=CARTESIAN_POINT ( 'NONE',  ( 1.555462896905692949, -0.4926004118482715799, -49.06288753989547757 ) ) ;
#3305=CARTESIAN_POINT ( 'NONE',  ( -6.078726893082806448, 5.475592473157355755, 18.46109228449450512 ) ) ;
#3306=CARTESIAN_POINT ( 'NONE',  ( 0.1157991065609915715, 33.54534060093158132, 28.66448132280070382 ) ) ;
#3312=CARTESIAN_POINT ( 'NONE',  ( 4.975610109902397937, -48.11736577406850301, -8.784561349451310619 ) ) ;
#3314=FACE_OUTER_BOUND ( 'NONE', #35504, .T. ) ;
#3318=ORIENTED_EDGE ( 'NONE', *, *, #41261, .T. ) ;
#3328=CARTESIAN_POINT ( 'NONE',  ( 4.226256110419178924, 43.52565652391797357, 6.028637835291145386 ) ) ;
#3329=CARTESIAN_POINT ( 'NONE',  ( 0.6026777506516368677, -48.72629457415274601, -6.106931120465691087 ) ) ;
#3330=CARTESIAN_POINT ( 'NONE',  ( 4.975610109902397937, -48.77192499014914517, 3.707929326866768349 ) ) ;
#3340=EDGE_CURVE ( 'NONE', #51387, #23810, #46188, .T. ) ;
#3341=CARTESIAN_POINT ( 'NONE',  ( 0.3676999524040323597, 29.04098611012938136, 33.20499524279608750 ) ) ;
#3352=CARTESIAN_POINT ( 'NONE',  ( 2.648799415243708655, -24.22471848649547610, 42.63426412569639012 ) ) ;
#3353=CARTESIAN_POINT ( 'NONE',  ( 0.6021448801613057400, 4.455338032995132203, 48.90491899225163763 ) ) ;
#3356=CARTESIAN_POINT ( 'NONE',  ( 0.5997462898726536595, -39.04071682475767346, -29.78882441375276358 ) ) ;
#3358=CARTESIAN_POINT ( 'NONE',  ( 4.975610109902397937, 0.000000000000000000, 0.000000000000000000 ) ) ;
#3361=CARTESIAN_POINT ( 'NONE',  ( 1.479689385636123067, 16.31572803950663442, 40.93141658687796536 ) ) ;
#3363=CONICAL_SURFACE ( 'NONE', #8378, 43.92652462719577500, 1.486293639869522343 ) ;
#3364=CARTESIAN_POINT ( 'NONE',  ( 0.6253024248130478746, 40.77684555828908231, 27.36225673684618798 ) ) ;
#3374=CARTESIAN_POINT ( 'NONE',  ( 4.060580049360325461, 27.79286080241194057, -34.04445010243171055 ) ) ;
#3381=ORIENTED_EDGE ( 'NONE', *, *, #9977, .T. ) ;
#3388=CARTESIAN_POINT ( 'NONE',  ( 4.553261556744875094, -9.554252317234240621, -42.87488575474295516 ) ) ;
#3391=CARTESIAN_POINT ( 'NONE',  ( 4.975610109902397937, -16.35148546628888866, -46.09857188876371481 ) ) ;
#3396=DIRECTION ( 'NONE',  ( 1.000000000000000000, 0.000000000000000000, 0.000000000000000000 ) ) ;
#3398=ORIENTED_EDGE ( 'NONE', *, *, #11696, .T. ) ;
#3401=CARTESIAN_POINT ( 'NONE',  ( 0.6026777506516367566, -25.60575673810485497, -41.90336039634789955 ) ) ;
#3407=CARTESIAN_POINT ( 'NONE',  ( 4.226256110419178924, 0.9953287626735226601, 43.92990519727287335 ) ) ;
#3412=FACE_OUTER_BOUND ( 'NONE', #34524, .T. ) ;
#3413=CARTESIAN_POINT ( 'NONE',  ( 3.678748215320120085, 6.540036259557823861, 48.53700382206501729 ) ) ;
#3419=CARTESIAN_POINT ( 'NONE',  ( 4.553261556744875094, -33.59363643963393997, 28.30206982864213217 ) ) ;
#3421=ORIENTED_EDGE ( 'NONE', *, *, #14387, .F. ) ;
#3423=DIRECTION ( 'NONE',  ( 0.000000000000000000, 0.000000000000000000, 1.000000000000000000 ) ) ;
#3430=CARTESIAN_POINT ( 'NONE',  ( 0.1129192098497455998, 20.83764143887614040, -38.89401608281131928 ) ) ;
#3431=CARTESIAN_POINT ( 'NONE',  ( -6.072942160501519915, -18.27069728648825730, 6.081593784077573339 ) ) ;
#3438=EDGE_CURVE ( 'NONE', #57990, #5134, #33119, .T. ) ;
#3445=CARTESIAN_POINT ( 'NONE',  ( 3.727782113643637096, 23.36895243144297396, -37.23801603419455120 ) ) ;
#3446=CARTESIAN_POINT ( 'NONE',  ( 4.975610109902397937, 0.000000000000000000, 0.000000000000000000 ) ) ;
#3452=B_SPLINE_CURVE_WITH_KNOTS ( 'NONE', 3,
 ( #34260, #56580, #10135, #27776, #8978, #46591, #39278, #24227, #46910, #48646, #3635, #29538, #56266, #10447, #29232, #38662 ),
 .UNSPECIFIED., .F., .F.,
 ( 4, 3, 3, 3, 3, 4 ),
 ( 2.030557555191247372E-17, 0.0002612764279487735423, 0.0003919131003184789198, 0.0005225497727000641716, 0.0007837925190632434027, 0.001045051706266715216 ),
 .UNSPECIFIED. ) ;
#3455=CARTESIAN_POINT ( 'NONE',  ( -6.078726893082806448, 19.25601281685051802, -0.003415553934477524867 ) ) ;
#3465=ADVANCED_FACE ( 'NONE', ( #23269 ), #31884, .F. ) ;
#3468=CIRCLE ( 'NONE', #37544, 48.91267123290010943 ) ;
#3470=LINE ( 'NONE', #22604, #1713 ) ;
#3471=CARTESIAN_POINT ( 'NONE',  ( 0.9268187852002115479, -0.4216597870159004002, 44.08601292850874387 ) ) ;
#3472=EDGE_LOOP ( 'NONE', ( #13047, #56227, #36663, #10106 ) ) ;
#3473=DIRECTION ( 'NONE',  ( 1.000000000000000000, 0.000000000000000000, 0.000000000000000000 ) ) ;
#3474=CARTESIAN_POINT ( 'NONE',  ( -6.057079549204054558, -14.66865672308403212, 12.47644745270303090 ) ) ;
#3475=CARTESIAN_POINT ( 'NONE',  ( 3.727782113643637096, -37.21166825045877857, 23.41088468904526110 ) ) ;
#3477=VERTEX_POINT ( 'NONE', #22655 ) ;
#3481=VERTEX_POINT ( 'NONE', #46791 ) ;
#3491=CARTESIAN_POINT ( 'NONE',  ( 2.299652685299201416, -2.858710868356232560, 48.95007147113572898 ) ) ;
#3496=CARTESIAN_POINT ( 'NONE',  ( -2.601141883200665639, 14.01836437022350168, 5.126488842574115523 ) ) ;
#3497=FACE_OUTER_BOUND ( 'NONE', #29084, .T. ) ;
#3499=CARTESIAN_POINT ( 'NONE',  ( 5.901764892641307547, 48.57275408226684732, -6.219246602548297531 ) ) ;
#3500=CARTESIAN_POINT ( 'NONE',  ( 3.559346040607745287, 11.77623459503632475, 42.36449669599129209 ) ) ;
#3503=VECTOR ( 'NONE', #45114, 1000.000000000000227 ) ;
#3506=CARTESIAN_POINT ( 'NONE',  ( 0.3676999524040323597, 9.009680404095913531, 43.18305503711946614 ) ) ;
#3508=CARTESIAN_POINT ( 'NONE',  ( 0.5997462898726536595, 16.46871699354475993, 46.26373299606117229 ) ) ;
#3518=ORIENTED_EDGE ( 'NONE', *, *, #42055, .F. ) ;
#3525=CARTESIAN_POINT ( 'NONE',  ( 3.559346040607745287, -30.12298026119279015, 32.03180203681612426 ) ) ;
#3531=B_SPLINE_CURVE_WITH_KNOTS ( 'NONE', 3,
 ( #21320, #35127, #16945, #25704 ),
 .UNSPECIFIED., .F., .F.,
 ( 4, 4 ),
 ( 0.000000000000000000, 0.004444103432399265294 ),
 .UNSPECIFIED. ) ;
#3537=EDGE_CURVE ( 'NONE', #34547, #42039, #44338, .T. ) ;
#3539=CARTESIAN_POINT ( 'NONE',  ( 0.8753041380234465318, -13.11588273819783623, -47.31925557181583741 ) ) ;
#3544=ORIENTED_EDGE ( 'NONE', *, *, #15917, .F. ) ;
#3552=CARTESIAN_POINT ( 'NONE',  ( 0.8744876279028263033, -2.462621419133342204, 49.03351451941333750 ) ) ;
#3556=CARTESIAN_POINT ( 'NONE',  ( -6.072942160501519915, -1.834587804586878645, 19.16868409349691049 ) ) ;
#3559=ADVANCED_FACE ( 'NONE', ( #22342 ), #37332, .F. ) ;
#3560=ORIENTED_EDGE ( 'NONE', *, *, #2239, .T. ) ;
#3570=CARTESIAN_POINT ( 'NONE',  ( 0.1149546198390368201, -17.60995280955134845, -40.45783146769726102 ) ) ;
#3571=CARTESIAN_POINT ( 'NONE',  ( 0.1129192098497447394, 10.29049805561828101, 42.90754522869457332 ) ) ;
#3583=CARTESIAN_POINT ( 'NONE',  ( 4.226256110419178924, -24.79946968843673716, -36.27414441664329559 ) ) ;
#3589=CARTESIAN_POINT ( 'NONE',  ( 0.6008122571543325074, -1.138706917017746623, 49.09437744816052884 ) ) ;
#3591=ORIENTED_EDGE ( 'NONE', *, *, #32008, .F. ) ;
#3594=CARTESIAN_POINT ( 'NONE',  ( 0.1156867017252034974, -7.165540636711854816, 43.53846385276836628 ) ) ;
#3598=ORIENTED_EDGE ( 'NONE', *, *, #5149, .T. ) ;
#3602=EDGE_CURVE ( 'NONE', #34420, #35039, #21116, .T. ) ;
#3606=AXIS2_PLACEMENT_3D ( 'NONE', #20256, #39997, #48138 ) ;
#3609=EDGE_CURVE ( 'NONE', #49479, #41448, #41337, .T. ) ;
#3612=CARTESIAN_POINT ( 'NONE',  ( 0.7948878604505668077, -24.70668313632145185, 42.42968837618095534 ) ) ;
#3614=CARTESIAN_POINT ( 'NONE',  ( 0.8753041380234530822, 10.05717963662871739, -48.06237057854679051 ) ) ;
#3617=CARTESIAN_POINT ( 'NONE',  ( -6.078726893082806448, 3.076629396955071538, 19.00863995194059086 ) ) ;
#3622=ORIENTED_EDGE ( 'NONE', *, *, #60515, .F. ) ;
#3623=CARTESIAN_POINT ( 'NONE',  ( 0.1149546198390367369, -44.12336736438651030, -0.2738931372102353934 ) ) ;
#3629=CIRCLE ( 'NONE', #11670, 43.92652462719577500 ) ;
#3630=ORIENTED_EDGE ( 'NONE', *, *, #48205, .F. ) ;
#3632=CARTESIAN_POINT ( 'NONE',  ( 3.678834586032788234, -12.15221970334232537, -47.44402940212869879 ) ) ;
#3633=( BOUNDED_SURFACE ( )  B_SPLINE_SURFACE ( 3, 1, ( 
 ( #59937, #31439 ),
 ( #1991, #25195 ),
 ( #49609, #1365 ),
 ( #49930, #20814 ) ),
 .UNSPECIFIED., .F., .F., .F. ) 
 B_SPLINE_SURFACE_WITH_KNOTS ( ( 4, 4 ),
 ( 2, 2 ),
 ( 0.000000000000000000, 1.000000000000000000 ),
 ( 0.000000000000000000, 1.000000000000000000 ),
 .UNSPECIFIED. ) 
 GEOMETRIC_REPRESENTATION_ITEM ( )  RATIONAL_B_SPLINE_SURFACE ( (
 ( 1.000000000000000000, 1.000000000000000000),
 ( 0.7211978278499968642, 0.9934217856018975334),
 ( 0.7211978278499968642, 0.9934217856018975334),
 ( 1.000000000000000000, 1.000000000000000000) ) ) 
 REPRESENTATION_ITEM ( '' )  SURFACE ( )  );
#3634=CIRCLE ( 'NONE', #40716, 43.92652462719577500 ) ;
#3635=CARTESIAN_POINT ( 'NONE',  ( 0.6029442701453591180, -14.05591772168299158, -47.05291066618041640 ) ) ;
#3637=CARTESIAN_POINT ( 'NONE',  ( 0.6252788684277220677, -8.514552591182596331, -48.36265837757115094 ) ) ;
#3640=CARTESIAN_POINT ( 'NONE',  ( -6.078075953587585900, 19.25604180663921738, 0.005309246513133128106 ) ) ;
#3643=EDGE_CURVE ( 'NONE', #3830, #44540, #38313, .T. ) ;
#3650=EDGE_LOOP ( 'NONE', ( #36557, #49775, #54341, #33565 ) ) ;
#3653=CARTESIAN_POINT ( 'NONE',  ( 0.8744876279028306332, -6.955970791788286256, 48.60004650947653460 ) ) ;
#3657=CARTESIAN_POINT ( 'NONE',  ( 2.648799415243708655, 46.08255460350053312, -16.76053771527007186 ) ) ;
#3662=CARTESIAN_POINT ( 'NONE',  ( 0.5997462898726536595, 5.235280152387000285, 48.82769165002921596 ) ) ;
#3665=CARTESIAN_POINT ( 'NONE',  ( 4.975610109902397937, 14.46773809681615575, -46.72401910687593585 ) ) ;
#3670=CARTESIAN_POINT ( 'NONE',  ( 0.6026777506516367566, -1.748060344709603253, -49.07637594269235137 ) ) ;
#3671=CARTESIAN_POINT ( 'NONE',  ( 3.050102900204245682, 16.87969600441305573, 40.62635981695458298 ) ) ;
#3674=CARTESIAN_POINT ( 'NONE',  ( 1.834102595619085951, 32.68067448320012858, -29.53254577886568200 ) ) ;
#3675=EDGE_CURVE ( 'NONE', #33022, #1834, #29498, .T. ) ;
#3678=CARTESIAN_POINT ( 'NONE',  ( 4.553261556744873317, 38.38432632180467863, 21.35844232721216684 ) ) ;
#3679=CARTESIAN_POINT ( 'NONE',  ( 2.706805983486679335, 28.34065445965364205, -33.66873056885675908 ) ) ;
#3681=AXIS2_PLACEMENT_3D ( 'NONE', #53613, #30438, #29829 ) ;
#3686=ORIENTED_EDGE ( 'NONE', *, *, #22881, .F. ) ;
#3687=CARTESIAN_POINT ( 'NONE',  ( 0.7413678028165011646, -26.75786355817048090, 35.05000470146295299 ) ) ;
#3700=CARTESIAN_POINT ( 'NONE',  ( -2.739355103387248747, -4.498893467419605940, -14.23402699589354370 ) ) ;
#3702=CARTESIAN_POINT ( 'NONE',  ( -6.057079549204054558, 17.84642505839085302, -7.234386203056722309 ) ) ;
#3703=ORIENTED_EDGE ( 'NONE', *, *, #15635, .T. ) ;
#3704=VECTOR ( 'NONE', #25561, 1000.000000000000000 ) ;
#3708=CARTESIAN_POINT ( 'NONE',  ( 0.3676999524040366896, -38.83470403830472151, -20.92406140260821346 ) ) ;
#3710=CARTESIAN_POINT ( 'NONE',  ( 4.060580049360325461, -29.17232330074064350, -32.87009655593170976 ) ) ;
#3722=CARTESIAN_POINT ( 'NONE',  ( 0.8744876279028263033, 5.599149760998344050, -48.77498920895221346 ) ) ;
#3725=EDGE_CURVE ( 'NONE', #60472, #51862, #18128, .T. ) ;
#3729=CONICAL_SURFACE ( 'NONE', #741, 43.92652462719577500, 1.486293639869522343 ) ;
#3730=EDGE_CURVE ( 'NONE', #39191, #24982, #911, .T. ) ;
#3733=CARTESIAN_POINT ( 'NONE',  ( 4.226256110419178924, -39.40860114104851419, -19.43680544978874281 ) ) ;
#3734=CARTESIAN_POINT ( 'NONE',  ( 1.296416391601052709, -43.55378818229317517, 6.736090041566987097 ) ) ;
#3736=( BOUNDED_SURFACE ( )  B_SPLINE_SURFACE ( 3, 1, ( 
 ( #38509, #14698 ),
 ( #563, #5866 ),
 ( #33810, #29087 ),
 ( #48204, #24701 ) ),
 .UNSPECIFIED., .F., .F., .F. ) 
 B_SPLINE_SURFACE_WITH_KNOTS ( ( 4, 4 ),
 ( 2, 2 ),
 ( 0.000000000000000000, 1.000000000000000000 ),
 ( 0.000000000000000000, 1.000000000000000000 ),
 .UNSPECIFIED. ) 
 GEOMETRIC_REPRESENTATION_ITEM ( )  RATIONAL_B_SPLINE_SURFACE ( (
 ( 1.000000000000000000, 1.000000000000000000),
 ( 0.7211978278499968642, 0.9934217856018975334),
 ( 0.7211978278499968642, 0.9934217856018975334),
 ( 1.000000000000000000, 1.000000000000000000) ) ) 
 REPRESENTATION_ITEM ( '' )  SURFACE ( )  );
#3747=CARTESIAN_POINT ( 'NONE',  ( 0.8744876279028306332, -48.79802643035336018, -5.394688766001929814 ) ) ;
#3748=FACE_OUTER_BOUND ( 'NONE', #4040, .T. ) ;
#3751=CARTESIAN_POINT ( 'NONE',  ( 0.2940133293163009753, 44.06980802084461857, -2.023010277765129761 ) ) ;
#3759=CARTESIAN_POINT ( 'NONE',  ( 0.000000000000000000, 0.000000000000000000, 0.000000000000000000 ) ) ;
#3770=CARTESIAN_POINT ( 'NONE',  ( -6.072942160501519915, -8.893884846139727074, 17.07931423191886822 ) ) ;
#3778=LINE ( 'NONE', #7003, #31838 ) ;
#3779=FACE_OUTER_BOUND ( 'NONE', #28853, .T. ) ;
#3780=VERTEX_POINT ( 'NONE', #21343 ) ;
#3788=CARTESIAN_POINT ( 'NONE',  ( 0.1145239942831223490, -31.46852519861557340, -30.93020210940707315 ) ) ;
#3799=CARTESIAN_POINT ( 'NONE',  ( -6.078726893082806448, 0.6205993875984882058, -19.24600991553398188 ) ) ;
#3803=EDGE_CURVE ( 'NONE', #61531, #57613, #26045, .T. ) ;
#3809=CARTESIAN_POINT ( 'NONE',  ( 0.1119898979215349921, -18.37259971277567416, -40.11743870246385768 ) ) ;
#3814=CONICAL_SURFACE ( 'NONE', #60829, 43.92652462719577500, 1.486293639869522343 ) ;
#3820=CARTESIAN_POINT ( 'NONE',  ( 0.5997462898726536595, -19.39900779840410294, -45.11352487427429736 ) ) ;
#3824=CARTESIAN_POINT ( 'NONE',  ( 3.050102900204245682, -21.23864880574211256, 38.52719878325451930 ) ) ;
#3830=VERTEX_POINT ( 'NONE', #2838 ) ;
#3836=CARTESIAN_POINT ( 'NONE',  ( 0.2940135542859036444, -23.55385452459446327, -37.30223164538097080 ) ) ;
#3837=FACE_OUTER_BOUND ( 'NONE', #31708, .T. ) ;
#3844=VERTEX_POINT ( 'NONE', #55763 ) ;
#3845=ORIENTED_EDGE ( 'NONE', *, *, #17343, .F. ) ;
#3847=VERTEX_POINT ( 'NONE', #22891 ) ;
#3849=CARTESIAN_POINT ( 'NONE',  ( -2.601141883200662974, -13.66110686928774953, 6.014115610402557266 ) ) ;
#3851=EDGE_LOOP ( 'NONE', ( #10410, #46252, #34471, #38827 ) ) ;
#3852=( BOUNDED_SURFACE ( )  B_SPLINE_SURFACE ( 3, 1, ( 
 ( #20012, #15308 ),
 ( #17922, #56718 ),
 ( #56105, #56410 ),
 ( #42051, #24689 ) ),
 .UNSPECIFIED., .F., .F., .F. ) 
 B_SPLINE_SURFACE_WITH_KNOTS ( ( 4, 4 ),
 ( 2, 2 ),
 ( 0.000000000000000000, 1.000000000000000000 ),
 ( 0.000000000000000000, 1.000000000000000000 ),
 .UNSPECIFIED. ) 
 GEOMETRIC_REPRESENTATION_ITEM ( )  RATIONAL_B_SPLINE_SURFACE ( (
 ( 1.000000000000000000, 1.000000000000000000),
 ( 0.7211978278499970862, 0.9934217856018976445),
 ( 0.7211978278499970862, 0.9934217856018976445),
 ( 1.000000000000000000, 1.000000000000000000) ) ) 
 REPRESENTATION_ITEM ( '' )  SURFACE ( )  );
#3859=CARTESIAN_POINT ( 'NONE',  ( 0.5997462898726536595, 46.76781179977606229, 14.97743000668126001 ) ) ;
#3861=CARTESIAN_POINT ( 'NONE',  ( 0.3676999524040366896, 24.55639947021014180, -36.64606156713571750 ) ) ;
#3862=CARTESIAN_POINT ( 'NONE',  ( 0.7948878604505675849, -29.92962973000293303, 38.92192070701729278 ) ) ;
#3864=B_SPLINE_CURVE_WITH_KNOTS ( 'NONE', 3,
 ( #31428, #22966, #22038, #27653, #32060, #17961, #8224, #41162, #17642, #7926, #41782, #27039, #3212, #60844, #22338, #18267 ),
 .UNSPECIFIED., .F., .F.,
 ( 4, 3, 3, 3, 3, 4 ),
 ( 2.030557555191247372E-17, 0.0002612764279487740302, 0.0003919131003184784861, 0.0005225497727000667737, 0.0007837925190632469806, 0.001045051706266716300 ),
 .UNSPECIFIED. ) ;
#3870=ORIENTED_EDGE ( 'NONE', *, *, #40700, .T. ) ;
#3872=EDGE_CURVE ( 'NONE', #41417, #51070, #42773, .T. ) ;
#3880=CARTESIAN_POINT ( 'NONE',  ( 0.8744876279028263033, 46.86690837902584406, -14.62336997314537790 ) ) ;
#3881=DIRECTION ( 'NONE',  ( -1.000000000000000000, -0.000000000000000000, -0.000000000000000000 ) ) ;
#3885=CARTESIAN_POINT ( 'NONE',  ( 0.5997462898726536595, -7.321308210775749004, 48.55872811583040516 ) ) ;
#3894=CARTESIAN_POINT ( 'NONE',  ( 0.8744876279028263033, -13.11369837310799547, -47.31153099783008997 ) ) ;
#3897=CARTESIAN_POINT ( 'NONE',  ( 0.9268187852002115479, -23.69707065591206430, -37.17799315774504265 ) ) ;
#3903=CARTESIAN_POINT ( 'NONE',  ( 0.2285344041767085332, -35.80691465027930320, -25.77529890269112656 ) ) ;
#3910=ORIENTED_EDGE ( 'NONE', *, *, #36823, .T. ) ;
#3911=CARTESIAN_POINT ( 'NONE',  ( 0.8753041380234471980, 48.36002538446257404, -8.511537621788180630 ) ) ;
#3916=ORIENTED_EDGE ( 'NONE', *, *, #21348, .F. ) ;
#3917=ADVANCED_FACE ( 'NONE', ( #13495 ), #43759, .F. ) ;
#3919=CARTESIAN_POINT ( 'NONE',  ( 1.112077966505211402, 37.50506094480364538, 23.16032660942239474 ) ) ;
#3921=CARTESIAN_POINT ( 'NONE',  ( 0.8744876279028306332, -47.70753782033967383, -11.59055156152427557 ) ) ;
#3922=CARTESIAN_POINT ( 'NONE',  ( 4.975610109902397937, 25.84633036597884725, -41.52609557555889808 ) ) ;
#3925=CARTESIAN_POINT ( 'NONE',  ( -2.601141883200665639, -12.22474371604808496, 8.564523836520711697 ) ) ;
#3927=VERTEX_POINT ( 'NONE', #51994 ) ;
#3929=CARTESIAN_POINT ( 'NONE',  ( 0.8753041380234530822, 44.61941359694259290, 20.49990873486889598 ) ) ;
#3946=CARTESIAN_POINT ( 'NONE',  ( 0.1145239942831223490, 37.15712298330992525, -23.79692611048441364 ) ) ;
#3950=CARTESIAN_POINT ( 'NONE',  ( 0.1145239942831223490, -27.76557412857819429, 34.29312429649860405 ) ) ;
#3958=EDGE_LOOP ( 'NONE', ( #41079, #26700, #60785, #20842 ) ) ;
#3968=CARTESIAN_POINT ( 'NONE',  ( 0.1129192098497447394, 19.97823103613683315, -39.34236993944178806 ) ) ;
#3972=CARTESIAN_POINT ( 'NONE',  ( 0.8744876279028263033, -29.90976330662845939, -38.93271258621668096 ) ) ;
#3974=FACE_OUTER_BOUND ( 'NONE', #38562, .T. ) ;
#3976=ORIENTED_EDGE ( 'NONE', *, *, #32612, .F. ) ;
#3977=CARTESIAN_POINT ( 'NONE',  ( 0.2940133293163015304, 40.08987453976585158, -18.41310698833514792 ) ) ;
#3982=CARTESIAN_POINT ( 'NONE',  ( 3.727782113643636652, 32.05026110430742392, -30.09249971424265269 ) ) ;
#3986=CARTESIAN_POINT ( 'NONE',  ( 2.879087469061463178, -32.78830311798584063, -29.34329319327431307 ) ) ;
#3987=CARTESIAN_POINT ( 'NONE',  ( 4.390527457369401532, 27.64241534123164712, -34.14794592258018469 ) ) ;
#3991=EDGE_CURVE ( 'NONE', #47069, #50438, #43933, .T. ) ;
#4002=CARTESIAN_POINT ( 'NONE',  ( 0.8753041380234471980, 41.63161868429074985, -26.03740873433439162 ) ) ;
#4006=B_SPLINE_CURVE_WITH_KNOTS ( 'NONE', 3,
 ( #4506, #58667, #1350, #20486, #11097, #9857 ),
 .UNSPECIFIED., .F., .F.,
 ( 4, 2, 4 ),
 ( 8.274813951709019538E-19, 0.0002293801035737093178, 0.0004587602071474177682 ),
 .UNSPECIFIED. ) ;
#4014=CARTESIAN_POINT ( 'NONE',  ( 0.6027444965799114707, -42.72396661545605667, -24.21159211057460681 ) ) ;
#4017=CARTESIAN_POINT ( 'NONE',  ( 0.2279481005628804513, -43.65339889723670552, -6.394079432697511223 ) ) ;
#4019=CARTESIAN_POINT ( 'NONE',  ( 0.5980271706414734822, 4.018631420205467819, -48.94792992916248409 ) ) ;
#4022=VERTEX_POINT ( 'NONE', #43553 ) ;
#4031=CARTESIAN_POINT ( 'NONE',  ( 4.975610109902397937, 39.54077024310177535, -28.79195887257430897 ) ) ;
#4035=CARTESIAN_POINT ( 'NONE',  ( -2.739355103387248747, -13.13414140434190180, -7.095202359465781150 ) ) ;
#4036=CARTESIAN_POINT ( 'NONE',  ( 3.559346040607745287, -41.48356477534394315, -14.57889347899322452 ) ) ;
#4040=EDGE_LOOP ( 'NONE', ( #56864, #30678, #8339, #46487 ) ) ;
#4042=CARTESIAN_POINT ( 'NONE',  ( 4.834790513006555379, 40.94190515849784617, -23.58706728096878891 ) ) ;
#4046=CARTESIAN_POINT ( 'NONE',  ( -6.078075953587585900, 18.62492360731181407, -4.889518879085647640 ) ) ;
#4053=CARTESIAN_POINT ( 'NONE',  ( 3.559346040607745287, 23.44433175904301692, -37.19937620329021399 ) ) ;
#4060=CARTESIAN_POINT ( 'NONE',  ( 0.6024113833632039894, 44.33830889028068611, -21.11057161355237000 ) ) ;
#4061=B_SPLINE_CURVE_WITH_KNOTS ( 'NONE', 3,
 ( #40366, #10924, #25308, #54723 ),
 .UNSPECIFIED., .F., .F.,
 ( 4, 4 ),
 ( 0.000000000000000000, 0.005013413432710150247 ),
 .UNSPECIFIED. ) ;
#4062=EDGE_CURVE ( 'NONE', #22341, #42399, #26994, .T. ) ;
#4065=DIRECTION ( 'NONE',  ( 0.09722883295013594329, -0.7201826484181126364, -0.6869377751737254512 ) ) ;
#4072=ORIENTED_EDGE ( 'NONE', *, *, #47899, .T. ) ;
#4075=ORIENTED_EDGE ( 'NONE', *, *, #846, .F. ) ;
#4086=CARTESIAN_POINT ( 'NONE',  ( 0.1149546198390367646, -22.63900799641087147, -37.87376244792249480 ) ) ;
#4087=ORIENTED_EDGE ( 'NONE', *, *, #45623, .F. ) ;
#4094=( BOUNDED_SURFACE ( )  B_SPLINE_SURFACE ( 3, 1, ( 
 ( #47441, #28944 ),
 ( #9840, #37761 ),
 ( #33049, #58041 ),
 ( #56819, #13948 ) ),
 .UNSPECIFIED., .F., .F., .F. ) 
 B_SPLINE_SURFACE_WITH_KNOTS ( ( 4, 4 ),
 ( 2, 2 ),
 ( 0.000000000000000000, 1.000000000000000000 ),
 ( 0.000000000000000000, 1.000000000000000000 ),
 .UNSPECIFIED. ) 
 GEOMETRIC_REPRESENTATION_ITEM ( )  RATIONAL_B_SPLINE_SURFACE ( (
 ( 1.000000000000000000, 1.000000000000000000),
 ( 0.7211978278499970862, 0.9934217856018976445),
 ( 0.7211978278499970862, 0.9934217856018976445),
 ( 1.000000000000000000, 1.000000000000000000) ) ) 
 REPRESENTATION_ITEM ( '' )  SURFACE ( )  );
#4104=FACE_OUTER_BOUND ( 'NONE', #53464, .T. ) ;
#4106=CARTESIAN_POINT ( 'NONE',  ( 0.7242486021783848260, -26.15101222305781192, 41.55882604313377726 ) ) ;
#4111=CARTESIAN_POINT ( 'NONE',  ( -6.057079549204054558, 5.470993133660444485, 18.46346298046979939 ) ) ;
#4115=B_SPLINE_CURVE_WITH_KNOTS ( 'NONE', 3,
 ( #20433, #6599, #39563, #54225, #1608, #24827 ),
 .UNSPECIFIED., .F., .F.,
 ( 4, 2, 4 ),
 ( 2.538052214298621590E-18, 0.0002447193893791693286, 0.0004894387787583360551 ),
 .UNSPECIFIED. ) ;
#4127=CARTESIAN_POINT ( 'NONE',  ( 0.1129192098497447394, 20.83764143887560749, 38.89401608281161060 ) ) ;
#4128=CARTESIAN_POINT ( 'NONE',  ( 4.975610109902397937, -40.67634447773578898, -27.16402781375298403 ) ) ;
#4132=DIRECTION ( 'NONE',  ( -0.1011922191286467460, 0.9655114622251724787, -0.2398911234281693727 ) ) ;
#4143=B_SPLINE_CURVE_WITH_KNOTS ( 'NONE', 3,
 ( #259, #57894, #38523, #33821 ),
 .UNSPECIFIED., .F., .F.,
 ( 4, 4 ),
 ( 2.148040924471974165E-17, 0.004559932413162187670 ),
 .UNSPECIFIED. ) ;
#4145=ADVANCED_FACE ( 'NONE', ( #31286 ), #13739, .F. ) ;
#4148=CARTESIAN_POINT ( 'NONE',  ( 0.5997462898726536595, 48.97040376101512749, 3.667585803694950464 ) ) ;
#4155=CARTESIAN_POINT ( 'NONE',  ( 0.1368894036331276542, 9.195786968782886817, -43.15436047432628186 ) ) ;
#4156=VERTEX_POINT ( 'NONE', #51609 ) ;
#4161=CARTESIAN_POINT ( 'NONE',  ( 0.1129192098497455998, -12.08918212651712132, -42.43587472053631160 ) ) ;
#4163=CARTESIAN_POINT ( 'NONE',  ( 1.657374760986086271, 34.33505663815240183, 27.60424483493635606 ) ) ;
#4174=ORIENTED_EDGE ( 'NONE', *, *, #20872, .T. ) ;
#4177=CARTESIAN_POINT ( 'NONE',  ( 3.050102900204245682, -5.228472987645193193, 43.68167029081563868 ) ) ;
#4182=DIRECTION ( 'NONE',  ( 0.000000000000000000, 0.000000000000000000, -1.000000000000000000 ) ) ;
#4187=CARTESIAN_POINT ( 'NONE',  ( -6.079354080745853928, -8.907665152502719508, -17.07180297388212864 ) ) ;
#4194=CARTESIAN_POINT ( 'NONE',  ( -6.079354080745853928, 0.6160181061929859148, 19.24612888195972715 ) ) ;
#4203=CARTESIAN_POINT ( 'NONE',  ( 0.6039202388192952409, -42.87364092186839315, 23.94607748571118933 ) ) ;
#4207=CARTESIAN_POINT ( 'NONE',  ( 0.1140933569871964703, -7.416386428228847194, 43.49651896912084226 ) ) ;
#4208=CARTESIAN_POINT ( 'NONE',  ( 0.8753041380234530822, -6.957149426674413384, 48.60798699522440813 ) ) ;
#4210=EDGE_CURVE ( 'NONE', #31513, #22365, #799, .T. ) ;
#4212=CARTESIAN_POINT ( 'NONE',  ( 0.5997462898726536595, 10.41743419021343087, -47.98988117339822423 ) ) ;
#4223=ADVANCED_FACE ( 'NONE', ( #35896 ), #20132, .F. ) ;
#4225=CARTESIAN_POINT ( 'NONE',  ( 0.1119899015040010243, 14.71105729511424087, 41.59983294981330459 ) ) ;
#4230=CARTESIAN_POINT ( 'NONE',  ( 0.1152339509894530906, 33.74256222853660603, 28.43206261790687961 ) ) ;
#4235=B_SPLINE_CURVE_WITH_KNOTS ( 'NONE', 3,
 ( #48146, #58432, #38451, #44692, #1124, #14956, #49363, #43783, #29952, #34663, #15867, #20263, #10235, #39378, #15252, #53128 ),
 .UNSPECIFIED., .F., .F.,
 ( 4, 3, 3, 3, 3, 4 ),
 ( 2.501947744657918636E-17, 0.0002612764279487730544, 0.0003919131003184758298, 0.0005225497727000631958, 0.0007837925190632400417, 0.001045051706266714566 ),
 .UNSPECIFIED. ) ;
#4237=CARTESIAN_POINT ( 'NONE',  ( 0.1156495703730067576, 41.83314862904525455, -14.03319739087566731 ) ) ;
#4244=CARTESIAN_POINT ( 'NONE',  ( 0.1157506346131639274, -44.12405299995102581, 0.09277208818792900824 ) ) ;
#4246=DIRECTION ( 'NONE',  ( 0.09722883295013594329, -0.03945211390406794250, -0.9944798061055111216 ) ) ;
#4254=CARTESIAN_POINT ( 'NONE',  ( -6.079354080745853928, -4.285997663762750598, 18.77293741731384813 ) ) ;
#4266=ORIENTED_EDGE ( 'NONE', *, *, #27095, .F. ) ;
#4271=CARTESIAN_POINT ( 'NONE',  ( 5.901764892641288895, -10.93876531158257492, -47.73190631954474838 ) ) ;
#4275=CARTESIAN_POINT ( 'NONE',  ( 0.5997462898726536595, -30.20781297212564454, -38.71743361310750231 ) ) ;
#4286=LINE ( 'NONE', #47549, #1807 ) ;
#4295=CARTESIAN_POINT ( 'NONE',  ( 0.6039202388192953519, 32.88598194813106090, -36.47020570487901381 ) ) ;
#4299=CARTESIAN_POINT ( 'NONE',  ( 0.9268187852002115479, -26.70623247702148362, 35.07893213585482783 ) ) ;
#4300=VERTEX_POINT ( 'NONE', #26190 ) ;
#4317=CARTESIAN_POINT ( 'NONE',  ( 0.6021447746440204973, -42.91583701453753719, -23.86989887766889140 ) ) ;
#4319=CARTESIAN_POINT ( 'NONE',  ( 4.553261556744875094, -29.36425772793644029, -32.66925058691983708 ) ) ;
#4321=ORIENTED_EDGE ( 'NONE', *, *, #48667, .F. ) ;
#4330=FACE_OUTER_BOUND ( 'NONE', #6866, .T. ) ;
#4332=CARTESIAN_POINT ( 'NONE',  ( 4.553261556744873317, 43.53643125131393532, -5.841123155973635406 ) ) ;
#4334=ORIENTED_EDGE ( 'NONE', *, *, #1048, .T. ) ;
#4337=CARTESIAN_POINT ( 'NONE',  ( 0.8744876279028263033, -24.68559978112701714, -42.43785119236734715 ) ) ;
#4344=CARTESIAN_POINT ( 'NONE',  ( 4.335381028904201628, 47.11764506933897678, -13.40463989759294527 ) ) ;
#4347=CARTESIAN_POINT ( 'NONE',  ( 0.5980271706414711508, -0.8742700727934676896, -49.10483575658795985 ) ) ;
#4349=VECTOR ( 'NONE', #51474, 1000.000000000000000 ) ;
#4352=CARTESIAN_POINT ( 'NONE',  ( 0.8744876279028263033, 21.91587810745035725, 43.93226988398016886 ) ) ;
#4353=( BOUNDED_SURFACE ( )  B_SPLINE_SURFACE ( 3, 1, ( 
 ( #4450, #23590 ),
 ( #18915, #33319 ),
 ( #52391, #5074 ),
 ( #24204, #9485 ) ),
 .UNSPECIFIED., .F., .F., .F. ) 
 B_SPLINE_SURFACE_WITH_KNOTS ( ( 4, 4 ),
 ( 2, 2 ),
 ( 0.000000000000000000, 1.000000000000000000 ),
 ( 0.000000000000000000, 1.000000000000000000 ),
 .UNSPECIFIED. ) 
 GEOMETRIC_REPRESENTATION_ITEM ( )  RATIONAL_B_SPLINE_SURFACE ( (
 ( 1.000000000000000000, 1.000000000000000000),
 ( 0.7211978278499970862, 0.9934217856018976445),
 ( 0.7211978278499970862, 0.9934217856018976445),
 ( 1.000000000000000000, 1.000000000000000000) ) ) 
 REPRESENTATION_ITEM ( '' )  SURFACE ( )  );
#4365=CARTESIAN_POINT ( 'NONE',  ( 0.1135584504625007790, 4.666723112812798391, -43.87680192907855314 ) ) ;
#4366=CARTESIAN_POINT ( 'NONE',  ( 4.834790513006555379, 34.26126461650152777, 32.53851698836996320 ) ) ;
#4369=B_SPLINE_CURVE_WITH_KNOTS ( 'NONE', 3,
 ( #2274, #21406, #35834, #40540 ),
 .UNSPECIFIED., .F., .F.,
 ( 4, 4 ),
 ( 0.000000000000000000, 0.004442905043737214836 ),
 .UNSPECIFIED. ) ;
#4371=ORIENTED_EDGE ( 'NONE', *, *, #26645, .F. ) ;
#4372=ORIENTED_EDGE ( 'NONE', *, *, #5786, .T. ) ;
#4373=CARTESIAN_POINT ( 'NONE',  ( 0.5997462898726536595, 41.43917033312134635, -26.35046094941917971 ) ) ;
#4375=ORIENTED_EDGE ( 'NONE', *, *, #29725, .F. ) ;
#4378=CIRCLE ( 'NONE', #32418, 48.91267123290010943 ) ;
#4379=ORIENTED_EDGE ( 'NONE', *, *, #18689, .T. ) ;
#4382=FACE_OUTER_BOUND ( 'NONE', #10805, .T. ) ;
#4390=CARTESIAN_POINT ( 'NONE',  ( 0.1156867017252033725, -31.60951488276809940, -30.78605814571343657 ) ) ;
#4398=DIRECTION ( 'NONE',  ( 0.000000000000000000, -1.000000000000000000, 0.000000000000000000 ) ) ;
#4400=CARTESIAN_POINT ( 'NONE',  ( 0.6039202388192952409, 46.66051417535201296, -15.30882522405831914 ) ) ;
#4404=EDGE_CURVE ( 'NONE', #20911, #41448, #46554, .T. ) ;
#4421=CARTESIAN_POINT ( 'NONE',  ( 3.727782113643637096, -20.93509053340439152, 38.65876045948883188 ) ) ;
#4425=CARTESIAN_POINT ( 'NONE',  ( 0.1129192098497447394, 37.24220309526806005, 23.66368729500878842 ) ) ;
#4428=CARTESIAN_POINT ( 'NONE',  ( -6.077587904424778920, 13.83688374988438241, -13.39166417911216911 ) ) ;
#4440=ORIENTED_EDGE ( 'NONE', *, *, #14558, .T. ) ;
#4443=CARTESIAN_POINT ( 'NONE',  ( 4.694002226626920127, 13.30107597157337196, 43.60465742835927472 ) ) ;
#4446=ORIENTED_EDGE ( 'NONE', *, *, #21155, .T. ) ;
#4449=CARTESIAN_POINT ( 'NONE',  ( -2.601141883200665639, -13.99736252863769259, 5.183557630747252176 ) ) ;
#4450=CARTESIAN_POINT ( 'NONE',  ( -6.077587904424778920, -8.912150607695132010, -17.06955163264957420 ) ) ;
#4458=EDGE_LOOP ( 'NONE', ( #58068, #25684, #17201, #37951 ) ) ;
#4462=CARTESIAN_POINT ( 'NONE',  ( 3.390910168358336918, 34.73058703434708150, 26.97931542465967070 ) ) ;
#4474=CARTESIAN_POINT ( 'NONE',  ( 0.6000166863083090663, -30.20952222014404143, -38.71961065066482632 ) ) ;
#4477=VECTOR ( 'NONE', #13728, 1000.000000000000114 ) ;
#4478=ORIENTED_EDGE ( 'NONE', *, *, #38452, .F. ) ;
#4485=CARTESIAN_POINT ( 'NONE',  ( 1.830465331921978356, 42.98436206491231104, 9.629157478768243905 ) ) ;
#4487=CARTESIAN_POINT ( 'NONE',  ( 4.553261556744875094, 0.000000000000000000, 0.000000000000000000 ) ) ;
#4496=EDGE_CURVE ( 'NONE', #34059, #31779, #54586, .T. ) ;
#4506=CARTESIAN_POINT ( 'NONE',  ( 0.3676999524040366896, 44.06746933160592050, 2.002181318165502599 ) ) ;
#4507=CARTESIAN_POINT ( 'NONE',  ( 0.6028777368367060907, 48.21841697337477939, -9.301832824386606191 ) ) ;
#4519=CARTESIAN_POINT ( 'NONE',  ( 0.6021448801613057400, 11.18197771114837558, -47.81740805495764590 ) ) ;
#4523=ORIENTED_EDGE ( 'NONE', *, *, #58325, .F. ) ;
#4526=CARTESIAN_POINT ( 'NONE',  ( 3.727782113643637096, -39.89987845506692565, 18.46015913194848679 ) ) ;
#4528=CARTESIAN_POINT ( 'NONE',  ( -6.072942160501519027, -16.13052748855422180, -10.51714054436931889 ) ) ;
#4534=CARTESIAN_POINT ( 'NONE',  ( 0.1140933569871964981, 33.35113380425563179, 28.89034136272091402 ) ) ;
#4535=VERTEX_POINT ( 'NONE', #26423 ) ;
#4547=CARTESIAN_POINT ( 'NONE',  ( -2.601141883200662974, 14.86024923780644436, -1.403003941427712009 ) ) ;
#4549=ORIENTED_EDGE ( 'NONE', *, *, #28358, .F. ) ;
#4550=CARTESIAN_POINT ( 'NONE',  ( 0.6029442701453591180, 4.628739180449442436, -48.88885352263488926 ) ) ;
#4551=VERTEX_POINT ( 'NONE', #55227 ) ;
#4552=CARTESIAN_POINT ( 'NONE',  ( 3.559346040607745287, 43.50545415529854409, 6.380105037004119239 ) ) ;
#4553=LINE ( 'NONE', #33417, #43447 ) ;
#4561=B_SPLINE_CURVE_WITH_KNOTS ( 'NONE', 3,
 ( #55860, #41800, #50855, #22984 ),
 .UNSPECIFIED., .F., .F.,
 ( 4, 4 ),
 ( 0.000000000000000000, 0.004442905043737214836 ),
 .UNSPECIFIED. ) ;
#4564=CARTESIAN_POINT ( 'NONE',  ( -6.078457390727109555, -8.910533588204199162, -17.07035155499126233 ) ) ;
#4570=EDGE_CURVE ( 'NONE', #4686, #38412, #25495, .T. ) ;
#4574=ADVANCED_FACE ( 'NONE', ( #35540 ), #3633, .F. ) ;
#4585=EDGE_LOOP ( 'NONE', ( #53563, #31360, #38347, #61022 ) ) ;
#4595=ORIENTED_EDGE ( 'NONE', *, *, #17307, .T. ) ;
#4597=B_SPLINE_CURVE_WITH_KNOTS ( 'NONE', 3,
 ( #48096, #5147, #26904, #47480, #47792, #61548 ),
 .UNSPECIFIED., .F., .F.,
 ( 4, 2, 4 ),
 ( 2.538052214298621590E-18, 0.0002447193893791698707, 0.0004894387787583371393 ),
 .UNSPECIFIED. ) ;
#4599=FACE_OUTER_BOUND ( 'NONE', #27913, .T. ) ;
#4603=ORIENTED_EDGE ( 'NONE', *, *, #51852, .F. ) ;
#4604=CARTESIAN_POINT ( 'NONE',  ( 0.1129192098497447394, 42.02659449688918869, 13.44310763102032702 ) ) ;
#4607=ORIENTED_EDGE ( 'NONE', *, *, #60043, .F. ) ;
#4614=CARTESIAN_POINT ( 'NONE',  ( 0.6027444965799114707, -7.708572526967942373, -48.49862292358326954 ) ) ;
#4616=CARTESIAN_POINT ( 'NONE',  ( 5.901764892641288895, -46.46096922681069685, 15.47158058974670425 ) ) ;
#4617=ORIENTED_EDGE ( 'NONE', *, *, #10329, .F. ) ;
#4620=LINE ( 'NONE', #9660, #22403 ) ;
#4621=VECTOR ( 'NONE', #44183, 1000.000000000000114 ) ;
#4626=CARTESIAN_POINT ( 'NONE',  ( 0.1135584504625008206, -38.65644560369402427, 21.27513255949062554 ) ) ;
#4629=EDGE_CURVE ( 'NONE', #35341, #15373, #10576, .T. ) ;
#4631=VERTEX_POINT ( 'NONE', #26739 ) ;
#4634=CARTESIAN_POINT ( 'NONE',  ( 0.8753041380234524160, 28.81806460335452158, 39.75748332565662935 ) ) ;
#4636=CARTESIAN_POINT ( 'NONE',  ( 0.1119898979215350338, -42.53546966996757561, 11.73435674449596533 ) ) ;
#4641=CARTESIAN_POINT ( 'NONE',  ( 0.6252788684277217346, -34.79439316893326861, 34.65248238119973934 ) ) ;
#4642=CARTESIAN_POINT ( 'NONE',  ( 2.359973842542475886, 42.89855597191755976, -9.891905284461445902 ) ) ;
#4643=CARTESIAN_POINT ( 'NONE',  ( 4.060580049360325461, -39.37537800281265987, -19.52043292283310549 ) ) ;
#4649=CARTESIAN_POINT ( 'NONE',  ( 0.8753041380234471980, -24.68967207985765100, -42.44476905888495111 ) ) ;
#4650=CONICAL_SURFACE ( 'NONE', #33726, 43.92652462719577500, 1.486293639869522343 ) ;
#4653=ADVANCED_FACE ( 'NONE', ( #3837 ), #10071, .F. ) ;
#4656=EDGE_CURVE ( 'NONE', #59176, #22696, #56161, .T. ) ;
#4670=B_SPLINE_CURVE_WITH_KNOTS ( 'NONE', 3,
 ( #36128, #59583, #12313, #35812, #54251, #16377, #48965, #7260, #26388, #16693, #54879, #45519, #11370, #25148, #1323, #53949, #49261, #30456, #37667, #32029, #3189, #2879, #60200, #27940, #22010 ),
 .UNSPECIFIED., .F., .F.,
 ( 4, 3, 3, 3, 3, 3, 3, 3, 4 ),
 ( 5.818439421673296370E-18, 0.0005656085177311399653, 0.001131215744874499839, 0.001696821861372766350, 0.002262427090022498151, 0.002828031679238745492, 0.003393635864401603995, 0.003977030878808131623, 0.004561030005651159000 ),
 .UNSPECIFIED. ) ;
#4673=EDGE_LOOP ( 'NONE', ( #18615, #11678, #52264, #16868 ) ) ;
#4686=VERTEX_POINT ( 'NONE', #32682 ) ;
#4689=CARTESIAN_POINT ( 'NONE',  ( 0.1365634738349431054, -43.83788975358855566, 5.010193766259522619 ) ) ;
#4692=ORIENTED_EDGE ( 'NONE', *, *, #7190, .T. ) ;
#4704=ORIENTED_EDGE ( 'NONE', *, *, #37160, .F. ) ;
#4708=CARTESIAN_POINT ( 'NONE',  ( 0.1158516988532803521, 25.20378146029254296, -36.21755871030804741 ) ) ;
#4715=CARTESIAN_POINT ( 'NONE',  ( 0.7948884756798498818, -26.19034543985806351, 41.53028353311662357 ) ) ;
#4721=CARTESIAN_POINT ( 'NONE',  ( 0.5997462898726536595, -42.52950339524503676, 24.55184251941493301 ) ) ;
#4727=EDGE_CURVE ( 'NONE', #19604, #47629, #25420, .T. ) ;
#4728=CARTESIAN_POINT ( 'NONE',  ( 0.1154773475650540809, -43.78456205353491271, -5.464042077644623241 ) ) ;
#4731=CARTESIAN_POINT ( 'NONE',  ( 2.648799415243708655, 44.76338677751262907, 20.01890774983506205 ) ) ;
#4735=ORIENTED_EDGE ( 'NONE', *, *, #57090, .F. ) ;
#4740=CARTESIAN_POINT ( 'NONE',  ( -2.601141883200665639, -14.54530301301458550, 3.351057703021155909 ) ) ;
#4742=CARTESIAN_POINT ( 'NONE',  ( 0.2285344041767122802, -23.51740999911909924, -37.32871009328864176 ) ) ;
#4748=CARTESIAN_POINT ( 'NONE',  ( 0.8744876279028263033, -31.30103973185235233, 37.82320666052117275 ) ) ;
#4753=VERTEX_POINT ( 'NONE', #38318 ) ;
#4755=ORIENTED_EDGE ( 'NONE', *, *, #3090, .F. ) ;
#4758=CARTESIAN_POINT ( 'NONE',  ( 0.1129192098497455998, 42.02659449688937343, -13.44310763101974260 ) ) ;
#4766=CARTESIAN_POINT ( 'NONE',  ( 0.8744876279028263033, 48.35212675551510841, -8.510105087370661181 ) ) ;
#4770=ORIENTED_EDGE ( 'NONE', *, *, #3143, .T. ) ;
#4772=ORIENTED_EDGE ( 'NONE', *, *, #58101, .F. ) ;
#4773=CARTESIAN_POINT ( 'NONE',  ( 1.834102595619085285, 34.36982342788820688, 27.54837531313729215 ) ) ;
#4775=CARTESIAN_POINT ( 'NONE',  ( 4.975610109902397937, 30.94437158899580353, 37.88001153774800400 ) ) ;
#4783=CARTESIAN_POINT ( 'NONE',  ( -6.078075953587585900, 12.01009662667709499, 15.05166945109463406 ) ) ;
#4785=CARTESIAN_POINT ( 'NONE',  ( 0.7242486021783839378, -24.75018186179863378, -42.40801764032205057 ) ) ;
#4786=ADVANCED_FACE ( 'NONE', ( #19821 ), #16465, .F. ) ;
#4797=CARTESIAN_POINT ( 'NONE',  ( 4.553261556744875094, -39.67390170502071811, 18.85526688551479424 ) ) ;
#4809=CARTESIAN_POINT ( 'NONE',  ( 0.6024113833632039894, 41.03720235841333164, 26.97202053416656042 ) ) ;
#4818=AXIS2_PLACEMENT_3D ( 'NONE', #8761, #5275, #56670 ) ;
#4822=ORIENTED_EDGE ( 'NONE', *, *, #28935, .F. ) ;
#4827=VERTEX_POINT ( 'NONE', #21659 ) ;
#4838=AXIS2_PLACEMENT_3D ( 'NONE', #38064, #61503, #23933 ) ;
#4849=B_SPLINE_CURVE_WITH_KNOTS ( 'NONE', 3,
 ( #12761, #31854, #8031, #3312 ),
 .UNSPECIFIED., .F., .F.,
 ( 4, 4 ),
 ( 0.000000000000000000, 0.005013413432710148512 ),
 .UNSPECIFIED. ) ;
#4850=DIRECTION ( 'NONE',  ( 0.000000000000000000, 0.000000000000000000, 1.000000000000000000 ) ) ;
#4851=CARTESIAN_POINT ( 'NONE',  ( 0.8753041380234471980, -48.57841546934875510, -7.160717726619150625 ) ) ;
#4853=VERTEX_POINT ( 'NONE', #45186 ) ;
#4855=DIRECTION ( 'NONE',  ( 0.09722883295013597105, -0.02434548463872390767, -0.9949642463027805750 ) ) ;
#4866=ORIENTED_EDGE ( 'NONE', *, *, #32109, .T. ) ;
#4868=ORIENTED_EDGE ( 'NONE', *, *, #53523, .F. ) ;
#4871=EDGE_CURVE ( 'NONE', #2370, #34487, #49274, .T. ) ;
#4876=B_SPLINE_CURVE_WITH_KNOTS ( 'NONE', 3,
 ( #46061, #45135, #17227, #46357, #6862, #2169, #55718, #60412, #36651, #27234, #26001, #3401, #2792, #49803, #59495, #12231 ),
 .UNSPECIFIED., .F., .F.,
 ( 4, 3, 3, 3, 3, 4 ),
 ( 2.221635811791082109E-17, 0.0002612764279487773370, 0.0003919131003184819014, 0.0005225497727000633042, 0.0007837925190632458964, 0.001045051706266715867 ),
 .UNSPECIFIED. ) ;
#4885=CARTESIAN_POINT ( 'NONE',  ( 0.9268187852002115479, -16.93486955123884385, 40.70582914265657593 ) ) ;
#4893=EDGE_CURVE ( 'NONE', #19414, #8016, #17236, .T. ) ;
#4904=VERTEX_POINT ( 'NONE', #50166 ) ;
#4914=( BOUNDED_SURFACE ( )  B_SPLINE_SURFACE ( 3, 1, ( 
 ( #32158, #27757 ),
 ( #45966, #3010 ),
 ( #31850, #50932 ),
 ( #13060, #31529 ) ),
 .UNSPECIFIED., .F., .F., .F. ) 
 B_SPLINE_SURFACE_WITH_KNOTS ( ( 4, 4 ),
 ( 2, 2 ),
 ( 0.000000000000000000, 1.000000000000000000 ),
 ( 0.000000000000000000, 1.000000000000000000 ),
 .UNSPECIFIED. ) 
 GEOMETRIC_REPRESENTATION_ITEM ( )  RATIONAL_B_SPLINE_SURFACE ( (
 ( 1.000000000000000000, 1.000000000000000000),
 ( 0.9953485035131437453, 0.8621029689291523912),
 ( 0.9953485035131437453, 0.8621029689291523912),
 ( 1.000000000000000000, 1.000000000000000000) ) ) 
 REPRESENTATION_ITEM ( '' )  SURFACE ( )  );
#4916=CARTESIAN_POINT ( 'NONE',  ( -2.739355103387247858, -14.37091041638168676, -4.040358988425336584 ) ) ;
#4919=EDGE_CURVE ( 'NONE', #16981, #13219, #32888, .T. ) ;
#4925=CARTESIAN_POINT ( 'NONE',  ( -6.077587904424778920, -8.901182807328710922, -17.07527352707552382 ) ) ;
#4928=EDGE_CURVE ( 'NONE', #8016, #33629, #12039, .T. ) ;
#4929=( BOUNDED_SURFACE ( )  B_SPLINE_SURFACE ( 3, 1, ( 
 ( #53652, #20186 ),
 ( #14566, #16637 ),
 ( #29252, #24248 ),
 ( #39298, #58352 ) ),
 .UNSPECIFIED., .F., .F., .F. ) 
 B_SPLINE_SURFACE_WITH_KNOTS ( ( 4, 4 ),
 ( 2, 2 ),
 ( 0.000000000000000000, 1.000000000000000000 ),
 ( 0.000000000000000000, 1.000000000000000000 ),
 .UNSPECIFIED. ) 
 GEOMETRIC_REPRESENTATION_ITEM ( )  RATIONAL_B_SPLINE_SURFACE ( (
 ( 1.000000000000000000, 1.000000000000000000),
 ( 0.9953485035131437453, 0.8621029689291523912),
 ( 0.9953485035131437453, 0.8621029689291523912),
 ( 1.000000000000000000, 1.000000000000000000) ) ) 
 REPRESENTATION_ITEM ( '' )  SURFACE ( )  );
#4932=CARTESIAN_POINT ( 'NONE',  ( 0.8744876279028263033, -14.81965677138014037, 46.80521149998127584 ) ) ;
#4937=CARTESIAN_POINT ( 'NONE',  ( 0.5980271706414711508, -48.79397779905849575, 5.585425085581966265 ) ) ;
#4953=CARTESIAN_POINT ( 'NONE',  ( 0.2279481005628812007, -28.09744832277539928, 34.01524488845964100 ) ) ;
#4955=ORIENTED_EDGE ( 'NONE', *, *, #2318, .F. ) ;
#4961=VERTEX_POINT ( 'NONE', #60776 ) ;
#4964=CARTESIAN_POINT ( 'NONE',  ( 0.3676999524040366896, 43.13409918076302318, -9.241215893319285613 ) ) ;
#4977=CARTESIAN_POINT ( 'NONE',  ( 4.553261556744875094, 27.56395660609745235, -34.20186927699732138 ) ) ;
#4980=VECTOR ( 'NONE', #14404, 1000.000000000000000 ) ;
#4982=CARTESIAN_POINT ( 'NONE',  ( 2.879087469061463178, 40.36424033792948052, 17.51655727376944327 ) ) ;
#4985=CARTESIAN_POINT ( 'NONE',  ( 0.3676999524040323597, -0.5887207181719652516, -44.10900124961835900 ) ) ;
#4987=B_SPLINE_CURVE_WITH_KNOTS ( 'NONE', 3,
 ( #23244, #18870, #46449, #51415 ),
 .UNSPECIFIED., .F., .F.,
 ( 4, 4 ),
 ( 0.000000000000000000, 0.005013413432710144176 ),
 .UNSPECIFIED. ) ;
#4988=EDGE_CURVE ( 'NONE', #41892, #54620, #42002, .T. ) ;
#5001=CARTESIAN_POINT ( 'NONE',  ( 0.2285344041767082557, -13.27967145753882505, -42.07316836506711866 ) ) ;
#5008=CARTESIAN_POINT ( 'NONE',  ( 4.553261556744875094, 0.000000000000000000, 0.000000000000000000 ) ) ;
#5016=VERTEX_POINT ( 'NONE', #52927 ) ;
#5019=CARTESIAN_POINT ( 'NONE',  ( 0.8753041380234465318, 5.600023814136007694, -48.78296896616778611 ) ) ;
#5027=VERTEX_POINT ( 'NONE', #57603 ) ;
#5029=CARTESIAN_POINT ( 'NONE',  ( 0.1156867017252034141, 25.34656052724063358, -36.11778892338390534 ) ) ;
#5040=CARTESIAN_POINT ( 'NONE',  ( 2.009741617377216460, -8.378475480318341440, -43.23546260014745002 ) ) ;
#5041=B_SPLINE_CURVE_WITH_KNOTS ( 'NONE', 3,
 ( #33606, #14498, #8858, #61758, #38016, #54 ),
 .UNSPECIFIED., .F., .F.,
 ( 4, 2, 4 ),
 ( 3.402737038855563874E-18, 0.0002447193893791695996, 0.0004894387787583357298 ),
 .UNSPECIFIED. ) ;
#5047=CARTESIAN_POINT ( 'NONE',  ( 4.553261556744873317, -9.554252317234828595, 42.87488575474283437 ) ) ;
#5048=CARTESIAN_POINT ( 'NONE',  ( 4.694002226626920127, -30.39302829899148506, 33.97864921186298659 ) ) ;
#5052=CARTESIAN_POINT ( 'NONE',  ( -6.078726893082806448, 19.09748444646209009, -2.465791776662926260 ) ) ;
#5053=EDGE_LOOP ( 'NONE', ( #18208, #9699, #29853, #5600, #14746, #55559 ) ) ;
#5059=CARTESIAN_POINT ( 'NONE',  ( 0.8753041380234465318, -39.87785955339043653, 28.65125905284175190 ) ) ;
#5068=ORIENTED_EDGE ( 'NONE', *, *, #27576, .F. ) ;
#5071=FACE_OUTER_BOUND ( 'NONE', #34121, .T. ) ;
#5074=CARTESIAN_POINT ( 'NONE',  ( 4.335381028904201628, 20.75278752742067567, 44.37430176922311631 ) ) ;
#5080=ORIENTED_EDGE ( 'NONE', *, *, #18952, .T. ) ;
#5082=B_SPLINE_CURVE_WITH_KNOTS ( 'NONE', 3,
 ( #58332, #94, #52725, #57719, #11071, #53632, #10762, #15457, #9826, #20460, #14848, #5707, #24540, #399, #19243, #5099 ),
 .UNSPECIFIED., .F., .F.,
 ( 4, 3, 3, 3, 3, 4 ),
 ( 1.962735358247463844E-17, 0.0002612764279487760901, 0.0003919131003184865634, 0.0005225497727000665569, 0.0007837925190632416680, 0.001045051706266717602 ),
 .UNSPECIFIED. ) ;
#5084=CARTESIAN_POINT ( 'NONE',  ( 0.6029442701453592290, 46.63311652831155385, 15.39148037114014045 ) ) ;
#5094=CARTESIAN_POINT ( 'NONE',  ( -6.079354080745853928, 9.983157571106950456, 16.46601105789171271 ) ) ;
#5096=CARTESIAN_POINT ( 'NONE',  ( -6.078457390727109555, 12.00936083188087089, 15.05223450013962250 ) ) ;
#5097=CARTESIAN_POINT ( 'NONE',  ( 0.1129192098497455998, 37.24220309526837980, -23.66368729500826618 ) ) ;
#5099=CARTESIAN_POINT ( 'NONE',  ( 0.5997462898726536595, -35.63787911784747564, -33.78599121124021565 ) ) ;
#5101=VERTEX_POINT ( 'NONE', #54769 ) ;
#5104=LINE ( 'NONE', #48355, #48836 ) ;
#5108=CARTESIAN_POINT ( 'NONE',  ( 0.1155031312995260795, -31.81355560820710338, 30.57514206173575033 ) ) ;
#5109=CARTESIAN_POINT ( 'NONE',  ( 0.6029442701453591180, -42.74546001881537904, 24.17376414500094839 ) ) ;
#5113=CARTESIAN_POINT ( 'NONE',  ( -6.077587904424778920, 19.09876248768971152, -2.456276212632990674 ) ) ;
#5122=CARTESIAN_POINT ( 'NONE',  ( 0.6027444965799114707, 33.11153390055023493, -36.26520148351796990 ) ) ;
#5125=DIRECTION ( 'NONE',  ( -0.1011922191286467321, 0.9589869809184654592, 0.2647717983787297169 ) ) ;
#5128=CARTESIAN_POINT ( 'NONE',  ( 0.6027444965799114707, -30.71998326625707776, 38.31215399854628600 ) ) ;
#5134=VERTEX_POINT ( 'NONE', #35085 ) ;
#5140=CARTESIAN_POINT ( 'NONE',  ( 0.5980271706414734822, -2.273683837877277902, -49.05995928093539504 ) ) ;
#5141=CARTESIAN_POINT ( 'NONE',  ( 0.8744876279028306332, -47.25615711918273121, 13.31186180466906954 ) ) ;
#5147=CARTESIAN_POINT ( 'NONE',  ( 0.7948884756798504370, -6.978576367878667419, -48.60039214325163925 ) ) ;
#5149=EDGE_CURVE ( 'NONE', #16494, #57030, #27648, .T. ) ;
#5150=CARTESIAN_POINT ( 'NONE',  ( 0.7242003506639983490, -47.69730471853326037, -11.66099467084223207 ) ) ;
#5155=CARTESIAN_POINT ( 'NONE',  ( 0.08486401232817714080, 9.539392014169456147, 3.000000000000000000 ) ) ;
#5156=ORIENTED_EDGE ( 'NONE', *, *, #31156, .T. ) ;
#5160=CARTESIAN_POINT ( 'NONE',  ( 2.359973842542475886, 44.00467994243045666, 1.313026198047289705 ) ) ;
#5162=CARTESIAN_POINT ( 'NONE',  ( 0.1154773475650540532, 41.81928631232078430, -14.07447769454556408 ) ) ;
#5165=DIRECTION ( 'NONE',  ( -1.000000000000000000, -0.000000000000000000, -0.000000000000000000 ) ) ;
#5174=CARTESIAN_POINT ( 'NONE',  ( 4.834790513006555379, -22.26269597880774143, -41.67687258755817226 ) ) ;
#5177=CARTESIAN_POINT ( 'NONE',  ( 0.1145239942831223490, 9.499891895270792475, 43.08941325526308219 ) ) ;
#5184=( BOUNDED_SURFACE ( )  B_SPLINE_SURFACE ( 3, 1, ( 
 ( #43363, #48648 ),
 ( #93, #61801 ),
 ( #5706, #23928 ),
 ( #20164, #48349 ) ),
 .UNSPECIFIED., .F., .F., .F. ) 
 B_SPLINE_SURFACE_WITH_KNOTS ( ( 4, 4 ),
 ( 2, 2 ),
 ( 0.000000000000000000, 1.000000000000000000 ),
 ( 0.000000000000000000, 1.000000000000000000 ),
 .UNSPECIFIED. ) 
 GEOMETRIC_REPRESENTATION_ITEM ( )  RATIONAL_B_SPLINE_SURFACE ( (
 ( 1.000000000000000000, 1.000000000000000000),
 ( 0.9953485035131437453, 0.8621029689291515030),
 ( 0.9953485035131437453, 0.8621029689291515030),
 ( 1.000000000000000000, 1.000000000000000000) ) ) 
 REPRESENTATION_ITEM ( '' )  SURFACE ( )  );
#5185=CARTESIAN_POINT ( 'NONE',  ( 0.7242486021783832717, -0.7549377848418828973, -49.09624762968133638 ) ) ;
#5206=CARTESIAN_POINT ( 'NONE',  ( 0.2285344041767107259, 39.41443120982247450, -19.82432300739741748 ) ) ;
#5213=ORIENTED_EDGE ( 'NONE', *, *, #23530, .T. ) ;
#5222=ORIENTED_EDGE ( 'NONE', *, *, #889, .F. ) ;
#5241=CARTESIAN_POINT ( 'NONE',  ( 0.6252788684277218456, 28.65511785929881938, 39.87892365201650335 ) ) ;
#5243=EDGE_LOOP ( 'NONE', ( #53000, #17728, #1539, #9040 ) ) ;
#5248=ADVANCED_FACE ( 'NONE', ( #13129 ), #38990, .F. ) ;
#5249=ORIENTED_EDGE ( 'NONE', *, *, #44191, .F. ) ;
#5252=B_SPLINE_CURVE_WITH_KNOTS ( 'NONE', 3,
 ( #55804, #17005, #8819, #13534 ),
 .UNSPECIFIED., .F., .F.,
 ( 4, 4 ),
 ( 9.813077866773594792E-18, 0.005013413432710153717 ),
 .UNSPECIFIED. ) ;
#5254=VERTEX_POINT ( 'NONE', #36018 ) ;
#5258=VERTEX_POINT ( 'NONE', #12207 ) ;
#5261=CARTESIAN_POINT ( 'NONE',  ( 0.1129192098497447394, -27.88830454350447852, -34.19348267541494124 ) ) ;
#5272=DIRECTION ( 'NONE',  ( 0.000000000000000000, 0.000000000000000000, -1.000000000000000000 ) ) ;
#5275=DIRECTION ( 'NONE',  ( -1.000000000000000000, -0.000000000000000000, -0.000000000000000000 ) ) ;
#5277=CARTESIAN_POINT ( 'NONE',  ( 0.8744876279028306332, 43.84003649649945089, -22.09980204357244560 ) ) ;
#5278=CARTESIAN_POINT ( 'NONE',  ( 5.901764892641288895, 25.42221402738026725, 41.85334516362757995 ) ) ;
#5281=CARTESIAN_POINT ( 'NONE',  ( 0.1135584504625008484, 29.34358894678132756, 32.95308543759726660 ) ) ;
#5283=ADVANCED_FACE ( 'NONE', ( #46955 ), #41019, .F. ) ;
#5284=CARTESIAN_POINT ( 'NONE',  ( 2.299652685299200972, -6.551234707231919252, -48.59385813730900594 ) ) ;
#5289=CARTESIAN_POINT ( 'NONE',  ( 0.3676999524040323597, 24.55639947020961600, 36.64606156713607277 ) ) ;
#5293=CARTESIAN_POINT ( 'NONE',  ( 4.060580049360325461, 40.54515549719436507, 16.95753696936963451 ) ) ;
#5301=ORIENTED_EDGE ( 'NONE', *, *, #13686, .T. ) ;
#5303=ORIENTED_EDGE ( 'NONE', *, *, #2997, .F. ) ;
#5308=CARTESIAN_POINT ( 'NONE',  ( 0.1149546198390367091, 29.86693622343102561, -32.47941941674333322 ) ) ;
#5311=CARTESIAN_POINT ( 'NONE',  ( 0.7242003506639987931, 3.899036689095574992, -48.94700386155533778 ) ) ;
#5315=ORIENTED_EDGE ( 'NONE', *, *, #17354, .F. ) ;
#5321=CARTESIAN_POINT ( 'NONE',  ( 4.390527457369401532, -36.64446048591713634, -24.23569376611028403 ) ) ;
#5324=CARTESIAN_POINT ( 'NONE',  ( 0.1152339509894530906, -23.06439601559337760, -37.61617108227687822 ) ) ;
#5327=CARTESIAN_POINT ( 'NONE',  ( 0.6000166863083090663, 5.235566842225173545, -48.83044461756462340 ) ) ;
#5332=CARTESIAN_POINT ( 'NONE',  ( 4.553261556744875094, 0.000000000000000000, 0.000000000000000000 ) ) ;
#5335=CARTESIAN_POINT ( 'NONE',  ( 0.1135584504625007374, 25.59731996755785133, -35.94063525612362753 ) ) ;
#5337=CARTESIAN_POINT ( 'NONE',  ( -6.057079549204054558, 15.43788712751053360, -11.51098919024698830 ) ) ;
#5348=CARTESIAN_POINT ( 'NONE',  ( 1.834102595619085729, -8.313124016454807474, -43.25609452949638012 ) ) ;
#5357=DIRECTION ( 'NONE',  ( 0.000000000000000000, 0.000000000000000000, 1.000000000000000000 ) ) ;
#5359=CARTESIAN_POINT ( 'NONE',  ( 0.2940135542859012574, 21.11549841703935826, 38.73469085059837624 ) ) ;
#5360=ORIENTED_EDGE ( 'NONE', *, *, #605, .F. ) ;
#5361=EDGE_CURVE ( 'NONE', #8488, #41223, #58379, .T. ) ;
#5379=ORIENTED_EDGE ( 'NONE', *, *, #16062, .F. ) ;
#5381=ORIENTED_EDGE ( 'NONE', *, *, #44725, .T. ) ;
#5389=ADVANCED_FACE ( 'NONE', ( #25501 ), #51381, .F. ) ;
#5393=B_SPLINE_CURVE_WITH_KNOTS ( 'NONE', 3,
 ( #51801, #8900, #28009, #42436, #23927, #92 ),
 .UNSPECIFIED., .F., .F.,
 ( 4, 2, 4 ),
 ( 0.000000000000000000, 0.0002447195606305749629, 0.0004894391212611499259 ),
 .UNSPECIFIED. ) ;
#5395=ORIENTED_EDGE ( 'NONE', *, *, #3090, .T. ) ;
#5401=CARTESIAN_POINT ( 'NONE',  ( 0.1139756605157202785, -1.811577870781945654, -44.08711155556820671 ) ) ;
#5406=DIRECTION ( 'NONE',  ( -0.9990097760809876215, 0.000000000000000000, 0.04449120468828399177 ) ) ;
#5407=CARTESIAN_POINT ( 'NONE',  ( 0.1147471544378676628, 36.80973225548471817, -24.33096380649096346 ) ) ;
#5409=CARTESIAN_POINT ( 'NONE',  ( 1.296416391601052265, -5.934581262136242152, 43.67022005118890604 ) ) ;
#5413=CARTESIAN_POINT ( 'NONE',  ( 4.553261556744875094, 0.000000000000000000, 0.000000000000000000 ) ) ;
#5418=CARTESIAN_POINT ( 'NONE',  ( 0.1156495703730067437, -31.60158840537683034, 30.79419691253894342 ) ) ;
#5428=CARTESIAN_POINT ( 'NONE',  ( 0.1149546198390366952, -35.52488601809844226, 26.17114897027513010 ) ) ;
#5429=CARTESIAN_POINT ( 'NONE',  ( 0.2940133293163023631, -26.87228827769844131, -34.98743592060318974 ) ) ;
#5437=CARTESIAN_POINT ( 'NONE',  ( 0.7242003506639974608, 23.43456264649780962, 43.14896230146672451 ) ) ;
#5449=CARTESIAN_POINT ( 'NONE',  ( 0.7242003506639991262, -47.28180849633769611, 13.24546184327587994 ) ) ;
#5467=CARTESIAN_POINT ( 'NONE',  ( 3.050102900204245682, 43.98187602336167856, 1.009866646495158671 ) ) ;
#5469=ORIENTED_EDGE ( 'NONE', *, *, #61650, .F. ) ;
#5480=VERTEX_POINT ( 'NONE', #46182 ) ;
#5481=CARTESIAN_POINT ( 'NONE',  ( 0.6029443199889047422, 4.715417708898021587, -48.88049179053964366 ) ) ;
#5501=EDGE_CURVE ( 'NONE', #13767, #6071, #36020, .T. ) ;
#5506=CARTESIAN_POINT ( 'NONE',  ( 0.6008123274975392114, -20.27530734412516367, 44.72657446373153078 ) ) ;
#5511=B_SPLINE_CURVE_WITH_KNOTS ( 'NONE', 3,
 ( #13294, #17676, #22371, #8257, #3862, #46198 ),
 .UNSPECIFIED., .F., .F.,
 ( 4, 2, 4 ),
 ( 0.000000000000000000, 0.0002447195606305732282, 0.0004894391212611464564 ),
 .UNSPECIFIED. ) ;
#5513=B_SPLINE_CURVE_WITH_KNOTS ( 'NONE', 3,
 ( #52802, #43439, #52490, #802, #9273, #29007, #479, #48418, #15228, #5481, #4550, #19939, #47200, #39050, #23688, #58106 ),
 .UNSPECIFIED., .F., .F.,
 ( 4, 3, 3, 3, 3, 4 ),
 ( 2.081781105835003463E-17, 0.0002612764279487753854, 0.0003919131003184801124, 0.0005225497727000663400, 0.0007837925190632469806, 0.001045051706266716084 ),
 .UNSPECIFIED. ) ;
#5514=CARTESIAN_POINT ( 'NONE',  ( 0.5987334308729319599, 48.31411601509184806, 8.792559368578421797 ) ) ;
#5520=CARTESIAN_POINT ( 'NONE',  ( -2.739355103387248747, 1.171460933655357417, -14.88204442379931614 ) ) ;
#5521=EDGE_CURVE ( 'NONE', #51544, #14950, #46804, .T. ) ;
#5522=AXIS2_PLACEMENT_3D ( 'NONE', #4487, #19250, #52119 ) ;
#5528=CARTESIAN_POINT ( 'NONE',  ( -6.078726893082806448, -11.01388439747515235, 15.79520154185357050 ) ) ;
#5530=VERTEX_POINT ( 'NONE', #52080 ) ;
#5537=CARTESIAN_POINT ( 'NONE',  ( 3.678834586032787790, -15.69774311151756940, 46.39173666541442032 ) ) ;
#5538=VERTEX_POINT ( 'NONE', #22356 ) ;
#5545=EDGE_CURVE ( 'NONE', #39018, #48274, #4561, .T. ) ;
#5547=CARTESIAN_POINT ( 'NONE',  ( 0.3676999524040366896, -0.5887207181726206162, 44.10900124961835900 ) ) ;
#5552=CARTESIAN_POINT ( 'NONE',  ( 0.3676999524040323597, 39.37931578712994707, 19.88014264185084912 ) ) ;
#5558=ORIENTED_EDGE ( 'NONE', *, *, #51071, .T. ) ;
#5559=CARTESIAN_POINT ( 'NONE',  ( 4.975610109902397937, 0.000000000000000000, 0.000000000000000000 ) ) ;
#5560=LINE ( 'NONE', #10606, #1014 ) ;
#5561=CONICAL_SURFACE ( 'NONE', #51582, 43.92652462719577500, 1.486293639869522343 ) ;
#5564=( BOUNDED_SURFACE ( )  B_SPLINE_SURFACE ( 3, 1, ( 
 ( #8589, #61816 ),
 ( #42156, #52738 ),
 ( #4187, #33050 ),
 ( #52123, #32424 ) ),
 .UNSPECIFIED., .F., .F., .F. ) 
 B_SPLINE_SURFACE_WITH_KNOTS ( ( 4, 4 ),
 ( 2, 2 ),
 ( 0.000000000000000000, 1.000000000000000000 ),
 ( 0.000000000000000000, 1.000000000000000000 ),
 .UNSPECIFIED. ) 
 GEOMETRIC_REPRESENTATION_ITEM ( )  RATIONAL_B_SPLINE_SURFACE ( (
 ( 1.000000000000000000, 1.000000000000000000),
 ( 0.9754377213608244057, 0.9999580625633939235),
 ( 0.9754377213608244057, 0.9999580625633939235),
 ( 1.000000000000000000, 1.000000000000000000) ) ) 
 REPRESENTATION_ITEM ( '' )  SURFACE ( )  );
#5565=CARTESIAN_POINT ( 'NONE',  ( 0.3676999524040323597, 37.41430475689418245, -23.36921870497780418 ) ) ;
#5566=CARTESIAN_POINT ( 'NONE',  ( -6.077587904424778920, -18.90214787454608469, 3.674891443665150970 ) ) ;
#5567=CARTESIAN_POINT ( 'NONE',  ( -6.078457390727109555, -12.94908628767718994, 14.25186567968553675 ) ) ;
#5568=CARTESIAN_POINT ( 'NONE',  ( 0.5987334308729317378, -13.39119755867282180, 47.24657378598286073 ) ) ;
#5569=CARTESIAN_POINT ( 'NONE',  ( 4.553261556744873317, 35.33793455049254106, 26.09156851415302825 ) ) ;
#5570=ORIENTED_EDGE ( 'NONE', *, *, #52536, .T. ) ;
#5571=EDGE_CURVE ( 'NONE', #37795, #1120, #28959, .T. ) ;
#5575=CARTESIAN_POINT ( 'NONE',  ( 0.1129192098497455998, -42.80154921430131054, 10.72283417016679508 ) ) ;
#5579=CARTESIAN_POINT ( 'NONE',  ( 0.8744876279028306332, -29.90976330662902427, 38.93271258621624042 ) ) ;
#5581=DIRECTION ( 'NONE',  ( 0.09722883295013597105, -0.6146093961964005370, -0.7828166095262992785 ) ) ;
#5583=CARTESIAN_POINT ( 'NONE',  ( 0.1156495703730067853, 29.76549459089011407, 32.57235461232057361 ) ) ;
#5589=CARTESIAN_POINT ( 'NONE',  ( 0.6028777368367060907, -47.47920655903965326, -12.54052526153192204 ) ) ;
#5590=CARTESIAN_POINT ( 'NONE',  ( 1.479689385636123067, 40.19566492452400297, 18.05248920628627118 ) ) ;
#5591=CARTESIAN_POINT ( 'NONE',  ( 0.1129192098497455998, 3.754263797494300725, 43.96427289429426821 ) ) ;
#5600=ORIENTED_EDGE ( 'NONE', *, *, #21251, .F. ) ;
#5601=CIRCLE ( 'NONE', #60664, 43.92652462719577500 ) ;
#5606=DIRECTION ( 'NONE',  ( 0.09722883295013597105, -0.5094590954038135111, -0.8549842011133788056 ) ) ;
#5611=ORIENTED_EDGE ( 'NONE', *, *, #14358, .F. ) ;
#5614=CARTESIAN_POINT ( 'NONE',  ( -6.079354080745853928, 17.84825706230203224, -7.227217658694646829 ) ) ;
#5622=CARTESIAN_POINT ( 'NONE',  ( 0.5997462898726536595, -34.91088276334701135, -34.53667463477266608 ) ) ;
#5624=EDGE_CURVE ( 'NONE', #43366, #24074, #16582, .T. ) ;
#5626=CARTESIAN_POINT ( 'NONE',  ( 0.1152809850208375564, -18.06278409025916432, 40.25768390504395455 ) ) ;
#5632=CARTESIAN_POINT ( 'NONE',  ( 0.1152339509894530906, 25.42708409640398415, 36.06114369802547515 ) ) ;
#5639=EDGE_CURVE ( 'NONE', #6245, #26600, #18811, .T. ) ;
#5653=B_SPLINE_CURVE_WITH_KNOTS ( 'NONE', 3,
 ( #3032, #26223, #55644, #17768, #12158, #50340, #50956, #7409, #50642, #45365, #26539, #45065, #55962, #40988, #2411, #21534, #7729, #59738, #54718 ),
 .UNSPECIFIED., .F., .F.,
 ( 4, 3, 3, 3, 3, 3, 4 ),
 ( 8.674676106452504675E-19, 0.0002612768053151716548, 0.0003919133833142916844, 0.0005225499612322607535, 0.0006531865391693360669, 0.0008112755173415198574, 0.0009693688056799731152 ),
 .UNSPECIFIED. ) ;
#5660=DIRECTION ( 'NONE',  ( 0.09722883295013598492, 0.7529176304110274387, 0.6508929219613607264 ) ) ;
#5671=CARTESIAN_POINT ( 'NONE',  ( 0.6252788684277227338, 37.83342009078897661, 31.30617599464285306 ) ) ;
#5683=EDGE_LOOP ( 'NONE', ( #45717, #23368, #43499, #25368 ) ) ;
#5684=EDGE_CURVE ( 'NONE', #4853, #60714, #58300, .T. ) ;
#5685=CARTESIAN_POINT ( 'NONE',  ( 0.2940133293163024186, 37.40612136450513248, -23.38851500292304308 ) ) ;
#5690=ORIENTED_EDGE ( 'NONE', *, *, #34450, .T. ) ;
#5699=CARTESIAN_POINT ( 'NONE',  ( 0.1158516988532803799, -1.463449468457666436, -44.09989200084357464 ) ) ;
#5700=CARTESIAN_POINT ( 'NONE',  ( 3.678834586032788678, 34.27179800835390466, -34.98651498653363490 ) ) ;
#5701=CARTESIAN_POINT ( 'NONE',  ( 4.975610109902397937, -5.269241389991576874, 48.62802178077752302 ) ) ;
#5702=CARTESIAN_POINT ( 'NONE',  ( 2.299746137290199943, 29.09984276079479315, 39.46492732773186418 ) ) ;
#5703=ORIENTED_EDGE ( 'NONE', *, *, #50087, .F. ) ;
#5706=CARTESIAN_POINT ( 'NONE',  ( -6.078457390727109555, 9.985927120572254623, -16.46437883979007921 ) ) ;
#5707=CARTESIAN_POINT ( 'NONE',  ( 0.6026777506516366456, -35.39729640274160971, -34.03788768436836421 ) ) ;
#5713=CARTESIAN_POINT ( 'NONE',  ( 2.881901170002227897, 8.474399077991585715E-12, -49.00591519830774700 ) ) ;
#5725=CARTESIAN_POINT ( 'NONE',  ( 0.1158816050234198480, -7.047819867384492731, -43.55766610393698812 ) ) ;
#5727=CARTESIAN_POINT ( 'NONE',  ( 0.3676999524040366896, 43.44964275340416293, 7.620966337964807380 ) ) ;
#5732=CARTESIAN_POINT ( 'NONE',  ( 4.975610109902397937, -17.43163075979710541, 45.70106843599904778 ) ) ;
#5734=ADVANCED_FACE ( 'NONE', ( #26357 ), #9320, .F. ) ;
#5736=CARTESIAN_POINT ( 'NONE',  ( 0.8744876279028263033, -34.64280934553510605, -34.78829991575325664 ) ) ;
#5741=ORIENTED_EDGE ( 'NONE', *, *, #14855, .F. ) ;
#5743=CARTESIAN_POINT ( 'NONE',  ( 0.3676999524040366896, -43.84864779214676389, -4.821480075983068048 ) ) ;
#5744=CARTESIAN_POINT ( 'NONE',  ( 0.1155031312995260795, 41.82288736169277854, 14.06370240238919145 ) ) ;
#5746=ORIENTED_EDGE ( 'NONE', *, *, #9922, .T. ) ;
#5753=CARTESIAN_POINT ( 'NONE',  ( 0.5549461598389366923, 28.99592290077940859, -33.23332891238644038 ) ) ;
#5757=CARTESIAN_POINT ( 'NONE',  ( 0.6039202388192952409, 33.14386950699269363, -36.23599904725178078 ) ) ;
#5762=B_SPLINE_CURVE_WITH_KNOTS ( 'NONE', 3,
 ( #986, #15110, #9780, #14805, #11029, #15732 ),
 .UNSPECIFIED., .F., .F.,
 ( 4, 2, 4 ),
 ( 0.000000000000000000, 0.0002447195606305748003, 0.0004894391212611496006 ),
 .UNSPECIFIED. ) ;
#5764=EDGE_CURVE ( 'NONE', #39035, #10587, #45012, .T. ) ;
#5765=ORIENTED_EDGE ( 'NONE', *, *, #56317, .F. ) ;
#5766=ORIENTED_EDGE ( 'NONE', *, *, #55692, .F. ) ;
#5774=CARTESIAN_POINT ( 'NONE',  ( 4.975610109902397937, -22.11219452748616021, 43.62912170003406942 ) ) ;
#5779=CARTESIAN_POINT ( 'NONE',  ( 0.7948884756798518803, 28.79738896807402071, -39.76693391778652398 ) ) ;
#5786=EDGE_CURVE ( 'NONE', #41582, #52129, #57955, .T. ) ;
#5789=CARTESIAN_POINT ( 'NONE',  ( -2.739355103387248747, 10.22927580983311913, 10.87241846864716699 ) ) ;
#5792=EDGE_CURVE ( 'NONE', #27245, #44212, #53178, .T. ) ;
#5794=CARTESIAN_POINT ( 'NONE',  ( 4.975610109902397937, 2.142807115709817189, -48.86571174967818365 ) ) ;
#5797=CARTESIAN_POINT ( 'NONE',  ( 0.1119899015040010798, -7.595748810241286897, 43.46568656082891380 ) ) ;
#5798=CARTESIAN_POINT ( 'NONE',  ( 0.5997462898726536595, 37.05192695178125462, 32.22896739432052016 ) ) ;
#5802=CARTESIAN_POINT ( 'NONE',  ( 1.657374760986086049, -16.69403132851356730, 40.77008419484624113 ) ) ;
#5805=CARTESIAN_POINT ( 'NONE',  ( 0.1129192098497455998, -27.88830454350494392, 34.19348267541455044 ) ) ;
#5806=CARTESIAN_POINT ( 'NONE',  ( 0.5997462898726536595, 10.41743419021343087, -47.98988117339822423 ) ) ;
#5807=CARTESIAN_POINT ( 'NONE',  ( 4.834790513006555379, 29.09828987666571010, -37.22739404226293658 ) ) ;
#5808=CARTESIAN_POINT ( 'NONE',  ( 0.5997462898726536595, -19.39900779840473888, 45.11352487427402025 ) ) ;
#5817=EDGE_LOOP ( 'NONE', ( #32491, #52925, #29291, #12463 ) ) ;
#5827=EDGE_LOOP ( 'NONE', ( #13290, #11219, #21295, #29013 ) ) ;
#5828=DIRECTION ( 'NONE',  ( 1.000000000000000000, 0.000000000000000000, 0.000000000000000000 ) ) ;
#5832=ORIENTED_EDGE ( 'NONE', *, *, #45294, .F. ) ;
#5834=CARTESIAN_POINT ( 'NONE',  ( 4.553261556744875094, 0.000000000000000000, 0.000000000000000000 ) ) ;
#5841=CARTESIAN_POINT ( 'NONE',  ( 3.678748215320120085, 43.29174540921691516, -22.90060247511034675 ) ) ;
#5858=CARTESIAN_POINT ( 'NONE',  ( 0.5997462898726536595, -48.63480578518795738, -6.797594896826151256 ) ) ;
#5866=CARTESIAN_POINT ( 'NONE',  ( 4.335381028904216727, -48.94118403004392093, 2.125406643849450550 ) ) ;
#5871=CARTESIAN_POINT ( 'NONE',  ( -6.078075953587585900, 7.799379819826266491, 17.60581860275808808 ) ) ;
#5878=ORIENTED_EDGE ( 'NONE', *, *, #46503, .F. ) ;
#5883=CARTESIAN_POINT ( 'NONE',  ( -6.077587904424778920, 19.09876248768967955, 2.456276212633274003 ) ) ;
#5889=CARTESIAN_POINT ( 'NONE',  ( 3.678748215320119197, 2.858834614276290154, -48.89212491749258760 ) ) ;
#5890=CARTESIAN_POINT ( 'NONE',  ( 2.879087469061463178, -19.38045785506447416, -39.50315848272703079 ) ) ;
#5896=AXIS2_PLACEMENT_3D ( 'NONE', #56429, #13544, #32650 ) ;
#5898=B_SPLINE_CURVE_WITH_KNOTS ( 'NONE', 3,
 ( #8427, #27553, #17858, #36983 ),
 .UNSPECIFIED., .F., .F.,
 ( 4, 4 ),
 ( 2.380113941701692686E-17, 0.004559932413162185935 ),
 .UNSPECIFIED. ) ;
#5901=CARTESIAN_POINT ( 'NONE',  ( 0.3676999524040323597, 5.056646555325726489, -43.82215089355327109 ) ) ;
#5919=CARTESIAN_POINT ( 'NONE',  ( 4.694002226626921015, 45.16857381419788453, 6.171281150417080141 ) ) ;
#5925=ADVANCED_FACE ( 'NONE', ( #33239 ), #60173, .F. ) ;
#5927=( BOUNDED_SURFACE ( )  B_SPLINE_SURFACE ( 3, 1, ( 
 ( #8942, #31510 ),
 ( #41551, #36541 ),
 ( #50917, #13658 ),
 ( #55607, #42179 ) ),
 .UNSPECIFIED., .F., .F., .F. ) 
 B_SPLINE_SURFACE_WITH_KNOTS ( ( 4, 4 ),
 ( 2, 2 ),
 ( 0.000000000000000000, 1.000000000000000000 ),
 ( 0.000000000000000000, 1.000000000000000000 ),
 .UNSPECIFIED. ) 
 GEOMETRIC_REPRESENTATION_ITEM ( )  RATIONAL_B_SPLINE_SURFACE ( (
 ( 1.000000000000000000, 1.000000000000000000),
 ( 0.9953485035131437453, 0.8621029689291515030),
 ( 0.9953485035131437453, 0.8621029689291515030),
 ( 1.000000000000000000, 1.000000000000000000) ) ) 
 REPRESENTATION_ITEM ( '' )  SURFACE ( )  );
#5930=FACE_OUTER_BOUND ( 'NONE', #51141, .T. ) ;
#5936=CARTESIAN_POINT ( 'NONE',  ( 0.1152339509894530906, -17.65621462967984812, 40.43761584720249402 ) ) ;
#5937=ORIENTED_EDGE ( 'NONE', *, *, #42970, .F. ) ;
#5941=CARTESIAN_POINT ( 'NONE',  ( 0.1156495703730067576, 25.35586003454986681, 36.11126299562765496 ) ) ;
#5944=DIRECTION ( 'NONE',  ( 1.000000000000000000, 0.000000000000000000, 0.000000000000000000 ) ) ;
#5953=CARTESIAN_POINT ( 'NONE',  ( 4.390527457369401532, -9.463175119887736741, -42.90260660238439527 ) ) ;
#5955=EDGE_CURVE ( 'NONE', #42350, #12019, #27665, .T. ) ;
#5956=VECTOR ( 'NONE', #28723, 1000.000000000000000 ) ;
#5959=EDGE_CURVE ( 'NONE', #12174, #21853, #56056, .T. ) ;
#5960=FACE_OUTER_BOUND ( 'NONE', #32634, .T. ) ;
#5961=CARTESIAN_POINT ( 'NONE',  ( 0.1155031312995260795, -43.74003612738039237, -5.809550077868878226 ) ) ;
#5962=CARTESIAN_POINT ( 'NONE',  ( 0.1156867017252034557, 39.70013168197753117, 19.25726750369402396 ) ) ;
#5966=LINE ( 'NONE', #52988, #47262 ) ;
#5967=CARTESIAN_POINT ( 'NONE',  ( 4.975610109902397937, 14.46773809681547718, 46.72401910687614190 ) ) ;
#5970=CARTESIAN_POINT ( 'NONE',  ( 3.050102900204245682, 18.72656562264871738, -39.80880542240235798 ) ) ;
#5985=ORIENTED_EDGE ( 'NONE', *, *, #18472, .T. ) ;
#5987=ORIENTED_EDGE ( 'NONE', *, *, #18436, .F. ) ;
#5993=B_SPLINE_CURVE_WITH_KNOTS ( 'NONE', 3,
 ( #48472, #34096, #28135, #28756 ),
 .UNSPECIFIED., .F., .F.,
 ( 4, 4 ),
 ( 0.000000000000000000, 0.004442905043737214836 ),
 .UNSPECIFIED. ) ;
#6012=ORIENTED_EDGE ( 'NONE', *, *, #44282, .F. ) ;
#6013=CARTESIAN_POINT ( 'NONE',  ( 2.009741617377216460, -42.92652007869518371, -9.839611351899232972 ) ) ;
#6022=B_SPLINE_CURVE_WITH_KNOTS ( 'NONE', 3,
 ( #15491, #43711, #33682, #39618 ),
 .UNSPECIFIED., .F., .F.,
 ( 4, 4 ),
 ( 0.000000000000000000, 0.004444103432399267896 ),
 .UNSPECIFIED. ) ;
#6027=( BOUNDED_SURFACE ( )  B_SPLINE_SURFACE ( 3, 1, ( 
 ( #44216, #950 ),
 ( #15998, #44523 ),
 ( #35110, #1246 ),
 ( #58252, #15383 ) ),
 .UNSPECIFIED., .F., .F., .F. ) 
 B_SPLINE_SURFACE_WITH_KNOTS ( ( 4, 4 ),
 ( 2, 2 ),
 ( 0.000000000000000000, 1.000000000000000000 ),
 ( 0.000000000000000000, 1.000000000000000000 ),
 .UNSPECIFIED. ) 
 GEOMETRIC_REPRESENTATION_ITEM ( )  RATIONAL_B_SPLINE_SURFACE ( (
 ( 1.000000000000000000, 1.000000000000000000),
 ( 0.9953485035131437453, 0.8621029689291515030),
 ( 0.9953485035131437453, 0.8621029689291515030),
 ( 1.000000000000000000, 1.000000000000000000) ) ) 
 REPRESENTATION_ITEM ( '' )  SURFACE ( )  );
#6032=CARTESIAN_POINT ( 'NONE',  ( 0.1149546198390367369, -6.771702484218997675, -43.60149780097516015 ) ) ;
#6040=EDGE_CURVE ( 'NONE', #36635, #5101, #30647, .T. ) ;
#6042=CARTESIAN_POINT ( 'NONE',  ( 0.6008122571543325074, -30.27643937426860887, 38.66383024587132411 ) ) ;
#6052=CARTESIAN_POINT ( 'NONE',  ( 2.533389852662419894, 43.79627363621963809, -4.397379596417775538 ) ) ;
#6054=DIRECTION ( 'NONE',  ( -0.1011922191286467460, 0.2953728085273335524, -0.9500079151093926422 ) ) ;
#6065=CARTESIAN_POINT ( 'NONE',  ( 0.6252788684277197362, -0.8874023922525490216, 49.09844038427176116 ) ) ;
#6066=CARTESIAN_POINT ( 'NONE',  ( 0.8753041380234530822, 49.05142151719380195, 2.257515230415335417 ) ) ;
#6069=CARTESIAN_POINT ( 'NONE',  ( 0.6000166863083090663, -13.47152005829796373, -47.22649287240509608 ) ) ;
#6071=VERTEX_POINT ( 'NONE', #16588 ) ;
#6073=CARTESIAN_POINT ( 'NONE',  ( 0.5980271706414734822, -19.23780022038743809, 45.18801041783234496 ) ) ;
#6079=CARTESIAN_POINT ( 'NONE',  ( 0.1152809850208375564, -40.81594088468489900, -16.76318144588499592 ) ) ;
#6083=CARTESIAN_POINT ( 'NONE',  ( 0.6016118706126977189, -35.51781829556208692, 33.91217536973064739 ) ) ;
#6087=LINE ( 'NONE', #49333, #40486 ) ;
#6099=B_SPLINE_CURVE_WITH_KNOTS ( 'NONE', 3,
 ( #441, #9869, #23656, #61837 ),
 .UNSPECIFIED., .F., .F.,
 ( 4, 4 ),
 ( 0.000000000000000000, 0.004442905043737215703 ),
 .UNSPECIFIED. ) ;
#6102=CARTESIAN_POINT ( 'NONE',  ( 0.1158403557922069033, 33.62268606590009057, -28.57368175258040566 ) ) ;
#6103=CARTESIAN_POINT ( 'NONE',  ( 3.390910168358336918, 22.06791622149280840, 38.04082294292292943 ) ) ;
#6104=CARTESIAN_POINT ( 'NONE',  ( 0.2940135542859010354, -41.18723742143126287, -15.80670814186408535 ) ) ;
#6108=DIRECTION ( 'NONE',  ( 0.000000000000000000, 0.000000000000000000, 1.000000000000000000 ) ) ;
#6110=VERTEX_POINT ( 'NONE', #35401 ) ;
#6132=FACE_OUTER_BOUND ( 'NONE', #2777, .T. ) ;
#6134=VECTOR ( 'NONE', #37824, 1000.000000000000114 ) ;
#6140=CARTESIAN_POINT ( 'NONE',  ( -6.077587904424778920, -11.01164173315302008, 15.79682777441765751 ) ) ;
#6141=CARTESIAN_POINT ( 'NONE',  ( 0.6008123274975391004, 37.10904484800355618, 32.16322965168950532 ) ) ;
#6147=EDGE_LOOP ( 'NONE', ( #47093, #8250, #48798, #1356 ) ) ;
#6153=CARTESIAN_POINT ( 'NONE',  ( 0.5997462898726536595, -48.63480578518795738, -6.797594896826151256 ) ) ;
#6157=CARTESIAN_POINT ( 'NONE',  ( -6.063463321072276813, 9.969191071288641126, -16.47530521306384088 ) ) ;
#6158=CARTESIAN_POINT ( 'NONE',  ( 0.8744876279028263033, -45.83369275826233036, 17.59609782084381280 ) ) ;
#6169=CARTESIAN_POINT ( 'NONE',  ( 0.1368894036331278208, 41.67016667612794834, -14.50718908359056947 ) ) ;
#6177=CARTESIAN_POINT ( 'NONE',  ( 4.390527457369401532, 31.33584375699295066, 30.79367195814660718 ) ) ;
#6178=CARTESIAN_POINT ( 'NONE',  ( -6.078457390727109555, -18.90176508385434317, 3.676654423833250807 ) ) ;
#6182=ORIENTED_EDGE ( 'NONE', *, *, #43419, .F. ) ;
#6199=CARTESIAN_POINT ( 'NONE',  ( 0.7242486021783856032, 27.41642097787600463, 40.73513622338652596 ) ) ;
#6204=ADVANCED_FACE ( 'NONE', ( #7787 ), #19767, .F. ) ;
#6208=CARTESIAN_POINT ( 'NONE',  ( 0.1129192098497455998, 4.719118110135312349, -43.87119455916086963 ) ) ;
#6212=CARTESIAN_POINT ( 'NONE',  ( 0.6008122571543325074, 27.73703307328602108, -40.52420939089070373 ) ) ;
#6214=CARTESIAN_POINT ( 'NONE',  ( 0.6029442701453591180, -13.88890752606295464, 47.10247841558604165 ) ) ;
#6218=CARTESIAN_POINT ( 'NONE',  ( 1.830465331921977246, 8.594330631025679068, 43.20316582014567786 ) ) ;
#6219=ORIENTED_EDGE ( 'NONE', *, *, #33268, .F. ) ;
#6224=CARTESIAN_POINT ( 'NONE',  ( 4.834790513006553603, 46.80118606150055882, 6.499101796493775396 ) ) ;
#6227=ORIENTED_EDGE ( 'NONE', *, *, #58180, .T. ) ;
#6229=CARTESIAN_POINT ( 'NONE',  ( -6.078726893082806448, 17.84743921491362073, -7.229312189875575889 ) ) ;
#6239=CARTESIAN_POINT ( 'NONE',  ( 2.648799415243696664, -38.45353011080844396, -30.42767630475167095 ) ) ;
#6242=ORIENTED_EDGE ( 'NONE', *, *, #24454, .F. ) ;
#6244=CARTESIAN_POINT ( 'NONE',  ( 0.1149546198390367369, 25.01907401799166308, 36.34546051854996307 ) ) ;
#6245=VERTEX_POINT ( 'NONE', #50398 ) ;
#6247=CARTESIAN_POINT ( 'NONE',  ( -6.078075953587585900, 5.473785299353282063, 18.46165888385222331 ) ) ;
#6253=CARTESIAN_POINT ( 'NONE',  ( 4.975610109902397937, 48.90928568712960356, 0.5754830253899292369 ) ) ;
#6255=FILL_AREA_STYLE ('',( #7199 ) ) ;
#6256=CARTESIAN_POINT ( 'NONE',  ( 0.8753041380234465318, 46.31375555491744223, 16.31485134079786192 ) ) ;
#6258=EDGE_CURVE ( 'NONE', #29973, #45131, #5993, .T. ) ;
#6261=CARTESIAN_POINT ( 'NONE',  ( 4.975610109902397937, 19.27143522741655701, 44.95621415792550124 ) ) ;
#6265=CARTESIAN_POINT ( 'NONE',  ( 3.678748215320120529, -44.67004451351987626, 20.07983907952543490 ) ) ;
#6268=B_SPLINE_CURVE_WITH_KNOTS ( 'NONE', 3,
 ( #12091, #27392, #50272, #3880 ),
 .UNSPECIFIED., .F., .F.,
 ( 4, 4 ),
 ( 0.000000000000000000, 0.004444103432399266161 ),
 .UNSPECIFIED. ) ;
#6273=CARTESIAN_POINT ( 'NONE',  ( 4.553261556744875094, 0.000000000000000000, 0.000000000000000000 ) ) ;
#6274=CARTESIAN_POINT ( 'NONE',  ( 0.6024113833632039894, -45.59977004659592126, 18.22643247589719095 ) ) ;
#6278=CARTESIAN_POINT ( 'NONE',  ( 4.553261556744875094, 17.98701270972463817, -40.07501640179128799 ) ) ;
#6288=CARTESIAN_POINT ( 'NONE',  ( 0.6000166863083090663, 22.25084548767559767, -43.78039923061506755 ) ) ;
#6293=CARTESIAN_POINT ( 'NONE',  ( 4.975610109902397937, 0.000000000000000000, 0.000000000000000000 ) ) ;
#6295=CARTESIAN_POINT ( 'NONE',  ( 0.2940133293163019190, -11.77874402649793240, -42.51472378760423965 ) ) ;
#6301=CARTESIAN_POINT ( 'NONE',  ( 0.8744876279028306332, 3.827863332835647281, -48.94586308039347955 ) ) ;
#6310=AXIS2_PLACEMENT_3D ( 'NONE', #31501, #7053, #60603 ) ;
#6319=CARTESIAN_POINT ( 'NONE',  ( 0.8744876279028263033, 46.30617036199606673, 16.31222353896886545 ) ) ;
#6321=ORIENTED_EDGE ( 'NONE', *, *, #58986, .F. ) ;
#6326=CARTESIAN_POINT ( 'NONE',  ( 0.7948878604505665857, -49.09120187693520876, 0.8674938480527389917 ) ) ;
#6328=CARTESIAN_POINT ( 'NONE',  ( -6.078726893082806448, -6.653559303940109082, -18.06998035022927596 ) ) ;
#6329=CARTESIAN_POINT ( 'NONE',  ( 2.533389852662419894, -14.03271582234461334, -41.71970060274805547 ) ) ;
#6330=EDGE_CURVE ( 'NONE', #3214, #55302, #35889, .T. ) ;
#6334=CARTESIAN_POINT ( 'NONE',  ( 0.1135584504625008206, -6.615454642350983683, -43.62554082198006000 ) ) ;
#6348=CARTESIAN_POINT ( 'NONE',  ( 0.6027444965799114707, 49.01471672440227678, -3.015967558519589531 ) ) ;
#6353=CARTESIAN_POINT ( 'NONE',  ( 0.8744876279028306332, 49.04340454744548339, 2.257104511336577968 ) ) ;
#6354=CARTESIAN_POINT ( 'NONE',  ( 0.1158516988532803105, 41.89178036391317761, 13.85716048743228335 ) ) ;
#6367=CARTESIAN_POINT ( 'NONE',  ( 3.050102900204245682, -10.77143531111902597, 42.65444209594632952 ) ) ;
#6369=CARTESIAN_POINT ( 'NONE',  ( 0.1119899015040013157, -1.975119189439954681, 44.08015667372350777 ) ) ;
#6370=CARTESIAN_POINT ( 'NONE',  ( -2.601141883200662974, -12.22474371604796417, -8.564523836520885780 ) ) ;
#6372=ORIENTED_EDGE ( 'NONE', *, *, #7058, .F. ) ;
#6375=ORIENTED_EDGE ( 'NONE', *, *, #4893, .F. ) ;
#6378=CARTESIAN_POINT ( 'NONE',  ( 0.7242486021783836048, -8.644155275603129240, 48.33518430651980680 ) ) ;
#6380=AXIS2_PLACEMENT_3D ( 'NONE', #36457, #27343, #36768 ) ;
#6381=VERTEX_POINT ( 'NONE', #30911 ) ;
#6393=CARTESIAN_POINT ( 'NONE',  ( 0.1158403557922069033, 9.781626696134630095, 43.02627204814850614 ) ) ;
#6395=ORIENTED_EDGE ( 'NONE', *, *, #59282, .F. ) ;
#6402=CARTESIAN_POINT ( 'NONE',  ( 0.2285344041767094769, -31.15968535845325604, 31.23419886370790266 ) ) ;
#6435=ADVANCED_FACE ( 'NONE', ( #12756 ), #13013, .F. ) ;
#6440=CARTESIAN_POINT ( 'NONE',  ( 0.6000166863083106206, 48.10206967781414278, -9.900220927795848169 ) ) ;
#6443=ORIENTED_EDGE ( 'NONE', *, *, #26369, .F. ) ;
#6449=ORIENTED_EDGE ( 'NONE', *, *, #26889, .F. ) ;
#6451=CARTESIAN_POINT ( 'NONE',  ( 0.6039202388192952409, -39.45949250020272814, 29.23204003273524521 ) ) ;
#6454=CARTESIAN_POINT ( 'NONE',  ( -6.079354080745853928, -18.27537090945901710, -6.066611358069764037 ) ) ;
#6463=( BOUNDED_SURFACE ( )  B_SPLINE_SURFACE ( 3, 1, ( 
 ( #34924, #48087 ),
 ( #58683, #24895 ),
 ( #53074, #5140 ),
 ( #44334, #39625 ) ),
 .UNSPECIFIED., .F., .F., .F. ) 
 B_SPLINE_SURFACE_WITH_KNOTS ( ( 4, 4 ),
 ( 2, 2 ),
 ( 0.000000000000000000, 1.000000000000000000 ),
 ( 0.000000000000000000, 1.000000000000000000 ),
 .UNSPECIFIED. ) 
 GEOMETRIC_REPRESENTATION_ITEM ( )  RATIONAL_B_SPLINE_SURFACE ( (
 ( 1.000000000000000000, 1.000000000000000000),
 ( 0.9953485035131437453, 0.8621029689291515030),
 ( 0.9953485035131437453, 0.8621029689291515030),
 ( 1.000000000000000000, 1.000000000000000000) ) ) 
 REPRESENTATION_ITEM ( '' )  SURFACE ( )  );
#6468=CARTESIAN_POINT ( 'NONE',  ( 0.5987334363312686314, 10.33658596697176257, 48.00747751152395182 ) ) ;
#6471=CARTESIAN_POINT ( 'NONE',  ( 0.8744876279028306332, 48.92939099258504143, -4.032957658373305776 ) ) ;
#6473=CARTESIAN_POINT ( 'NONE',  ( 0.2285344041767100043, 41.62591743292807678, -14.62135999702185707 ) ) ;
#6474=ADVANCED_FACE ( 'NONE', ( #60950 ), #4914, .F. ) ;
#6477=ORIENTED_EDGE ( 'NONE', *, *, #28715, .T. ) ;
#6480=CARTESIAN_POINT ( 'NONE',  ( 2.009741617377216460, 30.60835445554638312, 31.66437612122933487 ) ) ;
#6486=VERTEX_POINT ( 'NONE', #12436 ) ;
#6492=CARTESIAN_POINT ( 'NONE',  ( 0.6008123274975392114, -19.47899178227436323, -45.07907974110103311 ) ) ;
#6494=CARTESIAN_POINT ( 'NONE',  ( 0.1149546198390367646, -42.74978084130992073, 10.92715896485409210 ) ) ;
#6498=CARTESIAN_POINT ( 'NONE',  ( 0.1155031312995260795, 20.55835925191953351, -39.04222710605559854 ) ) ;
#6500=CARTESIAN_POINT ( 'NONE',  ( 0.1154773475650540532, 29.79763058674064169, 32.54296915559886827 ) ) ;
#6501=CARTESIAN_POINT ( 'NONE',  ( 0.1368894036331280706, -2.051263853491218647, -44.07554472183745276 ) ) ;
#6502=( NAMED_UNIT ( * ) SI_UNIT ( $, .STERADIAN. ) SOLID_ANGLE_UNIT ( ) );
#6503=CARTESIAN_POINT ( 'NONE',  ( 1.834102595619085507, -21.70983406038687491, 38.32598139549919836 ) ) ;
#6514=ORIENTED_EDGE ( 'NONE', *, *, #10630, .T. ) ;
#6519=VERTEX_POINT ( 'NONE', #7707 ) ;
#6520=CARTESIAN_POINT ( 'NONE',  ( 3.221118495291109163, -43.94535254261806045, 1.888758737044896163 ) ) ;
#6523=EDGE_LOOP ( 'NONE', ( #53541, #22587, #14587, #14213 ) ) ;
#6526=EDGE_LOOP ( 'NONE', ( #20989, #13168, #30900, #45280 ) ) ;
#6528=VERTEX_POINT ( 'NONE', #59716 ) ;
#6532=EDGE_CURVE ( 'NONE', #15927, #29824, #6650, .T. ) ;
#6537=EDGE_CURVE ( 'NONE', #26600, #24124, #58930, .T. ) ;
#6548=CARTESIAN_POINT ( 'NONE',  ( -6.078457390727109555, -18.27366031693659210, -6.071890122418616365 ) ) ;
#6551=ORIENTED_EDGE ( 'NONE', *, *, #33289, .T. ) ;
#6566=CARTESIAN_POINT ( 'NONE',  ( 0.1129192098497455998, 39.54191224844618802, 19.58032082273768637 ) ) ;
#6567=LINE ( 'NONE', #25397, #12808 ) ;
#6570=FACE_OUTER_BOUND ( 'NONE', #20810, .T. ) ;
#6572=CARTESIAN_POINT ( 'NONE',  ( 0.8744876279028306332, 36.80052600666260787, -32.49725120702428427 ) ) ;
#6574=CARTESIAN_POINT ( 'NONE',  ( 0.1119898979215349089, -27.07006246863960541, 34.84498566789457641 ) ) ;
#6580=CARTESIAN_POINT ( 'NONE',  ( 0.6029443199889047422, -45.51847136150880857, 18.42841302895899247 ) ) ;
#6583=CARTESIAN_POINT ( 'NONE',  ( 2.359973842542475886, -2.918503669880030849, -43.92742003534235806 ) ) ;
#6585=CARTESIAN_POINT ( 'NONE',  ( 0.8744876279028263033, -45.16590161814997373, -19.24555484778471026 ) ) ;
#6586=ORIENTED_EDGE ( 'NONE', *, *, #28861, .T. ) ;
#6587=EDGE_CURVE ( 'NONE', #45047, #33819, #55826, .T. ) ;
#6589=CARTESIAN_POINT ( 'NONE',  ( 0.1147471544378676350, 4.545905012546410440, 43.88948548445461029 ) ) ;
#6592=ORIENTED_EDGE ( 'NONE', *, *, #60446, .F. ) ;
#6593=CARTESIAN_POINT ( 'NONE',  ( 0.6253024248130486518, -45.25541762693965353, -19.06282777630130809 ) ) ;
#6594=CARTESIAN_POINT ( 'NONE',  ( 4.694002226626921015, -43.15593359350852154, -14.69184015427673273 ) ) ;
#6595=ORIENTED_EDGE ( 'NONE', *, *, #20872, .F. ) ;
#6596=CARTESIAN_POINT ( 'NONE',  ( 0.6008122571543325074, 11.35154853257121843, 47.77757733893585623 ) ) ;
#6599=CARTESIAN_POINT ( 'NONE',  ( 0.7948884756798505480, -48.79909643092307903, 5.417271649605749140 ) ) ;
#6605=CARTESIAN_POINT ( 'NONE',  ( 0.2279481005628805901, 37.38452800950467747, -23.42862677536759719 ) ) ;
#6620=CARTESIAN_POINT ( 'NONE',  ( -6.078726893082806448, -18.90156862012328887, -3.677600436084754509 ) ) ;
#6632=EDGE_CURVE ( 'NONE', #38290, #59505, #13991, .T. ) ;
#6633=CARTESIAN_POINT ( 'NONE',  ( 0.6000166863083106206, 32.62822748873707468, 36.70452632376116497 ) ) ;
#6635=( BOUNDED_SURFACE ( )  B_SPLINE_SURFACE ( 3, 1, ( 
 ( #6885, #54820 ),
 ( #39846, #40454 ),
 ( #31030, #50138 ),
 ( #45459, #55127 ) ),
 .UNSPECIFIED., .F., .F., .F. ) 
 B_SPLINE_SURFACE_WITH_KNOTS ( ( 4, 4 ),
 ( 2, 2 ),
 ( 0.000000000000000000, 1.000000000000000000 ),
 ( 0.000000000000000000, 1.000000000000000000 ),
 .UNSPECIFIED. ) 
 GEOMETRIC_REPRESENTATION_ITEM ( )  RATIONAL_B_SPLINE_SURFACE ( (
 ( 1.000000000000000000, 1.000000000000000000),
 ( 0.9953485035131437453, 0.8621029689291515030),
 ( 0.9953485035131437453, 0.8621029689291515030),
 ( 1.000000000000000000, 1.000000000000000000) ) ) 
 REPRESENTATION_ITEM ( '' )  SURFACE ( )  );
#6637=CARTESIAN_POINT ( 'NONE',  ( 4.226256110419179812, -41.57058058356821562, -14.23776948585163815 ) ) ;
#6638=CARTESIAN_POINT ( 'NONE',  ( 4.060580049360325461, -14.70525263353195378, -41.41525370371659420 ) ) ;
#6645=CARTESIAN_POINT ( 'NONE',  ( 1.834102595619085285, 41.37485482074667686, -15.11023273877077422 ) ) ;
#6646=B_SPLINE_CURVE_WITH_KNOTS ( 'NONE', 3,
 ( #19008, #61566, #27768, #14000, #57169, #23683, #4244, #46900, #56873, #51247, #23379, #8644, #61868, #42815, #3623, #22759, #51869, #33103, #42206 ),
 .UNSPECIFIED., .F., .F.,
 ( 4, 3, 3, 3, 3, 3, 4 ),
 ( 1.355320476548679676E-18, 0.0002612768053151710043, 0.0003919133833142910339, 0.0005225499612322606451, 0.0006531865391693356332, 0.0008112755173415187732, 0.0009693688056799720310 ),
 .UNSPECIFIED. ) ;
#6650=B_SPLINE_CURVE_WITH_KNOTS ( 'NONE', 3,
 ( #55011, #37178, #22136, #27441, #60321, #41566 ),
 .UNSPECIFIED., .F., .F.,
 ( 4, 2, 4 ),
 ( 0.000000000000000000, 0.0002447195606305735535, 0.0004894391212611471070 ),
 .UNSPECIFIED. ) ;
#6651=( BOUNDED_SURFACE ( )  B_SPLINE_SURFACE ( 3, 1, ( 
 ( #60734, #45751 ),
 ( #60130, #27552 ),
 ( #3115, #22244 ),
 ( #41366, #31326 ) ),
 .UNSPECIFIED., .F., .F., .F. ) 
 B_SPLINE_SURFACE_WITH_KNOTS ( ( 4, 4 ),
 ( 2, 2 ),
 ( 0.000000000000000000, 1.000000000000000000 ),
 ( 0.000000000000000000, 1.000000000000000000 ),
 .UNSPECIFIED. ) 
 GEOMETRIC_REPRESENTATION_ITEM ( )  RATIONAL_B_SPLINE_SURFACE ( (
 ( 1.000000000000000000, 1.000000000000000000),
 ( 0.9953485035131437453, 0.8621029689291523912),
 ( 0.9953485035131437453, 0.8621029689291523912),
 ( 1.000000000000000000, 1.000000000000000000) ) ) 
 REPRESENTATION_ITEM ( '' )  SURFACE ( )  );
#6652=CARTESIAN_POINT ( 'NONE',  ( 0.3676999524040366896, -34.85286720109691316, 27.04123205746257241 ) ) ;
#6654=CARTESIAN_POINT ( 'NONE',  ( 0.5997462898726536595, 23.17609050332868037, 43.29457771044576475 ) ) ;
#6655=CARTESIAN_POINT ( 'NONE',  ( 0.6016117650947689910, 48.98309729621151831, -3.493885160444671012 ) ) ;
#6669=B_SPLINE_CURVE_WITH_KNOTS ( 'NONE', 3,
 ( #13346, #23051, #8615, #4519, #46872, #42178, #42479, #61537, #47471, #61237, #37469, #32762, #8941, #28050, #47170, #4212 ),
 .UNSPECIFIED., .F., .F.,
 ( 4, 3, 3, 3, 3, 4 ),
 ( 2.194378057379452319E-17, 0.0002612764279487761443, 0.0003919131003184802209, 0.0005225497727000647137, 0.0007837925190632471974, 0.001045051706266716951 ),
 .UNSPECIFIED. ) ;
#6673=CARTESIAN_POINT ( 'NONE',  ( 2.648799415243696664, 47.84750745855099296, 10.73002764644649787 ) ) ;
#6677=B_SPLINE_CURVE_WITH_KNOTS ( 'NONE', 3,
 ( #25462, #6957, #2263, #21393, #6326, #53956 ),
 .UNSPECIFIED., .F., .F.,
 ( 4, 2, 4 ),
 ( 0.000000000000000000, 0.0002447195606305751798, 0.0004894391212611503596 ),
 .UNSPECIFIED. ) ;
#6679=EDGE_LOOP ( 'NONE', ( #19130, #54704, #54097, #48412 ) ) ;
#6683=DIRECTION ( 'NONE',  ( 0.000000000000000000, 0.000000000000000000, -1.000000000000000000 ) ) ;
#6691=CARTESIAN_POINT ( 'NONE',  ( 0.6021447746440204973, -7.579515948152010019, 48.51898676889489082 ) ) ;
#6702=CARTESIAN_POINT ( 'NONE',  ( -6.057079549204054558, 18.62933071312873068, 4.876399110062378028 ) ) ;
#6704=CARTESIAN_POINT ( 'NONE',  ( 0.5997462898726536595, -48.63480578518805686, 6.797594896825438049 ) ) ;
#6706=ORIENTED_EDGE ( 'NONE', *, *, #61784, .T. ) ;
#6711=EDGE_CURVE ( 'NONE', #31302, #27767, #31324, .T. ) ;
#6714=CARTESIAN_POINT ( 'NONE',  ( 4.226256110419178924, 22.42442410584029844, 37.78852277489284006 ) ) ;
#6716=CARTESIAN_POINT ( 'NONE',  ( 0.7413678028165010536, -32.31867156292732091, -29.99982600246001851 ) ) ;
#6730=CARTESIAN_POINT ( 'NONE',  ( 0.9268187852002115479, 36.39936320882078746, -24.87650881657170387 ) ) ;
#6732=CARTESIAN_POINT ( 'NONE',  ( -2.601141883200665639, 12.74835759521969791, -7.763685084661332780 ) ) ;
#6733=EDGE_CURVE ( 'NONE', #40756, #17512, #16339, .T. ) ;
#6734=CARTESIAN_POINT ( 'NONE',  ( 4.553261556744873317, -15.38244134641770167, -41.14510984366982171 ) ) ;
#6748=ORIENTED_EDGE ( 'NONE', *, *, #44945, .T. ) ;
#6751=ADVANCED_FACE ( 'NONE', ( #49022 ), #34961, .F. ) ;
#6753=CARTESIAN_POINT ( 'NONE',  ( 4.553261556744875094, 27.56395660609745235, -34.20186927699732138 ) ) ;
#6754=CARTESIAN_POINT ( 'NONE',  ( 0.6021447746440204973, 37.56149566485957081, 31.63345037309751007 ) ) ;
#6758=CARTESIAN_POINT ( 'NONE',  ( -2.601141883200662974, 9.698805021789313585, -11.34586306186986526 ) ) ;
#6759=VERTEX_POINT ( 'NONE', #15214 ) ;
#6761=CARTESIAN_POINT ( 'NONE',  ( 0.8753041380234530822, 28.81806460335451803, 39.75748332565663645 ) ) ;
#6766=CARTESIAN_POINT ( 'NONE',  ( -6.079354080745853928, 15.43270669589069222, -11.51627193525633075 ) ) ;
#6768=CARTESIAN_POINT ( 'NONE',  ( -6.079354080745853928, 3.072100940895722943, 19.00934378291659144 ) ) ;
#6784=DIRECTION ( 'NONE',  ( 0.1011922191286468431, 0.2338987173090816551, 0.9669806227784434327 ) ) ;
#6785=CARTESIAN_POINT ( 'NONE',  ( 0.1129192098497455998, 10.29049805561888498, -42.90754522869442411 ) ) ;
#6787=CARTESIAN_POINT ( 'NONE',  ( 0.1139756605157202368, 43.38486962273822911, 8.044147407465196409 ) ) ;
#6810=CARTESIAN_POINT ( 'NONE',  ( 0.1158403557922069033, -42.69064927979727742, 11.15566095097745425 ) ) ;
#6812=CARTESIAN_POINT ( 'NONE',  ( 4.553261556744875094, 31.39705178283641018, 30.72075365562384519 ) ) ;
#6813=CARTESIAN_POINT ( 'NONE',  ( 0.1129192098497455998, 20.83764143887614040, -38.89401608281131928 ) ) ;
#6822=CARTESIAN_POINT ( 'NONE',  ( 0.8744876279028306332, -8.712669995481570950, -48.31603700562917680 ) ) ;
#6829=B_SPLINE_CURVE_WITH_KNOTS ( 'NONE', 3,
 ( #55733, #12865, #31958, #51039 ),
 .UNSPECIFIED., .F., .F.,
 ( 4, 4 ),
 ( 0.000000000000000000, 0.005013413432710142441 ),
 .UNSPECIFIED. ) ;
#6830=EDGE_CURVE ( 'NONE', #4631, #25125, #56711, .T. ) ;
#6833=CARTESIAN_POINT ( 'NONE',  ( 0.6021448801613057400, -45.41983169298476497, -18.67029800533144268 ) ) ;
#6852=CARTESIAN_POINT ( 'NONE',  ( 4.553261556744873317, 1.182159483579998449, -43.91061448874312845 ) ) ;
#6857=CARTESIAN_POINT ( 'NONE',  ( 0.1158816050234199174, -1.408571594206387889, 44.10167760266219972 ) ) ;
#6862=CARTESIAN_POINT ( 'NONE',  ( 0.6024113833632039894, -25.27052062982265923, -42.10632560790092782 ) ) ;
#6864=CARTESIAN_POINT ( 'NONE',  ( 0.1129192098497447394, -32.03190746134960420, -30.34647742609823595 ) ) ;
#6866=EDGE_LOOP ( 'NONE', ( #52081, #37292, #53664, #26364 ) ) ;
#6868=CARTESIAN_POINT ( 'NONE',  ( 5.901764892641307547, -48.86589420182298937, -3.180542610297919737 ) ) ;
#6874=CARTESIAN_POINT ( 'NONE',  ( -6.078726893082806448, 13.83016815118539000, -13.39852567182887455 ) ) ;
#6879=CARTESIAN_POINT ( 'NONE',  ( 0.6000166863083090663, 37.05402083933981316, -32.23077754796219807 ) ) ;
#6885=CARTESIAN_POINT ( 'NONE',  ( -6.077587904424778920, 18.62786028128800098, -4.878405757493267103 ) ) ;
#6886=CARTESIAN_POINT ( 'NONE',  ( 0.5997462898726536595, -25.90236585764231947, -41.72072714036939090 ) ) ;
#6887=B_SPLINE_CURVE_WITH_KNOTS ( 'NONE', 3,
 ( #19195, #44787, #1511, #33910, #30339, #16565 ),
 .UNSPECIFIED., .F., .F.,
 ( 4, 2, 4 ),
 ( 1.029992063861229212E-18, 0.0002293801035737093720, 0.0004587602071474177140 ),
 .UNSPECIFIED. ) ;
#6896=CARTESIAN_POINT ( 'NONE',  ( 4.694002226626920127, 23.92658369670189700, 38.80468224391037069 ) ) ;
#6897=EDGE_CURVE ( 'NONE', #22282, #48887, #3778, .T. ) ;
#6899=DIRECTION ( 'NONE',  ( -1.000000000000000000, -0.000000000000000000, -0.000000000000000000 ) ) ;
#6900=ADVANCED_FACE ( 'NONE', ( #37038 ), #19403, .F. ) ;
#6904=ORIENTED_EDGE ( 'NONE', *, *, #59662, .F. ) ;
#6912=CARTESIAN_POINT ( 'NONE',  ( -6.077587904424778920, -18.89978312007031391, -3.687033958107209131 ) ) ;
#6914=FACE_OUTER_BOUND ( 'NONE', #40112, .T. ) ;
#6915=ORIENTED_EDGE ( 'NONE', *, *, #33643, .F. ) ;
#6920=ADVANCED_FACE ( 'NONE', ( #58246 ), #3814, .F. ) ;
#6925=CARTESIAN_POINT ( 'NONE',  ( 0.1129192098497455998, 43.99990943031669843, 3.310552508129313232 ) ) ;
#6928=CARTESIAN_POINT ( 'NONE',  ( 4.335381028904216727, 20.75278752742130450, -44.37430176922282499 ) ) ;
#6932=VECTOR ( 'NONE', #7544, 1000.000000000000000 ) ;
#6935=CARTESIAN_POINT ( 'NONE',  ( 0.1157991065609915715, 43.32597169134096760, -8.354791591585023269 ) ) ;
#6947=CARTESIAN_POINT ( 'NONE',  ( 0.3676999524040366896, -42.87209381266877983, -10.38913641457107673 ) ) ;
#6948=DIRECTION ( 'NONE',  ( 0.09722883295013594329, 0.7627152102960286228, 0.6393841271303498663 ) ) ;
#6957=CARTESIAN_POINT ( 'NONE',  ( 0.5987334308729319599, -49.10393657821489910, 0.6052430027486100927 ) ) ;
#6958=CARTESIAN_POINT ( 'NONE',  ( 4.390527457369401532, -41.59349320486530388, -14.14802670500178827 ) ) ;
#6962=FACE_OUTER_BOUND ( 'NONE', #60959, .T. ) ;
#6966=CARTESIAN_POINT ( 'NONE',  ( 0.7413678028165010536, 41.54644801266331200, -14.77764356388756006 ) ) ;
#6967=CARTESIAN_POINT ( 'NONE',  ( 4.553261556744873317, -24.94552653848474222, 36.15605442441679429 ) ) ;
#6973=CARTESIAN_POINT ( 'NONE',  ( 0.5997462898726536595, 17.44942740672405534, 45.90282249842351803 ) ) ;
#6979=CARTESIAN_POINT ( 'NONE',  ( 2.533389852662419894, 2.648867642851640003, -43.93670483712077157 ) ) ;
#6984=CARTESIAN_POINT ( 'NONE',  ( 0.3676999524040366896, -7.853951980431815194, -43.40813312746713848 ) ) ;
#6985=CARTESIAN_POINT ( 'NONE',  ( 4.975610109902397937, 48.58133226360775581, 5.683622315980952244 ) ) ;
#6987=AXIS2_PLACEMENT_3D ( 'NONE', #39483, #24122, #48251 ) ;
#6990=B_SPLINE_CURVE_WITH_KNOTS ( 'NONE', 3,
 ( #18780, #33188, #47901, #52889, #42907, #52263, #34119, #53191, #9359, #58191, #14086, #37907, #56964, #28461, #10295, #47588, #29696, #4626, #39131 ),
 .UNSPECIFIED., .F., .F.,
 ( 4, 3, 3, 3, 3, 3, 4 ),
 ( 0.000000000000000000, 0.0002612768053151736064, 0.0003919133833142934733, 0.0005225499612322633556, 0.0006531865391693374764, 0.0008112755173415215921, 0.0009693688056799695373 ),
 .UNSPECIFIED. ) ;
#7002=EDGE_LOOP ( 'NONE', ( #50884, #51629, #32003, #21627 ) ) ;
#7003=CARTESIAN_POINT ( 'NONE',  ( -2.601141883200665639, -3.815535891687811709, -14.43042318605489527 ) ) ;
#7009=CARTESIAN_POINT ( 'NONE',  ( 3.727782113643637096, -43.82423448898260432, -3.494888747963610598 ) ) ;
#7012=CARTESIAN_POINT ( 'NONE',  ( 0.6026112563231247332, -35.39723702811621564, 34.03787016955622136 ) ) ;
#7025=ORIENTED_EDGE ( 'NONE', *, *, #60749, .F. ) ;
#7026=CARTESIAN_POINT ( 'NONE',  ( 0.2285344041767103374, -11.82284706221704695, 42.50554619857131655 ) ) ;
#7031=DIRECTION ( 'NONE',  ( 0.000000000000000000, 0.000000000000000000, -1.000000000000000000 ) ) ;
#7035=CARTESIAN_POINT ( 'NONE',  ( 4.335381028904216727, 47.11764506933879915, 13.40463989759361674 ) ) ;
#7044=CARTESIAN_POINT ( 'NONE',  ( 0.1147471544378677460, 44.01263920499553706, -3.136842151612880603 ) ) ;
#7051=EDGE_CURVE ( 'NONE', #55688, #53648, #4286, .T. ) ;
#7053=DIRECTION ( 'NONE',  ( -1.000000000000000000, -0.000000000000000000, -0.000000000000000000 ) ) ;
#7057=CARTESIAN_POINT ( 'NONE',  ( 0.1129192098497455998, 41.72114954716776936, 14.36305915353748297 ) ) ;
#7058=EDGE_CURVE ( 'NONE', #26555, #48631, #44866, .T. ) ;
#7060=LINE ( 'NONE', #45950, #28487 ) ;
#7063=EDGE_CURVE ( 'NONE', #8350, #28177, #54367, .T. ) ;
#7064=ORIENTED_EDGE ( 'NONE', *, *, #41694, .F. ) ;
#7067=B_SPLINE_CURVE_WITH_KNOTS ( 'NONE', 3,
 ( #46820, #48035, #14224, #27997, #47119, #52715, #18925, #9496, #28602, #9812, #5084, #57392, #8564, #47417, #19231, #3859 ),
 .UNSPECIFIED., .F., .F.,
 ( 4, 3, 3, 3, 3, 4 ),
 ( 2.194378057379452319E-17, 0.0002612764279487727833, 0.0003919131003184789198, 0.0005225497727000618948, 0.0007837925190632441617, 0.001045051706266715216 ),
 .UNSPECIFIED. ) ;
#7072=ORIENTED_EDGE ( 'NONE', *, *, #49993, .T. ) ;
#7076=VECTOR ( 'NONE', #13958, 1000.000000000000000 ) ;
#7083=CARTESIAN_POINT ( 'NONE',  ( -6.057079549204054558, -11.02420820863788187, 15.78917554758130848 ) ) ;
#7086=ORIENTED_EDGE ( 'NONE', *, *, #43887, .F. ) ;
#7088=CARTESIAN_POINT ( 'NONE',  ( 0.1156495703730067437, 39.69517360536710271, -19.26748934528932722 ) ) ;
#7099=CARTESIAN_POINT ( 'NONE',  ( 0.1149546198390367091, -27.29633129785849022, -34.66780729582952603 ) ) ;
#7106=CARTESIAN_POINT ( 'NONE',  ( 0.3676999524040323597, 29.04098611012938136, 33.20499524279608750 ) ) ;
#7107=CARTESIAN_POINT ( 'NONE',  ( 3.390910168358337806, 30.99541111418804107, 31.19906451155395644 ) ) ;
#7108=CARTESIAN_POINT ( 'NONE',  ( 0.6016117650947689910, 33.27209104220542457, 36.11812580857002786 ) ) ;
#7116=VERTEX_POINT ( 'NONE', #15272 ) ;
#7121=CARTESIAN_POINT ( 'NONE',  ( 2.648799415243708655, 12.25810282899282200, 47.47900987092545222 ) ) ;
#7122=CARTESIAN_POINT ( 'NONE',  ( 5.901764892641307547, -22.68842833057569308, 43.39615982236225733 ) ) ;
#7126=CIRCLE ( 'NONE', #42193, 48.91267123290010943 ) ;
#7129=EDGE_CURVE ( 'NONE', #1309, #54294, #17021, .T. ) ;
#7135=CARTESIAN_POINT ( 'NONE',  ( 0.8744876279028263033, 40.65405044375290800, 27.52450240960382644 ) ) ;
#7139=EDGE_LOOP ( 'NONE', ( #53543, #26603, #26286, #55709 ) ) ;
#7141=CARTESIAN_POINT ( 'NONE',  ( 0.1154773475650540532, -38.53416957546567545, -21.49561362639775908 ) ) ;
#7142=CARTESIAN_POINT ( 'NONE',  ( -6.057079549204054558, -12.95277456599841592, 14.24980217905367930 ) ) ;
#7144=ORIENTED_EDGE ( 'NONE', *, *, #60795, .F. ) ;
#7148=CARTESIAN_POINT ( 'NONE',  ( 0.5997462898726536595, -14.47257175146309649, 46.92649887902422279 ) ) ;
#7152=ORIENTED_EDGE ( 'NONE', *, *, #42796, .T. ) ;
#7156=CARTESIAN_POINT ( 'NONE',  ( 0.3676999524040323597, -28.14442808720941969, 33.96824621564581292 ) ) ;
#7169=CARTESIAN_POINT ( 'NONE',  ( -6.072942160501519915, -4.270762779174508417, 18.77670758075115742 ) ) ;
#7175=CARTESIAN_POINT ( 'NONE',  ( 0.1154773475650540393, -1.594008704965688805, -44.09538259607931110 ) ) ;
#7186=B_SPLINE_CURVE_WITH_KNOTS ( 'NONE', 3,
 ( #13637, #61823, #52436, #61521, #32744, #37145, #51203, #28638, #22716, #28334, #38079, #8285, #18641, #32431, #42164, #13029, #41846, #33061, #32124 ),
 .UNSPECIFIED., .F., .F.,
 ( 4, 3, 3, 3, 3, 3, 4 ),
 ( 3.469685171791681197E-18, 0.0002612768053151709501, 0.0003919133833142916844, 0.0005225499612322625966, 0.0006531865391693322722, 0.0008112755173415197489, 0.0009693688056799745247 ),
 .UNSPECIFIED. ) ;
#7190=EDGE_CURVE ( 'NONE', #30308, #9806, #28200, .T. ) ;
#7192=ORIENTED_EDGE ( 'NONE', *, *, #42796, .F. ) ;
#7193=CARTESIAN_POINT ( 'NONE',  ( 4.553261556744873317, -41.61700166486752295, 14.05577241741092998 ) ) ;
#7194=VERTEX_POINT ( 'NONE', #47713 ) ;
#7195=EDGE_CURVE ( 'NONE', #61919, #48474, #33318, .T. ) ;
#7199=FILL_AREA_STYLE_COLOUR ( '', #30707 ) ;
#7201=EDGE_CURVE ( 'NONE', #60883, #52075, #45429, .T. ) ;
#7202=VERTEX_POINT ( 'NONE', #56780 ) ;
#7206=CARTESIAN_POINT ( 'NONE',  ( 0.1119899015040009965, 9.270611153904185997, 43.13950714861741176 ) ) ;
#7212=B_SPLINE_CURVE_WITH_KNOTS ( 'NONE', 3,
 ( #44900, #35486, #10434, #54542, #1937, #20148, #15443, #40205, #11672, #49876, #6935, #26069, #50185, #12918, #7559, #51091, #31080, #26682, #41429 ),
 .UNSPECIFIED., .F., .F.,
 ( 4, 3, 3, 3, 3, 3, 4 ),
 ( 1.734776414728241573E-18, 0.0002612768053151702454, 0.0003919133833142904918, 0.0005225499612322580430, 0.0006531865391693332480, 0.0008112755173415176890, 0.0009693688056799727899 ),
 .UNSPECIFIED. ) ;
#7215=CARTESIAN_POINT ( 'NONE',  ( 4.553261556744875094, 0.000000000000000000, 0.000000000000000000 ) ) ;
#7220=CARTESIAN_POINT ( 'NONE',  ( 1.112077966505211402, -42.35976605652983551, 12.19346319814910728 ) ) ;
#7236=VERTEX_POINT ( 'NONE', #4758 ) ;
#7237=CARTESIAN_POINT ( 'NONE',  ( 4.975610109902397937, 30.04451009524531102, -38.59762713269398660 ) ) ;
#7251=ADVANCED_FACE ( 'NONE', ( #57690 ), #15019, .F. ) ;
#7253=CARTESIAN_POINT ( 'NONE',  ( 0.1158816050234199174, -12.54909674931304941, 42.30203555482339084 ) ) ;
#7254=B_SPLINE_CURVE_WITH_KNOTS ( 'NONE', 3,
 ( #34086, #48169, #33772, #527, #208, #19982 ),
 .UNSPECIFIED., .F., .F.,
 ( 4, 2, 4 ),
 ( 1.553642821798679850E-17, 0.0002293755540694301259, 0.0004587511081388447477 ),
 .UNSPECIFIED. ) ;
#7260=CARTESIAN_POINT ( 'NONE',  ( 3.390910168358336918, 7.855615995994031486, -43.27108080296954995 ) ) ;
#7266=CARTESIAN_POINT ( 'NONE',  ( 2.009741617377216460, 42.20789687549766001, 12.56970639953054558 ) ) ;
#7267=DIRECTION ( 'NONE',  ( -0.1011922191286467460, -0.9400526519483206611, -0.3256703031483669242 ) ) ;
#7276=B_SPLINE_CURVE_WITH_KNOTS ( 'NONE', 3,
 ( #23699, #170, #13084, #14315, #32178, #33421, #37201, #52497, #8346, #27466, #46594, #60974, #8658, #27780, #46914, #3950, #23089, #42218, #33734 ),
 .UNSPECIFIED., .F., .F.,
 ( 4, 3, 3, 3, 3, 3, 4 ),
 ( 1.355252715606880543E-20, 0.0002612768053151697033, 0.0003919133833142910339, 0.0005225499612322614040, 0.0006531865391693344406, 0.0008112755173415172553, 0.0009693688056799748499 ),
 .UNSPECIFIED. ) ;
#7277=CARTESIAN_POINT ( 'NONE',  ( 4.553261556744875094, 40.80044851610500700, -16.27461110774390818 ) ) ;
#7278=CARTESIAN_POINT ( 'NONE',  ( 0.8744876279028263033, 17.78802839418742110, -45.75954650373051891 ) ) ;
#7293=CARTESIAN_POINT ( 'NONE',  ( 4.553261556744873317, -15.38244134641770167, -41.14510984366982171 ) ) ;
#7302=CARTESIAN_POINT ( 'NONE',  ( 0.3676999524040323597, 43.13409918076290950, 9.241215893319909114 ) ) ;
#7304=( BOUNDED_SURFACE ( )  B_SPLINE_SURFACE ( 3, 1, ( 
 ( #57010, #13826 ),
 ( #33237, #37025 ),
 ( #51380, #18828 ),
 ( #37955, #1 ) ),
 .UNSPECIFIED., .F., .F., .F. ) 
 B_SPLINE_SURFACE_WITH_KNOTS ( ( 4, 4 ),
 ( 2, 2 ),
 ( 0.000000000000000000, 1.000000000000000000 ),
 ( 0.000000000000000000, 1.000000000000000000 ),
 .UNSPECIFIED. ) 
 GEOMETRIC_REPRESENTATION_ITEM ( )  RATIONAL_B_SPLINE_SURFACE ( (
 ( 1.000000000000000000, 1.000000000000000000),
 ( 0.9953485035131437453, 0.8621029689291515030),
 ( 0.9953485035131437453, 0.8621029689291515030),
 ( 1.000000000000000000, 1.000000000000000000) ) ) 
 REPRESENTATION_ITEM ( '' )  SURFACE ( )  );
#7306=CARTESIAN_POINT ( 'NONE',  ( 4.975610109902397937, 20.32389311291233724, -44.49032227207044343 ) ) ;
#7310=CARTESIAN_POINT ( 'NONE',  ( 0.1156495703730067576, 15.11094602997547298, -41.45602806963348286 ) ) ;
#7312=EDGE_LOOP ( 'NONE', ( #38320, #11191, #54982, #8762 ) ) ;
#7317=CARTESIAN_POINT ( 'NONE',  ( 0.6024113833632039894, -8.052380081654970212, 48.44276049237319626 ) ) ;
#7319=CARTESIAN_POINT ( 'NONE',  ( 2.533389852662419894, -43.82923048324839499, -4.055747400899961441 ) ) ;
#7324=DIRECTION ( 'NONE',  ( 1.000000000000000000, 0.000000000000000000, 0.000000000000000000 ) ) ;
#7328=EDGE_CURVE ( 'NONE', #41448, #50438, #17794, .T. ) ;
#7342=CARTESIAN_POINT ( 'NONE',  ( 4.553261556744875094, -25.31600221269659201, 35.89762663172006540 ) ) ;
#7348=CARTESIAN_POINT ( 'NONE',  ( 0.1129192098497447394, -1.898585089631814826, -44.08341142019957459 ) ) ;
#7350=B_SPLINE_CURVE_WITH_KNOTS ( 'NONE', 3,
 ( #11436, #2320, #54624, #30837, #49955, #7009, #31148, #26142, #21446, #40582, #59645, #16757, #7319, #26448, #45579, #3245, #42134, #51794, #8258, #60566, #13295, #27377, #50870, #52099, #18308 ),
 .UNSPECIFIED., .F., .F.,
 ( 4, 3, 3, 3, 3, 3, 3, 3, 4 ),
 ( 5.057544569639794935E-18, 0.0005656085177311395316, 0.001131215744874499622, 0.001696821861372766133, 0.002262427090022498151, 0.002828031679238745925, 0.003393635864401604862, 0.003977030878808131623, 0.004561030005651158133 ),
 .UNSPECIFIED. ) ;
#7353=CARTESIAN_POINT ( 'NONE',  ( -6.078457390727109555, -1.844660340667949816, -19.16746564533440633 ) ) ;
#7364=CARTESIAN_POINT ( 'NONE',  ( 0.8753041380234471980, -2.462982411634902835, 49.04153388213869391 ) ) ;
#7374=B_SPLINE_CURVE_WITH_KNOTS ( 'NONE', 3,
 ( #36150, #7599, #55524, #55215, #12338, #41161, #12649, #50833, #3211, #22337, #60529, #36767, #31427, #26724, #60221, #17334 ),
 .UNSPECIFIED., .F., .F.,
 ( 4, 3, 3, 3, 3, 4 ),
 ( 2.194378057379452319E-17, 0.0002612764279487740844, 0.0003919131003184779440, 0.0005225497727000652558, 0.0007837925190632489322, 0.001045051706266716734 ),
 .UNSPECIFIED. ) ;
#7380=AXIS2_PLACEMENT_3D ( 'NONE', #20792, #59291, #25172 ) ;
#7386=CARTESIAN_POINT ( 'NONE',  ( -6.078075953587585900, -11.01234782890426445, -15.79630873154748549 ) ) ;
#7389=( BOUNDED_SURFACE ( )  B_SPLINE_SURFACE ( 3, 1, ( 
 ( #5337, #24468 ),
 ( #23856, #47980 ),
 ( #43926, #44231 ),
 ( #20396, #1259 ) ),
 .UNSPECIFIED., .F., .F., .F. ) 
 B_SPLINE_SURFACE_WITH_KNOTS ( ( 4, 4 ),
 ( 2, 2 ),
 ( 0.000000000000000000, 1.000000000000000000 ),
 ( 0.000000000000000000, 1.000000000000000000 ),
 .UNSPECIFIED. ) 
 GEOMETRIC_REPRESENTATION_ITEM ( )  RATIONAL_B_SPLINE_SURFACE ( (
 ( 1.000000000000000000, 1.000000000000000000),
 ( 0.7211978278499968642, 0.9934217856018975334),
 ( 0.7211978278499968642, 0.9934217856018975334),
 ( 1.000000000000000000, 1.000000000000000000) ) ) 
 REPRESENTATION_ITEM ( '' )  SURFACE ( )  );
#7390=CARTESIAN_POINT ( 'NONE',  ( -6.078726893082806448, -4.288195875146701752, 18.77246434022701749 ) ) ;
#7409=CARTESIAN_POINT ( 'NONE',  ( 0.1158516988532803244, -43.75558653473088810, 5.691292105881863073 ) ) ;
#7411=CARTESIAN_POINT ( 'NONE',  ( 0.1140933569871965259, -27.21347274398934246, -34.73293611683375559 ) ) ;
#7436=CARTESIAN_POINT ( 'NONE',  ( 0.1135584504625007929, -12.13985218845071579, -42.42141017196176023 ) ) ;
#7437=CARTESIAN_POINT ( 'NONE',  ( 4.553261556744875094, -41.61700166486733110, -14.05577241741153216 ) ) ;
#7439=CARTESIAN_POINT ( 'NONE',  ( 0.6253024248130485407, 4.031273609322430396, 48.94070964447109162 ) ) ;
#7440=FACE_OUTER_BOUND ( 'NONE', #38323, .T. ) ;
#7441=( NAMED_UNIT ( * ) PLANE_ANGLE_UNIT ( ) SI_UNIT ( $, .RADIAN. ) );
#7443=LINE ( 'NONE', #12813, #42522 ) ;
#7450=CARTESIAN_POINT ( 'NONE',  ( 0.1145239942831223490, -38.28493031833373550, -21.93648994768771132 ) ) ;
#7457=EDGE_CURVE ( 'NONE', #30599, #28421, #18565, .T. ) ;
#7459=ORIENTED_EDGE ( 'NONE', *, *, #9120, .F. ) ;
#7462=FACE_OUTER_BOUND ( 'NONE', #48271, .T. ) ;
#7470=LINE ( 'NONE', #26918, #13736 ) ;
#7474=CARTESIAN_POINT ( 'NONE',  ( 0.1129192098497447394, 36.71339784380064231, -24.47607416535520741 ) ) ;
#7480=ORIENTED_EDGE ( 'NONE', *, *, #257, .F. ) ;
#7491=CARTESIAN_POINT ( 'NONE',  ( 4.335381028904216727, -48.81116855472415494, -4.150502618557639245 ) ) ;
#7495=ORIENTED_EDGE ( 'NONE', *, *, #47385, .F. ) ;
#7497=CARTESIAN_POINT ( 'NONE',  ( -6.057079549204054558, -8.899553672604694654, -17.07715361318058811 ) ) ;
#7501=CARTESIAN_POINT ( 'NONE',  ( 1.112077966505210957, -34.68817258157839234, 27.19854790387139332 ) ) ;
#7507=EDGE_CURVE ( 'NONE', #21289, #35184, #28136, .T. ) ;
#7512=ORIENTED_EDGE ( 'NONE', *, *, #46999, .T. ) ;
#7525=CARTESIAN_POINT ( 'NONE',  ( 0.6039202388192953519, 27.95228209933789998, -40.37615185091348735 ) ) ;
#7528=AXIS2_PLACEMENT_3D ( 'NONE', #7540, #2541, #40804 ) ;
#7530=CARTESIAN_POINT ( 'NONE',  ( 3.727782113643637096, -41.93293375853455274, 13.20631827226376309 ) ) ;
#7535=CARTESIAN_POINT ( 'NONE',  ( 0.1129192098497455998, 3.754263797494300725, 43.96427289429426821 ) ) ;
#7540=CARTESIAN_POINT ( 'NONE',  ( 4.553261556744875094, 0.000000000000000000, 0.000000000000000000 ) ) ;
#7542=CARTESIAN_POINT ( 'NONE',  ( 3.894904216938898323, -10.35809250500306611, 42.71807875050094339 ) ) ;
#7544=DIRECTION ( 'NONE',  ( 0.09722883295013591554, -0.7096678276952463893, 0.6977951908529210767 ) ) ;
#7549=ORIENTED_EDGE ( 'NONE', *, *, #51958, .T. ) ;
#7550=CARTESIAN_POINT ( 'NONE',  ( -6.078457390727109555, 19.25602481922002340, -0.004381676659706296682 ) ) ;
#7553=CARTESIAN_POINT ( 'NONE',  ( 0.6039202388192953519, -42.87364092186805209, -23.94607748571178973 ) ) ;
#7555=EDGE_CURVE ( 'NONE', #43681, #17235, #20782, .T. ) ;
#7559=CARTESIAN_POINT ( 'NONE',  ( 0.1149546198390367924, 43.36205231031419061, -8.165720082196996188 ) ) ;
#7561=CARTESIAN_POINT ( 'NONE',  ( 0.9268187852002115479, -37.91842020551887060, 22.49328215326355718 ) ) ;
#7562=CARTESIAN_POINT ( 'NONE',  ( 0.5980271706414711508, -7.146479349117414337, -48.58988655836006387 ) ) ;
#7564=CARTESIAN_POINT ( 'NONE',  ( 3.678834586032788234, 2.858786927004010270, 48.89212315838150857 ) ) ;
#7571=VERTEX_POINT ( 'NONE', #541 ) ;
#7573=CARTESIAN_POINT ( 'NONE',  ( 0.6000166863083106206, -2.096232480232000039, 49.06556115135416007 ) ) ;
#7574=CARTESIAN_POINT ( 'NONE',  ( 0.6008122571543325074, 28.45128890504206609, 40.02597544229430326 ) ) ;
#7586=ADVANCED_FACE ( 'NONE', ( #52867 ), #60530, .F. ) ;
#7589=LINE ( 'NONE', #49584, #52739 ) ;
#7599=CARTESIAN_POINT ( 'NONE',  ( 0.6008123274975391004, 16.55074354900158440, 46.23448322554973799 ) ) ;
#7604=CARTESIAN_POINT ( 'NONE',  ( 0.6029443199889047422, 16.95996013332177554, -46.08576129490039364 ) ) ;
#7605=CARTESIAN_POINT ( 'NONE',  ( 3.221118495291109163, 2.339734729467391805, -43.92365036125158184 ) ) ;
#7610=CARTESIAN_POINT ( 'NONE',  ( 0.8753041380234530822, -39.87785955339003863, -28.65125905284232743 ) ) ;
#7611=B_SPLINE_CURVE_WITH_KNOTS ( 'NONE', 3,
 ( #47176, #19288, #18668, #18364, #51849, #14286 ),
 .UNSPECIFIED., .F., .F.,
 ( 4, 2, 4 ),
 ( 0.000000000000000000, 0.0002447195606305755050, 0.0004894391212611510101 ),
 .UNSPECIFIED. ) ;
#7612=EDGE_CURVE ( 'NONE', #19850, #41574, #31995, .T. ) ;
#7614=ORIENTED_EDGE ( 'NONE', *, *, #32151, .F. ) ;
#7634=CARTESIAN_POINT ( 'NONE',  ( 0.5980271706414711508, -24.85837266090859998, -42.35694218771055830 ) ) ;
#7640=CARTESIAN_POINT ( 'NONE',  ( 4.335381028904201628, -47.87967504119353634, 10.35826074271415287 ) ) ;
#7649=CARTESIAN_POINT ( 'NONE',  ( 2.648799415243696664, -40.11112523584315426, 28.20664984722760948 ) ) ;
#7659=CARTESIAN_POINT ( 'NONE',  ( 0.6016117650947689910, 40.96537808716857398, -27.08115308512227060 ) ) ;
#7660=( BOUNDED_SURFACE ( )  B_SPLINE_SURFACE ( 3, 1, ( 
 ( #29864, #28946 ),
 ( #33974, #24242 ),
 ( #48062, #38073 ),
 ( #5113, #413 ) ),
 .UNSPECIFIED., .F., .F., .F. ) 
 B_SPLINE_SURFACE_WITH_KNOTS ( ( 4, 4 ),
 ( 2, 2 ),
 ( 0.000000000000000000, 1.000000000000000000 ),
 ( 0.000000000000000000, 1.000000000000000000 ),
 .UNSPECIFIED. ) 
 GEOMETRIC_REPRESENTATION_ITEM ( )  RATIONAL_B_SPLINE_SURFACE ( (
 ( 1.000000000000000000, 1.000000000000000000),
 ( 0.7211978278499968642, 0.9934217856018975334),
 ( 0.7211978278499968642, 0.9934217856018975334),
 ( 1.000000000000000000, 1.000000000000000000) ) ) 
 REPRESENTATION_ITEM ( '' )  SURFACE ( )  );
#7663=CONICAL_SURFACE ( 'NONE', #35701, 43.92652462719577500, 1.486293639869522343 ) ;
#7667=CARTESIAN_POINT ( 'NONE',  ( 4.553261556744875094, 0.000000000000000000, 0.000000000000000000 ) ) ;
#7684=( BOUNDED_SURFACE ( )  B_SPLINE_SURFACE ( 3, 1, ( 
 ( #23320, #46516 ),
 ( #43059, #9513 ),
 ( #18624, #23020 ),
 ( #37433, #9210 ) ),
 .UNSPECIFIED., .F., .F., .F. ) 
 B_SPLINE_SURFACE_WITH_KNOTS ( ( 4, 4 ),
 ( 2, 2 ),
 ( 0.000000000000000000, 1.000000000000000000 ),
 ( 0.000000000000000000, 1.000000000000000000 ),
 .UNSPECIFIED. ) 
 GEOMETRIC_REPRESENTATION_ITEM ( )  RATIONAL_B_SPLINE_SURFACE ( (
 ( 1.000000000000000000, 1.000000000000000000),
 ( 0.7211978278499970862, 0.9934217856018976445),
 ( 0.7211978278499970862, 0.9934217856018976445),
 ( 1.000000000000000000, 1.000000000000000000) ) ) 
 REPRESENTATION_ITEM ( '' )  SURFACE ( )  );
#7690=EDGE_CURVE ( 'NONE', #52454, #3847, #47627, .T. ) ;
#7692=ORIENTED_EDGE ( 'NONE', *, *, #11259, .T. ) ;
#7699=ORIENTED_EDGE ( 'NONE', *, *, #60245, .T. ) ;
#7700=ADVANCED_FACE ( 'NONE', ( #58469 ), #11340, .F. ) ;
#7701=CARTESIAN_POINT ( 'NONE',  ( 2.706805983486679779, -43.97766765339521555, 1.655554616215038077 ) ) ;
#7702=CARTESIAN_POINT ( 'NONE',  ( 0.1152809850208375564, -42.62447063833258909, -11.40612928611975896 ) ) ;
#7704=CARTESIAN_POINT ( 'NONE',  ( 0.1158816050234199035, 33.60184995524097928, 28.59821184778224179 ) ) ;
#7705=CONICAL_SURFACE ( 'NONE', #60739, 43.92652462719577500, 1.486293639869522343 ) ;
#7707=CARTESIAN_POINT ( 'NONE',  ( 4.553261556744873317, 12.28162544311275006, -42.17465165592624032 ) ) ;
#7712=VERTEX_POINT ( 'NONE', #49098 ) ;
#7713=CARTESIAN_POINT ( 'NONE',  ( 0.6000166863083106206, -7.321729200002761395, -48.56146376737711279 ) ) ;
#7727=LINE ( 'NONE', #40360, #35705 ) ;
#7728=CARTESIAN_POINT ( 'NONE',  ( 0.6026112563231247332, -48.68169479572535607, -6.452409373253833458 ) ) ;
#7729=CARTESIAN_POINT ( 'NONE',  ( 0.1140933569871965675, -43.80888098664257058, 5.266108314694333714 ) ) ;
#7733=CARTESIAN_POINT ( 'NONE',  ( 0.8744876279028263033, 44.61213666265857825, -20.49651952824592982 ) ) ;
#7735=ORIENTED_EDGE ( 'NONE', *, *, #34684, .T. ) ;
#7736=CARTESIAN_POINT ( 'NONE',  ( 0.5987334363312686314, -38.99056171795593428, -29.85463118831556883 ) ) ;
#7755=CARTESIAN_POINT ( 'NONE',  ( 0.1139756605157203201, -12.93522790580227877, -42.18572150289689660 ) ) ;
#7758=CARTESIAN_POINT ( 'NONE',  ( 0.6024113833632039894, 22.90686952850539626, -43.43750910796909181 ) ) ;
#7764=CARTESIAN_POINT ( 'NONE',  ( 0.7413678028165011646, 16.10168025133689440, 41.05145533174129469 ) ) ;
#7769=B_SPLINE_CURVE_WITH_KNOTS ( 'NONE', 3,
 ( #48326, #52393, #47108, #4155, #43342, #57693 ),
 .UNSPECIFIED., .F., .F.,
 ( 4, 2, 4 ),
 ( 5.421010862427522170E-19, 0.0002293801035737099412, 0.0004587602071474193403 ),
 .UNSPECIFIED. ) ;
#7773=CARTESIAN_POINT ( 'NONE',  ( 2.706805983486679779, -32.74306943570211814, -29.40522942009712182 ) ) ;
#7774=CARTESIAN_POINT ( 'NONE',  ( 0.1135584504625007790, -38.23248975848313336, -22.02790909284708576 ) ) ;
#7775=CONICAL_SURFACE ( 'NONE', #44846, 43.92652462719577500, 1.486293639869522343 ) ;
#7777=ORIENTED_EDGE ( 'NONE', *, *, #15784, .T. ) ;
#7779=CARTESIAN_POINT ( 'NONE',  ( 2.009741617377216460, -40.28707309596673980, 17.78920512511105301 ) ) ;
#7780=CARTESIAN_POINT ( 'NONE',  ( -6.078726893082806448, 13.83016815118519638, 13.39852567182907350 ) ) ;
#7783=VERTEX_POINT ( 'NONE', #22137 ) ;
#7787=FACE_OUTER_BOUND ( 'NONE', #46509, .T. ) ;
#7790=CARTESIAN_POINT ( 'NONE',  ( -6.063463321072278589, -1.864608017455489097, 19.16621218239824032 ) ) ;
#7794=ADVANCED_FACE ( 'NONE', ( #55318 ), #36586, .F. ) ;
#7798=VERTEX_POINT ( 'NONE', #8322 ) ;
#7814=B_SPLINE_CURVE_WITH_KNOTS ( 'NONE', 3,
 ( #42063, #56420, #17612, #51102, #17006, #60811, #55491, #36738, #7253, #61116, #32331, #8193, #60495, #27620, #37346, #40831, #55807, #27312, #46439 ),
 .UNSPECIFIED., .F., .F.,
 ( 4, 3, 3, 3, 3, 3, 4 ),
 ( 1.734776414728241573E-18, 0.0002612768053151704622, 0.0003919133833142885402, 0.0005225499612322576093, 0.0006531865391693351995, 0.0008112755173415168216, 0.0009693688056799714889 ),
 .UNSPECIFIED. ) ;
#7817=CARTESIAN_POINT ( 'NONE',  ( -6.078075953587585900, 13.82887156709808707, -13.39990617235218195 ) ) ;
#7822=CARTESIAN_POINT ( 'NONE',  ( 0.3676999524040366896, -34.85286720109691316, 27.04123205746257241 ) ) ;
#7831=( NAMED_UNIT ( * ) SI_UNIT ( $, .STERADIAN. ) SOLID_ANGLE_UNIT ( ) );
#7832=CARTESIAN_POINT ( 'NONE',  ( 2.299652685299200972, 36.48832987231130431, 32.75490051866358954 ) ) ;
#7836=ADVANCED_FACE ( 'NONE', ( #22750 ), #45395, .F. ) ;
#7843=CARTESIAN_POINT ( 'NONE',  ( 0.6027444965799114707, -49.10724443700913611, -0.1306127531153215560 ) ) ;
#7845=B_SPLINE_CURVE_WITH_KNOTS ( 'NONE', 3,
 ( #15534, #22846, #56341, #3710, #237, #39351, #27851, #41979, #61342, #34638, #51955, #37903, #23456, #23769, #8737, #61045, #52258, #53705, #33184, #9047, #47274, #19091, #14384, #32882, #46983 ),
 .UNSPECIFIED., .F., .F.,
 ( 4, 3, 3, 3, 3, 3, 3, 3, 4 ),
 ( 6.254634441385501517E-18, 0.0005656085177311403990, 0.001131215744874501140, 0.001696821861372765916, 0.002262427090022497284, 0.002828031679238746793, 0.003393635864401604862, 0.003977030878808130755, 0.004561030005651156398 ),
 .UNSPECIFIED. ) ;
#7848=CARTESIAN_POINT ( 'NONE',  ( -6.078075953587585900, -4.290048539733304800, -18.77207121694002367 ) ) ;
#7849=CARTESIAN_POINT ( 'NONE',  ( 2.648799415243708655, 40.32403112341518892, -27.90143324719075579 ) ) ;
#7858=ADVANCED_FACE ( 'NONE', ( #47489 ), #51754, .F. ) ;
#7860=CARTESIAN_POINT ( 'NONE',  ( 0.1149546198390368201, 3.964231739604973104, 43.94577831530497747 ) ) ;
#7861=EDGE_CURVE ( 'NONE', #8195, #61878, #61035, .T. ) ;
#7865=DIRECTION ( 'NONE',  ( -1.000000000000000000, -0.000000000000000000, -0.000000000000000000 ) ) ;
#7866=EDGE_LOOP ( 'NONE', ( #59243, #8556, #55440, #24343 ) ) ;
#7870=VERTEX_POINT ( 'NONE', #57461 ) ;
#7873=CARTESIAN_POINT ( 'NONE',  ( 0.6000166863083090663, -49.10753961887881758, -0.5225268306041156441 ) ) ;
#7879=ORIENTED_EDGE ( 'NONE', *, *, #34759, .F. ) ;
#7881=CARTESIAN_POINT ( 'NONE',  ( -6.063463321072278589, -14.67303933398460103, 12.47086080360175586 ) ) ;
#7882=CARTESIAN_POINT ( 'NONE',  ( 3.050102900204245682, -37.41160462723878055, 23.14729116750437754 ) ) ;
#7889=ORIENTED_EDGE ( 'NONE', *, *, #39686, .F. ) ;
#7890=B_SPLINE_CURVE_WITH_KNOTS ( 'NONE', 3,
 ( #15512, #34620, #53685, #10815 ),
 .UNSPECIFIED., .F., .F.,
 ( 4, 4 ),
 ( 0.000000000000000000, 0.004444103432399267029 ),
 .UNSPECIFIED. ) ;
#7893=CARTESIAN_POINT ( 'NONE',  ( 2.706805983486680223, 13.63466385414067794, -41.84342307823710883 ) ) ;
#7897=CARTESIAN_POINT ( 'NONE',  ( 0.6024113833632039894, 27.91636117921130733, 40.40072583027055941 ) ) ;
#7901=ORIENTED_EDGE ( 'NONE', *, *, #25168, .F. ) ;
#7906=LINE ( 'NONE', #3496, #2808 ) ;
#7908=CARTESIAN_POINT ( 'NONE',  ( 0.7044674535453004927, 46.33602660604233847, -16.27191940660486935 ) ) ;
#7910=CARTESIAN_POINT ( 'NONE',  ( 3.894904216938898323, 11.93731129210782704, 42.30395881701280558 ) ) ;
#7916=CARTESIAN_POINT ( 'NONE',  ( 0.7044674535453004927, -48.80743866909963913, -5.443955673311811516 ) ) ;
#7917=DIRECTION ( 'NONE',  ( -1.000000000000000000, -0.000000000000000000, -0.000000000000000000 ) ) ;
#7926=CARTESIAN_POINT ( 'NONE',  ( 0.6029443199889047422, -47.50133849333689540, 12.45634309080449320 ) ) ;
#7930=CARTESIAN_POINT ( 'NONE',  ( 0.5997462898726536595, 16.46871699354542429, -46.26373299606095202 ) ) ;
#7934=ORIENTED_EDGE ( 'NONE', *, *, #12257, .F. ) ;
#7936=CARTESIAN_POINT ( 'NONE',  ( 0.7948878604505679180, 36.81796311561313928, -32.48286070092603239 ) ) ;
#7938=B_SPLINE_CURVE_WITH_KNOTS ( 'NONE', 3,
 ( #19490, #38607, #57659, #33906, #24484, #15100 ),
 .UNSPECIFIED., .F., .F.,
 ( 4, 2, 4 ),
 ( 9.825198971288231405E-18, 0.0002293755540694290146, 0.0004587511081388482171 ),
 .UNSPECIFIED. ) ;
#7939=ADVANCED_FACE ( 'NONE', ( #44967 ), #21550, .F. ) ;
#7945=CIRCLE ( 'NONE', #60970, 43.92652462719577500 ) ;
#7950=CARTESIAN_POINT ( 'NONE',  ( -6.077587904424778920, 16.78120357693994791, -9.443898977817823948 ) ) ;
#7951=( BOUNDED_SURFACE ( )  B_SPLINE_SURFACE ( 3, 1, ( 
 ( #27984, #14516 ),
 ( #13588, #8552 ),
 ( #33620, #9482 ),
 ( #38035, #28899 ) ),
 .UNSPECIFIED., .F., .F., .F. ) 
 B_SPLINE_SURFACE_WITH_KNOTS ( ( 4, 4 ),
 ( 2, 2 ),
 ( 0.000000000000000000, 1.000000000000000000 ),
 ( 0.000000000000000000, 1.000000000000000000 ),
 .UNSPECIFIED. ) 
 GEOMETRIC_REPRESENTATION_ITEM ( )  RATIONAL_B_SPLINE_SURFACE ( (
 ( 1.000000000000000000, 1.000000000000000000),
 ( 0.9754377213608244057, 0.9999580625633939235),
 ( 0.9754377213608244057, 0.9999580625633939235),
 ( 1.000000000000000000, 1.000000000000000000) ) ) 
 REPRESENTATION_ITEM ( '' )  SURFACE ( )  );
#7954=ORIENTED_EDGE ( 'NONE', *, *, #57829, .T. ) ;
#7956=CARTESIAN_POINT ( 'NONE',  ( -6.077587904424778920, 0.6233693561571294062, -19.24597183931574662 ) ) ;
#7962=CARTESIAN_POINT ( 'NONE',  ( 0.7044674535453004927, -31.27352687970047995, -37.86514544162691465 ) ) ;
#7963=CARTESIAN_POINT ( 'NONE',  ( -2.601141883200662974, -14.73982649082957330, 2.352220756992720929 ) ) ;
#7966=CARTESIAN_POINT ( 'NONE',  ( 2.648799415243696664, -47.76469914295827834, 11.09283458239048592 ) ) ;
#7977=EDGE_CURVE ( 'NONE', #56473, #16223, #37105, .T. ) ;
#7978=CARTESIAN_POINT ( 'NONE',  ( 0.7044674535452954967, -2.415488218027790790, 49.05066910328008589 ) ) ;
#7979=EDGE_CURVE ( 'NONE', #51706, #22341, #19237, .T. ) ;
#7990=ORIENTED_EDGE ( 'NONE', *, *, #20163, .T. ) ;
#7996=CARTESIAN_POINT ( 'NONE',  ( 0.3676999524040323597, 10.61898383218351860, -42.81574203134477585 ) ) ;
#7997=CARTESIAN_POINT ( 'NONE',  ( 0.8744876279028306332, -45.83369275826206746, -17.59609782084448071 ) ) ;
#8001=CARTESIAN_POINT ( 'NONE',  ( 3.221118495291108719, 35.79969342022239687, -25.55666978852753601 ) ) ;
#8006=AXIS2_PLACEMENT_3D ( 'NONE', #9681, #57575, #28793 ) ;
#8008=DIRECTION ( 'NONE',  ( -1.000000000000000000, -0.000000000000000000, -0.000000000000000000 ) ) ;
#8013=B_SPLINE_CURVE_WITH_KNOTS ( 'NONE', 3,
 ( #36577, #2413, #50644, #55646, #12779, #41283, #21536, #27465, #13083, #36271, #59740, #32177, #41587, #31873, #7099, #55964, #7411, #11857, #16856 ),
 .UNSPECIFIED., .F., .F.,
 ( 4, 3, 3, 3, 3, 3, 4 ),
 ( 1.355252715606880543E-20, 0.0002612768053151734980, 0.0003919133833142895702, 0.0005225499612322635724, 0.0006531865391693340069, 0.0008112755173415186647, 0.0009693688056799699710 ),
 .UNSPECIFIED. ) ;
#8015=ORIENTED_EDGE ( 'NONE', *, *, #44313, .T. ) ;
#8016=VERTEX_POINT ( 'NONE', #51166 ) ;
#8025=CARTESIAN_POINT ( 'NONE',  ( 0.1368894036331294861, 29.18906331529160170, -33.08866737569275074 ) ) ;
#8031=CARTESIAN_POINT ( 'NONE',  ( 4.834790513006555379, -46.46485498442988415, -8.579428430861931076 ) ) ;
#8036=VERTEX_POINT ( 'NONE', #17671 ) ;
#8037=CARTESIAN_POINT ( 'NONE',  ( -2.739355103387248747, 12.65256472621572570, 7.922131834294261488 ) ) ;
#8043=CARTESIAN_POINT ( 'NONE',  ( 0.8744876279028263033, -39.87136468799916145, 28.64654129726773846 ) ) ;
#8049=ORIENTED_EDGE ( 'NONE', *, *, #48591, .F. ) ;
#8050=CARTESIAN_POINT ( 'NONE',  ( 0.1158816050234199035, 43.31156486878287382, 8.429139334616255752 ) ) ;
#8054=ORIENTED_EDGE ( 'NONE', *, *, #56470, .F. ) ;
#8057=DIRECTION ( 'NONE',  ( -0.1011922191286467460, 0.04473873795208903326, -0.9938604429769173354 ) ) ;
#8060=ADVANCED_FACE ( 'NONE', ( #41495 ), #528, .F. ) ;
#8079=CARTESIAN_POINT ( 'NONE',  ( 0.2285344041767087553, -28.09782188418681059, -34.01490225856849747 ) ) ;
#8083=CARTESIAN_POINT ( 'NONE',  ( 4.694002226626920127, -38.39382765324673841, -24.58045503197449833 ) ) ;
#8084=CARTESIAN_POINT ( 'NONE',  ( 3.390910168358336918, 17.02218646828075421, 40.55049080310516274 ) ) ;
#8085=EDGE_CURVE ( 'NONE', #13905, #29266, #61182, .T. ) ;
#8088=CARTESIAN_POINT ( 'NONE',  ( 2.533389852662419894, 32.46881123593813356, -29.71913236719125706 ) ) ;
#8090=ORIENTED_EDGE ( 'NONE', *, *, #46081, .F. ) ;
#8095=ORIENTED_EDGE ( 'NONE', *, *, #50368, .F. ) ;
#8105=CARTESIAN_POINT ( 'NONE',  ( 4.694002226626921015, -9.808094470216147442, -44.52062504401135357 ) ) ;
#8114=CARTESIAN_POINT ( 'NONE',  ( 0.1157506346131639274, -1.321521084112260436, 44.10435626814069110 ) ) ;
#8116=VERTEX_POINT ( 'NONE', #36800 ) ;
#8119=CARTESIAN_POINT ( 'NONE',  ( 0.3676999524040366896, -41.19158123804976412, -15.78620342045500280 ) ) ;
#8120=CARTESIAN_POINT ( 'NONE',  ( 0.8744876279028263033, -0.6840263623742536270, -49.09055060105834656 ) ) ;
#8121=CARTESIAN_POINT ( 'NONE',  ( 0.8744876279028306332, 41.62483489565916983, 26.03311679935014666 ) ) ;
#8123=CARTESIAN_POINT ( 'NONE',  ( 2.533389852662419894, 5.798859955822282863, 43.63282886710852893 ) ) ;
#8131=B_SPLINE_CURVE_WITH_KNOTS ( 'NONE', 3,
 ( #5743, #24891, #44032, #1066, #20201, #39311 ),
 .UNSPECIFIED., .F., .F.,
 ( 4, 2, 4 ),
 ( 5.421010862427522170E-19, 0.0002293801035737082878, 0.0004587602071474160335 ),
 .UNSPECIFIED. ) ;
#8141=CARTESIAN_POINT ( 'NONE',  ( 0.8753041380234471980, -20.68664920503345428, 44.53314352862224013 ) ) ;
#8142=DIRECTION ( 'NONE',  ( -1.000000000000000000, -0.000000000000000000, -0.000000000000000000 ) ) ;
#8143=CARTESIAN_POINT ( 'NONE',  ( 3.221118495291109163, -39.21725469344816872, -19.91904500649992471 ) ) ;
#8144=CARTESIAN_POINT ( 'NONE',  ( 1.834102595619085507, -43.50031898818188125, 6.922426798753990695 ) ) ;
#8147=VERTEX_POINT ( 'NONE', #4161 ) ;
#8148=CARTESIAN_POINT ( 'NONE',  ( 0.3676999524040366896, -44.10520818713899871, 0.8253448321555690859 ) ) ;
#8153=CARTESIAN_POINT ( 'NONE',  ( 4.975610109902397937, 34.73360008816130318, 34.43873447229810836 ) ) ;
#8160=CARTESIAN_POINT ( 'NONE',  ( 0.6252788684277222897, 46.38381364802560114, -16.12408641253514219 ) ) ;
#8161=CARTESIAN_POINT ( 'NONE',  ( 2.359973842542475442, 23.93452390393565921, -36.94962056807123219 ) ) ;
#8162=CARTESIAN_POINT ( 'NONE',  ( 0.5987334363312692975, -42.48817524472720208, -24.62352271397064030 ) ) ;
#8165=CARTESIAN_POINT ( 'NONE',  ( 0.5997462898726536595, 44.01516392039513903, -21.77652348757843015 ) ) ;
#8169=CARTESIAN_POINT ( 'NONE',  ( 0.1129192098497455998, 4.719118110135312349, -43.87119455916086963 ) ) ;
#8174=DIRECTION ( 'NONE',  ( -1.000000000000000000, -0.000000000000000000, -0.000000000000000000 ) ) ;
#8177=CARTESIAN_POINT ( 'NONE',  ( -6.057079549204054558, 7.787131596469407668, 17.61226313109721531 ) ) ;
#8179=CARTESIAN_POINT ( 'NONE',  ( 0.1119899015040013157, -13.09165644557430852, 42.13751107627926729 ) ) ;
#8180=ORIENTED_EDGE ( 'NONE', *, *, #42372, .T. ) ;
#8183=VERTEX_POINT ( 'NONE', #33631 ) ;
#8186=CARTESIAN_POINT ( 'NONE',  ( 1.112077966505210957, -37.88145627207394739, 22.53942314779827427 ) ) ;
#8190=ORIENTED_EDGE ( 'NONE', *, *, #30401, .T. ) ;
#8193=CARTESIAN_POINT ( 'NONE',  ( 0.1156867017252034557, -12.67428682873097756, 42.26470466782232904 ) ) ;
#8195=VERTEX_POINT ( 'NONE', #37731 ) ;
#8197=CARTESIAN_POINT ( 'NONE',  ( 2.648799415243708655, -18.57388519568396390, 45.38202564922758597 ) ) ;
#8198=CARTESIAN_POINT ( 'NONE',  ( -6.079354080745853928, -18.90066517279534963, -3.682093327720422415 ) ) ;
#8199=CARTESIAN_POINT ( 'NONE',  ( 0.5997462898726536595, -45.71211507932765983, -17.94308126043611296 ) ) ;
#8205=CARTESIAN_POINT ( 'NONE',  ( 0.8744876279028263033, -26.20733431478184983, 41.51536677536103070 ) ) ;
#8207=ADVANCED_FACE ( 'NONE', ( #61786 ), #27920, .F. ) ;
#8208=CARTESIAN_POINT ( 'NONE',  ( 0.5980271706414734822, -26.05568637495906614, -41.63112357805678698 ) ) ;
#8211=CARTESIAN_POINT ( 'NONE',  ( 4.553261556744875094, 12.28162544311214432, 42.17465165592641796 ) ) ;
#8215=CARTESIAN_POINT ( 'NONE',  ( -6.072942160501519027, 13.82262479916533771, 13.40668512162942072 ) ) ;
#8216=CARTESIAN_POINT ( 'NONE',  ( -6.072942160501519027, 5.492864488351536068, -18.45623477314988747 ) ) ;
#8221=FACE_OUTER_BOUND ( 'NONE', #3472, .T. ) ;
#8224=CARTESIAN_POINT ( 'NONE',  ( 0.6027444965799114707, -47.53431580546581614, 12.32993660947551895 ) ) ;
#8228=CARTESIAN_POINT ( 'NONE',  ( 0.6029443449137436017, -39.38137730902946743, 29.33677997373246882 ) ) ;
#8234=CARTESIAN_POINT ( 'NONE',  ( 0.1119899015040013435, 43.19989886304176707, 8.984990062068465733 ) ) ;
#8240=EDGE_CURVE ( 'NONE', #18777, #36635, #52836, .T. ) ;
#8245=CARTESIAN_POINT ( 'NONE',  ( 0.8744876279028306332, -31.30103973185180521, -37.82320666052162039 ) ) ;
#8248=VERTEX_POINT ( 'NONE', #58951 ) ;
#8250=ORIENTED_EDGE ( 'NONE', *, *, #56975, .F. ) ;
#8252=B_SPLINE_CURVE_WITH_KNOTS ( 'NONE', 3,
 ( #50429, #22552, #60423, #60735 ),
 .UNSPECIFIED., .F., .F.,
 ( 4, 4 ),
 ( 2.308109569601360422E-17, 0.004559932413162185935 ),
 .UNSPECIFIED. ) ;
#8254=CARTESIAN_POINT ( 'NONE',  ( 0.6027444965799114707, -48.72077702715109382, 6.150154612533532905 ) ) ;
#8257=CARTESIAN_POINT ( 'NONE',  ( 0.7242003506639995702, -29.97003518583413140, 38.89484111146220613 ) ) ;
#8258=CARTESIAN_POINT ( 'NONE',  ( 1.479689385636123067, -43.83641450621821889, -4.466834282432383674 ) ) ;
#8264=VERTEX_POINT ( 'NONE', #1310 ) ;
#8267=CARTESIAN_POINT ( 'NONE',  ( -6.063463321072278589, 12.01854346922056749, -15.04576569530197006 ) ) ;
#8273=CARTESIAN_POINT ( 'NONE',  ( -6.078726893082806448, 0.6137717894420866571, -19.24622886331774652 ) ) ;
#8280=B_SPLINE_CURVE_WITH_KNOTS ( 'NONE', 3,
 ( #14858, #38367, #18629, #4797 ),
 .UNSPECIFIED., .F., .F.,
 ( 4, 4 ),
 ( 6.938893903907227607E-18, 0.005013413432710145043 ),
 .UNSPECIFIED. ) ;
#8281=CARTESIAN_POINT ( 'NONE',  ( 0.8744876279028306332, -2.462621419132613454, -49.03351451941336592 ) ) ;
#8285=CARTESIAN_POINT ( 'NONE',  ( 0.1156867017252034557, -35.28683493765469592, -26.49116998846783844 ) ) ;
#8287=ADVANCED_FACE ( 'NONE', ( #24840 ), #46603, .F. ) ;
#8296=EDGE_LOOP ( 'NONE', ( #13919, #10120, #9332, #16909 ) ) ;
#8303=CIRCLE ( 'NONE', #43354, 43.92652462719577500 ) ;
#8310=CARTESIAN_POINT ( 'NONE',  ( 0.9268187852002115479, 37.48124960562999775, 23.21444078389758303 ) ) ;
#8312=EDGE_CURVE ( 'NONE', #17976, #22076, #35662, .T. ) ;
#8313=CARTESIAN_POINT ( 'NONE',  ( 1.479689385636123067, -44.04772423883621002, 1.175514630760941648 ) ) ;
#8314=EDGE_CURVE ( 'NONE', #49156, #5480, #20665, .T. ) ;
#8315=CARTESIAN_POINT ( 'NONE',  ( 0.1158516988532803660, -42.69354052901408636, -11.14467388173511431 ) ) ;
#8316=( BOUNDED_SURFACE ( )  B_SPLINE_SURFACE ( 3, 1, ( 
 ( #14762, #48269 ),
 ( #39199, #35109 ),
 ( #10672, #45136 ),
 ( #11604, #26002 ) ),
 .UNSPECIFIED., .F., .F., .F. ) 
 B_SPLINE_SURFACE_WITH_KNOTS ( ( 4, 4 ),
 ( 2, 2 ),
 ( 0.000000000000000000, 1.000000000000000000 ),
 ( 0.000000000000000000, 1.000000000000000000 ),
 .UNSPECIFIED. ) 
 GEOMETRIC_REPRESENTATION_ITEM ( )  RATIONAL_B_SPLINE_SURFACE ( (
 ( 1.000000000000000000, 1.000000000000000000),
 ( 0.7211978278499970862, 0.9934217856018976445),
 ( 0.7211978278499970862, 0.9934217856018976445),
 ( 1.000000000000000000, 1.000000000000000000) ) ) 
 REPRESENTATION_ITEM ( '' )  SURFACE ( )  );
#8317=CARTESIAN_POINT ( 'NONE',  ( 0.6000166863083090663, 17.45040302316650838, -45.90541270958704700 ) ) ;
#8319=EDGE_CURVE ( 'NONE', #35750, #31302, #7212, .T. ) ;
#8322=CARTESIAN_POINT ( 'NONE',  ( 0.3676999524040366896, 9.009680404096547690, -43.18305503711933113 ) ) ;
#8325=ADVANCED_FACE ( 'NONE', ( #26372 ), #52471, .F. ) ;
#8326=DIRECTION ( 'NONE',  ( 0.09722883295013594329, 0.9421506058508687387, -0.3207784125186660673 ) ) ;
#8327=CARTESIAN_POINT ( 'NONE',  ( 2.706805983486680667, 38.90419121147174053, -20.57279804744605656 ) ) ;
#8328=CARTESIAN_POINT ( 'NONE',  ( 4.553261556744873317, -4.442710778081946366, -43.70128015019640344 ) ) ;
#8329=B_SPLINE_CURVE_WITH_KNOTS ( 'NONE', 3,
 ( #44628, #1360, #53373, #53670, #39312, #58370, #19904, #6354, #11407, #33999, #30192, #49298, #5744, #29270, #10175, #39622, #14893, #1067, #58679 ),
 .UNSPECIFIED., .F., .F.,
 ( 4, 3, 3, 3, 3, 3, 4 ),
 ( 0.000000000000000000, 0.0002612768053151685106, 0.0003919133833142900581, 0.0005225499612322606451, 0.0006531865391693344406, 0.0008112755173415184479, 0.0009693688056799704047 ),
 .UNSPECIFIED. ) ;
#8339=ORIENTED_EDGE ( 'NONE', *, *, #61076, .F. ) ;
#8346=CARTESIAN_POINT ( 'NONE',  ( 0.1158816050234199174, -27.50652624945415781, 34.50120367455677695 ) ) ;
#8347=CARTESIAN_POINT ( 'NONE',  ( 0.8753041380234524160, -0.6841799139051519818, 49.09857661601188283 ) ) ;
#8348=AXIS2_PLACEMENT_3D ( 'NONE', #14921, #10510, #58399 ) ;
#8350=VERTEX_POINT ( 'NONE', #60798 ) ;
#8361=CARTESIAN_POINT ( 'NONE',  ( 5.901764892641307547, 45.40663509823473731, -18.33654701669415843 ) ) ;
#8363=CARTESIAN_POINT ( 'NONE',  ( 0.1119898979215351448, 19.90994801901936739, -39.37709077791013357 ) ) ;
#8372=CARTESIAN_POINT ( 'NONE',  ( 0.7948884756798513251, 48.35174766733348406, -8.532710127190703986 ) ) ;
#8373=CARTESIAN_POINT ( 'NONE',  ( -6.072942160501519915, -18.27985097084430777, -6.054024345238677718 ) ) ;
#8375=CARTESIAN_POINT ( 'NONE',  ( 0.5997462898726536595, -1.051648045106814422, -49.09628974305016413 ) ) ;
#8378=AXIS2_PLACEMENT_3D ( 'NONE', #7667, #26792, #55906 ) ;
#8379=CARTESIAN_POINT ( 'NONE',  ( 0.8744876279028263033, -49.08725279547490317, -0.8897546699139439186 ) ) ;
#8383=LINE ( 'NONE', #23738, #23338 ) ;
#8385=CARTESIAN_POINT ( 'NONE',  ( 4.553261556744875094, 27.56395660609745235, -34.20186927699732138 ) ) ;
#8389=CARTESIAN_POINT ( 'NONE',  ( -6.078075953587585900, 13.82887156709789345, 13.39990617235237913 ) ) ;
#8390=VECTOR ( 'NONE', #52185, 1000.000000000000000 ) ;
#8394=CARTESIAN_POINT ( 'NONE',  ( -6.077587904424778920, -6.644566705894775716, -18.07334376049006508 ) ) ;
#8402=EDGE_CURVE ( 'NONE', #27686, #55688, #23531, .T. ) ;
#8406=CARTESIAN_POINT ( 'NONE',  ( 4.975610109902397937, 19.27143522741721426, -44.95621415792522413 ) ) ;
#8411=ORIENTED_EDGE ( 'NONE', *, *, #14855, .T. ) ;
#8416=CARTESIAN_POINT ( 'NONE',  ( 0.3676999524040323597, 42.11837424242189343, -13.11461530118710428 ) ) ;
#8427=CARTESIAN_POINT ( 'NONE',  ( 0.3676999524040323597, 21.13209774130321250, -38.72189339862975288 ) ) ;
#8430=CARTESIAN_POINT ( 'NONE',  ( 3.894904216938897878, -33.85124917310555759, 28.03956600763502749 ) ) ;
#8435=CARTESIAN_POINT ( 'NONE',  ( 0.7948878604505673628, -26.19034530854877119, -41.53028364841004105 ) ) ;
#8446=CARTESIAN_POINT ( 'NONE',  ( 0.7044674535452954967, -0.7321618212251337354, -49.10465010442948142 ) ) ;
#8448=CARTESIAN_POINT ( 'NONE',  ( 0.6016117650947689910, -49.10631026021277279, 0.3483487795599483627 ) ) ;
#8454=CARTESIAN_POINT ( 'NONE',  ( 2.009741617377216460, 24.05948448209586132, -36.88692565230712006 ) ) ;
#8455=CARTESIAN_POINT ( 'NONE',  ( 0.5997462898726536595, 33.39998138387845472, 35.99990102348730403 ) ) ;
#8464=FACE_OUTER_BOUND ( 'NONE', #52154, .T. ) ;
#8469=CARTESIAN_POINT ( 'NONE',  ( 0.8744876279028306332, 11.79038800009151089, 47.65854384249261244 ) ) ;
#8470=CIRCLE ( 'NONE', #32520, 48.91267123290010943 ) ;
#8474=CARTESIAN_POINT ( 'NONE',  ( 0.8753041380234471980, 23.49739456791673575, -43.11624724384784457 ) ) ;
#8488=VERTEX_POINT ( 'NONE', #19456 ) ;
#8491=CARTESIAN_POINT ( 'NONE',  ( 0.1129192098497455998, -31.35755906439593943, -31.04279751098591689 ) ) ;
#8492=VERTEX_POINT ( 'NONE', #61405 ) ;
#8500=VERTEX_POINT ( 'NONE', #51714 ) ;
#8501=CARTESIAN_POINT ( 'NONE',  ( 0.5997462898726536595, -47.36625756029525292, -12.96106765957508244 ) ) ;
#8502=CARTESIAN_POINT ( 'NONE',  ( 0.6028777368367060907, 28.02372537435406130, 40.32630215447304778 ) ) ;
#8503=CARTESIAN_POINT ( 'NONE',  ( 4.975610109902397937, 0.000000000000000000, 0.000000000000000000 ) ) ;
#8504=VERTEX_POINT ( 'NONE', #27924 ) ;
#8507=CARTESIAN_POINT ( 'NONE',  ( 0.5997462898726536595, -25.90236585764290922, 41.72072714036901431 ) ) ;
#8508=CARTESIAN_POINT ( 'NONE',  ( 0.1129192098497447394, -18.30288010335054949, -40.14917642626718930 ) ) ;
#8513=CARTESIAN_POINT ( 'NONE',  ( 0.5997462898726536595, 37.72933316222010802, -31.43324751403371664 ) ) ;
#8519=FACE_OUTER_BOUND ( 'NONE', #28588, .T. ) ;
#8524=CARTESIAN_POINT ( 'NONE',  ( 0.5997462898726536595, 27.66511329191646951, -40.57330571557777432 ) ) ;
#8532=ORIENTED_EDGE ( 'NONE', *, *, #2546, .T. ) ;
#8535=CARTESIAN_POINT ( 'NONE',  ( -6.077587904424778920, -17.34643006009198274, 8.360465630828690209 ) ) ;
#8536=LINE ( 'NONE', #51761, #1678 ) ;
#8539=CARTESIAN_POINT ( 'NONE',  ( 2.533389852662419894, -30.49798923258317629, 31.73835510077449484 ) ) ;
#8540=CARTESIAN_POINT ( 'NONE',  ( -6.078726893082806448, 15.42998809551227879, 11.51996131248145439 ) ) ;
#8550=EDGE_CURVE ( 'NONE', #41582, #27020, #19127, .T. ) ;
#8552=CARTESIAN_POINT ( 'NONE',  ( 0.6039202388192953519, 44.16863261170606592, -21.46382086351650287 ) ) ;
#8556=ORIENTED_EDGE ( 'NONE', *, *, #39328, .F. ) ;
#8560=ORIENTED_EDGE ( 'NONE', *, *, #50552, .F. ) ;
#8564=CARTESIAN_POINT ( 'NONE',  ( 0.6021447746440204973, 46.68736993825091730, 15.22598526655637485 ) ) ;
#8568=ADVANCED_FACE ( 'NONE', ( #5930 ), #12490, .F. ) ;
#8577=LINE ( 'NONE', #31792, #50645 ) ;
#8589=CARTESIAN_POINT ( 'NONE',  ( -6.078726893082806448, -8.903615017412294108, -17.07394743140643456 ) ) ;
#8594=EDGE_CURVE ( 'NONE', #34535, #25604, #45976, .T. ) ;
#8598=CARTESIAN_POINT ( 'NONE',  ( 2.533389852662419894, -24.15616722665976113, -36.79578938752730721 ) ) ;
#8615=CARTESIAN_POINT ( 'NONE',  ( 0.6016118706126977189, 11.26678578505916661, -47.79760028346109380 ) ) ;
#8617=CARTESIAN_POINT ( 'NONE',  ( -2.601141883200665639, -14.91960803315171269, -0.4480218817239748907 ) ) ;
#8619=VERTEX_POINT ( 'NONE', #8119 ) ;
#8625=CARTESIAN_POINT ( 'NONE',  ( 2.533389852662419894, 37.72904932230753161, 22.67089254900441020 ) ) ;
#8628=CARTESIAN_POINT ( 'NONE',  ( 0.9268187852002115479, -44.07687711066218128, 0.9915831181550756046 ) ) ;
#8629=CARTESIAN_POINT ( 'NONE',  ( 0.6008123274975391004, 48.97686038498178362, 3.580739866069544419 ) ) ;
#8630=EDGE_CURVE ( 'NONE', #41667, #24079, #4876, .T. ) ;
#8631=B_SPLINE_CURVE_WITH_KNOTS ( 'NONE', 3,
 ( #34444, #44178, #30336, #6501, #24724, #57905 ),
 .UNSPECIFIED., .F., .F.,
 ( 4, 2, 4 ),
 ( 7.818293051731876896E-19, 0.0002293801035737093178, 0.0004587602071474178225 ),
 .UNSPECIFIED. ) ;
#8633=ORIENTED_EDGE ( 'NONE', *, *, #18367, .F. ) ;
#8634=CARTESIAN_POINT ( 'NONE',  ( 0.5980271706414734822, 10.24496086146951157, -48.03217692119128657 ) ) ;
#8638=CARTESIAN_POINT ( 'NONE',  ( 0.8744876279028263033, -47.25615711918255357, -13.31186180466976587 ) ) ;
#8639=CARTESIAN_POINT ( 'NONE',  ( 4.060580049360325461, 38.53742723504589662, -21.12662766422393190 ) ) ;
#8640=CARTESIAN_POINT ( 'NONE',  ( 0.2940133293162998651, -34.86814990962280802, -27.02688793513072696 ) ) ;
#8644=CARTESIAN_POINT ( 'NONE',  ( 0.1156867017252034141, -44.12399792677806687, -0.1249569240610424042 ) ) ;
#8645=CARTESIAN_POINT ( 'NONE',  ( -6.078457390727109555, 18.62736532255352984, 4.880140589945982654 ) ) ;
#8646=CARTESIAN_POINT ( 'NONE',  ( 0.6000166863083106206, 16.46965316277444913, 46.26633772416363399 ) ) ;
#8651=CARTESIAN_POINT ( 'NONE',  ( 0.9268187852002115479, 43.45361200865025353, 7.452377896370549593 ) ) ;
#8656=CARTESIAN_POINT ( 'NONE',  ( 0.1129192098497455998, 25.64022107388826655, -35.91003830501005467 ) ) ;
#8658=CARTESIAN_POINT ( 'NONE',  ( 0.1155031312995260795, -27.64250437147500250, 34.39234776232634516 ) ) ;
#8666=ORIENTED_EDGE ( 'NONE', *, *, #34595, .F. ) ;
#8670=CARTESIAN_POINT ( 'NONE',  ( 0.5997462898726536595, -48.76843890605300658, -5.761162800241320880 ) ) ;
#8673=FACE_OUTER_BOUND ( 'NONE', #43508, .T. ) ;
#8676=B_SPLINE_CURVE_WITH_KNOTS ( 'NONE', 3,
 ( #6785, #25929, #19695, #24695, #43836, #15312 ),
 .UNSPECIFIED., .F., .F.,
 ( 4, 2, 4 ),
 ( 1.710636569715182240E-17, 0.0002293755540694310746, 0.0004587511081388450729 ),
 .UNSPECIFIED. ) ;
#8678=CARTESIAN_POINT ( 'NONE',  ( 0.2940135542859012019, -40.58327627078308097, 17.29850386075961666 ) ) ;
#8701=CARTESIAN_POINT ( 'NONE',  ( 4.390527457369401532, -33.24441824160808778, -28.72270865370560955 ) ) ;
#8703=CARTESIAN_POINT ( 'NONE',  ( 4.975610109902397937, 30.94437158899635776, -37.88001153774755636 ) ) ;
#8709=B_SPLINE_CURVE_WITH_KNOTS ( 'NONE', 3,
 ( #7996, #36522, #55589, #41531 ),
 .UNSPECIFIED., .F., .F.,
 ( 4, 4 ),
 ( 2.189128766608093164E-17, 0.004559932413162186803 ),
 .UNSPECIFIED. ) ;
#8719=CARTESIAN_POINT ( 'NONE',  ( -6.077587904424778920, -1.855182226446173921, 19.16648951426965652 ) ) ;
#8721=VERTEX_POINT ( 'NONE', #9904 ) ;
#8729=EDGE_CURVE ( 'NONE', #47950, #24982, #28690, .T. ) ;
#8730=ORIENTED_EDGE ( 'NONE', *, *, #44282, .T. ) ;
#8737=CARTESIAN_POINT ( 'NONE',  ( 2.185380717157383579, -28.56354028868287642, -33.51035614916662553 ) ) ;
#8741=CARTESIAN_POINT ( 'NONE',  ( 0.5980271706414711508, 48.33586592461352893, -8.700190122028747197 ) ) ;
#8743=EDGE_LOOP ( 'NONE', ( #38260, #32247, #50095, #31091 ) ) ;
#8748=CARTESIAN_POINT ( 'NONE',  ( 2.185380717157383579, -34.40864559835211622, 27.47480502486236631 ) ) ;
#8752=CARTESIAN_POINT ( 'NONE',  ( -2.739355103387248747, 11.19469682329931892, -9.875542009704030733 ) ) ;
#8756=CARTESIAN_POINT ( 'NONE',  ( 1.112077966505211624, 43.05397124352811744, -9.454410890690590819 ) ) ;
#8758=CARTESIAN_POINT ( 'NONE',  ( 1.657374760986086049, -38.97867883796889288, -20.53175694622165182 ) ) ;
#8759=CARTESIAN_POINT ( 'NONE',  ( 3.727782113643637540, -41.50446234663599654, -14.49680589725369906 ) ) ;
#8761=CARTESIAN_POINT ( 'NONE',  ( 4.975610109902397937, 0.000000000000000000, 0.000000000000000000 ) ) ;
#8762=ORIENTED_EDGE ( 'NONE', *, *, #51146, .F. ) ;
#8772=CARTESIAN_POINT ( 'NONE',  ( 0.6021448801613057400, -49.10674992472959843, -0.2612478842340035801 ) ) ;
#8773=VECTOR ( 'NONE', #37916, 1000.000000000000227 ) ;
#8778=EDGE_LOOP ( 'NONE', ( #51634, #40057, #32805, #57932 ) ) ;
#8781=CARTESIAN_POINT ( 'NONE',  ( 0.7948884756798503259, -42.34838783475078827, -24.84577816043769971 ) ) ;
#8786=ORIENTED_EDGE ( 'NONE', *, *, #12925, .T. ) ;
#8788=CARTESIAN_POINT ( 'NONE',  ( 0.1157506346131639274, 4.144581685519440839, -43.92906899144222876 ) ) ;
#8792=DIRECTION ( 'NONE',  ( 0.000000000000000000, 0.000000000000000000, 1.000000000000000000 ) ) ;
#8793=VECTOR ( 'NONE', #24862, 1000.000000000000227 ) ;
#8797=CARTESIAN_POINT ( 'NONE',  ( 0.1129192098497447394, 10.29049805561828101, 42.90754522869457332 ) ) ;
#8798=ORIENTED_EDGE ( 'NONE', *, *, #12257, .T. ) ;
#8815=B_SPLINE_CURVE_WITH_KNOTS ( 'NONE', 3,
 ( #55248, #40896, #6378, #59027, #2008, #16142 ),
 .UNSPECIFIED., .F., .F.,
 ( 4, 2, 4 ),
 ( 2.611104600503255956E-18, 0.0002447193893791698165, 0.0004894387787583370309 ),
 .UNSPECIFIED. ) ;
#8818=VERTEX_POINT ( 'NONE', #3708 ) ;
#8819=CARTESIAN_POINT ( 'NONE',  ( 4.694002226626921015, -34.48859517587319345, -29.81311077765740691 ) ) ;
#8825=CARTESIAN_POINT ( 'NONE',  ( -6.079354080745853928, 0.6183512803183812689, -19.24605406160677390 ) ) ;
#8826=CARTESIAN_POINT ( 'NONE',  ( 0.6016117650947691020, 28.38024422091337229, 40.07633706073713142 ) ) ;
#8827=CARTESIAN_POINT ( 'NONE',  ( 0.3676999524040323597, 43.96170928169360081, 3.649479463525401535 ) ) ;
#8829=CARTESIAN_POINT ( 'NONE',  ( 0.1147471544378676350, -40.78200343799206706, 16.84578238185594046 ) ) ;
#8840=CARTESIAN_POINT ( 'NONE',  ( 0.1119899015040011353, -41.10694703553422613, 16.03683926496394818 ) ) ;
#8850=CARTESIAN_POINT ( 'NONE',  ( 2.185380717157383135, -21.58356241136808862, 38.37928655800909894 ) ) ;
#8855=EDGE_CURVE ( 'NONE', #53370, #10587, #31155, .T. ) ;
#8858=CARTESIAN_POINT ( 'NONE',  ( 0.7242486021783839378, 5.529549040179291275, -48.78970741648514320 ) ) ;
#8863=CARTESIAN_POINT ( 'NONE',  ( 0.1129192098497447394, -23.28677643606880565, -37.47903188453118162 ) ) ;
#8869=CARTESIAN_POINT ( 'NONE',  ( 4.834790513006555379, 13.88525928490712325, 45.16402235757220041 ) ) ;
#8873=ORIENTED_EDGE ( 'NONE', *, *, #25606, .F. ) ;
#8875=EDGE_LOOP ( 'NONE', ( #2213, #27439, #19781, #12399 ) ) ;
#8886=CARTESIAN_POINT ( 'NONE',  ( 0.6000166863083106206, 40.87138819217342700, 27.22780029589463879 ) ) ;
#8887=CONICAL_SURFACE ( 'NONE', #4838, 43.92652462719577500, 1.486293639869522343 ) ;
#8893=CARTESIAN_POINT ( 'NONE',  ( 0.5997462898726536595, -2.096122762665173944, 49.06279547180476897 ) ) ;
#8897=B_SPLINE_CURVE_WITH_KNOTS ( 'NONE', 3,
 ( #41700, #36386, #17882, #8772, #46095, #56066, #7843, #23187, #42315, #12881, #22267, #42011, #51364, #8448, #2829, #61374 ),
 .UNSPECIFIED., .F., .F.,
 ( 4, 3, 3, 3, 3, 4 ),
 ( 2.081781105835003463E-17, 0.0002612764279487746265, 0.0003919131003184792451, 0.0005225497727000651474, 0.0007837925190632462217, 0.001045051706266716084 ),
 .UNSPECIFIED. ) ;
#8900=CARTESIAN_POINT ( 'NONE',  ( 0.5987334308729317378, 41.48360633127789754, 26.28066422907324906 ) ) ;
#8902=CARTESIAN_POINT ( 'NONE',  ( 3.727782113643637096, -4.897728981986997354, 43.68970160947520753 ) ) ;
#8904=ORIENTED_EDGE ( 'NONE', *, *, #18545, .F. ) ;
#8905=ORIENTED_EDGE ( 'NONE', *, *, #57389, .F. ) ;
#8909=CARTESIAN_POINT ( 'NONE',  ( 0.6021447746440204973, 33.20792045667346315, 36.17699763705849136 ) ) ;
#8913=CARTESIAN_POINT ( 'NONE',  ( 0.5997462898726536595, -42.52950339524503676, 24.55184251941493301 ) ) ;
#8916=DIRECTION ( 'NONE',  ( 0.000000000000000000, 0.000000000000000000, 1.000000000000000000 ) ) ;
#8917=EDGE_CURVE ( 'NONE', #36339, #21667, #6087, .T. ) ;
#8927=CARTESIAN_POINT ( 'NONE',  ( 0.3676999524040366896, -23.56959980820299094, -37.28839696479317212 ) ) ;
#8928=CARTESIAN_POINT ( 'NONE',  ( 0.3676999524040366896, -22.15802448780013378, 38.14410221935873579 ) ) ;
#8931=CARTESIAN_POINT ( 'NONE',  ( 0.6008123274975392114, -2.009114500091637279, 49.06646522915604436 ) ) ;
#8933=ORIENTED_EDGE ( 'NONE', *, *, #24644, .F. ) ;
#8936=CARTESIAN_POINT ( 'NONE',  ( 0.1152339509894530906, -6.821579089989193712, 43.59367785785303084 ) ) ;
#8941=CARTESIAN_POINT ( 'NONE',  ( 0.6021447746440204973, 10.67256517526007187, -47.93367805278783322 ) ) ;
#8942=CARTESIAN_POINT ( 'NONE',  ( -6.077587904424778920, 3.067159685105322442, 19.01022232536997691 ) ) ;
#8948=CARTESIAN_POINT ( 'NONE',  ( 0.8744876279028263033, 23.49358985382666631, -43.10917867646825385 ) ) ;
#8955=CARTESIAN_POINT ( 'NONE',  ( 0.5987334308729319599, -24.93754662327836868, 42.30462947458052270 ) ) ;
#8956=ORIENTED_EDGE ( 'NONE', *, *, #8402, .F. ) ;
#8958=B_SPLINE_CURVE_WITH_KNOTS ( 'NONE', 3,
 ( #26566, #55670, #46618, #3353, #16878, #12801, #59448, #55986, #40698, #36920, #51283, #12484, #45390, #55056, #35994, #3662 ),
 .UNSPECIFIED., .F., .F.,
 ( 4, 3, 3, 3, 3, 4 ),
 ( 2.081781105835003155E-17, 0.0002612764279487750059, 0.0003919131003184806545, 0.0005225497727000651474, 0.0007837925190632466553, 0.001045051706266716084 ),
 .UNSPECIFIED. ) ;
#8964=CARTESIAN_POINT ( 'NONE',  ( 0.8744876279028263033, 23.49358985382666631, -43.10917867646825385 ) ) ;
#8975=CARTESIAN_POINT ( 'NONE',  ( 1.479689385636123067, 43.46015683608160884, 7.266265412912084720 ) ) ;
#8978=CARTESIAN_POINT ( 'NONE',  ( 0.6024113833632039894, -13.76358228951890439, -47.13921585750561150 ) ) ;
#8981=CARTESIAN_POINT ( 'NONE',  ( 0.7044674535453004927, -49.10288787214295070, 0.8420958536080205281 ) ) ;
#8984=CARTESIAN_POINT ( 'NONE',  ( 0.1156495703730067576, 33.50965052305380709, -28.70620621144267304 ) ) ;
#8987=CARTESIAN_POINT ( 'NONE',  ( 0.3676999524040323597, -38.83470403830501994, 20.92406140260764857 ) ) ;
#9001=DIRECTION ( 'NONE',  ( 0.000000000000000000, 0.000000000000000000, -1.000000000000000000 ) ) ;
#9005=CARTESIAN_POINT ( 'NONE',  ( -2.601141883200662974, 13.63649176842536903, 6.069721552019974098 ) ) ;
#9011=CARTESIAN_POINT ( 'NONE',  ( -2.739355103387247858, 14.24824591804153151, -4.453656386614238905 ) ) ;
#9023=VECTOR ( 'NONE', #16272, 1000.000000000000114 ) ;
#9024=CARTESIAN_POINT ( 'NONE',  ( 4.390527457369401532, -25.39775462712438170, 35.84884093703730201 ) ) ;
#9025=ORIENTED_EDGE ( 'NONE', *, *, #22448, .T. ) ;
#9027=CIRCLE ( 'NONE', #50043, 44.12552607296456131 ) ;
#9031=CARTESIAN_POINT ( 'NONE',  ( -6.077587904424778920, -14.65844225831500225, -12.48703695652317158 ) ) ;
#9033=CARTESIAN_POINT ( 'NONE',  ( -6.078726893082806448, 19.09748444646209009, -2.465791776662926260 ) ) ;
#9036=ADVANCED_FACE ( 'NONE', ( #18004 ), #55897, .F. ) ;
#9040=ORIENTED_EDGE ( 'NONE', *, *, #7979, .F. ) ;
#9047=CARTESIAN_POINT ( 'NONE',  ( 1.296416391601052931, -28.33827876547036340, -33.75276774853657002 ) ) ;
#9050=CARTESIAN_POINT ( 'NONE',  ( 0.3676999524040366896, -42.87209381266877983, -10.38913641457107673 ) ) ;
#9052=FACE_OUTER_BOUND ( 'NONE', #54405, .T. ) ;
#9055=EDGE_LOOP ( 'NONE', ( #29051, #3381, #40249, #58939 ) ) ;
#9057=CARTESIAN_POINT ( 'NONE',  ( -6.063463321072278589, -11.00428472829034199, -15.80272666656567182 ) ) ;
#9064=CARTESIAN_POINT ( 'NONE',  ( 4.335381028904201628, -21.75407475222759146, 43.89210725561986948 ) ) ;
#9066=CARTESIAN_POINT ( 'NONE',  ( 2.009741617377216460, -39.02673983696633542, -20.40631410423721448 ) ) ;
#9084=EDGE_LOOP ( 'NONE', ( #51733, #47873, #37640, #53233 ) ) ;
#9085=CARTESIAN_POINT ( 'NONE',  ( 4.553261556744875094, 0.000000000000000000, 0.000000000000000000 ) ) ;
#9087=DIRECTION ( 'NONE',  ( -1.000000000000000000, -0.000000000000000000, -0.000000000000000000 ) ) ;
#9088=FACE_OUTER_BOUND ( 'NONE', #32004, .T. ) ;
#9094=VERTEX_POINT ( 'NONE', #5701 ) ;
#9099=CARTESIAN_POINT ( 'NONE',  ( 4.975610109902397937, 13.36434394399692316, 47.05150069959858428 ) ) ;
#9103=CARTESIAN_POINT ( 'NONE',  ( 0.8753041380234530822, -48.57841546934886168, 7.160717726618431200 ) ) ;
#9112=ADVANCED_FACE ( 'NONE', ( #20454 ), #30284, .F. ) ;
#9118=CARTESIAN_POINT ( 'NONE',  ( -6.077587904424778920, 3.079371755031420133, 19.00824797261034149 ) ) ;
#9119=ORIENTED_EDGE ( 'NONE', *, *, #44109, .F. ) ;
#9120=EDGE_CURVE ( 'NONE', #8619, #2209, #1629, .T. ) ;
#9122=CARTESIAN_POINT ( 'NONE',  ( 0.1147471544378677183, -31.91187174540620930, -30.47268662553386775 ) ) ;
#9128=CARTESIAN_POINT ( 'NONE',  ( 0.6026777506516368677, 46.55057256863531734, -15.63939206521266279 ) ) ;
#9129=ORIENTED_EDGE ( 'NONE', *, *, #2251, .T. ) ;
#9133=CARTESIAN_POINT ( 'NONE',  ( 3.678834586032787790, -3.416869612372130049, 48.85629306118508453 ) ) ;
#9157=CARTESIAN_POINT ( 'NONE',  ( 0.6039202388192952409, -48.72646899558821332, 6.106957677188616707 ) ) ;
#9168=( BOUNDED_SURFACE ( )  B_SPLINE_SURFACE ( 3, 1, ( 
 ( #37787, #4208 ),
 ( #42175, #18354 ),
 ( #37466, #33076 ),
 ( #32759, #56842 ) ),
 .UNSPECIFIED., .F., .F., .F. ) 
 B_SPLINE_SURFACE_WITH_KNOTS ( ( 4, 4 ),
 ( 2, 2 ),
 ( 0.000000000000000000, 1.000000000000000000 ),
 ( 0.000000000000000000, 1.000000000000000000 ),
 .UNSPECIFIED. ) 
 GEOMETRIC_REPRESENTATION_ITEM ( )  RATIONAL_B_SPLINE_SURFACE ( (
 ( 1.000000000000000000, 1.000000000000000000),
 ( 0.9953485035131437453, 0.8621029689291515030),
 ( 0.9953485035131437453, 0.8621029689291515030),
 ( 1.000000000000000000, 1.000000000000000000) ) ) 
 REPRESENTATION_ITEM ( '' )  SURFACE ( )  );
#9173=B_SPLINE_CURVE_WITH_KNOTS ( 'NONE', 3,
 ( #3430, #36072, #45773, #42004, #31971, #55131 ),
 .UNSPECIFIED., .F., .F.,
 ( 4, 2, 4 ),
 ( 1.870625823323990238E-17, 0.0002293755540694308035, 0.0004587511081388429045 ),
 .UNSPECIFIED. ) ;
#9177=ORIENTED_EDGE ( 'NONE', *, *, #52825, .T. ) ;
#9185=ADVANCED_FACE ( 'NONE', ( #26078 ), #54232, .F. ) ;
#9186=ORIENTED_EDGE ( 'NONE', *, *, #52351, .F. ) ;
#9192=CARTESIAN_POINT ( 'NONE',  ( 3.559346040607745287, 34.77628641160756473, 26.90799481492122069 ) ) ;
#9195=EDGE_CURVE ( 'NONE', #6486, #21289, #7814, .T. ) ;
#9207=CARTESIAN_POINT ( 'NONE',  ( 0.5997462898726536595, 49.03735788587799505, 2.624721264559015221 ) ) ;
#9210=CARTESIAN_POINT ( 'NONE',  ( 5.901764892641288895, -44.13851569553263943, -21.20808571358803363 ) ) ;
#9213=CARTESIAN_POINT ( 'NONE',  ( 0.3676999524040323597, 43.13409918076290950, 9.241215893319909114 ) ) ;
#9223=CARTESIAN_POINT ( 'NONE',  ( -2.601141883200662974, -3.815535891688014214, 14.43042318605484198 ) ) ;
#9238=CARTESIAN_POINT ( 'NONE',  ( 0.5987334308729320709, 49.04182532646215265, 2.542100552398203650 ) ) ;
#9241=CARTESIAN_POINT ( 'NONE',  ( 4.975610109902397937, 0.000000000000000000, 0.000000000000000000 ) ) ;
#9244=( BOUNDED_SURFACE ( )  B_SPLINE_SURFACE ( 3, 1, ( 
 ( #54733, #15936 ),
 ( #20327, #2106 ),
 ( #20934, #25941 ),
 ( #49428, #40078 ) ),
 .UNSPECIFIED., .F., .F., .F. ) 
 B_SPLINE_SURFACE_WITH_KNOTS ( ( 4, 4 ),
 ( 2, 2 ),
 ( 0.000000000000000000, 1.000000000000000000 ),
 ( 0.000000000000000000, 1.000000000000000000 ),
 .UNSPECIFIED. ) 
 GEOMETRIC_REPRESENTATION_ITEM ( )  RATIONAL_B_SPLINE_SURFACE ( (
 ( 1.000000000000000000, 1.000000000000000000),
 ( 0.9953485035131437453, 0.8621029689291515030),
 ( 0.9953485035131437453, 0.8621029689291515030),
 ( 1.000000000000000000, 1.000000000000000000) ) ) 
 REPRESENTATION_ITEM ( '' )  SURFACE ( )  );
#9248=CARTESIAN_POINT ( 'NONE',  ( 3.050102900204245682, -40.06446576558427353, 18.17316241319562309 ) ) ;
#9254=B_SPLINE_CURVE_WITH_KNOTS ( 'NONE', 3,
 ( #9592, #47211, #47833, #23704 ),
 .UNSPECIFIED., .F., .F.,
 ( 4, 4 ),
 ( 2.153172013482225773E-17, 0.004559932413162188537 ),
 .UNSPECIFIED. ) ;
#9265=CARTESIAN_POINT ( 'NONE',  ( 3.050102900204245682, 38.81779051020957638, -20.70276283696318131 ) ) ;
#9266=CARTESIAN_POINT ( 'NONE',  ( 1.830465331921977024, -43.82878250349589422, 4.406118489060570020 ) ) ;
#9268=ORIENTED_EDGE ( 'NONE', *, *, #53045, .F. ) ;
#9270=CARTESIAN_POINT ( 'NONE',  ( 0.8753041380234465318, -47.26389509135280775, -13.31399822241900210 ) ) ;
#9271=CARTESIAN_POINT ( 'NONE',  ( -6.078726893082806448, -6.653559303940109082, -18.06998035022927596 ) ) ;
#9273=CARTESIAN_POINT ( 'NONE',  ( 0.6024113833632038784, 4.932097281942475320, -48.85914740867182360 ) ) ;
#9275=CARTESIAN_POINT ( 'NONE',  ( 3.894904216938898323, 43.51529871852972065, 6.208309746889793423 ) ) ;
#9279=B_SPLINE_CURVE_WITH_KNOTS ( 'NONE', 3,
 ( #43735, #52472, #52783, #29595 ),
 .UNSPECIFIED., .F., .F.,
 ( 4, 4 ),
 ( 0.000000000000000000, 0.004442905043737214836 ),
 .UNSPECIFIED. ) ;
#9285=ORIENTED_EDGE ( 'NONE', *, *, #37599, .F. ) ;
#9286=CARTESIAN_POINT ( 'NONE',  ( 0.1368894036331257669, 24.71813664103433794, -36.54962444291990664 ) ) ;
#9287=CARTESIAN_POINT ( 'NONE',  ( 0.1129192098497447394, -43.69739906996321110, 6.122834499276631703 ) ) ;
#9289=CARTESIAN_POINT ( 'NONE',  ( 4.335381028904201628, -36.63547605605852198, 32.52074325427246748 ) ) ;
#9292=ORIENTED_EDGE ( 'NONE', *, *, #50010, .F. ) ;
#9293=CARTESIAN_POINT ( 'NONE',  ( -6.079354080745853928, 5.477739963082026264, -18.46042578449956295 ) ) ;
#9294=CARTESIAN_POINT ( 'NONE',  ( 3.727782113643637096, -15.81964116771539608, 41.01849252752591468 ) ) ;
#9303=B_SPLINE_CURVE_WITH_KNOTS ( 'NONE', 3,
 ( #8205, #4715, #4106, #14474, #28862, #8507 ),
 .UNSPECIFIED., .F., .F.,
 ( 4, 2, 4 ),
 ( 1.734723475976807094E-18, 0.0002447193893791677023, 0.0004894387787583336698 ),
 .UNSPECIFIED. ) ;
#9317=DIRECTION ( 'NONE',  ( 0.000000000000000000, 0.000000000000000000, 1.000000000000000000 ) ) ;
#9319=DIRECTION ( 'NONE',  ( 0.1011922191286468153, -0.6302926308031335800, -0.7697345869474001567 ) ) ;
#9320=( BOUNDED_SURFACE ( )  B_SPLINE_SURFACE ( 3, 1, ( 
 ( #54851, #11044 ),
 ( #11987, #45492 ),
 ( #54531, #21665 ),
 ( #34851, #11658 ) ),
 .UNSPECIFIED., .F., .F., .F. ) 
 B_SPLINE_SURFACE_WITH_KNOTS ( ( 4, 4 ),
 ( 2, 2 ),
 ( 0.000000000000000000, 1.000000000000000000 ),
 ( 0.000000000000000000, 1.000000000000000000 ),
 .UNSPECIFIED. ) 
 GEOMETRIC_REPRESENTATION_ITEM ( )  RATIONAL_B_SPLINE_SURFACE ( (
 ( 1.000000000000000000, 1.000000000000000000),
 ( 0.9953485035131437453, 0.8621029689291515030),
 ( 0.9953485035131437453, 0.8621029689291515030),
 ( 1.000000000000000000, 1.000000000000000000) ) ) 
 REPRESENTATION_ITEM ( '' )  SURFACE ( )  );
#9321=CARTESIAN_POINT ( 'NONE',  ( 0.6016117650947689910, -45.64818567478292977, -18.10508765085221938 ) ) ;
#9322=CARTESIAN_POINT ( 'NONE',  ( -6.057079549204054558, 0.6087215340718761247, 19.24735538181013794 ) ) ;
#9325=CONICAL_SURFACE ( 'NONE', #52336, 43.92652462719577500, 1.486293639869522343 ) ;
#9330=CARTESIAN_POINT ( 'NONE',  ( 3.894904216938898323, -25.63177498392933984, 35.70905268485031314 ) ) ;
#9332=ORIENTED_EDGE ( 'NONE', *, *, #61298, .F. ) ;
#9338=CARTESIAN_POINT ( 'NONE',  ( 4.694002226626921015, -44.81211596887084170, 8.376098963038019818 ) ) ;
#9341=CARTESIAN_POINT ( 'NONE',  ( -6.077587904424778920, 19.09718056542708453, -2.468545289316033120 ) ) ;
#9344=EDGE_LOOP ( 'NONE', ( #50484, #22064, #59969, #542 ) ) ;
#9349=ORIENTED_EDGE ( 'NONE', *, *, #17264, .T. ) ;
#9351=CARTESIAN_POINT ( 'NONE',  ( 0.6016117650947691020, -42.95818748055889102, -23.79380555164838640 ) ) ;
#9355=EDGE_LOOP ( 'NONE', ( #2923, #54842, #10669, #51163 ) ) ;
#9359=CARTESIAN_POINT ( 'NONE',  ( 0.1158816050234198480, -38.44342348468149595, 21.65745211428624017 ) ) ;
#9368=CARTESIAN_POINT ( 'NONE',  ( 0.5997462898726536595, -34.91088276334750873, 34.53667463477217581 ) ) ;
#9376=CARTESIAN_POINT ( 'NONE',  ( 0.1139756605157204450, 20.05585777468466091, -39.30289796715559447 ) ) ;
#9377=CARTESIAN_POINT ( 'NONE',  ( -6.072942160501519915, 9.994728154871237891, 16.45933083084620563 ) ) ;
#9380=FACE_OUTER_BOUND ( 'NONE', #23143, .T. ) ;
#9382=CARTESIAN_POINT ( 'NONE',  ( -6.063463321072276813, 7.809047921946303816, 17.60225051043803290 ) ) ;
#9391=DIRECTION ( 'NONE',  ( 0.09722883295013594329, -0.8021136117729473769, -0.5892031125611201237 ) ) ;
#9395=CARTESIAN_POINT ( 'NONE',  ( 4.975610109902397937, 0.000000000000000000, 0.000000000000000000 ) ) ;
#9406=ORIENTED_EDGE ( 'NONE', *, *, #3803, .T. ) ;
#9423=ORIENTED_EDGE ( 'NONE', *, *, #50453, .F. ) ;
#9433=VERTEX_POINT ( 'NONE', #53266 ) ;
#9435=CARTESIAN_POINT ( 'NONE',  ( -6.078457390727109555, -12.94259897003402493, -14.25775728992403835 ) ) ;
#9436=DIRECTION ( 'NONE',  ( 0.000000000000000000, 0.000000000000000000, 1.000000000000000000 ) ) ;
#9438=VERTEX_POINT ( 'NONE', #45147 ) ;
#9442=B_SPLINE_CURVE_WITH_KNOTS ( 'NONE', 3,
 ( #47358, #56738, #33277, #32340 ),
 .UNSPECIFIED., .F., .F.,
 ( 4, 4 ),
 ( 0.000000000000000000, 0.005013413432710141573 ),
 .UNSPECIFIED. ) ;
#9443=CARTESIAN_POINT ( 'NONE',  ( 0.7044674535453004927, -26.17468433047353216, -41.55344297421058997 ) ) ;
#9450=DIRECTION ( 'NONE',  ( -1.000000000000000000, -0.000000000000000000, -0.000000000000000000 ) ) ;
#9454=CARTESIAN_POINT ( 'NONE',  ( 0.1139756605157202229, 39.92552665614537233, 18.78583351689372805 ) ) ;
#9467=DIRECTION ( 'NONE',  ( -1.000000000000000000, 0.000000000000000000, 0.000000000000000000 ) ) ;
#9471=CARTESIAN_POINT ( 'NONE',  ( 1.296416391601052265, 26.11750747786893001, 35.49905882160285131 ) ) ;
#9482=CARTESIAN_POINT ( 'NONE',  ( 0.6039202388192952409, 44.31978288059539040, -21.14995409607015375 ) ) ;
#9485=CARTESIAN_POINT ( 'NONE',  ( 5.901764892641288895, 19.86141101510633433, 44.76065035194071839 ) ) ;
#9486=CARTESIAN_POINT ( 'NONE',  ( 0.6039202388192953519, -45.58380534490247982, -18.26692100839743205 ) ) ;
#9492=ORIENTED_EDGE ( 'NONE', *, *, #58968, .F. ) ;
#9496=CARTESIAN_POINT ( 'NONE',  ( 0.6028777368367060907, 46.57818122485500822, 15.55676261616270217 ) ) ;
#9501=ORIENTED_EDGE ( 'NONE', *, *, #54923, .T. ) ;
#9504=EDGE_CURVE ( 'NONE', #4300, #6071, #58262, .T. ) ;
#9510=CARTESIAN_POINT ( 'NONE',  ( 4.060580049360325461, -4.720430316018839889, 43.69422424063414212 ) ) ;
#9513=CARTESIAN_POINT ( 'NONE',  ( 2.648799415243696664, -44.91402171431661827, -19.67862080369183531 ) ) ;
#9516=CARTESIAN_POINT ( 'NONE',  ( -6.063463321072276813, 16.77106408806610460, -9.463184550321813049 ) ) ;
#9518=CARTESIAN_POINT ( 'NONE',  ( 0.1139756605157202923, -18.22362019290597601, -40.18525708216549930 ) ) ;
#9525=ORIENTED_EDGE ( 'NONE', *, *, #59237, .T. ) ;
#9527=CARTESIAN_POINT ( 'NONE',  ( 0.6016118706126976079, 40.96538442997461260, 27.08114350038277962 ) ) ;
#9528=EDGE_CURVE ( 'NONE', #33475, #24938, #56404, .T. ) ;
#9530=CARTESIAN_POINT ( 'NONE',  ( 3.894904216938897434, -24.65949896380412198, -36.38727034733911125 ) ) ;
#9532=DIRECTION ( 'NONE',  ( 1.000000000000000000, 0.000000000000000000, 0.000000000000000000 ) ) ;
#9534=CARTESIAN_POINT ( 'NONE',  ( 0.6026777506516368677, 22.55952138954113195, -43.61896818257001485 ) ) ;
#9549=ORIENTED_EDGE ( 'NONE', *, *, #43584, .T. ) ;
#9551=CARTESIAN_POINT ( 'NONE',  ( 0.7948878604505679180, -47.26562360489970871, 13.29133072865033682 ) ) ;
#9555=ADVANCED_FACE ( 'NONE', ( #46367 ), #6651, .F. ) ;
#9559=CONICAL_SURFACE ( 'NONE', #7528, 43.92652462719577500, 1.486293639869522343 ) ;
#9561=VECTOR ( 'NONE', #15395, 1000.000000000000114 ) ;
#9567=CARTESIAN_POINT ( 'NONE',  ( 0.7413678028165009426, 44.05566091053800193, 1.893365655634854372 ) ) ;
#9568=ORIENTED_EDGE ( 'NONE', *, *, #52001, .F. ) ;
#9573=VERTEX_POINT ( 'NONE', #36982 ) ;
#9579=ORIENTED_EDGE ( 'NONE', *, *, #27370, .T. ) ;
#9586=CARTESIAN_POINT ( 'NONE',  ( -6.078726893082806448, 19.25601281685051802, 0.003415553934478593023 ) ) ;
#9587=B_SPLINE_CURVE_WITH_KNOTS ( 'NONE', 3,
 ( #877, #43515, #44748, #10916 ),
 .UNSPECIFIED., .F., .F.,
 ( 4, 4 ),
 ( 0.000000000000000000, 0.004444103432399267896 ),
 .UNSPECIFIED. ) ;
#9592=CARTESIAN_POINT ( 'NONE',  ( 0.3676999524040323597, -42.87209381266892194, 10.38913641457044434 ) ) ;
#9598=CARTESIAN_POINT ( 'NONE',  ( 2.185380717157383135, -16.49852742981111930, 40.82423784610031703 ) ) ;
#9599=EDGE_LOOP ( 'NONE', ( #10284, #54599, #52012, #38499 ) ) ;
#9603=CARTESIAN_POINT ( 'NONE',  ( 3.678748215320120973, 40.00785673245739815, -28.24861437264927133 ) ) ;
#9605=CARTESIAN_POINT ( 'NONE',  ( -2.601141883200665639, -14.85441002404438571, 1.463533500456443592 ) ) ;
#9606=B_SPLINE_CURVE_WITH_KNOTS ( 'NONE', 3,
 ( #30958, #26247, #21561, #59764 ),
 .UNSPECIFIED., .F., .F.,
 ( 4, 4 ),
 ( 2.153172013482225773E-17, 0.004559932413162188537 ),
 .UNSPECIFIED. ) ;
#9608=CARTESIAN_POINT ( 'NONE',  ( 0.1368894036331265163, -40.65507205369316068, 17.14719925329937311 ) ) ;
#9612=EDGE_CURVE ( 'NONE', #10587, #27245, #10829, .T. ) ;
#9613=( BOUNDED_SURFACE ( )  B_SPLINE_SURFACE ( 3, 1, ( 
 ( #18179, #56367 ),
 ( #13483, #19118 ),
 ( #56673, #38230 ),
 ( #57277, #42308 ) ),
 .UNSPECIFIED., .F., .F., .F. ) 
 B_SPLINE_SURFACE_WITH_KNOTS ( ( 4, 4 ),
 ( 2, 2 ),
 ( 0.000000000000000000, 1.000000000000000000 ),
 ( 0.000000000000000000, 1.000000000000000000 ),
 .UNSPECIFIED. ) 
 GEOMETRIC_REPRESENTATION_ITEM ( )  RATIONAL_B_SPLINE_SURFACE ( (
 ( 1.000000000000000000, 1.000000000000000000),
 ( 0.9754377213608244057, 0.9999580625633939235),
 ( 0.9754377213608244057, 0.9999580625633939235),
 ( 1.000000000000000000, 1.000000000000000000) ) ) 
 REPRESENTATION_ITEM ( '' )  SURFACE ( )  );
#9624=ADVANCED_FACE ( 'NONE', ( #3412 ), #27490, .F. ) ;
#9639=ORIENTED_EDGE ( 'NONE', *, *, #13375, .T. ) ;
#9647=AXIS2_PLACEMENT_3D ( 'NONE', #37352, #27626, #46755 ) ;
#9648=DIRECTION ( 'NONE',  ( 0.000000000000000000, 0.000000000000000000, 1.000000000000000000 ) ) ;
#9656=EDGE_CURVE ( 'NONE', #20911, #39074, #33957, .T. ) ;
#9660=CARTESIAN_POINT ( 'NONE',  ( -2.601141883200662974, -11.68881050534889532, 9.282625514337734529 ) ) ;
#9671=ORIENTED_EDGE ( 'NONE', *, *, #59670, .F. ) ;
#9680=CARTESIAN_POINT ( 'NONE',  ( 3.727782113643637540, 42.69290976567378237, -10.49253218465454296 ) ) ;
#9681=CARTESIAN_POINT ( 'NONE',  ( 4.553261556744875094, 0.000000000000000000, 0.000000000000000000 ) ) ;
#9683=CARTESIAN_POINT ( 'NONE',  ( 4.553261556744875094, 0.000000000000000000, 0.000000000000000000 ) ) ;
#9686=CARTESIAN_POINT ( 'NONE',  ( 0.1154773475650541087, 20.24948860305302389, -39.20333967101458938 ) ) ;
#9687=CARTESIAN_POINT ( 'NONE',  ( -6.063463321072276813, -11.02986456480170752, -15.78488327994861962 ) ) ;
#9689=VECTOR ( 'NONE', #2336, 1000.000000000000000 ) ;
#9692=CARTESIAN_POINT ( 'NONE',  ( 0.6000166863083106206, 23.17738933882536401, -43.29702189694988590 ) ) ;
#9694=VECTOR ( 'NONE', #20895, 999.9999999999998863 ) ;
#9699=ORIENTED_EDGE ( 'NONE', *, *, #36793, .F. ) ;
#9700=( BOUNDED_SURFACE ( )  B_SPLINE_SURFACE ( 3, 1, ( 
 ( #18318, #32722 ),
 ( #18618, #17691 ),
 ( #23317, #56500 ),
 ( #13616, #52110 ) ),
 .UNSPECIFIED., .F., .F., .F. ) 
 B_SPLINE_SURFACE_WITH_KNOTS ( ( 4, 4 ),
 ( 2, 2 ),
 ( 0.000000000000000000, 1.000000000000000000 ),
 ( 0.000000000000000000, 1.000000000000000000 ),
 .UNSPECIFIED. ) 
 GEOMETRIC_REPRESENTATION_ITEM ( )  RATIONAL_B_SPLINE_SURFACE ( (
 ( 1.000000000000000000, 1.000000000000000000),
 ( 0.9953485035131437453, 0.8621029689291523912),
 ( 0.9953485035131437453, 0.8621029689291523912),
 ( 1.000000000000000000, 1.000000000000000000) ) ) 
 REPRESENTATION_ITEM ( '' )  SURFACE ( )  );
#9701=B_SPLINE_CURVE_WITH_KNOTS ( 'NONE', 3,
 ( #23323, #47747, #726, #23937 ),
 .UNSPECIFIED., .F., .F.,
 ( 4, 4 ),
 ( 0.000000000000000000, 0.005013413432710151114 ),
 .UNSPECIFIED. ) ;
#9702=CARTESIAN_POINT ( 'NONE',  ( -6.072942160501519027, -12.93525546908854018, -14.26475826077803788 ) ) ;
#9717=ORIENTED_EDGE ( 'NONE', *, *, #54918, .T. ) ;
#9733=B_SPLINE_CURVE_WITH_KNOTS ( 'NONE', 3,
 ( #19146, #39184, #29747, #616 ),
 .UNSPECIFIED., .F., .F.,
 ( 4, 4 ),
 ( 0.000000000000000000, 0.004442905043737214836 ),
 .UNSPECIFIED. ) ;
#9737=ORIENTED_EDGE ( 'NONE', *, *, #28548, .F. ) ;
#9740=VERTEX_POINT ( 'NONE', #20622 ) ;
#9745=CARTESIAN_POINT ( 'NONE',  ( 0.1140933569871964842, 24.93221288801916202, 36.40514675963271429 ) ) ;
#9748=LINE ( 'NONE', #646, #37303 ) ;
#9751=FACE_OUTER_BOUND ( 'NONE', #47596, .T. ) ;
#9752=VERTEX_POINT ( 'NONE', #10928 ) ;
#9759=CARTESIAN_POINT ( 'NONE',  ( 2.359973842542475886, -8.511856589336208145, -43.19356655840164905 ) ) ;
#9765=CARTESIAN_POINT ( 'NONE',  ( 0.3676999524040323597, 14.45783756353398175, 41.67639039443440652 ) ) ;
#9768=B_SPLINE_CURVE_WITH_KNOTS ( 'NONE', 3,
 ( #40195, #8179, #36106, #21988, #59246, #21670 ),
 .UNSPECIFIED., .F., .F.,
 ( 4, 2, 4 ),
 ( 2.032917020132191951E-17, 0.0002293755540694313185, 0.0004587511081388423082 ),
 .UNSPECIFIED. ) ;
#9769=CARTESIAN_POINT ( 'NONE',  ( 0.1135584504625007790, 39.56526998914637261, 19.53308636189390057 ) ) ;
#9771=DIRECTION ( 'NONE',  ( 1.000000000000000000, 0.000000000000000000, 0.000000000000000000 ) ) ;
#9773=CARTESIAN_POINT ( 'NONE',  ( 0.6252788684277226228, -45.77085809703806518, -17.78968465809531807 ) ) ;
#9776=VERTEX_POINT ( 'NONE', #5565 ) ;
#9779=CARTESIAN_POINT ( 'NONE',  ( 0.3676999524040323597, -44.10520818713899871, -0.8253448321555690859 ) ) ;
#9780=CARTESIAN_POINT ( 'NONE',  ( 0.6252788684277188480, -7.158686030355511321, 48.58186436822340681 ) ) ;
#9783=ORIENTED_EDGE ( 'NONE', *, *, #44718, .F. ) ;
#9797=VERTEX_POINT ( 'NONE', #57885 ) ;
#9798=CARTESIAN_POINT ( 'NONE',  ( 0.1365634738349406074, -23.41534997664304285, 37.39764705291722180 ) ) ;
#9806=VERTEX_POINT ( 'NONE', #29699 ) ;
#9812=CARTESIAN_POINT ( 'NONE',  ( 0.6029443199889047422, 46.60567665519338476, 15.47412502747618035 ) ) ;
#9819=CARTESIAN_POINT ( 'NONE',  ( 4.975610109902397937, 34.73360008816180056, -34.43873447229760387 ) ) ;
#9823=CARTESIAN_POINT ( 'NONE',  ( 0.1129192098497447394, 33.28205046155626690, -28.96993104685574139 ) ) ;
#9826=CARTESIAN_POINT ( 'NONE',  ( 0.6029443449137436017, -35.24599845889794381, -34.19443128081963579 ) ) ;
#9829=ORIENTED_EDGE ( 'NONE', *, *, #4629, .F. ) ;
#9830=ORIENTED_EDGE ( 'NONE', *, *, #48672, .F. ) ;
#9834=B_SPLINE_CURVE_WITH_KNOTS ( 'NONE', 3,
 ( #4128, #56452, #23267, #51756 ),
 .UNSPECIFIED., .F., .F.,
 ( 4, 4 ),
 ( 0.000000000000000000, 0.005013413432710142441 ),
 .UNSPECIFIED. ) ;
#9840=CARTESIAN_POINT ( 'NONE',  ( -6.072942160501519915, -14.65319399899862596, 12.49352103759107813 ) ) ;
#9843=EDGE_CURVE ( 'NONE', #47838, #15681, #28673, .T. ) ;
#9851=CARTESIAN_POINT ( 'NONE',  ( 0.1158403557922069033, -35.38432672690284164, 26.36076116631703314 ) ) ;
#9852=CARTESIAN_POINT ( 'NONE',  ( 0.3676999524040323597, -26.85386693986589890, -34.99743438737782242 ) ) ;
#9857=CARTESIAN_POINT ( 'NONE',  ( 0.1129192098497447394, 44.06201484046244587, 2.343210614524684487 ) ) ;
#9858=EDGE_CURVE ( 'NONE', #57398, #23436, #30891, .T. ) ;
#9859=CARTESIAN_POINT ( 'NONE',  ( 0.6016117650947689910, 22.40470300146127514, -43.69874526414702132 ) ) ;
#9863=DIRECTION ( 'NONE',  ( 0.09722883295013594329, -0.1662994675516027976, -0.9812701162958178402 ) ) ;
#9869=CARTESIAN_POINT ( 'NONE',  ( 2.299746137290199943, -48.44936871168312820, 7.545860396635869272 ) ) ;
#9870=EDGE_CURVE ( 'NONE', #19741, #26818, #59747, .T. ) ;
#9883=B_SPLINE_CURVE_WITH_KNOTS ( 'NONE', 3,
 ( #28263, #57985, #52064, #15107, #42392, #18569 ),
 .UNSPECIFIED., .F., .F.,
 ( 4, 2, 4 ),
 ( 0.000000000000000000, 0.0002447195606305764808, 0.0004894391212611529617 ),
 .UNSPECIFIED. ) ;
#9887=ORIENTED_EDGE ( 'NONE', *, *, #11183, .T. ) ;
#9889=CARTESIAN_POINT ( 'NONE',  ( 4.335381028904201628, -48.26758661664241856, -8.366416787924562115 ) ) ;
#9892=CARTESIAN_POINT ( 'NONE',  ( 0.1139756605157205421, 41.74945270199659575, -14.28070092043005701 ) ) ;
#9894=CARTESIAN_POINT ( 'NONE',  ( 4.975610109902397937, -40.67634447773578898, -27.16402781375298403 ) ) ;
#9897=ORIENTED_EDGE ( 'NONE', *, *, #19326, .T. ) ;
#9904=CARTESIAN_POINT ( 'NONE',  ( 4.975610109902397937, -46.59897809419055648, 14.86555238512586463 ) ) ;
#9911=EDGE_CURVE ( 'NONE', #14140, #14065, #52633, .T. ) ;
#9917=B_SPLINE_CURVE_WITH_KNOTS ( 'NONE', 3,
 ( #60608, #17727, #36854, #31829 ),
 .UNSPECIFIED., .F., .F.,
 ( 4, 4 ),
 ( 0.000000000000000000, 0.004444103432399269631 ),
 .UNSPECIFIED. ) ;
#9922=EDGE_CURVE ( 'NONE', #29558, #51387, #9254, .T. ) ;
#9924=( BOUNDED_SURFACE ( )  B_SPLINE_SURFACE ( 3, 1, ( 
 ( #46446, #47356 ),
 ( #46142, #12935 ),
 ( #52037, #4400 ),
 ( #41753, #46756 ) ),
 .UNSPECIFIED., .F., .F., .F. ) 
 B_SPLINE_SURFACE_WITH_KNOTS ( ( 4, 4 ),
 ( 2, 2 ),
 ( 0.000000000000000000, 1.000000000000000000 ),
 ( 0.000000000000000000, 1.000000000000000000 ),
 .UNSPECIFIED. ) 
 GEOMETRIC_REPRESENTATION_ITEM ( )  RATIONAL_B_SPLINE_SURFACE ( (
 ( 1.000000000000000000, 1.000000000000000000),
 ( 0.9754377213608244057, 0.9999580625633939235),
 ( 0.9754377213608244057, 0.9999580625633939235),
 ( 1.000000000000000000, 1.000000000000000000) ) ) 
 REPRESENTATION_ITEM ( '' )  SURFACE ( )  );
#9926=ORIENTED_EDGE ( 'NONE', *, *, #41681, .T. ) ;
#9939=CARTESIAN_POINT ( 'NONE',  ( 0.1129192098497447394, 3.754263797494919341, -43.96427289429421137 ) ) ;
#9954=EDGE_CURVE ( 'NONE', #61199, #14671, #27244, .T. ) ;
#9958=DIRECTION ( 'NONE',  ( 0.09722883295013595717, -0.9607671998409456071, -0.2597555422949489046 ) ) ;
#9959=ORIENTED_EDGE ( 'NONE', *, *, #44454, .F. ) ;
#9973=CARTESIAN_POINT ( 'NONE',  ( 0.6253024248130470975, 22.10248858687955931, 43.85115991264656543 ) ) ;
#9977=EDGE_CURVE ( 'NONE', #55549, #12205, #23094, .T. ) ;
#9986=B_SPLINE_CURVE_WITH_KNOTS ( 'NONE', 3,
 ( #60800, #51092, #16676, #49878 ),
 .UNSPECIFIED., .F., .F.,
 ( 4, 4 ),
 ( 2.271992152883876391E-17, 0.004559932413162184200 ),
 .UNSPECIFIED. ) ;
#9988=CIRCLE ( 'NONE', #8006, 43.92652462719577500 ) ;
#9991=DIRECTION ( 'NONE',  ( 0.000000000000000000, 0.000000000000000000, 1.000000000000000000 ) ) ;
#9995=VERTEX_POINT ( 'NONE', #56276 ) ;
#9997=( BOUNDED_SURFACE ( )  B_SPLINE_SURFACE ( 3, 1, ( 
 ( #5528, #10888 ),
 ( #529, #58456 ),
 ( #61923, #48774 ),
 ( #6140, #38474 ) ),
 .UNSPECIFIED., .F., .F., .F. ) 
 B_SPLINE_SURFACE_WITH_KNOTS ( ( 4, 4 ),
 ( 2, 2 ),
 ( 0.000000000000000000, 1.000000000000000000 ),
 ( 0.000000000000000000, 1.000000000000000000 ),
 .UNSPECIFIED. ) 
 GEOMETRIC_REPRESENTATION_ITEM ( )  RATIONAL_B_SPLINE_SURFACE ( (
 ( 1.000000000000000000, 1.000000000000000000),
 ( 0.9953485035131437453, 0.8621029689291523912),
 ( 0.9953485035131437453, 0.8621029689291523912),
 ( 1.000000000000000000, 1.000000000000000000) ) ) 
 REPRESENTATION_ITEM ( '' )  SURFACE ( )  );
#9998=DIRECTION ( 'NONE',  ( 0.000000000000000000, 0.000000000000000000, -1.000000000000000000 ) ) ;
#10000=LINE ( 'NONE', #38516, #61550 ) ;
#10002=ORIENTED_EDGE ( 'NONE', *, *, #25992, .T. ) ;
#10006=CARTESIAN_POINT ( 'NONE',  ( 0.8753041380234524160, -47.26389509135299249, 13.31399822241830755 ) ) ;
#10018=CARTESIAN_POINT ( 'NONE',  ( 0.3676999524040323597, -22.15802448779959377, -38.14410221935904843 ) ) ;
#10026=CARTESIAN_POINT ( 'NONE',  ( 0.6026112563231247332, -47.45690295771330369, -12.62471213796142422 ) ) ;
#10029=VERTEX_POINT ( 'NONE', #14629 ) ;
#10036=VERTEX_POINT ( 'NONE', #23396 ) ;
#10041=CARTESIAN_POINT ( 'NONE',  ( 0.1158403557922069033, 29.69272295667737893, -32.63866588268925284 ) ) ;
#10043=ORIENTED_EDGE ( 'NONE', *, *, #25894, .F. ) ;
#10044=CARTESIAN_POINT ( 'NONE',  ( 0.6252788684277206244, 4.031327004993904950, -48.94070630622808693 ) ) ;
#10051=VECTOR ( 'NONE', #17047, 1000.000000000000114 ) ;
#10055=CARTESIAN_POINT ( 'NONE',  ( 0.1158816050234199035, -22.87849723619521214, -37.72951637005925107 ) ) ;
#10057=EDGE_CURVE ( 'NONE', #55165, #22556, #21256, .T. ) ;
#10062=ORIENTED_EDGE ( 'NONE', *, *, #30145, .F. ) ;
#10063=AXIS2_PLACEMENT_3D ( 'NONE', #46224, #23631, #8916 ) ;
#10066=VERTEX_POINT ( 'NONE', #10847 ) ;
#10068=CARTESIAN_POINT ( 'NONE',  ( -6.078075953587585900, -12.94192373113783390, -14.25839347137493363 ) ) ;
#10071=( BOUNDED_SURFACE ( )  B_SPLINE_SURFACE ( 3, 1, ( 
 ( #60543, #7610 ),
 ( #17972, #42103 ),
 ( #45875, #61159 ),
 ( #8540, #60855 ) ),
 .UNSPECIFIED., .F., .F., .F. ) 
 B_SPLINE_SURFACE_WITH_KNOTS ( ( 4, 4 ),
 ( 2, 2 ),
 ( 0.000000000000000000, 1.000000000000000000 ),
 ( 0.000000000000000000, 1.000000000000000000 ),
 .UNSPECIFIED. ) 
 GEOMETRIC_REPRESENTATION_ITEM ( )  RATIONAL_B_SPLINE_SURFACE ( (
 ( 1.000000000000000000, 1.000000000000000000),
 ( 0.9953485035131437453, 0.8621029689291515030),
 ( 0.9953485035131437453, 0.8621029689291515030),
 ( 1.000000000000000000, 1.000000000000000000) ) ) 
 REPRESENTATION_ITEM ( '' )  SURFACE ( )  );
#10073=ORIENTED_EDGE ( 'NONE', *, *, #51684, .T. ) ;
#10078=CARTESIAN_POINT ( 'NONE',  ( 0.6039202388192952409, -39.25113122883236372, -29.51122515426921211 ) ) ;
#10079=CARTESIAN_POINT ( 'NONE',  ( 3.390910168358336474, -8.956706784861477644, -43.05664339104539096 ) ) ;
#10083=CARTESIAN_POINT ( 'NONE',  ( 1.830465331921979022, 14.04846951621181894, 41.74944981829649038 ) ) ;
#10089=LINE ( 'NONE', #40394, #37799 ) ;
#10095=CARTESIAN_POINT ( 'NONE',  ( 2.533389852662419894, 18.94327543464629571, -39.73163534943841313 ) ) ;
#10106=ORIENTED_EDGE ( 'NONE', *, *, #57624, .T. ) ;
#10109=ORIENTED_EDGE ( 'NONE', *, *, #8240, .F. ) ;
#10110=CARTESIAN_POINT ( 'NONE',  ( 4.975610109902397937, 24.86209007718959185, 42.12274782266089801 ) ) ;
#10111=CARTESIAN_POINT ( 'NONE',  ( 0.2279481005628809787, -11.82334179845439515, -42.50543583813526283 ) ) ;
#10112=B_SPLINE_CURVE_WITH_KNOTS ( 'NONE', 3,
 ( #44541, #29169, #24785, #29788 ),
 .UNSPECIFIED., .F., .F.,
 ( 4, 4 ),
 ( 0.000000000000000000, 0.005013413432710140706 ),
 .UNSPECIFIED. ) ;
#10118=ORIENTED_EDGE ( 'NONE', *, *, #43988, .F. ) ;
#10119=EDGE_CURVE ( 'NONE', #40756, #33475, #53421, .T. ) ;
#10120=ORIENTED_EDGE ( 'NONE', *, *, #38954, .F. ) ;
#10128=CARTESIAN_POINT ( 'NONE',  ( 0.6039202388192952409, -19.71856863334322796, -44.97490148850938141 ) ) ;
#10134=FACE_OUTER_BOUND ( 'NONE', #45353, .T. ) ;
#10135=CARTESIAN_POINT ( 'NONE',  ( 0.6016118706126976079, -13.63816021288923608, -47.17575267859004384 ) ) ;
#10136=CARTESIAN_POINT ( 'NONE',  ( 0.8753041380234524160, -31.30612550145381334, -37.82941757363181523 ) ) ;
#10138=ORIENTED_EDGE ( 'NONE', *, *, #39716, .T. ) ;
#10147=VECTOR ( 'NONE', #28351, 1000.000000000000000 ) ;
#10150=CARTESIAN_POINT ( 'NONE',  ( -6.078075953587585900, -6.655346486686200436, -18.06935354099004698 ) ) ;
#10161=CARTESIAN_POINT ( 'NONE',  ( 0.6029443199889047422, 33.01493686021951390, -36.35315097718657285 ) ) ;
#10165=CARTESIAN_POINT ( 'NONE',  ( 0.5987334363312689645, 48.31411593427914397, -8.792559807081808287 ) ) ;
#10167=B_SPLINE_CURVE_WITH_KNOTS ( 'NONE', 3,
 ( #56203, #51497, #59664, #27093, #55896, #3571 ),
 .UNSPECIFIED., .F., .F.,
 ( 4, 2, 4 ),
 ( 4.878909776184769953E-19, 0.0002293801035737080981, 0.0004587602071474157083 ),
 .UNSPECIFIED. ) ;
#10168=CARTESIAN_POINT ( 'NONE',  ( 4.553261556744873317, -36.93702150832076825, -23.77385134801438937 ) ) ;
#10175=CARTESIAN_POINT ( 'NONE',  ( 0.1149546198390368201, 41.78922939623867450, 14.16357551932990155 ) ) ;
#10177=EDGE_LOOP ( 'NONE', ( #23582, #45017, #50603, #37230 ) ) ;
#10180=CARTESIAN_POINT ( 'NONE',  ( 4.553261556744873317, -43.15908619232978083, -8.175135770535248980 ) ) ;
#10190=CIRCLE ( 'NONE', #30161, 43.92652462719577500 ) ;
#10191=CARTESIAN_POINT ( 'NONE',  ( 0.8744876279028263033, -42.33402326122615733, -24.86323641237110493 ) ) ;
#10201=CARTESIAN_POINT ( 'NONE',  ( -6.063463321072278589, 17.84349906452534640, 7.240855861965011186 ) ) ;
#10205=ORIENTED_EDGE ( 'NONE', *, *, #57903, .T. ) ;
#10208=ADVANCED_FACE ( 'NONE', ( #32658 ), #41856, .F. ) ;
#10217=ORIENTED_EDGE ( 'NONE', *, *, #52003, .F. ) ;
#10223=CARTESIAN_POINT ( 'NONE',  ( 0.3676999524040323597, -28.14442808720941969, 33.96824621564581292 ) ) ;
#10226=CARTESIAN_POINT ( 'NONE',  ( 0.1365634738349406074, -7.669977273387969419, 43.45151399259823677 ) ) ;
#10231=CARTESIAN_POINT ( 'NONE',  ( 4.553261556744875094, -14.95853073564453339, -41.30111286702108941 ) ) ;
#10235=CARTESIAN_POINT ( 'NONE',  ( 0.6021447746440204973, 22.94538958722560906, 43.41716522043932969 ) ) ;
#10238=AXIS2_PLACEMENT_3D ( 'NONE', #44179, #43866, #48837 ) ;
#10239=CARTESIAN_POINT ( 'NONE',  ( 4.975610109902397937, -23.13264022976583334, 43.09675583078141869 ) ) ;
#10243=VECTOR ( 'NONE', #17454, 1000.000000000000000 ) ;
#10258=VERTEX_POINT ( 'NONE', #12945 ) ;
#10259=CARTESIAN_POINT ( 'NONE',  ( 4.553261556744875094, -33.30082861731464305, -28.64601855797546648 ) ) ;
#10260=EDGE_CURVE ( 'NONE', #45251, #59386, #39917, .T. ) ;
#10270=ADVANCED_FACE ( 'NONE', ( #40607 ), #45146, .F. ) ;
#10271=FACE_OUTER_BOUND ( 'NONE', #25820, .T. ) ;
#10273=ADVANCED_FACE ( 'NONE', ( #49658 ), #58261, .F. ) ;
#10279=CARTESIAN_POINT ( 'NONE',  ( 0.5997462898726536595, 28.52220283460625438, 39.97543715340569292 ) ) ;
#10284=ORIENTED_EDGE ( 'NONE', *, *, #40341, .F. ) ;
#10288=ORIENTED_EDGE ( 'NONE', *, *, #57389, .T. ) ;
#10290=CARTESIAN_POINT ( 'NONE',  ( 0.6029443199889047422, -30.61798795696924813, -38.39370332907843419 ) ) ;
#10291=CARTESIAN_POINT ( 'NONE',  ( 0.5997462898726536595, -35.63787911784747564, -33.78599121124021565 ) ) ;
#10292=ORIENTED_EDGE ( 'NONE', *, *, #46186, .F. ) ;
#10294=CARTESIAN_POINT ( 'NONE',  ( 0.1119898979215349782, -38.16786793124121147, 22.13989986054947323 ) ) ;
#10295=CARTESIAN_POINT ( 'NONE',  ( 0.1149546198390367646, -38.57991944330028389, 21.41346260583937067 ) ) ;
#10297=ORIENTED_EDGE ( 'NONE', *, *, #33638, .F. ) ;
#10300=FACE_OUTER_BOUND ( 'NONE', #59110, .T. ) ;
#10312=CARTESIAN_POINT ( 'NONE',  ( 0.1157506346131639274, -42.65743773788693716, 11.28200626844061638 ) ) ;
#10313=CARTESIAN_POINT ( 'NONE',  ( 0.1119899015040012186, -32.08462141187705186, 30.29089594331977153 ) ) ;
#10316=CARTESIAN_POINT ( 'NONE',  ( 0.6026777506516367566, 37.27955795947347895, -31.96530852320179150 ) ) ;
#10329=EDGE_CURVE ( 'NONE', #5538, #28574, #33897, .T. ) ;
#10332=CARTESIAN_POINT ( 'NONE',  ( 5.901764892641307547, 35.14701960959006755, 34.09807149976035134 ) ) ;
#10335=ADVANCED_FACE ( 'NONE', ( #37998 ), #2278, .F. ) ;
#10348=ORIENTED_EDGE ( 'NONE', *, *, #54801, .T. ) ;
#10351=CARTESIAN_POINT ( 'NONE',  ( 0.1147471544378677460, 29.43420442011967353, -32.87217362189262815 ) ) ;
#10366=CARTESIAN_POINT ( 'NONE',  ( 2.533389852662419894, -36.19900187127336011, -25.04162125856002774 ) ) ;
#10368=CARTESIAN_POINT ( 'NONE',  ( 0.3676999524040323597, -6.224421213753346116, -43.67158302462387098 ) ) ;
#10369=ORIENTED_EDGE ( 'NONE', *, *, #36670, .T. ) ;
#10371=CARTESIAN_POINT ( 'NONE',  ( 0.1154773475650540948, -17.69611726026696985, 40.42018139440992996 ) ) ;
#10372=VERTEX_POINT ( 'NONE', #57970 ) ;
#10383=DIRECTION ( 'NONE',  ( -1.000000000000000000, -0.000000000000000000, -0.000000000000000000 ) ) ;
#10386=VERTEX_POINT ( 'NONE', #37680 ) ;
#10387=CARTESIAN_POINT ( 'NONE',  ( 0.1145239942831223490, -41.02090207429923652, 16.25518605600765909 ) ) ;
#10394=CARTESIAN_POINT ( 'NONE',  ( 0.5997462898726536595, -47.36625756029543055, 12.96106765957438789 ) ) ;
#10398=CARTESIAN_POINT ( 'NONE',  ( 0.1158816050234199174, -43.76263342502616638, -5.636839274978773240 ) ) ;
#10404=CARTESIAN_POINT ( 'NONE',  ( 0.5997462898726536595, -45.31995669577361951, 18.91172004968117903 ) ) ;
#10406=DIRECTION ( 'NONE',  ( 0.09722883295013597105, -0.6264263058867871603, 0.7733929385093892828 ) ) ;
#10410=ORIENTED_EDGE ( 'NONE', *, *, #53238, .F. ) ;
#10412=CARTESIAN_POINT ( 'NONE',  ( 0.9268187852002115479, 26.03038468280454865, 35.58333045365259295 ) ) ;
#10416=CARTESIAN_POINT ( 'NONE',  ( 0.1129192098497455998, -43.82135468580280957, 5.161459220629533107 ) ) ;
#10422=CARTESIAN_POINT ( 'NONE',  ( -6.078457390727109555, 7.790511441124012393, 17.60972579352738521 ) ) ;
#10425=CARTESIAN_POINT ( 'NONE',  ( 3.240649175237395596, -43.95364737320741710, -1.828059077105528951 ) ) ;
#10430=CARTESIAN_POINT ( 'NONE',  ( 0.8753041380234465318, 27.35839019124359339, 40.77568900725830758 ) ) ;
#10434=CARTESIAN_POINT ( 'NONE',  ( 0.1147471544378677183, 43.25016557451949240, -8.739300100688538464 ) ) ;
#10439=ORIENTED_EDGE ( 'NONE', *, *, #9858, .T. ) ;
#10440=CARTESIAN_POINT ( 'NONE',  ( 0.1155031312995260795, -1.245823167979823065, -44.10657045345890026 ) ) ;
#10442=CARTESIAN_POINT ( 'NONE',  ( 5.901764892641288895, -10.85461099010664654, 47.75111399426337044 ) ) ;
#10446=CARTESIAN_POINT ( 'NONE',  ( 0.1129192098497455998, -38.20615368646939203, -22.07354996984027196 ) ) ;
#10447=CARTESIAN_POINT ( 'NONE',  ( 0.6016117650947689910, -14.30605072330158833, -46.97752619015630415 ) ) ;
#10455=LINE ( 'NONE', #10771, #8793 ) ;
#10458=CARTESIAN_POINT ( 'NONE',  ( 0.1140933569871965259, -31.95931914376139105, 30.42288398477553812 ) ) ;
#10464=ORIENTED_EDGE ( 'NONE', *, *, #32109, .F. ) ;
#10467=CARTESIAN_POINT ( 'NONE',  ( 4.335381028904216727, -43.68634339260488275, -22.16439145674328159 ) ) ;
#10468=CARTESIAN_POINT ( 'NONE',  ( 3.678748215320120529, -47.80914536661616410, -10.62536745779876313 ) ) ;
#10470=CARTESIAN_POINT ( 'NONE',  ( -6.078726893082806448, 7.791390017580341443, -17.60932374802251132 ) ) ;
#10472=DIRECTION ( 'NONE',  ( 0.1011922191286468292, 0.8407325376063271571, 0.5319106456895233981 ) ) ;
#10492=FACE_OUTER_BOUND ( 'NONE', #46819, .T. ) ;
#10494=CARTESIAN_POINT ( 'NONE',  ( 0.5997462898726536595, -1.051648045107538954, 49.09628974305014992 ) ) ;
#10495=CARTESIAN_POINT ( 'NONE',  ( 0.6253024248130483187, 36.94306049113323809, 32.35204025971334119 ) ) ;
#10496=ADVANCED_FACE ( 'NONE', ( #11015 ), #15115, .F. ) ;
#10498=CARTESIAN_POINT ( 'NONE',  ( -6.078726893082806448, -16.14009859332552921, 10.50196451462540992 ) ) ;
#10503=CARTESIAN_POINT ( 'NONE',  ( 0.1129192098497455998, 43.40062318508800843, -7.958498283668546947 ) ) ;
#10504=CARTESIAN_POINT ( 'NONE',  ( -6.063463321072276813, 19.10058954492596328, 2.447025033736856425 ) ) ;
#10505=VECTOR ( 'NONE', #12494, 1000.000000000000000 ) ;
#10508=CARTESIAN_POINT ( 'NONE',  ( 2.648799415243708655, -45.95403142182570377, -17.10977671892458929 ) ) ;
#10510=DIRECTION ( 'NONE',  ( 1.000000000000000000, 0.000000000000000000, 0.000000000000000000 ) ) ;
#10533=ORIENTED_EDGE ( 'NONE', *, *, #60624, .F. ) ;
#10538=ORIENTED_EDGE ( 'NONE', *, *, #42818, .T. ) ;
#10545=CARTESIAN_POINT ( 'NONE',  ( 0.6016118706126977189, -20.19594048258466756, 44.76242891988579942 ) ) ;
#10554=VERTEX_POINT ( 'NONE', #40775 ) ;
#10564=B_SPLINE_CURVE_WITH_KNOTS ( 'NONE', 3,
 ( #10981, #15372, #10044, #5311, #10665, #38883 ),
 .UNSPECIFIED., .F., .F.,
 ( 4, 2, 4 ),
 ( 0.000000000000000000, 0.0002447195606305751256, 0.0004894391212611502512 ),
 .UNSPECIFIED. ) ;
#10573=EDGE_CURVE ( 'NONE', #7870, #47838, #53781, .T. ) ;
#10576=B_SPLINE_CURVE_WITH_KNOTS ( 'NONE', 3,
 ( #47096, #13895, #12975, #27051, #46480, #55534 ),
 .UNSPECIFIED., .F., .F.,
 ( 4, 2, 4 ),
 ( 0.000000000000000000, 0.0002447195606305753966, 0.0004894391212611507933 ),
 .UNSPECIFIED. ) ;
#10581=CARTESIAN_POINT ( 'NONE',  ( -6.072942160501519915, -1.863502906426155015, -19.16589468839797306 ) ) ;
#10585=CARTESIAN_POINT ( 'NONE',  ( 0.8744876279028263033, 21.91587810745035725, 43.93226988398016886 ) ) ;
#10587=VERTEX_POINT ( 'NONE', #16955 ) ;
#10597=CARTESIAN_POINT ( 'NONE',  ( 0.1368894036331262665, 36.62752315710398676, -24.60255826736611340 ) ) ;
#10601=CARTESIAN_POINT ( 'NONE',  ( 0.8753041380234465318, -42.34096624980154644, -24.86726573039640087 ) ) ;
#10606=CARTESIAN_POINT ( 'NONE',  ( -2.601141883200665639, -6.448885681770727629, 13.46132612088575442 ) ) ;
#10609=EDGE_CURVE ( 'NONE', #12769, #17976, #45771, .T. ) ;
#10613=CARTESIAN_POINT ( 'NONE',  ( 2.114184763582917181, 7.651710973661706259E-12, 44.03514965515166324 ) ) ;
#10615=FACE_OUTER_BOUND ( 'NONE', #16521, .T. ) ;
#10623=CARTESIAN_POINT ( 'NONE',  ( 4.975610109902397937, 48.43414999183897862, -6.825138951392602849 ) ) ;
#10628=CARTESIAN_POINT ( 'NONE',  ( 0.1135584504625008068, 20.79117989877105899, -38.91887576166853080 ) ) ;
#10630=EDGE_CURVE ( 'NONE', #54620, #57409, #34559, .T. ) ;
#10634=CARTESIAN_POINT ( 'NONE',  ( 2.299746137290199499, 3.424328853209327672, -48.91375378757203407 ) ) ;
#10644=CARTESIAN_POINT ( 'NONE',  ( 0.5997462898726536595, 22.24958391914565681, -43.77793560195825506 ) ) ;
#10654=EDGE_CURVE ( 'NONE', #35248, #31520, #42306, .T. ) ;
#10663=CARTESIAN_POINT ( 'NONE',  ( 4.975610109902397937, -48.84566763821283786, 2.559328059280373768 ) ) ;
#10664=ORIENTED_EDGE ( 'NONE', *, *, #60018, .F. ) ;
#10665=CARTESIAN_POINT ( 'NONE',  ( 0.7948878604505665857, 3.850400492704748601, -48.94765636212009952 ) ) ;
#10668=FACE_OUTER_BOUND ( 'NONE', #59726, .T. ) ;
#10669=ORIENTED_EDGE ( 'NONE', *, *, #21633, .F. ) ;
#10672=CARTESIAN_POINT ( 'NONE',  ( -6.063463321072276813, 13.84388120595868799, 13.38534294049927631 ) ) ;
#10686=CARTESIAN_POINT ( 'NONE',  ( -6.078726893082806448, 5.475592473157355755, 18.46109228449450512 ) ) ;
#10689=CIRCLE ( 'NONE', #43708, 48.91267123290010943 ) ;
#10690=EDGE_CURVE ( 'NONE', #855, #21977, #31867, .T. ) ;
#10694=CARTESIAN_POINT ( 'NONE',  ( 0.1156867017252034419, -40.94616529006326999, 16.44245587842656064 ) ) ;
#10709=VECTOR ( 'NONE', #37218, 1000.000000000000227 ) ;
#10717=CARTESIAN_POINT ( 'NONE',  ( 0.8744876279028263033, -43.20725972823498040, 23.31271664041618052 ) ) ;
#10718=CARTESIAN_POINT ( 'NONE',  ( 1.479689385636123067, 19.33154860216732018, -39.59640228492652625 ) ) ;
#10721=CARTESIAN_POINT ( 'NONE',  ( 0.7948884756798504370, -14.79943981595577185, 46.81533109713159035 ) ) ;
#10723=( BOUNDED_SURFACE ( )  B_SPLINE_SURFACE ( 3, 1, ( 
 ( #36180, #55245 ),
 ( #31458, #7634 ),
 ( #22069, #37734 ),
 ( #384, #47726 ) ),
 .UNSPECIFIED., .F., .F., .F. ) 
 B_SPLINE_SURFACE_WITH_KNOTS ( ( 4, 4 ),
 ( 2, 2 ),
 ( 0.000000000000000000, 1.000000000000000000 ),
 ( 0.000000000000000000, 1.000000000000000000 ),
 .UNSPECIFIED. ) 
 GEOMETRIC_REPRESENTATION_ITEM ( )  RATIONAL_B_SPLINE_SURFACE ( (
 ( 1.000000000000000000, 1.000000000000000000),
 ( 0.9953485035131437453, 0.8621029689291523912),
 ( 0.9953485035131437453, 0.8621029689291523912),
 ( 1.000000000000000000, 1.000000000000000000) ) ) 
 REPRESENTATION_ITEM ( '' )  SURFACE ( )  );
#10736=ORIENTED_EDGE ( 'NONE', *, *, #25764, .T. ) ;
#10742=EDGE_LOOP ( 'NONE', ( #37385, #58414, #55327, #45865 ) ) ;
#10752=CARTESIAN_POINT ( 'NONE',  ( 0.5980271706414711508, -45.78139539622871013, 17.77956912908273068 ) ) ;
#10754=CARTESIAN_POINT ( 'NONE',  ( -2.601141883200662974, -13.99736252863761798, -5.183557630747456457 ) ) ;
#10756=CARTESIAN_POINT ( 'NONE',  ( 0.6039202388192953519, -25.60584472520843491, -41.90351332236362936 ) ) ;
#10760=EDGE_CURVE ( 'NONE', #16502, #22341, #13796, .T. ) ;
#10761=CARTESIAN_POINT ( 'NONE',  ( -6.063463321072278589, 11.99415941893228421, 15.06521132652004979 ) ) ;
#10762=CARTESIAN_POINT ( 'NONE',  ( 0.6027444965799114707, -35.18529211318709571, -34.25687864936231364 ) ) ;
#10763=CONICAL_SURFACE ( 'NONE', #38913, 43.92652462719577500, 1.486293639869522343 ) ;
#10766=ORIENTED_EDGE ( 'NONE', *, *, #49050, .F. ) ;
#10771=CARTESIAN_POINT ( 'NONE',  ( -2.601141883200662974, -0.03040527887401129128, 14.92630238834806811 ) ) ;
#10773=CARTESIAN_POINT ( 'NONE',  ( 0.1129192098497455998, -32.03190746135001632, 30.34647742609778831 ) ) ;
#10781=CARTESIAN_POINT ( 'NONE',  ( 0.1157991065609916270, -6.961833292486440783, -43.57149575978917966 ) ) ;
#10783=CARTESIAN_POINT ( 'NONE',  ( 0.1156495703730067715, -35.28001429893448915, 26.50025555156116397 ) ) ;
#10787=CARTESIAN_POINT ( 'NONE',  ( 0.6029443449137436017, 33.04717288230519046, -36.32387510261487762 ) ) ;
#10798=LINE ( 'NONE', #49000, #53736 ) ;
#10801=FACE_OUTER_BOUND ( 'NONE', #28315, .T. ) ;
#10805=EDGE_LOOP ( 'NONE', ( #29708, #60667, #637, #27147 ) ) ;
#10806=ORIENTED_EDGE ( 'NONE', *, *, #56988, .T. ) ;
#10810=( BOUNDED_SURFACE ( )  B_SPLINE_SURFACE ( 3, 1, ( 
 ( #16669, #7873 ),
 ( #7550, #60181 ),
 ( #32007, #27293 ),
 ( #40496, #17291 ) ),
 .UNSPECIFIED., .F., .F., .F. ) 
 B_SPLINE_SURFACE_WITH_KNOTS ( ( 4, 4 ),
 ( 2, 2 ),
 ( 0.000000000000000000, 1.000000000000000000 ),
 ( 0.000000000000000000, 1.000000000000000000 ),
 .UNSPECIFIED. ) 
 GEOMETRIC_REPRESENTATION_ITEM ( )  RATIONAL_B_SPLINE_SURFACE ( (
 ( 1.000000000000000000, 1.000000000000000000),
 ( 0.9953485035131437453, 0.8621029689291523912),
 ( 0.9953485035131437453, 0.8621029689291523912),
 ( 1.000000000000000000, 1.000000000000000000) ) ) 
 REPRESENTATION_ITEM ( '' )  SURFACE ( )  );
#10811=CARTESIAN_POINT ( 'NONE',  ( -6.077587904424778920, -17.35179747939691808, -8.349320069797613542 ) ) ;
#10813=CARTESIAN_POINT ( 'NONE',  ( 1.296416391601052487, -11.47028222229313599, 42.55279074064478806 ) ) ;
#10815=CARTESIAN_POINT ( 'NONE',  ( 0.8744876279028263033, 43.84003649649913115, 22.09980204357308153 ) ) ;
#10821=AXIS2_PLACEMENT_3D ( 'NONE', #50139, #8142, #21631 ) ;
#10827=ORIENTED_EDGE ( 'NONE', *, *, #41553, .F. ) ;
#10829=B_SPLINE_CURVE_WITH_KNOTS ( 'NONE', 3,
 ( #46674, #36660, #55729, #22853, #41988, #45448 ),
 .UNSPECIFIED., .F., .F.,
 ( 4, 2, 4 ),
 ( 0.000000000000000000, 0.0002447195606305742040, 0.0004894391212611484080 ),
 .UNSPECIFIED. ) ;
#10834=CARTESIAN_POINT ( 'NONE',  ( 0.1119899015040014545, 42.04997222364495713, -13.37015871944657341 ) ) ;
#10836=CARTESIAN_POINT ( 'NONE',  ( 0.1119899015040012741, -43.68681032745429604, -6.198702413048826187 ) ) ;
#10837=VERTEX_POINT ( 'NONE', #34136 ) ;
#10840=AXIS2_PLACEMENT_3D ( 'NONE', #21247, #45382, #35675 ) ;
#10846=CARTESIAN_POINT ( 'NONE',  ( 4.834790513006553603, -32.10612123254752959, 34.66678987626835351 ) ) ;
#10847=CARTESIAN_POINT ( 'NONE',  ( 0.8744876279028306332, 28.81338721758086052, 39.75095932715638014 ) ) ;
#10849=CARTESIAN_POINT ( 'NONE',  ( 0.1129192098497447394, -31.35755906439637641, 31.04279751098549056 ) ) ;
#10850=CARTESIAN_POINT ( 'NONE',  ( 4.694002226626921015, -45.51532087759711942, 2.576885107160884925 ) ) ;
#10860=CARTESIAN_POINT ( 'NONE',  ( -6.078726893082806448, -14.66462719274117887, 12.47969352855413838 ) ) ;
#10861=CARTESIAN_POINT ( 'NONE',  ( -6.077587904424778920, -14.66646125808240164, -12.47761738310237334 ) ) ;
#10865=B_SPLINE_CURVE_WITH_KNOTS ( 'NONE', 3,
 ( #60891, #17380, #32410, #32720, #37426, #36499 ),
 .UNSPECIFIED., .F., .F.,
 ( 4, 2, 4 ),
 ( 0.000000000000000000, 0.0002293801035737106188, 0.0004587602071474212377 ),
 .UNSPECIFIED. ) ;
#10872=ORIENTED_EDGE ( 'NONE', *, *, #50835, .F. ) ;
#10875=CONICAL_SURFACE ( 'NONE', #23870, 43.92652462719577500, 1.486293639869522343 ) ;
#10888=CARTESIAN_POINT ( 'NONE',  ( 0.6000166863083090663, 28.52380356231424940, -39.97769518177558012 ) ) ;
#10893=ORIENTED_EDGE ( 'NONE', *, *, #8917, .F. ) ;
#10895=FACE_OUTER_BOUND ( 'NONE', #24126, .T. ) ;
#10901=CARTESIAN_POINT ( 'NONE',  ( -6.079354080745853928, -18.27463532918889300, -6.068826808644588233 ) ) ;
#10903=CARTESIAN_POINT ( 'NONE',  ( -6.079354080745853928, -1.850179728782415545, -19.16689307684906751 ) ) ;
#10904=B_SPLINE_CURVE_WITH_KNOTS ( 'NONE', 3,
 ( #50929, #2386, #25907, #8025, #21825, #35943 ),
 .UNSPECIFIED., .F., .F.,
 ( 4, 2, 4 ),
 ( 2.114194236346733646E-18, 0.0002293801035737086944, 0.0004587602071474152746 ),
 .UNSPECIFIED. ) ;
#10907=CARTESIAN_POINT ( 'NONE',  ( 2.299652685299201416, -45.91772179304631152, 17.20013227258888477 ) ) ;
#10908=ORIENTED_EDGE ( 'NONE', *, *, #17560, .F. ) ;
#10910=( BOUNDED_SURFACE ( )  B_SPLINE_SURFACE ( 3, 1, ( 
 ( #35286, #59366 ),
 ( #30249, #50287 ),
 ( #7353, #1422 ),
 ( #31181, #40311 ) ),
 .UNSPECIFIED., .F., .F., .F. ) 
 B_SPLINE_SURFACE_WITH_KNOTS ( ( 4, 4 ),
 ( 2, 2 ),
 ( 0.000000000000000000, 1.000000000000000000 ),
 ( 0.000000000000000000, 1.000000000000000000 ),
 .UNSPECIFIED. ) 
 GEOMETRIC_REPRESENTATION_ITEM ( )  RATIONAL_B_SPLINE_SURFACE ( (
 ( 1.000000000000000000, 1.000000000000000000),
 ( 0.9953485035131437453, 0.8621029689291515030),
 ( 0.9953485035131437453, 0.8621029689291515030),
 ( 1.000000000000000000, 1.000000000000000000) ) ) 
 REPRESENTATION_ITEM ( '' )  SURFACE ( )  );
#10915=CARTESIAN_POINT ( 'NONE',  ( 0.1119898979215350199, 36.67093969866893133, -24.53983475633885547 ) ) ;
#10916=CARTESIAN_POINT ( 'NONE',  ( 0.8744876279028263033, 40.65405044375290800, 27.52450240960382644 ) ) ;
#10918=AXIS2_PLACEMENT_3D ( 'NONE', #5559, #58488, #24697 ) ;
#10924=CARTESIAN_POINT ( 'NONE',  ( 4.694002226626920127, -38.01786027345654162, 25.15804188870963287 ) ) ;
#10928=CARTESIAN_POINT ( 'NONE',  ( 0.5997462898726536595, -45.31995669577334240, -18.91172004968183984 ) ) ;
#10929=FACE_OUTER_BOUND ( 'NONE', #9355, .T. ) ;
#10931=LINE ( 'NONE', #44161, #44968 ) ;
#10937=ORIENTED_EDGE ( 'NONE', *, *, #38356, .T. ) ;
#10938=B_SPLINE_CURVE_WITH_KNOTS ( 'NONE', 3,
 ( #59360, #2655, #41221, #31485, #35594, #40923, #50280, #26788, #17096, #50894, #21470, #59671, #17704, #7659, #3265, #54966 ),
 .UNSPECIFIED., .F., .F.,
 ( 4, 3, 3, 3, 3, 4 ),
 ( 2.221635811791082109E-17, 0.0002612764279487775538, 0.0003919131003184807630, 0.0005225497727000644969, 0.0007837925190632461132, 0.001045051706266715433 ),
 .UNSPECIFIED. ) ;
#10941=EDGE_CURVE ( 'NONE', #60001, #8147, #927, .T. ) ;
#10944=CARTESIAN_POINT ( 'NONE',  ( 3.050102900204245682, 11.54593035058338124, 42.45134557958719768 ) ) ;
#10948=CARTESIAN_POINT ( 'NONE',  ( -6.063463321072276813, 3.088760411028184549, 19.00736729804353331 ) ) ;
#10956=CARTESIAN_POINT ( 'NONE',  ( 4.553261556744873317, -41.61700166486752295, 14.05577241741092998 ) ) ;
#10959=CARTESIAN_POINT ( 'NONE',  ( 1.296416391601052265, 24.29467132511798511, -36.77059041245664162 ) ) ;
#10962=VERTEX_POINT ( 'NONE', #22488 ) ;
#10964=CARTESIAN_POINT ( 'NONE',  ( 0.9594984694709473017, -0.4222239975805204826, -44.08486519868079512 ) ) ;
#10965=CARTESIAN_POINT ( 'NONE',  ( 0.6021448801613057400, 28.30905802261198900, -40.12652953470227857 ) ) ;
#10968=ORIENTED_EDGE ( 'NONE', *, *, #58806, .F. ) ;
#10972=VERTEX_POINT ( 'NONE', #3972 ) ;
#10978=CARTESIAN_POINT ( 'NONE',  ( 4.975610109902397937, 48.58133226360775581, 5.683622315980952244 ) ) ;
#10981=CARTESIAN_POINT ( 'NONE',  ( 0.5997462898726536595, 4.195097405483644515, -48.92803682862019343 ) ) ;
#10993=ADVANCED_FACE ( 'NONE', ( #32832 ), #10763, .F. ) ;
#10998=EDGE_CURVE ( 'NONE', #10972, #43985, #24120, .T. ) ;
#10999=ORIENTED_EDGE ( 'NONE', *, *, #56070, .T. ) ;
#11001=CARTESIAN_POINT ( 'NONE',  ( 0.1129192098497447394, 25.64022107388777272, 35.91003830501040994 ) ) ;
#11008=EDGE_LOOP ( 'NONE', ( #28735, #56263, #6443, #24231 ) ) ;
#11012=B_SPLINE_CURVE_WITH_KNOTS ( 'NONE', 3,
 ( #33147, #58147, #52221, #33768, #52850, #24350 ),
 .UNSPECIFIED., .F., .F.,
 ( 4, 2, 4 ),
 ( 0.000000000000000000, 0.0002447195606305733366, 0.0004894391212611466733 ),
 .UNSPECIFIED. ) ;
#11014=( NAMED_UNIT ( * ) PLANE_ANGLE_UNIT ( ) SI_UNIT ( $, .RADIAN. ) );
#11015=FACE_OUTER_BOUND ( 'NONE', #27422, .T. ) ;
#11016=CARTESIAN_POINT ( 'NONE',  ( 4.553261556744875094, 0.000000000000000000, 0.000000000000000000 ) ) ;
#11020=CARTESIAN_POINT ( 'NONE',  ( 1.830465331921977912, -2.645429179032414257, 43.97019172504383988 ) ) ;
#11028=CARTESIAN_POINT ( 'NONE',  ( 2.299652685299201416, -43.34123383624062598, 22.93074735830615651 ) ) ;
#11029=CARTESIAN_POINT ( 'NONE',  ( 0.7948878604505666967, -6.978576542600043453, 48.60039214592296730 ) ) ;
#11033=CARTESIAN_POINT ( 'NONE',  ( 0.3676999524040323597, -22.15802448779959377, -38.14410221935904843 ) ) ;
#11034=CARTESIAN_POINT ( 'NONE',  ( 0.1156867017252034419, 4.112540283844289490, 43.93210465808513021 ) ) ;
#11036=EDGE_CURVE ( 'NONE', #31232, #21995, #12267, .T. ) ;
#11039=LINE ( 'NONE', #11339, #56548 ) ;
#11040=EDGE_CURVE ( 'NONE', #34042, #46958, #51588, .T. ) ;
#11041=ORIENTED_EDGE ( 'NONE', *, *, #33591, .T. ) ;
#11044=CARTESIAN_POINT ( 'NONE',  ( 0.8753041380234530822, 11.79227530596865847, 47.66634631457734628 ) ) ;
#11046=ORIENTED_EDGE ( 'NONE', *, *, #41415, .T. ) ;
#11048=CARTESIAN_POINT ( 'NONE',  ( 0.6039202388192952409, -48.68192096202334085, -6.452463428513433463 ) ) ;
#11051=CARTESIAN_POINT ( 'NONE',  ( 0.5987334363312689645, 41.48360609181539616, -26.28066460520305725 ) ) ;
#11068=CARTESIAN_POINT ( 'NONE',  ( 2.879087469061463178, -42.96833078670570671, -9.477564359455300291 ) ) ;
#11069=CARTESIAN_POINT ( 'NONE',  ( -6.078726893082806448, 9.985094725776445301, -16.46486940689149137 ) ) ;
#11071=CARTESIAN_POINT ( 'NONE',  ( 0.6024113833632039894, -35.12450729357964718, -34.31924906643699558 ) ) ;
#11078=CARTESIAN_POINT ( 'NONE',  ( -6.078075953587585900, -19.21613803895145622, 1.239037172605796489 ) ) ;
#11086=CARTESIAN_POINT ( 'NONE',  ( 1.112077966505211624, -13.54489572197889302, -41.94718256342459739 ) ) ;
#11089=CARTESIAN_POINT ( 'NONE',  ( 0.1157506346131639274, -7.133777142707746322, -43.54365491642857933 ) ) ;
#11094=DIRECTION ( 'NONE',  ( 1.000000000000000000, 0.000000000000000000, 0.000000000000000000 ) ) ;
#11097=CARTESIAN_POINT ( 'NONE',  ( 0.1119898979215350893, 44.06612418549229915, 2.266717344663642386 ) ) ;
#11107=CARTESIAN_POINT ( 'NONE',  ( 3.221118495291109163, 43.73404891492205593, -4.700466484186104132 ) ) ;
#11111=ORIENTED_EDGE ( 'NONE', *, *, #45565, .T. ) ;
#11120=CARTESIAN_POINT ( 'NONE',  ( 0.8753041380234465318, 43.84722337925211377, 22.10337824412700058 ) ) ;
#11126=CARTESIAN_POINT ( 'NONE',  ( 0.1135584504625008484, 15.64364923084964332, -41.25806940317724525 ) ) ;
#11128=ORIENTED_EDGE ( 'NONE', *, *, #13882, .F. ) ;
#11133=CARTESIAN_POINT ( 'NONE',  ( 0.6027444965799114707, -7.966449588082729072, 48.45693136020871350 ) ) ;
#11135=CARTESIAN_POINT ( 'NONE',  ( 0.1156495703730067576, -40.95039897516667082, -16.43191337019942111 ) ) ;
#11136=VERTEX_POINT ( 'NONE', #35290 ) ;
#11140=B_SPLINE_CURVE_WITH_KNOTS ( 'NONE', 3,
 ( #40021, #1435, #39705, #20879 ),
 .UNSPECIFIED., .F., .F.,
 ( 4, 4 ),
 ( 0.000000000000000000, 0.005013413432710153717 ),
 .UNSPECIFIED. ) ;
#11145=ORIENTED_EDGE ( 'NONE', *, *, #32909, .F. ) ;
#11148=ORIENTED_EDGE ( 'NONE', *, *, #4656, .F. ) ;
#11149=CARTESIAN_POINT ( 'NONE',  ( 0.5997462898726536595, -8.352924653000044941, -48.39194436975655123 ) ) ;
#11153=CARTESIAN_POINT ( 'NONE',  ( 0.1129192098497447394, -7.520259262076021578, -43.47870154933693243 ) ) ;
#11155=CARTESIAN_POINT ( 'NONE',  ( 3.894904216938898323, 22.27749296280804714, 37.89244832111325678 ) ) ;
#11159=CARTESIAN_POINT ( 'NONE',  ( 0.7044674535453004927, 48.94804745615595465, -3.986398505018412308 ) ) ;
#11167=FACE_OUTER_BOUND ( 'NONE', #58950, .T. ) ;
#11168=CARTESIAN_POINT ( 'NONE',  ( 0.6029442701453591180, -19.79821103535463322, 44.93969364557171531 ) ) ;
#11175=ORIENTED_EDGE ( 'NONE', *, *, #25863, .T. ) ;
#11183=EDGE_CURVE ( 'NONE', #6759, #27417, #36901, .T. ) ;
#11186=EDGE_LOOP ( 'NONE', ( #52947, #9568, #59157, #37040 ) ) ;
#11188=CARTESIAN_POINT ( 'NONE',  ( 3.678834586032788234, 20.99745812816111723, 44.24611985004418813 ) ) ;
#11190=CARTESIAN_POINT ( 'NONE',  ( 4.553261556744873317, -33.59363643963353496, -28.30206982864260112 ) ) ;
#11191=ORIENTED_EDGE ( 'NONE', *, *, #9911, .F. ) ;
#11198=EDGE_LOOP ( 'NONE', ( #45030, #3255, #24839, #49544 ) ) ;
#11202=EDGE_LOOP ( 'NONE', ( #18023, #25248, #21193, #7901 ) ) ;
#11207=EDGE_CURVE ( 'NONE', #10372, #885, #1797, .T. ) ;
#11211=VERTEX_POINT ( 'NONE', #55911 ) ;
#11213=ORIENTED_EDGE ( 'NONE', *, *, #52028, .F. ) ;
#11215=ORIENTED_EDGE ( 'NONE', *, *, #19800, .F. ) ;
#11219=ORIENTED_EDGE ( 'NONE', *, *, #12906, .F. ) ;
#11225=ORIENTED_EDGE ( 'NONE', *, *, #20503, .F. ) ;
#11228=CARTESIAN_POINT ( 'NONE',  ( 0.7044674535453004927, 48.03641533699669708, -10.21300760708892419 ) ) ;
#11232=CARTESIAN_POINT ( 'NONE',  ( 0.5987334363312689645, -45.74238923172318749, 17.86607774094835577 ) ) ;
#11233=VERTEX_POINT ( 'NONE', #49991 ) ;
#11238=CARTESIAN_POINT ( 'NONE',  ( -6.079354080745853928, 18.62651132414728394, -4.883239819994009245 ) ) ;
#11239=CARTESIAN_POINT ( 'NONE',  ( 2.706805983486679779, 11.39999808494296474, 42.50666014853498353 ) ) ;
#11242=CARTESIAN_POINT ( 'NONE',  ( 0.1156495703730067437, 20.28816457620965252, -39.18332976355763719 ) ) ;
#11244=CARTESIAN_POINT ( 'NONE',  ( 0.1149546198390367646, 29.46142209737721984, 32.84769661670956964 ) ) ;
#11245=CARTESIAN_POINT ( 'NONE',  ( 2.299746137290199943, -29.55404911945319668, 39.12594431232409420 ) ) ;
#11246=( LENGTH_UNIT ( ) NAMED_UNIT ( * ) SI_UNIT ( .MILLI., .METRE. ) );
#11254=CARTESIAN_POINT ( 'NONE',  ( 2.648799415243696664, -15.27490784895089071, 46.59607980823770390 ) ) ;
#11257=CARTESIAN_POINT ( 'NONE',  ( 3.678748215320120973, -5.985490030740792555, 48.60850464056045439 ) ) ;
#11259=EDGE_CURVE ( 'NONE', #59478, #30308, #49622, .T. ) ;
#11260=CARTESIAN_POINT ( 'NONE',  ( -2.601141883200662974, -6.448885681770537559, -13.46132612088584679 ) ) ;
#11261=VECTOR ( 'NONE', #49221, 999.9999999999998863 ) ;
#11263=CARTESIAN_POINT ( 'NONE',  ( 4.975610109902397937, 25.84633036597884725, -41.52609557555889808 ) ) ;
#11265=VECTOR ( 'NONE', #59816, 1000.000000000000227 ) ;
#11267=CARTESIAN_POINT ( 'NONE',  ( 2.879087469061463178, -43.96707328741540977, 1.731514747965036349 ) ) ;
#11268=CARTESIAN_POINT ( 'NONE',  ( 4.975610109902397937, -43.81605102859442979, -21.73943604138302987 ) ) ;
#11269=ORIENTED_EDGE ( 'NONE', *, *, #58523, .F. ) ;
#11272=ORIENTED_EDGE ( 'NONE', *, *, #27943, .F. ) ;
#11273=CARTESIAN_POINT ( 'NONE',  ( 4.553261556744873317, -29.36425772793689859, 32.66925058691941075 ) ) ;
#11276=DIRECTION ( 'NONE',  ( 1.000000000000000000, 0.000000000000000000, 0.000000000000000000 ) ) ;
#11285=CARTESIAN_POINT ( 'NONE',  ( 0.7044674535453004927, 43.87480159924536594, -22.06364673932585774 ) ) ;
#11286=CARTESIAN_POINT ( 'NONE',  ( 0.3676999524040366896, -35.84016207189403502, -25.71834687500748373 ) ) ;
#11299=B_SPLINE_CURVE_WITH_KNOTS ( 'NONE', 3,
 ( #24246, #57126, #37450, #56520 ),
 .UNSPECIFIED., .F., .F.,
 ( 4, 4 ),
 ( 7.152448122690996019E-18, 0.005013413432710144176 ),
 .UNSPECIFIED. ) ;
#11300=CARTESIAN_POINT ( 'NONE',  ( -2.601141883200665639, 4.732256851928614338, 14.15631211003640288 ) ) ;
#11313=CARTESIAN_POINT ( 'NONE',  ( 0.3676999524040366896, -7.853951980431815194, -43.40813312746713848 ) ) ;
#11315=CARTESIAN_POINT ( 'NONE',  ( -6.077587904424778920, 18.62472241188249811, 4.890371813497665698 ) ) ;
#11321=B_SPLINE_CURVE_WITH_KNOTS ( 'NONE', 3,
 ( #5967, #20417, #35455, #58596 ),
 .UNSPECIFIED., .F., .F.,
 ( 4, 4 ),
 ( 0.000000000000000000, 0.004444103432399266161 ),
 .UNSPECIFIED. ) ;
#11325=CARTESIAN_POINT ( 'NONE',  ( 0.6028777368367060907, -45.55110310871040014, 18.34766565235772262 ) ) ;
#11329=CARTESIAN_POINT ( 'NONE',  ( 4.975610109902397937, -44.31543648230385202, -20.70245146161840211 ) ) ;
#11330=ORIENTED_EDGE ( 'NONE', *, *, #33591, .F. ) ;
#11331=ADVANCED_FACE ( 'NONE', ( #23039 ), #60862, .F. ) ;
#11332=CARTESIAN_POINT ( 'NONE',  ( -6.078726893082806448, -18.90026279491055305, -3.684305572565921949 ) ) ;
#11334=B_SPLINE_CURVE_WITH_KNOTS ( 'NONE', 3,
 ( #40266, #29592, #24915, #59016, #16127, #53997 ),
 .UNSPECIFIED., .F., .F.,
 ( 4, 2, 4 ),
 ( 8.131516293641283255E-19, 0.0002293801035737095075, 0.0004587602071474182019 ),
 .UNSPECIFIED. ) ;
#11339=CARTESIAN_POINT ( 'NONE',  ( -2.739355103387247858, 14.08251715046641905, 4.952805029257269176 ) ) ;
#11340=( BOUNDED_SURFACE ( )  B_SPLINE_SURFACE ( 3, 1, ( 
 ( #49709, #2700 ),
 ( #6766, #45046 ),
 ( #2074, #6451 ),
 ( #30912, #25911 ) ),
 .UNSPECIFIED., .F., .F., .F. ) 
 B_SPLINE_SURFACE_WITH_KNOTS ( ( 4, 4 ),
 ( 2, 2 ),
 ( 0.000000000000000000, 1.000000000000000000 ),
 ( 0.000000000000000000, 1.000000000000000000 ),
 .UNSPECIFIED. ) 
 GEOMETRIC_REPRESENTATION_ITEM ( )  RATIONAL_B_SPLINE_SURFACE ( (
 ( 1.000000000000000000, 1.000000000000000000),
 ( 0.9754377213608244057, 0.9999580625633939235),
 ( 0.9754377213608244057, 0.9999580625633939235),
 ( 1.000000000000000000, 1.000000000000000000) ) ) 
 REPRESENTATION_ITEM ( '' )  SURFACE ( )  );
#11344=ORIENTED_EDGE ( 'NONE', *, *, #24038, .T. ) ;
#11350=CARTESIAN_POINT ( 'NONE',  ( 0.5987334363312691865, 46.79309011824572906, -14.89864502757918174 ) ) ;
#11356=CARTESIAN_POINT ( 'NONE',  ( 0.1129192098497447394, 43.40062318508790895, 7.958498283669150020 ) ) ;
#11361=( BOUNDED_SURFACE ( )  B_SPLINE_SURFACE ( 3, 1, ( 
 ( #6874, #26013 ),
 ( #45148, #2178 ),
 ( #7817, #55730 ),
 ( #21314, #40445 ) ),
 .UNSPECIFIED., .F., .F., .F. ) 
 B_SPLINE_SURFACE_WITH_KNOTS ( ( 4, 4 ),
 ( 2, 2 ),
 ( 0.000000000000000000, 1.000000000000000000 ),
 ( 0.000000000000000000, 1.000000000000000000 ),
 .UNSPECIFIED. ) 
 GEOMETRIC_REPRESENTATION_ITEM ( )  RATIONAL_B_SPLINE_SURFACE ( (
 ( 1.000000000000000000, 1.000000000000000000),
 ( 0.9953485035131437453, 0.8621029689291523912),
 ( 0.9953485035131437453, 0.8621029689291523912),
 ( 1.000000000000000000, 1.000000000000000000) ) ) 
 REPRESENTATION_ITEM ( '' )  SURFACE ( )  );
#11362=VECTOR ( 'NONE', #58096, 1000.000000000000000 ) ;
#11369=CARTESIAN_POINT ( 'NONE',  ( 0.8744876279028263033, 48.01195819035220325, 10.25679877483054625 ) ) ;
#11370=CARTESIAN_POINT ( 'NONE',  ( 2.533389852662419894, 8.245621584460703701, -43.23725542191009197 ) ) ;
#11376=CARTESIAN_POINT ( 'NONE',  ( 1.479689385636123067, 42.17416015216831227, 12.76417097687706104 ) ) ;
#11383=CARTESIAN_POINT ( 'NONE',  ( 2.359973842542475886, -13.96544505891846200, -41.75047591272259240 ) ) ;
#11385=EDGE_CURVE ( 'NONE', #61878, #43179, #4006, .T. ) ;
#11388=CARTESIAN_POINT ( 'NONE',  ( 0.1129192098497447394, 15.69290830752478882, 41.23935519181615206 ) ) ;
#11389=B_SPLINE_CURVE_WITH_KNOTS ( 'NONE', 3,
 ( #11440, #54015, #6083, #49959, #2012, #7012, #35572, #16442, #59338, #34951, #15837, #54629, #49331, #30841, #25221, #26146 ),
 .UNSPECIFIED., .F., .F.,
 ( 4, 3, 3, 3, 3, 4 ),
 ( 1.962735358247463844E-17, 0.0002612764279487719702, 0.0003919131003184767514, 0.0005225497727000664484, 0.0007837925190632497995, 0.001045051706266717818 ),
 .UNSPECIFIED. ) ;
#11391=CARTESIAN_POINT ( 'NONE',  ( 4.975610109902397937, 0.9924324126403755164, 48.90260202733708894 ) ) ;
#11399=EDGE_CURVE ( 'NONE', #60643, #40797, #24254, .T. ) ;
#11403=ORIENTED_EDGE ( 'NONE', *, *, #44639, .T. ) ;
#11404=ORIENTED_EDGE ( 'NONE', *, *, #45028, .T. ) ;
#11406=CARTESIAN_POINT ( 'NONE',  ( 0.9268187852002115479, 43.92278549089876805, -3.813561016834528417 ) ) ;
#11407=CARTESIAN_POINT ( 'NONE',  ( 0.1158816050234199313, 41.87808310636262377, 13.89849620073145431 ) ) ;
#11409=VERTEX_POINT ( 'NONE', #34286 ) ;
#11410=CARTESIAN_POINT ( 'NONE',  ( 0.7242003506640025678, 36.85244696242455831, -32.44855662441259625 ) ) ;
#11416=ORIENTED_EDGE ( 'NONE', *, *, #45528, .T. ) ;
#11418=CARTESIAN_POINT ( 'NONE',  ( -6.057079549204054558, -18.90348671888457588, -3.672794708215112003 ) ) ;
#11420=CARTESIAN_POINT ( 'NONE',  ( 0.7044674535452954967, 43.87480159924503198, 22.06364673932647591 ) ) ;
#11423=CARTESIAN_POINT ( 'NONE',  ( 0.2279481005628795909, -2.172801660577914351, 44.06566032657064369 ) ) ;
#11427=CARTESIAN_POINT ( 'NONE',  ( 0.1368894036331281816, 43.98715317849343620, -3.462900688019952877 ) ) ;
#11428=ORIENTED_EDGE ( 'NONE', *, *, #3675, .F. ) ;
#11434=CARTESIAN_POINT ( 'NONE',  ( 0.6016118706126976079, -8.181234200593557659, 48.42126043112642009 ) ) ;
#11435=CARTESIAN_POINT ( 'NONE',  ( 0.5980271706414734822, -38.93680501037979980, 29.93283244909049756 ) ) ;
#11436=CARTESIAN_POINT ( 'NONE',  ( 4.553261556744875094, -43.82122302957815663, -3.039733214544628748 ) ) ;
#11440=CARTESIAN_POINT ( 'NONE',  ( 0.5997462898726536595, -35.63787911784795170, 33.78599121123970406 ) ) ;
#11441=( BOUNDED_SURFACE ( )  B_SPLINE_SURFACE ( 3, 1, ( 
 ( #53902, #35142 ),
 ( #53291, #19811 ),
 ( #20724, #38931 ),
 ( #57984, #1586 ) ),
 .UNSPECIFIED., .F., .F., .F. ) 
 B_SPLINE_SURFACE_WITH_KNOTS ( ( 4, 4 ),
 ( 2, 2 ),
 ( 0.000000000000000000, 1.000000000000000000 ),
 ( 0.000000000000000000, 1.000000000000000000 ),
 .UNSPECIFIED. ) 
 GEOMETRIC_REPRESENTATION_ITEM ( )  RATIONAL_B_SPLINE_SURFACE ( (
 ( 1.000000000000000000, 1.000000000000000000),
 ( 0.9953485035131437453, 0.8621029689291523912),
 ( 0.9953485035131437453, 0.8621029689291523912),
 ( 1.000000000000000000, 1.000000000000000000) ) ) 
 REPRESENTATION_ITEM ( '' )  SURFACE ( )  );
#11445=DIRECTION ( 'NONE',  ( 0.000000000000000000, 0.000000000000000000, -1.000000000000000000 ) ) ;
#11457=CARTESIAN_POINT ( 'NONE',  ( 2.359973842542476330, 21.68887420214251094, 38.31094661420071645 ) ) ;
#11460=FACE_OUTER_BOUND ( 'NONE', #46351, .T. ) ;
#11462=CARTESIAN_POINT ( 'NONE',  ( 2.648799415243708655, -15.27490784895023879, -46.59607980823791706 ) ) ;
#11463=EDGE_CURVE ( 'NONE', #34962, #26589, #224, .T. ) ;
#11479=CARTESIAN_POINT ( 'NONE',  ( 0.08486401232817714080, 0.000000000000000000, 0.000000000000000000 ) ) ;
#11481=ORIENTED_EDGE ( 'NONE', *, *, #61934, .F. ) ;
#11486=CARTESIAN_POINT ( 'NONE',  ( 0.1157991065609915715, -22.94322095412508133, 37.69019736997796599 ) ) ;
#11490=ORIENTED_EDGE ( 'NONE', *, *, #5149, .F. ) ;
#11492=AXIS2_PLACEMENT_3D ( 'NONE', #22551, #50428, #21934 ) ;
#11495=CARTESIAN_POINT ( 'NONE',  ( 0.6039202388192952409, 48.23508111734889781, -9.216325865102767523 ) ) ;
#11500=CARTESIAN_POINT ( 'NONE',  ( 0.8753041380234465318, -26.21158409634571740, 41.52217705074212972 ) ) ;
#11503=EDGE_CURVE ( 'NONE', #31302, #60250, #45858, .T. ) ;
#11511=CARTESIAN_POINT ( 'NONE',  ( 0.7948884756798512141, 11.76956421775548378, -47.66734734306368892 ) ) ;
#11514=ORIENTED_EDGE ( 'NONE', *, *, #11463, .T. ) ;
#11518=CARTESIAN_POINT ( 'NONE',  ( 0.6000166863083106206, -30.20952222014405919, -38.71961065066481211 ) ) ;
#11522=ORIENTED_EDGE ( 'NONE', *, *, #4496, .T. ) ;
#11524=CARTESIAN_POINT ( 'NONE',  ( 0.5997462898726536595, -31.02483596213004091, -38.06587952047387091 ) ) ;
#11534=ORIENTED_EDGE ( 'NONE', *, *, #11503, .T. ) ;
#11536=CARTESIAN_POINT ( 'NONE',  ( 2.533389852662419894, 30.74453978043937141, 31.49958421031297817 ) ) ;
#11540=B_SPLINE_CURVE_WITH_KNOTS ( 'NONE', 3,
 ( #5774, #24925, #39042, #28683 ),
 .UNSPECIFIED., .F., .F.,
 ( 4, 4 ),
 ( 0.000000000000000000, 0.004444103432399269631 ),
 .UNSPECIFIED. ) ;
#11553=CARTESIAN_POINT ( 'NONE',  ( 0.6029442701453591180, 44.28204046225096846, 21.22842711219661993 ) ) ;
#11555=CARTESIAN_POINT ( 'NONE',  ( 0.1156867017252034280, -42.71261242789667989, 11.07138414379485170 ) ) ;
#11557=CARTESIAN_POINT ( 'NONE',  ( 4.694002226626921015, 32.50760209236001685, 31.96154842386279071 ) ) ;
#11560=CARTESIAN_POINT ( 'NONE',  ( 0.6027444965799114707, 37.47717969856460485, -31.73325570641842575 ) ) ;
#11562=CARTESIAN_POINT ( 'NONE',  ( 0.1129192098497447394, -27.88830454350447852, -34.19348267541494124 ) ) ;
#11563=CARTESIAN_POINT ( 'NONE',  ( 0.08486401232817714080, 12.80000000000000071, 0.000000000000000000 ) ) ;
#11564=ADVANCED_FACE ( 'NONE', ( #44934 ), #59924, .F. ) ;
#11567=ADVANCED_FACE ( 'NONE', ( #8221 ), #46771, .F. ) ;
#11573=CARTESIAN_POINT ( 'NONE',  ( -6.072942160501519915, 5.465015824219198848, -18.46450011048374051 ) ) ;
#11574=CARTESIAN_POINT ( 'NONE',  ( 0.1140933569871965259, -38.25874881921380677, -21.98222210951867694 ) ) ;
#11581=ORIENTED_EDGE ( 'NONE', *, *, #23420, .T. ) ;
#11582=CARTESIAN_POINT ( 'NONE',  ( 4.060580049360325461, -43.88752239372906416, 2.313670784519497481 ) ) ;
#11585=ORIENTED_EDGE ( 'NONE', *, *, #25606, .T. ) ;
#11601=CARTESIAN_POINT ( 'NONE',  ( -6.057079549204054558, -4.276794256740849676, 18.77605554916279473 ) ) ;
#11604=CARTESIAN_POINT ( 'NONE',  ( -6.057079549204054558, 13.83914966176537398, 13.39063731638631971 ) ) ;
#11616=DIRECTION ( 'NONE',  ( -1.000000000000000000, -0.000000000000000000, -0.000000000000000000 ) ) ;
#11617=FACE_OUTER_BOUND ( 'NONE', #52685, .T. ) ;
#11620=EDGE_CURVE ( 'NONE', #8264, #49921, #18126, .T. ) ;
#11635=CARTESIAN_POINT ( 'NONE',  ( -6.078457390727109555, -12.94908628767698211, -14.25186567968572326 ) ) ;
#11637=CARTESIAN_POINT ( 'NONE',  ( 2.299746137290200831, -44.95078339314706284, 19.58847646011585653 ) ) ;
#11640=( BOUNDED_SURFACE ( )  B_SPLINE_SURFACE ( 3, 1, ( 
 ( #6328, #15782 ),
 ( #1041, #24241 ),
 ( #10150, #1645 ),
 ( #20784, #39919 ) ),
 .UNSPECIFIED., .F., .F., .F. ) 
 B_SPLINE_SURFACE_WITH_KNOTS ( ( 4, 4 ),
 ( 2, 2 ),
 ( 0.000000000000000000, 1.000000000000000000 ),
 ( 0.000000000000000000, 1.000000000000000000 ),
 .UNSPECIFIED. ) 
 GEOMETRIC_REPRESENTATION_ITEM ( )  RATIONAL_B_SPLINE_SURFACE ( (
 ( 1.000000000000000000, 1.000000000000000000),
 ( 0.9953485035131437453, 0.8621029689291523912),
 ( 0.9953485035131437453, 0.8621029689291523912),
 ( 1.000000000000000000, 1.000000000000000000) ) ) 
 REPRESENTATION_ITEM ( '' )  SURFACE ( )  );
#11641=CARTESIAN_POINT ( 'NONE',  ( -2.601141883200665639, 2.883136076037970064, 14.64523655788587853 ) ) ;
#11648=EDGE_LOOP ( 'NONE', ( #15008, #49052, #51950, #51240 ) ) ;
#11650=CARTESIAN_POINT ( 'NONE',  ( 0.6253024248130503171, 44.53704952457137978, -20.68563383277205148 ) ) ;
#11653=CARTESIAN_POINT ( 'NONE',  ( 3.240649175237394264, 40.39403302172326704, -17.42374855298310976 ) ) ;
#11658=CARTESIAN_POINT ( 'NONE',  ( 0.6000166863083090663, 11.43688157230898383, 47.76003791465657144 ) ) ;
#11662=ORIENTED_EDGE ( 'NONE', *, *, #3259, .F. ) ;
#11664=EDGE_CURVE ( 'NONE', #61039, #52564, #46534, .T. ) ;
#11665=CARTESIAN_POINT ( 'NONE',  ( 0.7948884756798506590, 46.86364173482099460, -14.64574094918027747 ) ) ;
#11670=AXIS2_PLACEMENT_3D ( 'NONE', #820, #38759, #48436 ) ;
#11672=CARTESIAN_POINT ( 'NONE',  ( 0.1158816050234199174, 43.30939313556643810, -8.440290725686597995 ) ) ;
#11678=ORIENTED_EDGE ( 'NONE', *, *, #45848, .F. ) ;
#11684=DIRECTION ( 'NONE',  ( -1.000000000000000000, -0.000000000000000000, -0.000000000000000000 ) ) ;
#11696=EDGE_CURVE ( 'NONE', #21722, #56788, #58474, .T. ) ;
#11698=B_SPLINE_CURVE_WITH_KNOTS ( 'NONE', 3,
 ( #52257, #28456, #18775, #4319 ),
 .UNSPECIFIED., .F., .F.,
 ( 4, 4 ),
 ( 0.000000000000000000, 0.005013413432710138971 ),
 .UNSPECIFIED. ) ;
#11699=FACE_OUTER_BOUND ( 'NONE', #4458, .T. ) ;
#11700=CIRCLE ( 'NONE', #40738, 43.92652462719577500 ) ;
#11702=ADVANCED_FACE ( 'NONE', ( #46 ), #29743, .F. ) ;
#11703=CARTESIAN_POINT ( 'NONE',  ( 4.060580049360325461, -43.23134078854796059, 7.906887376435675741 ) ) ;
#11726=CIRCLE ( 'NONE', #22712, 48.91267123290010943 ) ;
#11729=ORIENTED_EDGE ( 'NONE', *, *, #47, .F. ) ;
#11730=FACE_OUTER_BOUND ( 'NONE', #49057, .T. ) ;
#11733=ORIENTED_EDGE ( 'NONE', *, *, #34562, .T. ) ;
#11739=EDGE_CURVE ( 'NONE', #58614, #27427, #6887, .T. ) ;
#11751=CARTESIAN_POINT ( 'NONE',  ( 0.8744876279028306332, -19.05609938969034545, 45.24616145519679122 ) ) ;
#11753=DIRECTION ( 'NONE',  ( -1.000000000000000000, -0.000000000000000000, -0.000000000000000000 ) ) ;
#11757=B_SPLINE_CURVE_WITH_KNOTS ( 'NONE', 3,
 ( #1640, #44603, #26394, #2886, #20777, #45230, #2578, #49574, #31099, #50200, #40524, #54255, #59589, #22017, #41143, #7266, #49267, #35819, #11376, #45524, #21699, #17317, #17016, #21391, #60205 ),
 .UNSPECIFIED., .F., .F.,
 ( 4, 3, 3, 3, 3, 3, 3, 3, 4 ),
 ( 6.254634441385501517E-18, 0.0005656085177311396400, 0.001131215744874500273, 0.001696821861372766783, 0.002262427090022499018, 0.002828031679238746359, 0.003393635864401605296, 0.003977030878808132490, 0.004561030005651159867 ),
 .UNSPECIFIED. ) ;
#11767=EDGE_CURVE ( 'NONE', #35750, #3477, #10089, .T. ) ;
#11770=CARTESIAN_POINT ( 'NONE',  ( 4.553261556744873317, 42.43205150231990075, -11.36048287389704292 ) ) ;
#11772=EDGE_CURVE ( 'NONE', #10837, #873, #38308, .T. ) ;
#11778=CARTESIAN_POINT ( 'NONE',  ( 1.479689385636123067, 21.41596951469469090, 38.50896122999632354 ) ) ;
#11779=CARTESIAN_POINT ( 'NONE',  ( 0.1129192098497447394, -41.07894348801345075, -16.10814047907924973 ) ) ;
#11780=CARTESIAN_POINT ( 'NONE',  ( 4.975610109902397937, -28.45381238669816426, 39.78479568629648355 ) ) ;
#11796=EDGE_CURVE ( 'NONE', #53243, #41822, #26327, .T. ) ;
#11807=CARTESIAN_POINT ( 'NONE',  ( 0.6253024248130480967, -47.32157158351321868, -13.11918786678801574 ) ) ;
#11815=DIRECTION ( 'NONE',  ( 0.000000000000000000, 0.000000000000000000, -1.000000000000000000 ) ) ;
#11816=AXIS2_PLACEMENT_3D ( 'NONE', #54730, #44761, #21858 ) ;
#11826=ORIENTED_EDGE ( 'NONE', *, *, #60096, .T. ) ;
#11827=CARTESIAN_POINT ( 'NONE',  ( -6.077587904424778920, -11.01164173315279271, -15.79682777441781738 ) ) ;
#11829=ORIENTED_EDGE ( 'NONE', *, *, #22474, .F. ) ;
#11832=( BOUNDED_SURFACE ( )  B_SPLINE_SURFACE ( 3, 1, ( 
 ( #28612, #4474 ),
 ( #5096, #48347 ),
 ( #4783, #24536 ),
 ( #56497, #32719 ) ),
 .UNSPECIFIED., .F., .F., .F. ) 
 B_SPLINE_SURFACE_WITH_KNOTS ( ( 4, 4 ),
 ( 2, 2 ),
 ( 0.000000000000000000, 1.000000000000000000 ),
 ( 0.000000000000000000, 1.000000000000000000 ),
 .UNSPECIFIED. ) 
 GEOMETRIC_REPRESENTATION_ITEM ( )  RATIONAL_B_SPLINE_SURFACE ( (
 ( 1.000000000000000000, 1.000000000000000000),
 ( 0.9953485035131437453, 0.8621029689291523912),
 ( 0.9953485035131437453, 0.8621029689291523912),
 ( 1.000000000000000000, 1.000000000000000000) ) ) 
 REPRESENTATION_ITEM ( '' )  SURFACE ( )  );
#11837=CARTESIAN_POINT ( 'NONE',  ( -6.077587904424778920, -11.02178778841139284, 15.78975032548507151 ) ) ;
#11841=CARTESIAN_POINT ( 'NONE',  ( 3.678748215320119197, -41.73555123697755675, 25.62726238296056636 ) ) ;
#11842=VERTEX_POINT ( 'NONE', #28737 ) ;
#11846=CARTESIAN_POINT ( 'NONE',  ( -6.078726893082806448, 12.00859800336337280, 15.05282748397580406 ) ) ;
#11854=CARTESIAN_POINT ( 'NONE',  ( 0.5997462898726536595, -25.90236585764290922, 41.72072714036901431 ) ) ;
#11856=VERTEX_POINT ( 'NONE', #27812 ) ;
#11857=CARTESIAN_POINT ( 'NONE',  ( 0.1135584504625007651, -27.17198796317027742, -34.76542998820209363 ) ) ;
#11862=CARTESIAN_POINT ( 'NONE',  ( 0.2940133293163001982, 29.05872899538194432, 33.19383705977649157 ) ) ;
#11863=CARTESIAN_POINT ( 'NONE',  ( 2.648799415243708655, 47.84750745855113507, -10.73002764644580687 ) ) ;
#11864=CARTESIAN_POINT ( 'NONE',  ( 0.6021448801613057400, 32.82111563175431712, 36.52828366230692581 ) ) ;
#11878=EDGE_CURVE ( 'NONE', #48571, #57030, #33454, .T. ) ;
#11879=CARTESIAN_POINT ( 'NONE',  ( -6.072942160501519027, -4.270762779174233970, -18.77670758075122137 ) ) ;
#11880=CARTESIAN_POINT ( 'NONE',  ( -6.057079549204054558, 9.989941839883096364, -16.46305843807557778 ) ) ;
#11881=CARTESIAN_POINT ( 'NONE',  ( -2.739355103387247858, 14.60025052884536123, 3.111310245855882339 ) ) ;
#11883=CARTESIAN_POINT ( 'NONE',  ( 0.1157991065609915854, -12.47647594550060823, -42.32351490033694574 ) ) ;
#11890=CARTESIAN_POINT ( 'NONE',  ( -2.601141883200662974, -8.117336596316121700, -12.52614362249992830 ) ) ;
#11894=ORIENTED_EDGE ( 'NONE', *, *, #11183, .F. ) ;
#11905=CARTESIAN_POINT ( 'NONE',  ( 0.6029443199889047422, -13.97238921213527263, 47.07770153224356591 ) ) ;
#11906=VERTEX_POINT ( 'NONE', #28117 ) ;
#11907=EDGE_CURVE ( 'NONE', #58000, #11842, #32842, .T. ) ;
#11915=CARTESIAN_POINT ( 'NONE',  ( -6.079354080745853928, 13.83171223607755174, -13.39689112691838702 ) ) ;
#11921=ORIENTED_EDGE ( 'NONE', *, *, #47380, .F. ) ;
#11922=CARTESIAN_POINT ( 'NONE',  ( 4.553261556744873317, 6.787618719204111528, -43.39893775135914922 ) ) ;
#11924=B_SPLINE_CURVE_WITH_KNOTS ( 'NONE', 3,
 ( #39860, #11637, #6265, #55138 ),
 .UNSPECIFIED., .F., .F.,
 ( 4, 4 ),
 ( 0.000000000000000000, 0.004442905043737217438 ),
 .UNSPECIFIED. ) ;
#11929=LINE ( 'NONE', #36043, #28429 ) ;
#11933=CARTESIAN_POINT ( 'NONE',  ( 4.834790513006553603, 1.053669480798183011, 47.23853428663527154 ) ) ;
#11935=ORIENTED_EDGE ( 'NONE', *, *, #41997, .F. ) ;
#11936=CARTESIAN_POINT ( 'NONE',  ( 0.1158816050234198897, -1.419926652724121441, -44.10131346803680685 ) ) ;
#11938=CARTESIAN_POINT ( 'NONE',  ( 2.648799415243708655, -48.79107182468955273, -4.893748408692878193 ) ) ;
#11939=ORIENTED_EDGE ( 'NONE', *, *, #25591, .T. ) ;
#11946=CARTESIAN_POINT ( 'NONE',  ( 0.6000166863083090663, 40.87138819217341279, 27.22780029589465656 ) ) ;
#11949=VERTEX_POINT ( 'NONE', #18731 ) ;
#11953=CARTESIAN_POINT ( 'NONE',  ( 0.5987334308729319599, -25.97268497059796744, -41.67712252528723127 ) ) ;
#11955=CARTESIAN_POINT ( 'NONE',  ( -6.077587904424778920, -18.27702681447043886, -6.061873655649631765 ) ) ;
#11957=( BOUNDED_SURFACE ( )  B_SPLINE_SURFACE ( 3, 1, ( 
 ( #3474, #55177 ),
 ( #7881, #46127 ),
 ( #21678, #36729 ),
 ( #16998, #45821 ) ),
 .UNSPECIFIED., .F., .F., .F. ) 
 B_SPLINE_SURFACE_WITH_KNOTS ( ( 4, 4 ),
 ( 2, 2 ),
 ( 0.000000000000000000, 1.000000000000000000 ),
 ( 0.000000000000000000, 1.000000000000000000 ),
 .UNSPECIFIED. ) 
 GEOMETRIC_REPRESENTATION_ITEM ( )  RATIONAL_B_SPLINE_SURFACE ( (
 ( 1.000000000000000000, 1.000000000000000000),
 ( 0.7211978278499968642, 0.9934217856018975334),
 ( 0.7211978278499968642, 0.9934217856018975334),
 ( 1.000000000000000000, 1.000000000000000000) ) ) 
 REPRESENTATION_ITEM ( '' )  SURFACE ( )  );
#11958=EDGE_CURVE ( 'NONE', #873, #2365, #24898, .T. ) ;
#11963=B_SPLINE_CURVE_WITH_KNOTS ( 'NONE', 3,
 ( #39759, #25018, #34123, #44160, #53494, #15013 ),
 .UNSPECIFIED., .F., .F.,
 ( 4, 2, 4 ),
 ( 1.252479364305869630E-17, 0.0002293755540694283640, 0.0004587511081388442056 ),
 .UNSPECIFIED. ) ;
#11966=CARTESIAN_POINT ( 'NONE',  ( -6.077587904424778920, -1.842868750311569270, -19.16767738050324610 ) ) ;
#11972=CARTESIAN_POINT ( 'NONE',  ( 2.009741617377216460, -2.780860071019173763, -43.95191571352101789 ) ) ;
#11977=CARTESIAN_POINT ( 'NONE',  ( 0.5987334363312689645, 44.50372305613552726, -20.76009490861898499 ) ) ;
#11978=EDGE_CURVE ( 'NONE', #36339, #43965, #18916, .T. ) ;
#11979=DIRECTION ( 'NONE',  ( 0.000000000000000000, 0.000000000000000000, 1.000000000000000000 ) ) ;
#11987=CARTESIAN_POINT ( 'NONE',  ( -6.078075953587585900, -4.279696274496690656, -18.77443405392543596 ) ) ;
#11988=ORIENTED_EDGE ( 'NONE', *, *, #5764, .T. ) ;
#11990=ORIENTED_EDGE ( 'NONE', *, *, #36382, .T. ) ;
#11996=AXIS2_PLACEMENT_3D ( 'NONE', #47316, #19743, #57295 ) ;
#11999=DIRECTION ( 'NONE',  ( 0.000000000000000000, 0.000000000000000000, -1.000000000000000000 ) ) ;
#12011=CARTESIAN_POINT ( 'NONE',  ( 1.296416391601052487, 14.17308196082959526, -41.73045796307255983 ) ) ;
#12018=ORIENTED_EDGE ( 'NONE', *, *, #39603, .T. ) ;
#12019=VERTEX_POINT ( 'NONE', #58445 ) ;
#12025=( BOUNDED_SURFACE ( )  B_SPLINE_SURFACE ( 3, 1, ( 
 ( #33272, #42987 ),
 ( #10068, #23538 ),
 ( #9435, #28237 ),
 ( #53270, #14469 ) ),
 .UNSPECIFIED., .F., .F., .F. ) 
 B_SPLINE_SURFACE_WITH_KNOTS ( ( 4, 4 ),
 ( 2, 2 ),
 ( 0.000000000000000000, 1.000000000000000000 ),
 ( 0.000000000000000000, 1.000000000000000000 ),
 .UNSPECIFIED. ) 
 GEOMETRIC_REPRESENTATION_ITEM ( )  RATIONAL_B_SPLINE_SURFACE ( (
 ( 1.000000000000000000, 1.000000000000000000),
 ( 0.9953485035131437453, 0.8621029689291515030),
 ( 0.9953485035131437453, 0.8621029689291515030),
 ( 1.000000000000000000, 1.000000000000000000) ) ) 
 REPRESENTATION_ITEM ( '' )  SURFACE ( )  );
#12026=EDGE_CURVE ( 'NONE', #8116, #46207, #35000, .T. ) ;
#12028=CARTESIAN_POINT ( 'NONE',  ( 0.1368894036331273489, 25.76388777123410634, 35.82015372432938705 ) ) ;
#12030=CARTESIAN_POINT ( 'NONE',  ( 2.299652685299200527, -24.30812083016131808, -42.58399918472231604 ) ) ;
#12034=B_SPLINE_CURVE_WITH_KNOTS ( 'NONE', 3,
 ( #44872, #55150, #21972, #21346, #16653, #7530, #36700, #54519, #50462, #35774, #25731, #1912, #21038, #40796, #26658, #40178, #2840, #50163, #45794, #17273, #7220, #59226, #26348, #45479, #35459 ),
 .UNSPECIFIED., .F., .F.,
 ( 4, 3, 3, 3, 3, 3, 3, 3, 4 ),
 ( 5.485677294651095664E-18, 0.0005656085177311396400, 0.001131215744874498972, 0.001696821861372766133, 0.002262427090022498585, 0.002828031679238745925, 0.003393635864401604862, 0.003977030878808131623, 0.004561030005651157265 ),
 .UNSPECIFIED. ) ;
#12035=CARTESIAN_POINT ( 'NONE',  ( 2.706805983486679335, 41.21557936162371760, -15.42893811010504912 ) ) ;
#12037=CARTESIAN_POINT ( 'NONE',  ( 3.771699521203193850, 0.7273600638980093347, -43.95767829216813283 ) ) ;
#12039=B_SPLINE_CURVE_WITH_KNOTS ( 'NONE', 3,
 ( #23199, #60164, #46405, #45798, #4060, #17277, #42330, #16980, #46716, #36090, #2843, #41408, #60464, #36398, #51073, #8165 ),
 .UNSPECIFIED., .F., .F.,
 ( 4, 3, 3, 3, 3, 4 ),
 ( 2.194378057379452319E-17, 0.0002612764279487728375, 0.0003919131003184776188, 0.0005225497727000641716, 0.0007837925190632419933, 0.001045051706266716084 ),
 .UNSPECIFIED. ) ;
#12046=CARTESIAN_POINT ( 'NONE',  ( 0.6026777506516368677, 16.79643818398497501, -46.14570462100229520 ) ) ;
#12055=CARTESIAN_POINT ( 'NONE',  ( 4.975610109902397937, -28.45381238669758872, -39.78479568629688856 ) ) ;
#12063=CARTESIAN_POINT ( 'NONE',  ( -6.078075953587585900, 16.78075473395873374, -9.444651650847566415 ) ) ;
#12072=CARTESIAN_POINT ( 'NONE',  ( 0.3676999524040366896, 37.41430475689384139, 23.36921870497834774 ) ) ;
#12075=B_SPLINE_CURVE_WITH_KNOTS ( 'NONE', 3,
 ( #44818, #19758, #38881, #10663 ),
 .UNSPECIFIED., .F., .F.,
 ( 4, 4 ),
 ( 0.000000000000000000, 0.004442905043737216571 ),
 .UNSPECIFIED. ) ;
#12077=EDGE_LOOP ( 'NONE', ( #14003, #24435, #15988, #1699 ) ) ;
#12084=CARTESIAN_POINT ( 'NONE',  ( 5.901764892641288895, -46.48816889762525761, -15.38965951493231898 ) ) ;
#12091=CARTESIAN_POINT ( 'NONE',  ( 4.975610109902397937, 47.16372689271670993, -12.96272628450527264 ) ) ;
#12096=CARTESIAN_POINT ( 'NONE',  ( -6.077587904424778920, -18.27312872431374657, -6.073614082125261326 ) ) ;
#12105=CARTESIAN_POINT ( 'NONE',  ( 4.553261556744873317, -39.47791437445913942, 19.26223877088302672 ) ) ;
#12111=CARTESIAN_POINT ( 'NONE',  ( 4.553261556744873317, -14.95853073564509828, 41.30111286702087625 ) ) ;
#12113=EDGE_CURVE ( 'NONE', #33819, #13208, #9917, .T. ) ;
#12116=ORIENTED_EDGE ( 'NONE', *, *, #3210, .F. ) ;
#12126=CARTESIAN_POINT ( 'NONE',  ( 2.299652685299201860, 21.52981099345398519, 44.05393244018406307 ) ) ;
#12138=FACE_OUTER_BOUND ( 'NONE', #59901, .T. ) ;
#12158=CARTESIAN_POINT ( 'NONE',  ( 0.1154773475650539977, -43.73856127446700981, 5.820815036214034954 ) ) ;
#12160=CARTESIAN_POINT ( 'NONE',  ( 0.5987334308729318488, -8.434467990461143927, -48.37791496424389948 ) ) ;
#12171=ORIENTED_EDGE ( 'NONE', *, *, #37160, .T. ) ;
#12174=VERTEX_POINT ( 'NONE', #7057 ) ;
#12177=CARTESIAN_POINT ( 'NONE',  ( 0.1368894036331290698, -38.75424303169170059, -21.09431138871115508 ) ) ;
#12178=CARTESIAN_POINT ( 'NONE',  ( 0.6029443449137436017, 44.22536370377634540, 21.34611775597693395 ) ) ;
#12182=VECTOR ( 'NONE', #4246, 1000.000000000000000 ) ;
#12194=CARTESIAN_POINT ( 'NONE',  ( 3.727782113643637096, 17.17182055185172374, 40.47105576632487356 ) ) ;
#12197=( BOUNDED_SURFACE ( )  B_SPLINE_SURFACE ( 3, 1, ( 
 ( #44312, #21400 ),
 ( #39607, #49279 ),
 ( #16708, #30470 ),
 ( #35827, #35208 ) ),
 .UNSPECIFIED., .F., .F., .F. ) 
 B_SPLINE_SURFACE_WITH_KNOTS ( ( 4, 4 ),
 ( 2, 2 ),
 ( 0.000000000000000000, 1.000000000000000000 ),
 ( 0.000000000000000000, 1.000000000000000000 ),
 .UNSPECIFIED. ) 
 GEOMETRIC_REPRESENTATION_ITEM ( )  RATIONAL_B_SPLINE_SURFACE ( (
 ( 1.000000000000000000, 1.000000000000000000),
 ( 0.7211978278499970862, 0.9934217856018976445),
 ( 0.7211978278499970862, 0.9934217856018976445),
 ( 1.000000000000000000, 1.000000000000000000) ) ) 
 REPRESENTATION_ITEM ( '' )  SURFACE ( )  );
#12198=EDGE_CURVE ( 'NONE', #61727, #4551, #16810, .T. ) ;
#12201=EDGE_CURVE ( 'NONE', #50810, #12769, #38332, .T. ) ;
#12205=VERTEX_POINT ( 'NONE', #60006 ) ;
#12207=CARTESIAN_POINT ( 'NONE',  ( 0.3676999524040366896, -26.85386693986640338, 34.99743438737744583 ) ) ;
#12209=CARTESIAN_POINT ( 'NONE',  ( 0.1129192098497455998, 43.99990943031669843, 3.310552508129313232 ) ) ;
#12216=EDGE_LOOP ( 'NONE', ( #20680, #47590, #34927, #1288 ) ) ;
#12217=CARTESIAN_POINT ( 'NONE',  ( -6.078726893082806448, 13.83492043373111180, -13.39361854993076406 ) ) ;
#12223=CARTESIAN_POINT ( 'NONE',  ( 2.648799415243708655, -34.24682227764526488, 35.09519379021831043 ) ) ;
#12225=CARTESIAN_POINT ( 'NONE',  ( 0.1152809850208375703, -1.635316795157891745, 44.09388870885884160 ) ) ;
#12230=CARTESIAN_POINT ( 'NONE',  ( -2.739355103387248747, -13.93362462427441706, -5.357394122223096744 ) ) ;
#12231=CARTESIAN_POINT ( 'NONE',  ( 0.5997462898726536595, -25.90236585764231947, -41.72072714036939090 ) ) ;
#12235=CARTESIAN_POINT ( 'NONE',  ( 3.894904216938897878, 6.429595949874166827, 43.48315338608232850 ) ) ;
#12237=FACE_OUTER_BOUND ( 'NONE', #61933, .T. ) ;
#12241=FACE_OUTER_BOUND ( 'NONE', #5817, .T. ) ;
#12245=CARTESIAN_POINT ( 'NONE',  ( 1.479689385636123067, -34.59735853788245663, 27.28748114921756596 ) ) ;
#12257=EDGE_CURVE ( 'NONE', #56898, #58292, #6099, .T. ) ;
#12261=B_SPLINE_CURVE_WITH_KNOTS ( 'NONE', 3,
 ( #18762, #36957, #37889, #23754 ),
 .UNSPECIFIED., .F., .F.,
 ( 4, 4 ),
 ( 0.000000000000000000, 0.005013413432710145910 ),
 .UNSPECIFIED. ) ;
#12263=CARTESIAN_POINT ( 'NONE',  ( 4.694002226626920127, -45.51532087759709810, -2.576885107160872490 ) ) ;
#12267=B_SPLINE_CURVE_WITH_KNOTS ( 'NONE', 3,
 ( #29040, #38457, #5206, #24337, #37222, #13409 ),
 .UNSPECIFIED., .F., .F.,
 ( 4, 2, 4 ),
 ( 1.192622389734054877E-18, 0.0002293801035737094533, 0.0004587602071474177140 ),
 .UNSPECIFIED. ) ;
#12268=DIRECTION ( 'NONE',  ( 0.000000000000000000, 0.000000000000000000, 1.000000000000000000 ) ) ;
#12272=CARTESIAN_POINT ( 'NONE',  ( 0.6039202388192952409, 28.23800208753110752, -40.17684595576886153 ) ) ;
#12276=CARTESIAN_POINT ( 'NONE',  ( 0.1129192098497455998, -18.30288010335110016, 40.14917642626692640 ) ) ;
#12279=CARTESIAN_POINT ( 'NONE',  ( 0.1140933569871964010, 3.859258926286197156, 43.95515977247479356 ) ) ;
#12289=ORIENTED_EDGE ( 'NONE', *, *, #40543, .F. ) ;
#12291=ORIENTED_EDGE ( 'NONE', *, *, #2251, .F. ) ;
#12296=CARTESIAN_POINT ( 'NONE',  ( 0.8744876279028306332, 40.65405044375329879, -27.52450240960324024 ) ) ;
#12301=CARTESIAN_POINT ( 'NONE',  ( 0.6000166863083090663, -7.321729200002740967, -48.56146376737711989 ) ) ;
#12302=EDGE_LOOP ( 'NONE', ( #20306, #18435, #56648, #34130 ) ) ;
#12312=CARTESIAN_POINT ( 'NONE',  ( 0.6000166863083106206, -1.051715750664326876, 49.09905676984292455 ) ) ;
#12313=CARTESIAN_POINT ( 'NONE',  ( 4.226256110419179812, 7.420606375272879696, -43.31006639351232934 ) ) ;
#12329=EDGE_CURVE ( 'NONE', #30486, #61495, #60582, .T. ) ;
#12330=CARTESIAN_POINT ( 'NONE',  ( 0.8744876279028263033, 43.84003649649913115, 22.09980204357308153 ) ) ;
#12331=CARTESIAN_POINT ( 'NONE',  ( 4.553261556744875094, 0.000000000000000000, 0.000000000000000000 ) ) ;
#12333=CARTESIAN_POINT ( 'NONE',  ( 3.390910168358336918, 41.07524454790360124, -15.71373354310021142 ) ) ;
#12338=CARTESIAN_POINT ( 'NONE',  ( 0.6024113833632039894, 16.75552346327387809, 46.16052753784931895 ) ) ;
#12342=ORIENTED_EDGE ( 'NONE', *, *, #54399, .T. ) ;
#12345=CARTESIAN_POINT ( 'NONE',  ( 2.185380717157383135, 2.793969434617936010, -43.94329912359357593 ) ) ;
#12353=AXIS2_PLACEMENT_3D ( 'NONE', #49691, #36237, #11815 ) ;
#12356=VERTEX_POINT ( 'NONE', #34295 ) ;
#12365=EDGE_CURVE ( 'NONE', #55302, #12174, #8329, .T. ) ;
#12370=B_SPLINE_CURVE_WITH_KNOTS ( 'NONE', 3,
 ( #35789, #31691, #60477, #55786, #12909, #40494, #40192, #32005, #36408, #55474, #26059, #2854, #30747, #46117, #41117, #54534, #2549, #49865, #6925 ),
 .UNSPECIFIED., .F., .F.,
 ( 4, 3, 3, 3, 3, 3, 4 ),
 ( 1.301113191146877164E-18, 0.0002612768053151710043, 0.0003919133833142906544, 0.0005225499612322604282, 0.0006531865391693357416, 0.0008112755173415182311, 0.0009693688056799726815 ),
 .UNSPECIFIED. ) ;
#12375=LINE ( 'NONE', #59963, #31394 ) ;
#12382=CARTESIAN_POINT ( 'NONE',  ( 0.3676999524040323597, 16.00695768809450215, -41.10629986868669761 ) ) ;
#12386=ORIENTED_EDGE ( 'NONE', *, *, #59594, .T. ) ;
#12399=ORIENTED_EDGE ( 'NONE', *, *, #257, .T. ) ;
#12400=EDGE_CURVE ( 'NONE', #17235, #10372, #10798, .T. ) ;
#12401=CARTESIAN_POINT ( 'NONE',  ( 0.1129192098497447394, -43.82135468580274562, -5.161459220630158384 ) ) ;
#12402=CARTESIAN_POINT ( 'NONE',  ( 0.7948878604505692502, 32.36187211755012783, -36.92435348581946641 ) ) ;
#12406=DIRECTION ( 'NONE',  ( 0.000000000000000000, 0.000000000000000000, 1.000000000000000000 ) ) ;
#12411=CARTESIAN_POINT ( 'NONE',  ( 0.6000166863083106206, -43.04473087058023850, 23.64264422580037461 ) ) ;
#12414=FACE_OUTER_BOUND ( 'NONE', #49191, .T. ) ;
#12415=CARTESIAN_POINT ( 'NONE',  ( 4.553261556744875094, -20.11719049292643646, -39.04917684785361587 ) ) ;
#12417=CARTESIAN_POINT ( 'NONE',  ( 2.299652685299201860, 38.15857472714130694, -30.79293587255566322 ) ) ;
#12429=CARTESIAN_POINT ( 'NONE',  ( 2.299746137290199499, 26.98651929683142114, -40.93909029189441640 ) ) ;
#12431=ORIENTED_EDGE ( 'NONE', *, *, #22921, .F. ) ;
#12432=B_SPLINE_CURVE_WITH_KNOTS ( 'NONE', 3,
 ( #1509, #11245, #58518, #49143 ),
 .UNSPECIFIED., .F., .F.,
 ( 4, 4 ),
 ( 0.000000000000000000, 0.004442905043737218305 ),
 .UNSPECIFIED. ) ;
#12434=CARTESIAN_POINT ( 'NONE',  ( 0.1157506346131639274, 33.65821932553335927, 28.53182313903419143 ) ) ;
#12436=CARTESIAN_POINT ( 'NONE',  ( 0.1129192098497447394, -12.08918212651769686, 42.43587472053614817 ) ) ;
#12444=AXIS2_PLACEMENT_3D ( 'NONE', #8503, #42666, #13861 ) ;
#12455=ORIENTED_EDGE ( 'NONE', *, *, #7507, .F. ) ;
#12457=CARTESIAN_POINT ( 'NONE',  ( 0.6027444965799114707, -48.68737225085462939, -6.409235460969727960 ) ) ;
#12462=CARTESIAN_POINT ( 'NONE',  ( -6.063463321072278589, 0.6327935495819126954, -19.24629898975586073 ) ) ;
#12463=ORIENTED_EDGE ( 'NONE', *, *, #32042, .F. ) ;
#12467=B_SPLINE_CURVE_WITH_KNOTS ( 'NONE', 3,
 ( #7148, #50094, #49780, #30051, #26276, #54144, #21587, #45414, #40725, #11905, #6214, #21280, #15973, #30662, #1526, #59795 ),
 .UNSPECIFIED., .F., .F.,
 ( 4, 3, 3, 3, 3, 4 ),
 ( 2.194378057379452319E-17, 0.0002612764279487737591, 0.0003919131003184764261, 0.0005225497727000642800, 0.0007837925190632450290, 0.001045051706266714132 ),
 .UNSPECIFIED. ) ;
#12473=EDGE_CURVE ( 'NONE', #28574, #37964, #58354, .T. ) ;
#12481=CARTESIAN_POINT ( 'NONE',  ( 0.1158816050234199313, -42.67963805895574581, 11.19779158859894252 ) ) ;
#12483=CARTESIAN_POINT ( 'NONE',  ( -6.072942160501519027, 9.994728154871472370, -16.45933083084606352 ) ) ;
#12484=CARTESIAN_POINT ( 'NONE',  ( 0.6026777506516367566, 4.888802969756627981, 48.86354465406822811 ) ) ;
#12486=CARTESIAN_POINT ( 'NONE',  ( 0.1149546198390367924, -12.29174268441242113, -42.37758401328954250 ) ) ;
#12489=CARTESIAN_POINT ( 'NONE',  ( 0.6000166863083106206, -34.91285637184653012, -34.53861522509651394 ) ) ;
#12490=CONICAL_SURFACE ( 'NONE', #18469, 43.92652462719577500, 1.486293639869522343 ) ;
#12494=DIRECTION ( 'NONE',  ( 0.09722883295013597105, -0.9952333609815530169, -0.007557197398263266856 ) ) ;
#12495=FILL_AREA_STYLE ('',( #38852 ) ) ;
#12504=CARTESIAN_POINT ( 'NONE',  ( 0.5997462898726536595, -47.63132954987522538, -11.95023328037962251 ) ) ;
#12505=CARTESIAN_POINT ( 'NONE',  ( -2.739355103387247858, -12.87605224490601330, -7.553465796405506971 ) ) ;
#12507=CARTESIAN_POINT ( 'NONE',  ( 2.879087469061463178, -40.10403664819293112, 18.10436194136033450 ) ) ;
#12509=B_SPLINE_CURVE_WITH_KNOTS ( 'NONE', 3,
 ( #746, #38998, #19264, #38381, #5429, #9852 ),
 .UNSPECIFIED., .F., .F.,
 ( 4, 2, 4 ),
 ( 2.224043620450101781E-17, 0.0002293755540694328906, 0.0004587511081388435008 ),
 .UNSPECIFIED. ) ;
#12511=ORIENTED_EDGE ( 'NONE', *, *, #44454, .T. ) ;
#12512=AXIS2_PLACEMENT_3D ( 'NONE', #28417, #47547, #56615 ) ;
#12519=VERTEX_POINT ( 'NONE', #26418 ) ;
#12521=ORIENTED_EDGE ( 'NONE', *, *, #58285, .F. ) ;
#12529=CARTESIAN_POINT ( 'NONE',  ( 0.1140933569871964287, -1.793286609244197027, 44.08779959604483878 ) ) ;
#12547=CARTESIAN_POINT ( 'NONE',  ( 4.335381028904216727, 24.52155563981566289, 42.40813785899788968 ) ) ;
#12558=CARTESIAN_POINT ( 'NONE',  ( 0.6252788684277231779, -26.04119143542666848, -41.63292783119062790 ) ) ;
#12560=EDGE_CURVE ( 'NONE', #5530, #12519, #22044, .T. ) ;
#12561=CARTESIAN_POINT ( 'NONE',  ( 4.975610109902397937, 35.53430708602537891, 33.61193875773635398 ) ) ;
#12567=CARTESIAN_POINT ( 'NONE',  ( -6.078726893082806448, -1.852420388636412119, -19.16670498475114570 ) ) ;
#12586=CIRCLE ( 'NONE', #5522, 43.92652462719577500 ) ;
#12587=CARTESIAN_POINT ( 'NONE',  ( 0.1155031312995260795, 4.069181162214699832, 43.93612860961791711 ) ) ;
#12591=CARTESIAN_POINT ( 'NONE',  ( 4.553261556744873317, 40.63093864075514006, -16.69330377710856084 ) ) ;
#12593=CARTESIAN_POINT ( 'NONE',  ( 1.834102595619085507, -11.27825010024307595, 42.57932385012767895 ) ) ;
#12596=EDGE_LOOP ( 'NONE', ( #52795, #42106, #12741, #48092 ) ) ;
#12603=EDGE_CURVE ( 'NONE', #18917, #29558, #47092, .T. ) ;
#12604=CARTESIAN_POINT ( 'NONE',  ( 2.881901169982995725, 1.330622528702777754E-16, 49.00591519830862808 ) ) ;
#12605=CARTESIAN_POINT ( 'NONE',  ( 0.8753041380234530822, 37.96023374381034188, 31.14737520222631417 ) ) ;
#12609=B_SPLINE_CURVE_WITH_KNOTS ( 'NONE', 3,
 ( #48217, #6492, #15637, #29403, #44771, #20035, #48514, #54114, #49134, #1813, #20942, #59133, #16244, #54424, #29099, #578 ),
 .UNSPECIFIED., .F., .F.,
 ( 4, 3, 3, 3, 3, 4 ),
 ( 1.868480190406682863E-17, 0.0002612764279487741928, 0.0003919131003184782693, 0.0005225497727000676411, 0.0007837925190632453543, 0.001045051706266716951 ),
 .UNSPECIFIED. ) ;
#12611=CARTESIAN_POINT ( 'NONE',  ( 3.894904216938897878, -37.15895100125024442, 23.48055989457843395 ) ) ;
#12623=CARTESIAN_POINT ( 'NONE',  ( 4.553261556744875094, 0.000000000000000000, 0.000000000000000000 ) ) ;
#12625=CARTESIAN_POINT ( 'NONE',  ( 0.6016118706126976079, 27.80884168916806942, 40.47492283736583829 ) ) ;
#12636=CARTESIAN_POINT ( 'NONE',  ( 4.226256110419178924, 12.10579822316747922, 42.24070192796447287 ) ) ;
#12641=DIRECTION ( 'NONE',  ( 0.09722883295013597105, -0.1513788123411373143, -0.9836823721188365788 ) ) ;
#12649=CARTESIAN_POINT ( 'NONE',  ( 0.6027444965799114707, 16.83735020315194220, 46.13070727859980025 ) ) ;
#12659=EDGE_LOOP ( 'NONE', ( #24209, #61259, #48562, #29278 ) ) ;
#12661=CARTESIAN_POINT ( 'NONE',  ( 0.2279481005628784251, 43.15403823156285057, 9.177824980992246751 ) ) ;
#12668=CARTESIAN_POINT ( 'NONE',  ( 0.7948884756798508811, 48.93475817450405430, 4.010995762022314004 ) ) ;
#12670=ORIENTED_EDGE ( 'NONE', *, *, #32454, .T. ) ;
#12671=CARTESIAN_POINT ( 'NONE',  ( 4.834790513006553603, 19.54670848745993439, -43.01761881172228641 ) ) ;
#12676=EDGE_CURVE ( 'NONE', #34042, #14204, #8536, .T. ) ;
#12679=ORIENTED_EDGE ( 'NONE', *, *, #38134, .F. ) ;
#12683=CARTESIAN_POINT ( 'NONE',  ( 0.6021448801613057400, -48.73699182459426993, 6.020528757208808202 ) ) ;
#12692=ORIENTED_EDGE ( 'NONE', *, *, #55036, .T. ) ;
#12694=DIRECTION ( 'NONE',  ( 0.000000000000000000, 0.000000000000000000, -1.000000000000000000 ) ) ;
#12699=CARTESIAN_POINT ( 'NONE',  ( 0.8753041380234471980, -39.87785955339043653, 28.65125905284175190 ) ) ;
#12700=LINE ( 'NONE', #35582, #41693 ) ;
#12712=ORIENTED_EDGE ( 'NONE', *, *, #6733, .T. ) ;
#12714=AXIS2_PLACEMENT_3D ( 'NONE', #60020, #16199, #40037 ) ;
#12726=CONICAL_SURFACE ( 'NONE', #20715, 43.92652462719577500, 1.486293639869522343 ) ;
#12732=CARTESIAN_POINT ( 'NONE',  ( 3.894904216938897878, -19.80394396472108554, -39.24191809683094334 ) ) ;
#12735=ORIENTED_EDGE ( 'NONE', *, *, #2970, .T. ) ;
#12736=CARTESIAN_POINT ( 'NONE',  ( 3.240649175237396484, 43.98046403787316905, -0.9918167224828714490 ) ) ;
#12741=ORIENTED_EDGE ( 'NONE', *, *, #21077, .T. ) ;
#12747=CARTESIAN_POINT ( 'NONE',  ( 0.6252788684277231779, 43.94110077395946945, -21.92313832338802371 ) ) ;
#12748=CARTESIAN_POINT ( 'NONE',  ( 0.6016117650947689910, 49.02773486208430143, 2.798619041181271694 ) ) ;
#12749=( BOUNDED_SURFACE ( )  B_SPLINE_SURFACE ( 3, 1, ( 
 ( #7142, #26271 ),
 ( #45715, #40718 ),
 ( #55384, #40404 ),
 ( #35080, #2455 ) ),
 .UNSPECIFIED., .F., .F., .F. ) 
 B_SPLINE_SURFACE_WITH_KNOTS ( ( 4, 4 ),
 ( 2, 2 ),
 ( 0.000000000000000000, 1.000000000000000000 ),
 ( 0.000000000000000000, 1.000000000000000000 ),
 .UNSPECIFIED. ) 
 GEOMETRIC_REPRESENTATION_ITEM ( )  RATIONAL_B_SPLINE_SURFACE ( (
 ( 1.000000000000000000, 1.000000000000000000),
 ( 0.7211978278499968642, 0.9934217856018975334),
 ( 0.7211978278499968642, 0.9934217856018975334),
 ( 1.000000000000000000, 1.000000000000000000) ) ) 
 REPRESENTATION_ITEM ( '' )  SURFACE ( )  );
#12750=CARTESIAN_POINT ( 'NONE',  ( -6.078457390727109555, -11.01309887717671288, -15.79576412077101644 ) ) ;
#12756=FACE_OUTER_BOUND ( 'NONE', #19671, .T. ) ;
#12761=CARTESIAN_POINT ( 'NONE',  ( 4.553261556744873317, -43.15908619232978083, -8.175135770535248980 ) ) ;
#12764=CARTESIAN_POINT ( 'NONE',  ( -6.057079549204054558, 16.78313491342506936, 9.442330939842715765 ) ) ;
#12768=CARTESIAN_POINT ( 'NONE',  ( -6.077587904424778920, -14.65844225831517633, 12.48703695652296553 ) ) ;
#12769=VERTEX_POINT ( 'NONE', #58291 ) ;
#12773=ORIENTED_EDGE ( 'NONE', *, *, #57139, .F. ) ;
#12775=CARTESIAN_POINT ( 'NONE',  ( 0.6029443449137436017, -48.69867271451428792, -6.322880184532521319 ) ) ;
#12779=CARTESIAN_POINT ( 'NONE',  ( 0.1154773475650540393, -27.65137296628978802, -34.38524688184250522 ) ) ;
#12784=CONICAL_SURFACE ( 'NONE', #20763, 43.92652462719577500, 1.486293639869522343 ) ;
#12785=ORIENTED_EDGE ( 'NONE', *, *, #685, .F. ) ;
#12794=EDGE_LOOP ( 'NONE', ( #30607, #10664, #1521, #5469 ) ) ;
#12798=CARTESIAN_POINT ( 'NONE',  ( 0.2940135542859017570, 19.68859029487963141, -39.47910790395081193 ) ) ;
#12801=CARTESIAN_POINT ( 'NONE',  ( 0.6026112563231247332, 4.542062193711753793, 48.89693922867424902 ) ) ;
#12808=VECTOR ( 'NONE', #39528, 1000.000000000000227 ) ;
#12811=CARTESIAN_POINT ( 'NONE',  ( 0.6026112563231247332, -1.399892387035774233, -49.08748614676582633 ) ) ;
#12812=CARTESIAN_POINT ( 'NONE',  ( 2.359973842542475442, 16.61171373028292919, 40.76992594518206658 ) ) ;
#12813=CARTESIAN_POINT ( 'NONE',  ( -2.739355103387248747, -11.80442426703895897, 9.138004961410270965 ) ) ;
#12818=CARTESIAN_POINT ( 'NONE',  ( -6.057079549204054558, 5.470993133660704721, -18.46346298046971768 ) ) ;
#12821=CARTESIAN_POINT ( 'NONE',  ( 0.3676999524040323597, -18.60775935196367925, 39.99627326667132365 ) ) ;
#12822=EDGE_LOOP ( 'NONE', ( #40863, #20372, #46472, #50472 ) ) ;
#12827=CARTESIAN_POINT ( 'NONE',  ( 0.6000166863083090663, 17.45040302316585112, 45.90541270958728148 ) ) ;
#12847=CARTESIAN_POINT ( 'NONE',  ( -6.063463321072276813, -4.269814012169966588, 18.77735712982385863 ) ) ;
#12851=AXIS2_PLACEMENT_3D ( 'NONE', #43854, #34742, #897 ) ;
#12852=CARTESIAN_POINT ( 'NONE',  ( -2.601141883200662974, -13.21958573851844143, -6.930943685483855532 ) ) ;
#12857=EDGE_CURVE ( 'NONE', #30264, #28594, #41999, .T. ) ;
#12864=ORIENTED_EDGE ( 'NONE', *, *, #7979, .T. ) ;
#12865=CARTESIAN_POINT ( 'NONE',  ( 4.694002226626920127, 18.13772657221557694, -41.82472529781492909 ) ) ;
#12869=CARTESIAN_POINT ( 'NONE',  ( -6.063463321072276813, 7.780528881867387447, -17.61487504349370425 ) ) ;
#12881=CARTESIAN_POINT ( 'NONE',  ( 0.6029443199889047422, -49.10740923581496986, 2.443331554578143732E-05 ) ) ;
#12884=EDGE_CURVE ( 'NONE', #38412, #27210, #16566, .T. ) ;
#12894=ORIENTED_EDGE ( 'NONE', *, *, #56986, .F. ) ;
#12896=CARTESIAN_POINT ( 'NONE',  ( 0.1135584504625008623, 3.806764484040820129, 43.95976110374461854 ) ) ;
#12899=CARTESIAN_POINT ( 'NONE',  ( 0.6039202388192953519, -49.10736577297868166, 0.1741829149863364512 ) ) ;
#12901=CARTESIAN_POINT ( 'NONE',  ( 0.3676999524040366896, -11.75791688508890331, 42.51707861373098041 ) ) ;
#12903=ORIENTED_EDGE ( 'NONE', *, *, #58325, .T. ) ;
#12906=EDGE_CURVE ( 'NONE', #6528, #16502, #2216, .T. ) ;
#12909=CARTESIAN_POINT ( 'NONE',  ( 0.1154773475650540671, 44.04468435281491878, 2.647529094650572734 ) ) ;
#12910=ORIENTED_EDGE ( 'NONE', *, *, #53724, .T. ) ;
#12918=CARTESIAN_POINT ( 'NONE',  ( 0.1152809850208375148, 43.35225507947838253, -8.217497308402093026 ) ) ;
#12921=CARTESIAN_POINT ( 'NONE',  ( 0.3676999524040366896, -38.02468164711607557, 22.36233818182511257 ) ) ;
#12925=EDGE_CURVE ( 'NONE', #7194, #35355, #12034, .T. ) ;
#12926=ORIENTED_EDGE ( 'NONE', *, *, #10573, .T. ) ;
#12928=( BOUNDED_SURFACE ( )  B_SPLINE_SURFACE ( 3, 1, ( 
 ( #34075, #34677 ),
 ( #19658, #517 ),
 ( #4046, #53741 ),
 ( #58142, #43475 ) ),
 .UNSPECIFIED., .F., .F., .F. ) 
 B_SPLINE_SURFACE_WITH_KNOTS ( ( 4, 4 ),
 ( 2, 2 ),
 ( 0.000000000000000000, 1.000000000000000000 ),
 ( 0.000000000000000000, 1.000000000000000000 ),
 .UNSPECIFIED. ) 
 GEOMETRIC_REPRESENTATION_ITEM ( )  RATIONAL_B_SPLINE_SURFACE ( (
 ( 1.000000000000000000, 1.000000000000000000),
 ( 0.9953485035131437453, 0.8621029689291523912),
 ( 0.9953485035131437453, 0.8621029689291523912),
 ( 1.000000000000000000, 1.000000000000000000) ) ) 
 REPRESENTATION_ITEM ( '' )  SURFACE ( )  );
#12935=CARTESIAN_POINT ( 'NONE',  ( 0.6039202388192953519, 46.55074123944901743, -15.63944381705600684 ) ) ;
#12938=ORIENTED_EDGE ( 'NONE', *, *, #22213, .F. ) ;
#12943=B_SPLINE_CURVE_WITH_KNOTS ( 'NONE', 3,
 ( #6704, #54637, #50268, #30531, #21767, #17082 ),
 .UNSPECIFIED., .F., .F.,
 ( 4, 2, 4 ),
 ( 0.000000000000000000, 0.0002447195606305745293, 0.0004894391212611490585 ),
 .UNSPECIFIED. ) ;
#12945=CARTESIAN_POINT ( 'NONE',  ( 4.975610109902397937, 48.58133226360784818, -5.683622315980244366 ) ) ;
#12951=CARTESIAN_POINT ( 'NONE',  ( 0.6253024248130456542, 43.94107594871452704, 21.92318571483041012 ) ) ;
#12958=CARTESIAN_POINT ( 'NONE',  ( 4.553261556744875094, -20.51767157960516741, 38.84024612145369559 ) ) ;
#12972=VERTEX_POINT ( 'NONE', #14124 ) ;
#12973=ORIENTED_EDGE ( 'NONE', *, *, #18619, .F. ) ;
#12975=CARTESIAN_POINT ( 'NONE',  ( 0.6252788684277207354, 5.398452368597682849, 48.80882136661001880 ) ) ;
#12977=VERTEX_POINT ( 'NONE', #37946 ) ;
#12979=ADVANCED_FACE ( 'NONE', ( #9088 ), #12726, .F. ) ;
#12985=B_SPLINE_CURVE_WITH_KNOTS ( 'NONE', 3,
 ( #14110, #9376, #28480, #33518, #9686, #11242, #54121, #20949, #15336, #49754, #44779, #1820, #6498, #44477, #53212, #35065, #43860, #10628, #6813 ),
 .UNSPECIFIED., .F., .F.,
 ( 4, 3, 3, 3, 3, 3, 4 ),
 ( 0.000000000000000000, 0.0002612768053151712211, 0.0003919133833142921181, 0.0005225499612322617293, 0.0006531865391693382353, 0.0008112755173415196405, 0.0009693688056799733320 ),
 .UNSPECIFIED. ) ;
#13000=CARTESIAN_POINT ( 'NONE',  ( 0.8753041380234530822, -31.30612550145381334, -37.82941757363182234 ) ) ;
#13001=CARTESIAN_POINT ( 'NONE',  ( -2.601141883200662974, 6.503674101141085018, -13.43494140871240639 ) ) ;
#13007=CARTESIAN_POINT ( 'NONE',  ( -6.057079549204054558, 3.065021114850809081, -19.01149327815301504 ) ) ;
#13010=CARTESIAN_POINT ( 'NONE',  ( 0.3676999524040366896, 44.06746933160592050, 2.002181318165502599 ) ) ;
#13011=CARTESIAN_POINT ( 'NONE',  ( -6.072942160501519027, 12.01744408475444992, -15.04610248399301398 ) ) ;
#13012=CARTESIAN_POINT ( 'NONE',  ( 0.8744876279028263033, -24.68559978112701714, -42.43785119236734715 ) ) ;
#13013=( BOUNDED_SURFACE ( )  B_SPLINE_SURFACE ( 3, 1, ( 
 ( #36872, #3614 ),
 ( #41262, #50320 ),
 ( #36558, #8634 ),
 ( #7390, #40966 ) ),
 .UNSPECIFIED., .F., .F., .F. ) 
 B_SPLINE_SURFACE_WITH_KNOTS ( ( 4, 4 ),
 ( 2, 2 ),
 ( 0.000000000000000000, 1.000000000000000000 ),
 ( 0.000000000000000000, 1.000000000000000000 ),
 .UNSPECIFIED. ) 
 GEOMETRIC_REPRESENTATION_ITEM ( )  RATIONAL_B_SPLINE_SURFACE ( (
 ( 1.000000000000000000, 1.000000000000000000),
 ( 0.9953485035131437453, 0.8621029689291515030),
 ( 0.9953485035131437453, 0.8621029689291515030),
 ( 1.000000000000000000, 1.000000000000000000) ) ) 
 REPRESENTATION_ITEM ( '' )  SURFACE ( )  );
#13014=ORIENTED_EDGE ( 'NONE', *, *, #31196, .T. ) ;
#13015=CARTESIAN_POINT ( 'NONE',  ( 0.1129192098497447394, -12.08918212651769686, 42.43587472053614817 ) ) ;
#13019=CARTESIAN_POINT ( 'NONE',  ( 0.6026112563231247332, -42.87342733809637707, 23.94598553388809492 ) ) ;
#13029=CARTESIAN_POINT ( 'NONE',  ( 0.1145239942831223490, -35.16543549781121669, -26.65215989284831011 ) ) ;
#13031=CARTESIAN_POINT ( 'NONE',  ( 0.7413678028165010536, -23.65209160105352382, -37.21645677204664793 ) ) ;
#13032=CARTESIAN_POINT ( 'NONE',  ( 0.1129192098497455998, -38.68182264534154058, 21.22895156665764915 ) ) ;
#13037=CARTESIAN_POINT ( 'NONE',  ( 0.6029443199889047422, -1.573945515703186748, 49.08217942764971298 ) ) ;
#13039=CARTESIAN_POINT ( 'NONE',  ( 0.5997462898726536595, -45.31995669577361951, 18.91172004968117903 ) ) ;
#13041=VERTEX_POINT ( 'NONE', #24115 ) ;
#13043=CARTESIAN_POINT ( 'NONE',  ( 4.975610109902397937, -27.50982196586548412, -40.44328253918266824 ) ) ;
#13045=EDGE_CURVE ( 'NONE', #45706, #11842, #53809, .T. ) ;
#13047=ORIENTED_EDGE ( 'NONE', *, *, #32341, .F. ) ;
#13054=CARTESIAN_POINT ( 'NONE',  ( 1.834102595619085507, 37.61045569671126998, 22.92708806506842834 ) ) ;
#13060=CARTESIAN_POINT ( 'NONE',  ( -6.077587904424778920, 12.00112336472187025, -15.05885318935865236 ) ) ;
#13061=ORIENTED_EDGE ( 'NONE', *, *, #24473, .F. ) ;
#13062=CARTESIAN_POINT ( 'NONE',  ( -6.077587904424778920, 17.85108912406252912, -7.220432014686311462 ) ) ;
#13066=ORIENTED_EDGE ( 'NONE', *, *, #14558, .F. ) ;
#13068=CARTESIAN_POINT ( 'NONE',  ( 4.553261556744875094, 43.92594400279101308, 0.2258523573163287723 ) ) ;
#13069=DIRECTION ( 'NONE',  ( 1.000000000000000000, 0.000000000000000000, 0.000000000000000000 ) ) ;
#13072=VECTOR ( 'NONE', #39176, 1000.000000000000114 ) ;
#13076=ORIENTED_EDGE ( 'NONE', *, *, #181, .T. ) ;
#13082=B_SPLINE_CURVE_WITH_KNOTS ( 'NONE', 3,
 ( #38182, #52863, #39107, #24672 ),
 .UNSPECIFIED., .F., .F.,
 ( 4, 4 ),
 ( 0.000000000000000000, 0.004444103432399267896 ),
 .UNSPECIFIED. ) ;
#13083=CARTESIAN_POINT ( 'NONE',  ( 0.1158816050234198897, -27.51540855527343865, -34.49412027203399589 ) ) ;
#13084=CARTESIAN_POINT ( 'NONE',  ( 0.1147471544378677183, -27.26760129513139930, 34.69049016781103489 ) ) ;
#13088=CARTESIAN_POINT ( 'NONE',  ( 0.8744876279028263033, -38.80702141274021955, -30.07266432244763621 ) ) ;
#13090=LINE ( 'NONE', #23096, #57928 ) ;
#13091=DIRECTION ( 'NONE',  ( -0.1011922191286467043, -0.08272061902645741482, -0.9914219253051141933 ) ) ;
#13097=CARTESIAN_POINT ( 'NONE',  ( 4.335381028904216727, 45.77817886910109024, -17.43889867775290625 ) ) ;
#13098=CARTESIAN_POINT ( 'NONE',  ( 0.2940135542858993145, -34.86814986296420926, 27.02688797892369976 ) ) ;
#13099=CARTESIAN_POINT ( 'NONE',  ( 0.1368894036331293751, 19.84133884650108115, -39.41043768726326135 ) ) ;
#13102=DIRECTION ( 'NONE',  ( 0.09722883295013592941, -0.9607671998409492709, 0.2597555422949351933 ) ) ;
#13108=CARTESIAN_POINT ( 'NONE',  ( 0.6039202388192952409, 27.95228209933733865, 40.37615185091387815 ) ) ;
#13109=CARTESIAN_POINT ( 'NONE',  ( 4.834790513006555379, -4.995710817784499547, -46.98544683568999858 ) ) ;
#13111=CARTESIAN_POINT ( 'NONE',  ( 4.553261556744875094, -25.31600221269659201, 35.89762663172006540 ) ) ;
#13116=CARTESIAN_POINT ( 'NONE',  ( 0.9268187852002115479, 16.15318250627089469, 41.02229915335962573 ) ) ;
#13117=LINE ( 'NONE', #31906, #36480 ) ;
#13125=CARTESIAN_POINT ( 'NONE',  ( 3.390910168358336918, 28.07862399391833819, -33.84801340022468708 ) ) ;
#13129=FACE_OUTER_BOUND ( 'NONE', #24353, .T. ) ;
#13130=B_SPLINE_CURVE_WITH_KNOTS ( 'NONE', 3,
 ( #52349, #51734, #8829, #42370, #39219, #19177, #53886, #33580, #34198, #53571, #24472, #10694, #58270, #58578, #14780, #10387, #15090, #652, #33893 ),
 .UNSPECIFIED., .F., .F.,
 ( 4, 3, 3, 3, 3, 3, 4 ),
 ( 0.000000000000000000, 0.0002612768053151668301, 0.0003919133833142900581, 0.0005225499612322602114, 0.0006531865391693349827, 0.0008112755173415168216, 0.0009693688056799697542 ),
 .UNSPECIFIED. ) ;
#13132=CARTESIAN_POINT ( 'NONE',  ( 1.479689385636123067, -26.54425251156986576, 35.17081892520713637 ) ) ;
#13138=CARTESIAN_POINT ( 'NONE',  ( -6.072942160501519027, -14.65319399899845543, -12.49352103759128596 ) ) ;
#13142=B_SPLINE_CURVE_WITH_KNOTS ( 'NONE', 3,
 ( #13859, #38591, #33576, #28537, #47978, #28855, #57640, #4708, #14775, #33887, #52650, #5029, #24154, #326, #52964, #29165, #19787, #5335, #52035 ),
 .UNSPECIFIED., .F., .F.,
 ( 4, 3, 3, 3, 3, 3, 4 ),
 ( 1.355252715606880543E-20, 0.0002612768053151681854, 0.0003919133833142889739, 0.0005225499612322556577, 0.0006531865391693332480, 0.0008112755173415167132, 0.0009693688056799707299 ),
 .UNSPECIFIED. ) ;
#13144=CARTESIAN_POINT ( 'NONE',  ( -6.077587904424778920, 13.83688374988438241, -13.39166417911216911 ) ) ;
#13155=ORIENTED_EDGE ( 'NONE', *, *, #181, .F. ) ;
#13156=CARTESIAN_POINT ( 'NONE',  ( 0.5549461598389365813, 5.107917383263871791, 43.80784034248385694 ) ) ;
#13160=ORIENTED_EDGE ( 'NONE', *, *, #57829, .F. ) ;
#13168=ORIENTED_EDGE ( 'NONE', *, *, #58806, .T. ) ;
#13169=CARTESIAN_POINT ( 'NONE',  ( 4.694002226626921015, 36.74006825548360666, -26.98985283451062855 ) ) ;
#13173=CARTESIAN_POINT ( 'NONE',  ( 3.727782113643637096, -39.30990089286451195, -19.68526016335944107 ) ) ;
#13174=CARTESIAN_POINT ( 'NONE',  ( 3.894904216938897878, -41.52606794860570005, -14.41214811206100599 ) ) ;
#13186=CARTESIAN_POINT ( 'NONE',  ( -6.063463321072276813, -12.95783560055426697, -14.24482183210721509 ) ) ;
#13188=CARTESIAN_POINT ( 'NONE',  ( -6.063463321072276813, 19.25669258467947387, -0.01559418547018221260 ) ) ;
#13189=CARTESIAN_POINT ( 'NONE',  ( 3.221118495291108719, 23.59276081282231274, -37.12334921435170543 ) ) ;
#13190=DIRECTION ( 'NONE',  ( 0.000000000000000000, 0.000000000000000000, -1.000000000000000000 ) ) ;
#13192=ORIENTED_EDGE ( 'NONE', *, *, #20997, .T. ) ;
#13202=CARTESIAN_POINT ( 'NONE',  ( 0.8753041380234471980, 49.05142151719384458, -2.257515230414626206 ) ) ;
#13207=CARTESIAN_POINT ( 'NONE',  ( -6.077587904424778920, -8.901182807328959612, 17.07527352707539592 ) ) ;
#13208=VERTEX_POINT ( 'NONE', #38243 ) ;
#13217=CARTESIAN_POINT ( 'NONE',  ( 0.7413678028165008316, -37.95542240817268009, 22.44709338839723500 ) ) ;
#13219=VERTEX_POINT ( 'NONE', #5591 ) ;
#13225=EDGE_CURVE ( 'NONE', #27212, #9094, #22434, .T. ) ;
#13230=DIRECTION ( 'NONE',  ( -1.000000000000000000, -0.000000000000000000, -0.000000000000000000 ) ) ;
#13236=LINE ( 'NONE', #14172, #16963 ) ;
#13256=CARTESIAN_POINT ( 'NONE',  ( 3.240649175237394708, -16.12010403042567575, -40.93173785030273137 ) ) ;
#13263=ORIENTED_EDGE ( 'NONE', *, *, #44191, .T. ) ;
#13272=ORIENTED_EDGE ( 'NONE', *, *, #42970, .T. ) ;
#13273=ORIENTED_EDGE ( 'NONE', *, *, #34200, .T. ) ;
#13279=CARTESIAN_POINT ( 'NONE',  ( 0.8744876279028306332, -26.20733431478126008, -41.51536677536140729 ) ) ;
#13281=CIRCLE ( 'NONE', #51264, 43.92652462719577500 ) ;
#13284=( BOUNDED_SURFACE ( )  B_SPLINE_SURFACE ( 3, 1, ( 
 ( #20510, #15817 ),
 ( #34932, #48701 ),
 ( #39323, #11420 ),
 ( #10811, #11120 ) ),
 .UNSPECIFIED., .F., .F., .F. ) 
 B_SPLINE_SURFACE_WITH_KNOTS ( ( 4, 4 ),
 ( 2, 2 ),
 ( 0.000000000000000000, 1.000000000000000000 ),
 ( 0.000000000000000000, 1.000000000000000000 ),
 .UNSPECIFIED. ) 
 GEOMETRIC_REPRESENTATION_ITEM ( )  RATIONAL_B_SPLINE_SURFACE ( (
 ( 1.000000000000000000, 1.000000000000000000),
 ( 0.9953485035131437453, 0.8621029689291523912),
 ( 0.9953485035131437453, 0.8621029689291523912),
 ( 1.000000000000000000, 1.000000000000000000) ) ) 
 REPRESENTATION_ITEM ( '' )  SURFACE ( )  );
#13288=ADVANCED_FACE ( 'NONE', ( #1115 ), #20859, .F. ) ;
#13289=CARTESIAN_POINT ( 'NONE',  ( -6.078726893082806448, 0.6205993875984882058, -19.24600991553398188 ) ) ;
#13290=ORIENTED_EDGE ( 'NONE', *, *, #10760, .F. ) ;
#13294=CARTESIAN_POINT ( 'NONE',  ( 0.5997462898726536595, -30.20781297212619165, 38.71743361310707598 ) ) ;
#13295=CARTESIAN_POINT ( 'NONE',  ( 1.112077966505211624, -43.83978140853107419, -4.593897166977904511 ) ) ;
#13307=CARTESIAN_POINT ( 'NONE',  ( 4.335381028904216727, -28.85261930641616956, 39.58892783119247127 ) ) ;
#13311=CARTESIAN_POINT ( 'NONE',  ( 4.975610109902397937, -46.59897809419055648, 14.86555238512586463 ) ) ;
#13312=CARTESIAN_POINT ( 'NONE',  ( 4.694002226626921015, 7.615834493547636974, -44.94756763622505247 ) ) ;
#13330=CARTESIAN_POINT ( 'NONE',  ( 0.1129192098497455998, -1.898585089632445433, 44.08341142019953907 ) ) ;
#13337=DIRECTION ( 'NONE',  ( 0.1011922191286468015, -0.1460712814909308488, 0.9840850143719378496 ) ) ;
#13338=CARTESIAN_POINT ( 'NONE',  ( 0.1368894036331279040, -35.73859056403340873, -25.87690998592599456 ) ) ;
#13345=VERTEX_POINT ( 'NONE', #4721 ) ;
#13346=CARTESIAN_POINT ( 'NONE',  ( 0.5997462898726536595, 11.43624519451716992, -47.75734421002901797 ) ) ;
#13354=CARTESIAN_POINT ( 'NONE',  ( 4.553261556744875094, 38.16266689001181334, 21.75202109381179483 ) ) ;
#13359=CARTESIAN_POINT ( 'NONE',  ( 0.7044674535452954967, 17.74870190915637025, -45.79067921914693073 ) ) ;
#13368=EDGE_CURVE ( 'NONE', #6110, #22076, #37637, .T. ) ;
#13374=FACE_OUTER_BOUND ( 'NONE', #10177, .T. ) ;
#13375=EDGE_CURVE ( 'NONE', #2228, #51399, #24166, .T. ) ;
#13376=DIRECTION ( 'NONE',  ( 0.000000000000000000, 0.000000000000000000, 1.000000000000000000 ) ) ;
#13381=CARTESIAN_POINT ( 'NONE',  ( 3.390910168358336918, 43.50063370814297770, 6.464673504796084380 ) ) ;
#13382=CARTESIAN_POINT ( 'NONE',  ( 0.5997462898726536595, -25.00873172704263325, 42.26245340191598387 ) ) ;
#13399=CARTESIAN_POINT ( 'NONE',  ( 0.6000166863083106206, -13.47152005829862276, 47.22649287240490423 ) ) ;
#13401=ORIENTED_EDGE ( 'NONE', *, *, #20926, .F. ) ;
#13402=FACE_OUTER_BOUND ( 'NONE', #6526, .T. ) ;
#13407=CARTESIAN_POINT ( 'NONE',  ( -6.078726893082806448, -4.288195875146425529, -18.77246434022707788 ) ) ;
#13409=CARTESIAN_POINT ( 'NONE',  ( 0.1129192098497447394, 39.54191224844646513, -19.58032082273713570 ) ) ;
#13413=ORIENTED_EDGE ( 'NONE', *, *, #526, .T. ) ;
#13419=CARTESIAN_POINT ( 'NONE',  ( 4.226256110419179812, 31.85118181789737335, -30.27093435608539096 ) ) ;
#13420=EDGE_CURVE ( 'NONE', #32705, #53183, #55614, .T. ) ;
#13423=CARTESIAN_POINT ( 'NONE',  ( 5.901764892641288895, -16.87177170878354104, 45.97102116384157000 ) ) ;
#13424=CARTESIAN_POINT ( 'NONE',  ( 1.296416391601052487, 28.79733114477846101, -33.36197076034524400 ) ) ;
#13426=ORIENTED_EDGE ( 'NONE', *, *, #34759, .T. ) ;
#13435=ORIENTED_EDGE ( 'NONE', *, *, #39603, .F. ) ;
#13436=CARTESIAN_POINT ( 'NONE',  ( 4.975610109902397937, -10.32228546579698403, -47.81108480154335183 ) ) ;
#13442=CARTESIAN_POINT ( 'NONE',  ( 0.5997462898726536595, -39.04071682475809268, 29.78882441375220580 ) ) ;
#13443=EDGE_CURVE ( 'NONE', #1361, #462, #30633, .T. ) ;
#13452=EDGE_CURVE ( 'NONE', #11409, #21723, #54579, .T. ) ;
#13469=CARTESIAN_POINT ( 'NONE',  ( 2.879087469061463178, -34.20017424174309895, 27.68482903356619929 ) ) ;
#13471=ADVANCED_FACE ( 'NONE', ( #21953 ), #36359, .F. ) ;
#13472=ORIENTED_EDGE ( 'NONE', *, *, #42954, .F. ) ;
#13476=CARTESIAN_POINT ( 'NONE',  ( 1.657374760986086493, 42.98942532183876608, -9.633263089436098880 ) ) ;
#13479=CARTESIAN_POINT ( 'NONE',  ( 3.221118495291108719, -41.44247251342186189, -14.74051870308588441 ) ) ;
#13483=CARTESIAN_POINT ( 'NONE',  ( -6.079354080745853928, -19.21634661680158374, -1.234899976152050272 ) ) ;
#13485=CARTESIAN_POINT ( 'NONE',  ( 0.6039202388192952409, -8.009480623390196286, 48.45009734760630948 ) ) ;
#13486=CARTESIAN_POINT ( 'NONE',  ( 4.975610109902397937, -5.269241389991576874, 48.62802178077752302 ) ) ;
#13495=FACE_OUTER_BOUND ( 'NONE', #2417, .T. ) ;
#13500=EDGE_LOOP ( 'NONE', ( #17290, #5080, #3560, #11939 ) ) ;
#13504=CARTESIAN_POINT ( 'NONE',  ( 0.1149546198390367924, 4.509486755524008572, -43.89317821968435851 ) ) ;
#13508=VERTEX_POINT ( 'NONE', #16960 ) ;
#13513=CARTESIAN_POINT ( 'NONE',  ( -6.063463321072276813, -8.893131869789778321, 17.08018319649995220 ) ) ;
#13517=B_SPLINE_CURVE_WITH_KNOTS ( 'NONE', 3,
 ( #11001, #53878, #52961, #5632, #29779, #5941, #30083, #48279, #20698, #34809, #49195, #39520, #15393, #24151, #6244, #19471, #9745, #643, #48890 ),
 .UNSPECIFIED., .F., .F.,
 ( 4, 3, 3, 3, 3, 3, 4 ),
 ( 9.813227601316442057E-18, 0.0002612768053151707875, 0.0003919133833142900581, 0.0005225499612322555493, 0.0006531865391693305375, 0.0008112755173415146532, 0.0009693688056799714889 ),
 .UNSPECIFIED. ) ;
#13534=CARTESIAN_POINT ( 'NONE',  ( 4.553261556744875094, -33.30082861731464305, -28.64601855797546648 ) ) ;
#13541=CARTESIAN_POINT ( 'NONE',  ( 0.6039202388192953519, 48.23508111734878412, 9.216325865103440762 ) ) ;
#13544=DIRECTION ( 'NONE',  ( 0.000000000000000000, 0.000000000000000000, -1.000000000000000000 ) ) ;
#13549=CARTESIAN_POINT ( 'NONE',  ( 0.8744876279028263033, 40.65405044375290800, 27.52450240960382644 ) ) ;
#13552=CARTESIAN_POINT ( 'NONE',  ( 0.1365634738349449651, -41.13330695003092785, 15.96601637785038541 ) ) ;
#13561=CARTESIAN_POINT ( 'NONE',  ( 2.359973842542475886, -21.51797753960544313, 38.40719382143839056 ) ) ;
#13567=ORIENTED_EDGE ( 'NONE', *, *, #25584, .T. ) ;
#13569=B_SPLINE_CURVE_WITH_KNOTS ( 'NONE', 3,
 ( #36000, #50983, #35689, #60369 ),
 .UNSPECIFIED., .F., .F.,
 ( 4, 4 ),
 ( 0.000000000000000000, 0.004444103432399265294 ),
 .UNSPECIFIED. ) ;
#13570=CARTESIAN_POINT ( 'NONE',  ( 0.6021448801613057400, -39.51107342597083516, 29.16189663506967378 ) ) ;
#13575=CARTESIAN_POINT ( 'NONE',  ( 0.3676999524040366896, -31.10876963919527682, 31.27610965031171020 ) ) ;
#13588=CARTESIAN_POINT ( 'NONE',  ( -6.079354080745853928, -17.34954932540448524, 8.353807123313236715 ) ) ;
#13590=CARTESIAN_POINT ( 'NONE',  ( 0.8753041380234465318, 33.66554281472474486, -35.74590263041227445 ) ) ;
#13591=DIRECTION ( 'NONE',  ( 0.1011922191286468015, -0.9172554449906691332, 0.3852305587862797642 ) ) ;
#13616=CARTESIAN_POINT ( 'NONE',  ( -6.077587904424778920, 13.83688374988418879, 13.39166417911236984 ) ) ;
#13617=AXIS2_PLACEMENT_3D ( 'NONE', #19119, #39156, #54947 ) ;
#13619=EDGE_LOOP ( 'NONE', ( #47269, #10872, #46471, #53095 ) ) ;
#13624=CARTESIAN_POINT ( 'NONE',  ( 4.834790513006555379, -36.27562111512906284, -30.27653635467542870 ) ) ;
#13626=CARTESIAN_POINT ( 'NONE',  ( 0.1154773475650540671, -18.02505553582892972, -40.27457017742589329 ) ) ;
#13637=CARTESIAN_POINT ( 'NONE',  ( 0.1129192098497447394, -35.64954734424924965, -26.00118385641864194 ) ) ;
#13639=CARTESIAN_POINT ( 'NONE',  ( 0.08486401232817714080, 12.80000000000000071, 3.000000000000000000 ) ) ;
#13646=B_SPLINE_CURVE_WITH_KNOTS ( 'NONE', 3,
 ( #32101, #51182, #27385, #42143, #60890, #12382 ),
 .UNSPECIFIED., .F., .F.,
 ( 4, 2, 4 ),
 ( 2.197222038435329413E-17, 0.0002293755540694313185, 0.0004587511081388406277 ),
 .UNSPECIFIED. ) ;
#13649=EDGE_LOOP ( 'NONE', ( #19310, #6375, #49697, #52186 ) ) ;
#13651=CARTESIAN_POINT ( 'NONE',  ( 0.1152809850208375148, -7.260492202596367406, 43.52275882186000189 ) ) ;
#13657=DIRECTION ( 'NONE',  ( 0.000000000000000000, 0.000000000000000000, 1.000000000000000000 ) ) ;
#13658=CARTESIAN_POINT ( 'NONE',  ( 0.5980271706414734822, -8.528665270201470250, -48.36642545765111123 ) ) ;
#13661=( BOUNDED_SURFACE ( )  B_SPLINE_SURFACE ( 3, 1, ( 
 ( #26881, #46313 ),
 ( #55672, #27189 ),
 ( #46019, #13108 ),
 ( #45697, #59769 ) ),
 .UNSPECIFIED., .F., .F., .F. ) 
 B_SPLINE_SURFACE_WITH_KNOTS ( ( 4, 4 ),
 ( 2, 2 ),
 ( 0.000000000000000000, 1.000000000000000000 ),
 ( 0.000000000000000000, 1.000000000000000000 ),
 .UNSPECIFIED. ) 
 GEOMETRIC_REPRESENTATION_ITEM ( )  RATIONAL_B_SPLINE_SURFACE ( (
 ( 1.000000000000000000, 1.000000000000000000),
 ( 0.9754377213608244057, 0.9999580625633939235),
 ( 0.9754377213608244057, 0.9999580625633939235),
 ( 1.000000000000000000, 1.000000000000000000) ) ) 
 REPRESENTATION_ITEM ( '' )  SURFACE ( )  );
#13667=CARTESIAN_POINT ( 'NONE',  ( 1.657374760986086271, -40.35518271633839049, 17.67341719032251390 ) ) ;
#13671=CARTESIAN_POINT ( 'NONE',  ( 0.6028777368367060907, 49.00087957688494811, 3.233207386279532969 ) ) ;
#13673=ADVANCED_FACE ( 'NONE', ( #51982 ), #46407, .F. ) ;
#13680=CARTESIAN_POINT ( 'NONE',  ( 3.559346040607745287, 38.68187159388032370, -20.90796717848347441 ) ) ;
#13685=CARTESIAN_POINT ( 'NONE',  ( -6.078075953587585900, -14.65899360350508296, 12.48635578459675699 ) ) ;
#13686=EDGE_CURVE ( 'NONE', #4961, #37380, #1437, .T. ) ;
#13699=CARTESIAN_POINT ( 'NONE',  ( 4.553261556744873317, 31.39705178283683296, -30.72075365562339755 ) ) ;
#13704=CARTESIAN_POINT ( 'NONE',  ( 0.1147471544378677183, 33.39615026987465995, -28.83833101317058123 ) ) ;
#13712=ORIENTED_EDGE ( 'NONE', *, *, #55036, .F. ) ;
#13715=CARTESIAN_POINT ( 'NONE',  ( 0.1119898979215351309, -35.02332270898327948, 26.83893020733585644 ) ) ;
#13723=CARTESIAN_POINT ( 'NONE',  ( -6.078075953587585900, 12.01009662667731170, -15.05166945109445820 ) ) ;
#13724=CARTESIAN_POINT ( 'NONE',  ( -6.079354080745853928, 13.83333621897982368, 13.39521423124031330 ) ) ;
#13728=DIRECTION ( 'NONE',  ( 0.1011922191286468153, -0.3909116750758017123, 0.9148487290679540029 ) ) ;
#13736=VECTOR ( 'NONE', #45730, 1000.000000000000114 ) ;
#13739=( BOUNDED_SURFACE ( )  B_SPLINE_SURFACE ( 3, 1, ( 
 ( #45712, #44488 ),
 ( #11573, #11254 ),
 ( #1517, #27819 ),
 ( #12818, #13423 ) ),
 .UNSPECIFIED., .F., .F., .F. ) 
 B_SPLINE_SURFACE_WITH_KNOTS ( ( 4, 4 ),
 ( 2, 2 ),
 ( 0.000000000000000000, 1.000000000000000000 ),
 ( 0.000000000000000000, 1.000000000000000000 ),
 .UNSPECIFIED. ) 
 GEOMETRIC_REPRESENTATION_ITEM ( )  RATIONAL_B_SPLINE_SURFACE ( (
 ( 1.000000000000000000, 1.000000000000000000),
 ( 0.7211978278499970862, 0.9934217856018976445),
 ( 0.7211978278499970862, 0.9934217856018976445),
 ( 1.000000000000000000, 1.000000000000000000) ) ) 
 REPRESENTATION_ITEM ( '' )  SURFACE ( )  );
#13740=ADVANCED_FACE ( 'NONE', ( #48227 ), #31952, .F. ) ;
#13744=VECTOR ( 'NONE', #14448, 1000.000000000000000 ) ;
#13745=EDGE_CURVE ( 'NONE', #10258, #54854, #26875, .T. ) ;
#13752=CARTESIAN_POINT ( 'NONE',  ( 2.706805983486680667, -26.12526257152286391, 35.41534651657021016 ) ) ;
#13759=ORIENTED_EDGE ( 'NONE', *, *, #27870, .T. ) ;
#13764=( BOUNDED_SURFACE ( )  B_SPLINE_SURFACE ( 3, 1, ( 
 ( #4925, #61932 ),
 ( #19994, #19364 ),
 ( #20291, #38483 ),
 ( #29982, #59092 ) ),
 .UNSPECIFIED., .F., .F., .F. ) 
 B_SPLINE_SURFACE_WITH_KNOTS ( ( 4, 4 ),
 ( 2, 2 ),
 ( 0.000000000000000000, 1.000000000000000000 ),
 ( 0.000000000000000000, 1.000000000000000000 ),
 .UNSPECIFIED. ) 
 GEOMETRIC_REPRESENTATION_ITEM ( )  RATIONAL_B_SPLINE_SURFACE ( (
 ( 1.000000000000000000, 1.000000000000000000),
 ( 0.9953485035131437453, 0.8621029689291515030),
 ( 0.9953485035131437453, 0.8621029689291515030),
 ( 1.000000000000000000, 1.000000000000000000) ) ) 
 REPRESENTATION_ITEM ( '' )  SURFACE ( )  );
#13767=VERTEX_POINT ( 'NONE', #24103 ) ;
#13769=ORIENTED_EDGE ( 'NONE', *, *, #27670, .F. ) ;
#13773=DIRECTION ( 'NONE',  ( 0.1011922191286468292, -0.7895409829358921439, 0.6052975888374620972 ) ) ;
#13779=CARTESIAN_POINT ( 'NONE',  ( 4.390527457369401532, 1.087462747309237310, 43.92041394843443669 ) ) ;
#13780=EDGE_CURVE ( 'NONE', #2209, #61591, #17899, .T. ) ;
#13781=EDGE_LOOP ( 'NONE', ( #16840, #4266, #60012, #43779 ) ) ;
#13782=ORIENTED_EDGE ( 'NONE', *, *, #26289, .T. ) ;
#13794=CARTESIAN_POINT ( 'NONE',  ( 0.5549461598389363592, -38.85229981621156270, -20.87382318738021425 ) ) ;
#13796=LINE ( 'NONE', #37924, #39890 ) ;
#13797=B_SPLINE_CURVE_WITH_KNOTS ( 'NONE', 3,
 ( #55864, #60554, #17989, #51161 ),
 .UNSPECIFIED., .F., .F.,
 ( 4, 4 ),
 ( 0.000000000000000000, 0.004444103432399267896 ),
 .UNSPECIFIED. ) ;
#13808=ADVANCED_FACE ( 'NONE', ( #42927 ), #52283, .T. ) ;
#13809=B_SPLINE_CURVE_WITH_KNOTS ( 'NONE', 3,
 ( #27781, #46915, #50648, #7733 ),
 .UNSPECIFIED., .F., .F.,
 ( 4, 4 ),
 ( 0.000000000000000000, 0.004444103432399267029 ),
 .UNSPECIFIED. ) ;
#13818=ADVANCED_FACE ( 'NONE', ( #48833 ), #38009, .F. ) ;
#13819=ORIENTED_EDGE ( 'NONE', *, *, #16358, .T. ) ;
#13822=DIRECTION ( 'NONE',  ( 1.000000000000000000, 0.000000000000000000, 0.000000000000000000 ) ) ;
#13824=CARTESIAN_POINT ( 'NONE',  ( 0.1140933569871964287, 4.614317128159971304, -43.88232021583037579 ) ) ;
#13826=CARTESIAN_POINT ( 'NONE',  ( 0.8753041380234530822, -45.84117188851829638, -17.59901382919792212 ) ) ;
#13829=CIRCLE ( 'NONE', #11816, 48.91267123290010943 ) ;
#13832=CARTESIAN_POINT ( 'NONE',  ( 0.8744876279028306332, -45.16590161815026505, 19.24555484778404590 ) ) ;
#13835=EDGE_LOOP ( 'NONE', ( #58299, #23501, #14318, #60604 ) ) ;
#13841=ORIENTED_EDGE ( 'NONE', *, *, #3602, .F. ) ;
#13845=CARTESIAN_POINT ( 'NONE',  ( -6.078726893082806448, -14.66462719274100479, -12.47969352855434444 ) ) ;
#13847=CARTESIAN_POINT ( 'NONE',  ( 0.1129192098497447394, -23.28677643606880565, -37.47903188453118162 ) ) ;
#13850=CARTESIAN_POINT ( 'NONE',  ( 0.1157991065609915993, -31.63987847695578992, -30.75484442329644352 ) ) ;
#13856=CARTESIAN_POINT ( 'NONE',  ( 0.6029443449137436017, 46.61938292040374421, -15.43284400569447001 ) ) ;
#13859=CARTESIAN_POINT ( 'NONE',  ( 0.1129192098497447394, 24.84520063729181416, -36.46461014569973713 ) ) ;
#13860=CARTESIAN_POINT ( 'NONE',  ( 0.3676999524040366896, -0.5887207181726206162, 44.10900124961835900 ) ) ;
#13861=DIRECTION ( 'NONE',  ( 0.000000000000000000, 0.000000000000000000, 1.000000000000000000 ) ) ;
#13870=AXIS2_PLACEMENT_3D ( 'NONE', #57159, #463, #4850 ) ;
#13882=EDGE_CURVE ( 'NONE', #40357, #18777, #46306, .T. ) ;
#13886=ORIENTED_EDGE ( 'NONE', *, *, #10119, .T. ) ;
#13894=CARTESIAN_POINT ( 'NONE',  ( 3.050102900204245682, -30.31663646424969372, 31.87988084470495664 ) ) ;
#13895=CARTESIAN_POINT ( 'NONE',  ( 0.5987334308729319599, 5.317554817413186363, 48.81891556900394846 ) ) ;
#13905=VERTEX_POINT ( 'NONE', #1507 ) ;
#13916=CARTESIAN_POINT ( 'NONE',  ( 0.2940135542859016460, -7.834165714058259233, -43.41504803931575651 ) ) ;
#13919=ORIENTED_EDGE ( 'NONE', *, *, #38543, .F. ) ;
#13923=CARTESIAN_POINT ( 'NONE',  ( 2.879087469061462734, 34.60096728254691101, 27.18225045678699203 ) ) ;
#13924=CARTESIAN_POINT ( 'NONE',  ( -2.739355103387248747, 4.908046929417360538, -14.09817868696712040 ) ) ;
#13929=CARTESIAN_POINT ( 'NONE',  ( 5.901764892641288895, -32.89013534638917235, 36.27989063290957006 ) ) ;
#13933=ORIENTED_EDGE ( 'NONE', *, *, #18689, .F. ) ;
#13936=CARTESIAN_POINT ( 'NONE',  ( 4.553261556744875094, -4.442710778082547662, 43.70128015019636791 ) ) ;
#13937=CONICAL_SURFACE ( 'NONE', #28882, 43.92652462719577500, 1.486293639869522343 ) ;
#13940=CARTESIAN_POINT ( 'NONE',  ( 0.2279481005628787582, 19.73059023567995141, 39.46146596395783490 ) ) ;
#13948=CARTESIAN_POINT ( 'NONE',  ( 5.901764892641288895, 39.21882766674634979, -29.32362569474874903 ) ) ;
#13954=CARTESIAN_POINT ( 'NONE',  ( 3.678834586032787790, -38.11572800053880883, -30.75392086575784489 ) ) ;
#13955=LINE ( 'NONE', #57127, #1389 ) ;
#13957=CARTESIAN_POINT ( 'NONE',  ( 0.5997462898726536595, -39.04071682475767346, -29.78882441375276358 ) ) ;
#13958=DIRECTION ( 'NONE',  ( 0.1011922191286468292, -0.7056551247449976971, 0.7012923639317212299 ) ) ;
#13968=CARTESIAN_POINT ( 'NONE',  ( 0.1129192098497447394, -35.64954734424924965, -26.00118385641864194 ) ) ;
#13969=VERTEX_POINT ( 'NONE', #7437 ) ;
#13971=AXIS2_PLACEMENT_3D ( 'NONE', #32036, #41758, #37671 ) ;
#13972=CARTESIAN_POINT ( 'NONE',  ( 0.1157991065609915576, -7.122568489526775792, 43.54550933965177251 ) ) ;
#13976=EDGE_LOOP ( 'NONE', ( #44625, #21183, #10908, #46865 ) ) ;
#13978=LINE ( 'NONE', #33081, #10147 ) ;
#13981=VERTEX_POINT ( 'NONE', #31582 ) ;
#13984=CARTESIAN_POINT ( 'NONE',  ( 2.299652685299202304, 23.81424953469105077, -42.86214231647340966 ) ) ;
#13985=CARTESIAN_POINT ( 'NONE',  ( 0.2940135542859017015, -44.10887657611353774, 0.8047085712246067057 ) ) ;
#13989=CARTESIAN_POINT ( 'NONE',  ( 4.553261556744875094, 40.63093864075490558, 16.69330377710913993 ) ) ;
#13990=ORIENTED_EDGE ( 'NONE', *, *, #37704, .F. ) ;
#13991=LINE ( 'NONE', #3925, #32879 ) ;
#13995=CARTESIAN_POINT ( 'NONE',  ( -6.077587904424778920, 17.84644683124306397, 7.231898567703008318 ) ) ;
#14000=CARTESIAN_POINT ( 'NONE',  ( 0.1152339509894530906, -44.12360796003454055, 0.2234077984745104495 ) ) ;
#14001=CARTESIAN_POINT ( 'NONE',  ( -6.078075953587585900, 18.62761703674207325, 4.879247665328402483 ) ) ;
#14003=ORIENTED_EDGE ( 'NONE', *, *, #50876, .T. ) ;
#14007=CARTESIAN_POINT ( 'NONE',  ( 0.6026777506516367566, -25.30784732013451688, 42.08395483623157673 ) ) ;
#14012=CARTESIAN_POINT ( 'NONE',  ( -6.078457390727109555, 19.25602481922002340, 0.004381676659707368741 ) ) ;
#14013=CARTESIAN_POINT ( 'NONE',  ( 4.553261556744875094, 0.000000000000000000, 0.000000000000000000 ) ) ;
#14014=EDGE_CURVE ( 'NONE', #55761, #41166, #16607, .T. ) ;
#14023=ADVANCED_FACE ( 'NONE', ( #3974 ), #17132, .F. ) ;
#14024=CARTESIAN_POINT ( 'NONE',  ( 0.6000166863083106206, -14.47337940799720002, 46.92914627628140067 ) ) ;
#14041=CARTESIAN_POINT ( 'NONE',  ( 4.553261556744875094, 40.80044851610500700, -16.27461110774390818 ) ) ;
#14042=VERTEX_POINT ( 'NONE', #50981 ) ;
#14046=CARTESIAN_POINT ( 'NONE',  ( -6.077587904424778920, 3.079371755031687474, -19.00824797261030241 ) ) ;
#14048=CARTESIAN_POINT ( 'NONE',  ( 0.7413678028165014977, 32.96453683174787130, -29.28865656254279060 ) ) ;
#14052=CARTESIAN_POINT ( 'NONE',  ( 0.6027444965799114707, -45.46931311909032303, -18.54939568734145894 ) ) ;
#14056=ADVANCED_FACE ( 'NONE', ( #37536 ), #47634, .F. ) ;
#14058=EDGE_LOOP ( 'NONE', ( #41407, #56849, #15286, #55870 ) ) ;
#14060=CARTESIAN_POINT ( 'NONE',  ( 3.727782113643637096, -25.70678629131670689, 35.66425261348605602 ) ) ;
#14065=VERTEX_POINT ( 'NONE', #3356 ) ;
#14071=ORIENTED_EDGE ( 'NONE', *, *, #32980, .T. ) ;
#14076=ORIENTED_EDGE ( 'NONE', *, *, #6532, .T. ) ;
#14082=VERTEX_POINT ( 'NONE', #46314 ) ;
#14083=CARTESIAN_POINT ( 'NONE',  ( -6.078457390727109555, -1.853383199521769331, 19.16662416163155314 ) ) ;
#14086=CARTESIAN_POINT ( 'NONE',  ( 0.1157991065609916270, -38.48609893810574789, 21.58153270887022046 ) ) ;
#14087=EDGE_LOOP ( 'NONE', ( #16335, #60573, #28777, #33435 ) ) ;
#14095=EDGE_CURVE ( 'NONE', #45275, #28349, #55921, .T. ) ;
#14101=CARTESIAN_POINT ( 'NONE',  ( 2.185380717157383135, 42.92198960651596451, -9.824592168906281842 ) ) ;
#14102=B_SPLINE_CURVE_WITH_KNOTS ( 'NONE', 3,
 ( #44752, #53788, #43839, #38823, #10294, #54407 ),
 .UNSPECIFIED., .F., .F.,
 ( 4, 2, 4 ),
 ( 1.355252715606880735E-18, 0.0002293801035737095346, 0.0004587602071474177140 ),
 .UNSPECIFIED. ) ;
#14110=CARTESIAN_POINT ( 'NONE',  ( 0.1129192098497447394, 19.97823103613683315, -39.34236993944178806 ) ) ;
#14111=CARTESIAN_POINT ( 'NONE',  ( 0.8744876279028306332, -45.83369275826206746, -17.59609782084448071 ) ) ;
#14114=CARTESIAN_POINT ( 'NONE',  ( 0.6000166863083106206, 22.25084548767560122, -43.78039923061506755 ) ) ;
#14123=CARTESIAN_POINT ( 'NONE',  ( 4.694002226626920127, -43.37309735483326278, -14.03777750551312664 ) ) ;
#14124=CARTESIAN_POINT ( 'NONE',  ( 4.975610109902397937, -10.32228546579698403, -47.81108480154335183 ) ) ;
#14126=( BOUNDED_SURFACE ( )  B_SPLINE_SURFACE ( 3, 1, ( 
 ( #32001, #13202 ),
 ( #17906, #61693 ),
 ( #23822, #61089 ),
 ( #42952, #37635 ) ),
 .UNSPECIFIED., .F., .F., .F. ) 
 B_SPLINE_SURFACE_WITH_KNOTS ( ( 4, 4 ),
 ( 2, 2 ),
 ( 0.000000000000000000, 1.000000000000000000 ),
 ( 0.000000000000000000, 1.000000000000000000 ),
 .UNSPECIFIED. ) 
 GEOMETRIC_REPRESENTATION_ITEM ( )  RATIONAL_B_SPLINE_SURFACE ( (
 ( 1.000000000000000000, 1.000000000000000000),
 ( 0.7211978278499970862, 0.9934217856018976445),
 ( 0.7211978278499970862, 0.9934217856018976445),
 ( 1.000000000000000000, 1.000000000000000000) ) ) 
 REPRESENTATION_ITEM ( '' )  SURFACE ( )  );
#14132=EDGE_LOOP ( 'NONE', ( #15590, #295, #36062, #37525 ) ) ;
#14133=CARTESIAN_POINT ( 'NONE',  ( 0.1145239942831223490, 4.561901227362215039, -43.88774929176096151 ) ) ;
#14140=VERTEX_POINT ( 'NONE', #16099 ) ;
#14142=CARTESIAN_POINT ( 'NONE',  ( 0.8744876279028263033, 48.01195819035220325, 10.25679877483054625 ) ) ;
#14143=ORIENTED_EDGE ( 'NONE', *, *, #27906, .F. ) ;
#14150=ORIENTED_EDGE ( 'NONE', *, *, #8729, .T. ) ;
#14152=CARTESIAN_POINT ( 'NONE',  ( -6.057079549204054558, 18.62501892953336835, 4.892841809650328777 ) ) ;
#14154=CARTESIAN_POINT ( 'NONE',  ( 0.7044674535452954967, -38.84805681606425054, -30.04382140185815331 ) ) ;
#14164=ORIENTED_EDGE ( 'NONE', *, *, #53999, .F. ) ;
#14166=CARTESIAN_POINT ( 'NONE',  ( -6.079354080745853928, -19.21634661680160505, 1.234899976151772716 ) ) ;
#14171=ORIENTED_EDGE ( 'NONE', *, *, #20124, .T. ) ;
#14172=CARTESIAN_POINT ( 'NONE',  ( -2.739355103387247858, 1.694972997839761186, -14.83154184458281755 ) ) ;
#14185=CARTESIAN_POINT ( 'NONE',  ( 4.975610109902397937, 35.53430708602585497, -33.61193875773584949 ) ) ;
#14188=CARTESIAN_POINT ( 'NONE',  ( 0.8753041380234524160, 44.61941359694259290, 20.49990873486889242 ) ) ;
#14195=CARTESIAN_POINT ( 'NONE',  ( 0.5980271706414734822, -34.78940872471004297, 34.66621241824281441 ) ) ;
#14200=CARTESIAN_POINT ( 'NONE',  ( 2.706805983486679335, 26.51819630001240569, 35.12209245352223519 ) ) ;
#14204=VERTEX_POINT ( 'NONE', #1349 ) ;
#14205=EDGE_CURVE ( 'NONE', #45637, #51265, #15181, .T. ) ;
#14207=VERTEX_POINT ( 'NONE', #34909 ) ;
#14209=CARTESIAN_POINT ( 'NONE',  ( -2.739355103387248747, -10.53896796905794986, 10.57249833758263513 ) ) ;
#14213=ORIENTED_EDGE ( 'NONE', *, *, #11620, .F. ) ;
#14214=CARTESIAN_POINT ( 'NONE',  ( 0.7044674535452954967, 33.63530026269786788, -35.78364569253756144 ) ) ;
#14216=FACE_OUTER_BOUND ( 'NONE', #380, .T. ) ;
#14224=CARTESIAN_POINT ( 'NONE',  ( 0.6016118706126977189, 46.49486210791674523, 15.80439345086480429 ) ) ;
#14225=CARTESIAN_POINT ( 'NONE',  ( -6.077587904424778920, -14.66646125808240164, -12.47761738310237334 ) ) ;
#14240=EDGE_CURVE ( 'NONE', #52565, #36974, #17669, .T. ) ;
#14260=CARTESIAN_POINT ( 'NONE',  ( 0.7948884756798507700, -13.13616255639797181, -47.30898305704783979 ) ) ;
#14263=CARTESIAN_POINT ( 'NONE',  ( -6.078726893082806448, 7.797636468844896918, -17.60655862934208216 ) ) ;
#14267=CARTESIAN_POINT ( 'NONE',  ( 0.6021447746440204973, 48.15123689037863386, -9.643626134143064021 ) ) ;
#14271=ORIENTED_EDGE ( 'NONE', *, *, #6040, .T. ) ;
#14272=EDGE_LOOP ( 'NONE', ( #15730, #43195, #29006, #53925 ) ) ;
#14273=CARTESIAN_POINT ( 'NONE',  ( 4.694002226626921015, -25.79840873770003284, -37.58625916540110978 ) ) ;
#14281=VECTOR ( 'NONE', #25378, 1000.000000000000114 ) ;
#14283=VERTEX_POINT ( 'NONE', #40856 ) ;
#14286=CARTESIAN_POINT ( 'NONE',  ( 0.8744876279028306332, -20.68330519280286239, -44.52584571550401193 ) ) ;
#14294=CARTESIAN_POINT ( 'NONE',  ( 5.901764892641288895, 19.78248028302103734, -44.79559064563790827 ) ) ;
#14308=EDGE_CURVE ( 'NONE', #31693, #40643, #52928, .T. ) ;
#14310=FACE_OUTER_BOUND ( 'NONE', #26512, .T. ) ;
#14315=CARTESIAN_POINT ( 'NONE',  ( 0.1152339509894530906, -27.33595233401855396, 34.63651830723620151 ) ) ;
#14318=ORIENTED_EDGE ( 'NONE', *, *, #48453, .T. ) ;
#14325=ORIENTED_EDGE ( 'NONE', *, *, #43960, .F. ) ;
#14327=CARTESIAN_POINT ( 'NONE',  ( 2.533389852662419894, -16.35873982657418679, 40.86370226766137392 ) ) ;
#14328=EDGE_LOOP ( 'NONE', ( #55290, #20438, #55194, #17592 ) ) ;
#14329=CARTESIAN_POINT ( 'NONE',  ( 0.5997462898726536595, -49.10477184366966696, 0.5225058138009974762 ) ) ;
#14337=CARTESIAN_POINT ( 'NONE',  ( 0.3676999524040366896, -40.57213187173863389, 17.31625533148228513 ) ) ;
#14343=ORIENTED_EDGE ( 'NONE', *, *, #45623, .T. ) ;
#14354=FACE_OUTER_BOUND ( 'NONE', #39470, .T. ) ;
#14358=EDGE_CURVE ( 'NONE', #35248, #15688, #18548, .T. ) ;
#14367=EDGE_LOOP ( 'NONE', ( #45121, #21987, #57890, #858 ) ) ;
#14373=B_SPLINE_CURVE_WITH_KNOTS ( 'NONE', 3,
 ( #51412, #55498, #12625, #50807, #7897, #36744, #46141, #8502, #55812, #60500, #42068, #32646, #61122, #8826, #7574, #17617 ),
 .UNSPECIFIED., .F., .F.,
 ( 4, 3, 3, 3, 3, 4 ),
 ( 2.221635811791082109E-17, 0.0002612764279487765238, 0.0003919131003184790824, 0.0005225497727000667737, 0.0007837925190632461132, 0.001045051706266717818 ),
 .UNSPECIFIED. ) ;
#14384=CARTESIAN_POINT ( 'NONE',  ( 0.7413678028165009426, -28.21704311592099756, -33.88634783455570698 ) ) ;
#14387=EDGE_CURVE ( 'NONE', #61878, #39018, #28258, .T. ) ;
#14390=VERTEX_POINT ( 'NONE', #22646 ) ;
#14395=CARTESIAN_POINT ( 'NONE',  ( -6.072942160501519915, -6.664073831083357824, -18.06638542329068642 ) ) ;
#14397=CARTESIAN_POINT ( 'NONE',  ( -6.072942160501519915, -17.35560219702253093, -8.341896347217875984 ) ) ;
#14398=DIRECTION ( 'NONE',  ( 0.09722883295013594329, -0.5094590954038252795, 0.8549842011133718112 ) ) ;
#14404=DIRECTION ( 'NONE',  ( 0.09722883295013594329, -0.02434548463873833016, 0.9949642463027802419 ) ) ;
#14419=B_SPLINE_CURVE_WITH_KNOTS ( 'NONE', 3,
 ( #821, #52510, #61892, #29630, #19955, #9294, #23713, #14636, #15248, #19032, #38147, #57192, #14327, #34354, #9598, #28716, #47840, #5802, #24952, #38446, #44088, #4885, #24018, #43147, #18711 ),
 .UNSPECIFIED., .F., .F.,
 ( 4, 3, 3, 3, 3, 3, 3, 3, 4 ),
 ( 3.878959614448864246E-18, 0.0005656085177311386642, 0.001131215744874498972, 0.001696821861372764615, 0.002262427090022496416, 0.002828031679238744624, 0.003393635864401603561, 0.003977030878808131623, 0.004561030005651159000 ),
 .UNSPECIFIED. ) ;
#14420=CARTESIAN_POINT ( 'NONE',  ( 5.901764892641288895, 30.56558498815964242, 38.25880920482585879 ) ) ;
#14421=VERTEX_POINT ( 'NONE', #18886 ) ;
#14432=CARTESIAN_POINT ( 'NONE',  ( -6.072942160501519027, -6.636811946999439549, -18.07641804863966684 ) ) ;
#14434=CARTESIAN_POINT ( 'NONE',  ( 4.975610109902397937, -33.30777373088848492, -35.81957029655308133 ) ) ;
#14437=ORIENTED_EDGE ( 'NONE', *, *, #42818, .F. ) ;
#14440=CARTESIAN_POINT ( 'NONE',  ( 4.694002226626921015, 42.38457918174899675, 16.78785927485048646 ) ) ;
#14442=CARTESIAN_POINT ( 'NONE',  ( 0.8744876279028306332, 16.11801507201633399, -46.37412684372340266 ) ) ;
#14448=DIRECTION ( 'NONE',  ( 0.09722883295013594329, 0.9936727386027179865, -0.05622315004452352327 ) ) ;
#14455=CARTESIAN_POINT ( 'NONE',  ( 0.1155031312995260795, -22.72937730850169302, -37.81953251561390061 ) ) ;
#14464=VERTEX_POINT ( 'NONE', #44248 ) ;
#14466=DIRECTION ( 'NONE',  ( 0.000000000000000000, 0.000000000000000000, 1.000000000000000000 ) ) ;
#14469=CARTESIAN_POINT ( 'NONE',  ( 0.6000166863083090663, 33.40185771989251862, 36.00193581696004230 ) ) ;
#14472=ORIENTED_EDGE ( 'NONE', *, *, #5959, .F. ) ;
#14474=CARTESIAN_POINT ( 'NONE',  ( 0.6253024248130498730, -26.04123622408341276, 41.63289856999066529 ) ) ;
#14481=CARTESIAN_POINT ( 'NONE',  ( 3.050102900204245682, -8.802340948619855610, -43.10387503464520620 ) ) ;
#14482=CARTESIAN_POINT ( 'NONE',  ( 0.5997462898726536595, 46.76781179977606229, 14.97743000668126001 ) ) ;
#14488=CARTESIAN_POINT ( 'NONE',  ( 0.1152809850208375841, 39.65805943382677867, 19.34382600296067878 ) ) ;
#14496=CARTESIAN_POINT ( 'NONE',  ( 3.678834586032787790, -43.55038525248056658, 22.40482791696642195 ) ) ;
#14498=CARTESIAN_POINT ( 'NONE',  ( 0.7948884756798513251, 5.577371174960814137, -48.78105754672471761 ) ) ;
#14504=CARTESIAN_POINT ( 'NONE',  ( 0.7044674535452954967, -39.85538961151654291, 28.69408722585759719 ) ) ;
#14512=CARTESIAN_POINT ( 'NONE',  ( 2.299746137290199055, 47.86635935193019264, -10.63451832844456746 ) ) ;
#14513=EDGE_CURVE ( 'NONE', #53665, #1366, #21539, .T. ) ;
#14515=EDGE_LOOP ( 'NONE', ( #37509, #29201, #8730, #49541 ) ) ;
#14516=CARTESIAN_POINT ( 'NONE',  ( 0.6000166863083106206, 44.01764848084281567, -21.77774331572052802 ) ) ;
#14524=EDGE_CURVE ( 'NONE', #24124, #43366, #34672, .T. ) ;
#14525=B_SPLINE_CURVE_WITH_KNOTS ( 'NONE', 3,
 ( #12821, #18430, #56006, #55686 ),
 .UNSPECIFIED., .F., .F.,
 ( 4, 4 ),
 ( 2.301370753934467307E-17, 0.004559932413162187670 ),
 .UNSPECIFIED. ) ;
#14531=CARTESIAN_POINT ( 'NONE',  ( 3.894904216938897434, 34.86916712789552975, 26.76313726533365767 ) ) ;
#14537=CARTESIAN_POINT ( 'NONE',  ( 2.299652685299200972, 33.90758011679142925, -35.41973652473327405 ) ) ;
#14540=B_SPLINE_CURVE_WITH_KNOTS ( 'NONE', 3,
 ( #53098, #38415, #53695, #9894 ),
 .UNSPECIFIED., .F., .F.,
 ( 4, 4 ),
 ( 0.000000000000000000, 0.004442905043737213969 ),
 .UNSPECIFIED. ) ;
#14544=CARTESIAN_POINT ( 'NONE',  ( 2.648799415243708655, -31.64453936086600194, -37.45851828260430239 ) ) ;
#14546=CIRCLE ( 'NONE', #49529, 48.91267123290010943 ) ;
#14548=ORIENTED_EDGE ( 'NONE', *, *, #52104, .T. ) ;
#14555=CARTESIAN_POINT ( 'NONE',  ( 0.1158816050234199313, -17.86592162500884839, -40.34539485237691991 ) ) ;
#14558=EDGE_CURVE ( 'NONE', #19604, #41057, #5601, .T. ) ;
#14565=CARTESIAN_POINT ( 'NONE',  ( 0.6028777368367060907, 41.10879128012145856, 26.86274574198404963 ) ) ;
#14566=CARTESIAN_POINT ( 'NONE',  ( -6.078457390727109555, -8.902764005229952815, 17.07440494145227561 ) ) ;
#14567=CARTESIAN_POINT ( 'NONE',  ( 4.975610109902397937, -47.89734868211972696, -9.914302615979444511 ) ) ;
#14568=FACE_OUTER_BOUND ( 'NONE', #38594, .T. ) ;
#14572=CARTESIAN_POINT ( 'NONE',  ( 0.6026112563231247332, 22.86833861538397628, -43.45779658330994977 ) ) ;
#14575=CARTESIAN_POINT ( 'NONE',  ( 0.8744876279028306332, 27.35388303025845147, -40.76904626731451486 ) ) ;
#14579=CARTESIAN_POINT ( 'NONE',  ( 4.975610109902397937, -47.89734868211986907, 9.914302615978730415 ) ) ;
#14583=CARTESIAN_POINT ( 'NONE',  ( 5.901764892641288895, 48.56171591663485287, -6.304856435457647734 ) ) ;
#14587=ORIENTED_EDGE ( 'NONE', *, *, #21660, .F. ) ;
#14590=DIRECTION ( 'NONE',  ( 0.1011922191286468292, 0.6783146913069540984, 0.7277700971769667238 ) ) ;
#14592=CARTESIAN_POINT ( 'NONE',  ( 4.975610109902397937, 24.86209007719020647, -42.12274782266053563 ) ) ;
#14594=CARTESIAN_POINT ( 'NONE',  ( 0.3676999524040323597, 14.45783756353398175, 41.67639039443440652 ) ) ;
#14595=ADVANCED_FACE ( 'NONE', ( #40788 ), #50658, .T. ) ;
#14604=CARTESIAN_POINT ( 'NONE',  ( 2.533389852662419894, 43.99903125671219328, 1.239265994240477342 ) ) ;
#14606=CARTESIAN_POINT ( 'NONE',  ( 0.1158403557922069033, 41.88819111113468097, -13.86793973958918080 ) ) ;
#14607=CARTESIAN_POINT ( 'NONE',  ( 5.901764892641307547, -46.46096922681047658, -15.47158058974737038 ) ) ;
#14614=DIRECTION ( 'NONE',  ( -1.000000000000000000, -0.000000000000000000, -0.000000000000000000 ) ) ;
#14619=CARTESIAN_POINT ( 'NONE',  ( 0.3676999524040323597, -26.85386693986589890, -34.99743438737782242 ) ) ;
#14620=ORIENTED_EDGE ( 'NONE', *, *, #56317, .T. ) ;
#14622=CARTESIAN_POINT ( 'NONE',  ( 0.8744876279028263033, -13.11369837310799547, -47.31153099783008997 ) ) ;
#14623=ORIENTED_EDGE ( 'NONE', *, *, #39161, .T. ) ;
#14628=CARTESIAN_POINT ( 'NONE',  ( 0.7948884756798504370, -0.7064021483319558037, -49.09378413409362452 ) ) ;
#14629=CARTESIAN_POINT ( 'NONE',  ( 0.8744876279028306332, -24.68559978112762110, 42.43785119236699188 ) ) ;
#14633=ORIENTED_EDGE ( 'NONE', *, *, #50876, .F. ) ;
#14636=CARTESIAN_POINT ( 'NONE',  ( 3.390910168358336918, -15.98239228339566687, 40.97145681365616099 ) ) ;
#14649=CARTESIAN_POINT ( 'NONE',  ( 4.694002226626921015, 39.88981857773283934, -22.07005086722039522 ) ) ;
#14656=DIRECTION ( 'NONE',  ( -0.1011922191286467460, -0.1083236746284043789, 0.9889520293233740045 ) ) ;
#14657=CARTESIAN_POINT ( 'NONE',  ( 4.335381028904216727, -5.712845112848606632, 48.65306001045512829 ) ) ;
#14660=VERTEX_POINT ( 'NONE', #31664 ) ;
#14663=B_SPLINE_CURVE_WITH_KNOTS ( 'NONE', 3,
 ( #16458, #45297, #59352, #36509, #17698, #21158 ),
 .UNSPECIFIED., .F., .F.,
 ( 4, 2, 4 ),
 ( 0.000000000000000000, 0.0002447195606305753966, 0.0004894391212611507933 ),
 .UNSPECIFIED. ) ;
#14665=DIRECTION ( 'NONE',  ( 0.000000000000000000, 0.000000000000000000, 1.000000000000000000 ) ) ;
#14671=VERTEX_POINT ( 'NONE', #25723 ) ;
#14677=AXIS2_PLACEMENT_3D ( 'NONE', #3759, #61387, #13822 ) ;
#14687=ORIENTED_EDGE ( 'NONE', *, *, #58400, .F. ) ;
#14688=CARTESIAN_POINT ( 'NONE',  ( 4.553261556744875094, -39.47791437445886942, -19.26223877088359515 ) ) ;
#14693=AXIS2_PLACEMENT_3D ( 'NONE', #60154, #36081, #12268 ) ;
#14695=ORIENTED_EDGE ( 'NONE', *, *, #60096, .F. ) ;
#14698=CARTESIAN_POINT ( 'NONE',  ( 5.901764892641307547, -48.87142464753282667, 3.094401454271700214 ) ) ;
#14708=ORIENTED_EDGE ( 'NONE', *, *, #1811, .T. ) ;
#14710=CARTESIAN_POINT ( 'NONE',  ( 2.879087469061462734, 42.82528940656273164, -10.10426959396493274 ) ) ;
#14712=CARTESIAN_POINT ( 'NONE',  ( 4.553261556744875094, 0.000000000000000000, 0.000000000000000000 ) ) ;
#14717=CARTESIAN_POINT ( 'NONE',  ( 3.678748215320120085, -46.05789111167558758, -16.65183114989213919 ) ) ;
#14725=B_SPLINE_CURVE_WITH_KNOTS ( 'NONE', 3,
 ( #15544, #44680, #6402, #49047, #29941, #10849 ),
 .UNSPECIFIED., .F., .F.,
 ( 4, 2, 4 ),
 ( 8.673617379884035472E-19, 0.0002293801035737077186, 0.0004587602071474145699 ),
 .UNSPECIFIED. ) ;
#14730=CARTESIAN_POINT ( 'NONE',  ( 0.6016118706126977189, -47.41192439221646282, -12.79298558627663773 ) ) ;
#14739=( BOUNDED_SURFACE ( )  B_SPLINE_SURFACE ( 3, 1, ( 
 ( #33485, #42277 ),
 ( #41970, #47267 ),
 ( #52561, #37895 ),
 ( #3702, #4616 ) ),
 .UNSPECIFIED., .F., .F., .F. ) 
 B_SPLINE_SURFACE_WITH_KNOTS ( ( 4, 4 ),
 ( 2, 2 ),
 ( 0.000000000000000000, 1.000000000000000000 ),
 ( 0.000000000000000000, 1.000000000000000000 ),
 .UNSPECIFIED. ) 
 GEOMETRIC_REPRESENTATION_ITEM ( )  RATIONAL_B_SPLINE_SURFACE ( (
 ( 1.000000000000000000, 1.000000000000000000),
 ( 0.7211978278499970862, 0.9934217856018976445),
 ( 0.7211978278499970862, 0.9934217856018976445),
 ( 1.000000000000000000, 1.000000000000000000) ) ) 
 REPRESENTATION_ITEM ( '' )  SURFACE ( )  );
#14745=CARTESIAN_POINT ( 'NONE',  ( -6.078726893082806448, -6.653559303940370206, 18.06998035022918359 ) ) ;
#14746=ORIENTED_EDGE ( 'NONE', *, *, #18052, .F. ) ;
#14749=CARTESIAN_POINT ( 'NONE',  ( 0.1139756605157201536, 29.36928842959055430, -32.93023104739080509 ) ) ;
#14756=DIRECTION ( 'NONE',  ( -0.1011922191286467460, -0.6592733245820187049, -0.7450629626295969254 ) ) ;
#14762=CARTESIAN_POINT ( 'NONE',  ( -6.077587904424778920, 13.83688374988418879, 13.39166417911236984 ) ) ;
#14764=CARTESIAN_POINT ( 'NONE',  ( 0.1129192098497455998, -22.45785791439690371, -37.98152716363461678 ) ) ;
#14765=ORIENTED_EDGE ( 'NONE', *, *, #58733, .F. ) ;
#14767=CARTESIAN_POINT ( 'NONE',  ( 0.1156867017252034696, -17.97492158142190988, 40.29696020070147711 ) ) ;
#14773=ORIENTED_EDGE ( 'NONE', *, *, #45653, .T. ) ;
#14775=CARTESIAN_POINT ( 'NONE',  ( 0.1158816050234198897, 25.23951143218047122, -36.19266643907288028 ) ) ;
#14780=CARTESIAN_POINT ( 'NONE',  ( 0.1149546198390368063, -41.00147165784255776, 16.30416777742285106 ) ) ;
#14783=CARTESIAN_POINT ( 'NONE',  ( 4.298462506757085855, 0.6202153076419610889, -48.94031900834726656 ) ) ;
#14785=EDGE_CURVE ( 'NONE', #40747, #56645, #49044, .T. ) ;
#14788=CARTESIAN_POINT ( 'NONE',  ( 0.6253024248130490959, -35.74992959045948737, 33.66580998126782021 ) ) ;
#14805=CARTESIAN_POINT ( 'NONE',  ( 0.7242003506639952404, -7.027071004854443359, 48.59662485418876088 ) ) ;
#14807=ORIENTED_EDGE ( 'NONE', *, *, #11772, .T. ) ;
#14813=CARTESIAN_POINT ( 'NONE',  ( 4.834790513006553603, -44.69577334950020031, -15.32570342967947497 ) ) ;
#14814=ORIENTED_EDGE ( 'NONE', *, *, #35674, .F. ) ;
#14819=CARTESIAN_POINT ( 'NONE',  ( -6.079354080745853928, 19.09804277166044173, 2.461243088358096465 ) ) ;
#14821=CARTESIAN_POINT ( 'NONE',  ( -6.078457390727109555, -12.94259897003423099, 14.25775728992385183 ) ) ;
#14826=VERTEX_POINT ( 'NONE', #4977 ) ;
#14839=CARTESIAN_POINT ( 'NONE',  ( -6.079354080745853928, 7.793434646514300290, 17.60838810506720975 ) ) ;
#14848=CARTESIAN_POINT ( 'NONE',  ( 0.6029442701453591180, -35.33687315128987905, -34.10059561133684980 ) ) ;
#14855=EDGE_CURVE ( 'NONE', #17365, #28495, #39469, .T. ) ;
#14857=CARTESIAN_POINT ( 'NONE',  ( -6.057079549204054558, 16.77479338118054386, -9.457142175014601193 ) ) ;
#14858=CARTESIAN_POINT ( 'NONE',  ( 4.975610109902397937, -44.31543648230415755, 20.70245146161774841 ) ) ;
#14862=( BOUNDED_SURFACE ( )  B_SPLINE_SURFACE ( 3, 1, ( 
 ( #29153, #56721 ),
 ( #52021, #48270 ),
 ( #28526, #14154 ),
 ( #52639, #27926 ) ),
 .UNSPECIFIED., .F., .F., .F. ) 
 B_SPLINE_SURFACE_WITH_KNOTS ( ( 4, 4 ),
 ( 2, 2 ),
 ( 0.000000000000000000, 1.000000000000000000 ),
 ( 0.000000000000000000, 1.000000000000000000 ),
 .UNSPECIFIED. ) 
 GEOMETRIC_REPRESENTATION_ITEM ( )  RATIONAL_B_SPLINE_SURFACE ( (
 ( 1.000000000000000000, 1.000000000000000000),
 ( 0.9953485035131437453, 0.8621029689291523912),
 ( 0.9953485035131437453, 0.8621029689291523912),
 ( 1.000000000000000000, 1.000000000000000000) ) ) 
 REPRESENTATION_ITEM ( '' )  SURFACE ( )  );
#14863=LINE ( 'NONE', #24556, #42830 ) ;
#14868=DIRECTION ( 'NONE',  ( 0.09722883295013597105, 0.8999532196066800660, -0.4250067723727768421 ) ) ;
#14873=CARTESIAN_POINT ( 'NONE',  ( 0.3676999524040323597, -35.84016207189440451, 25.71834687500696859 ) ) ;
#14875=CARTESIAN_POINT ( 'NONE',  ( -2.739355103387247858, -10.90485690860422707, 10.19468796746048689 ) ) ;
#14876=CARTESIAN_POINT ( 'NONE',  ( -6.079354080745853928, 7.793434646514551645, -17.60838810506710317 ) ) ;
#14880=CARTESIAN_POINT ( 'NONE',  ( 4.694002226626921015, -16.06750747807337021, 42.66286411960865621 ) ) ;
#14886=CARTESIAN_POINT ( 'NONE',  ( 0.6016117650947689910, -1.922104516163298804, -49.06991510562703240 ) ) ;
#14891=CARTESIAN_POINT ( 'NONE',  ( 4.834790513006555379, -46.28862912354751558, 9.484310981144012942 ) ) ;
#14892=CARTESIAN_POINT ( 'NONE',  ( 4.060580049360325461, 43.64911337592206308, -5.120800313926658909 ) ) ;
#14893=CARTESIAN_POINT ( 'NONE',  ( 0.1140933569871964148, 41.75531667278490744, 14.26336144249862947 ) ) ;
#14896=CARTESIAN_POINT ( 'NONE',  ( 0.5997462898726536595, -13.47075269803089803, -47.22383351542737984 ) ) ;
#14899=VERTEX_POINT ( 'NONE', #29727 ) ;
#14906=CARTESIAN_POINT ( 'NONE',  ( 4.553261556744875094, 27.21079963941838997, 34.48350256002230196 ) ) ;
#14913=ORIENTED_EDGE ( 'NONE', *, *, #29687, .F. ) ;
#14915=CARTESIAN_POINT ( 'NONE',  ( 2.706805983486679779, 43.99338256706222694, 1.165505739093682269 ) ) ;
#14918=CARTESIAN_POINT ( 'NONE',  ( 0.1156867017252034419, 41.91550876716623719, -13.78524327187579246 ) ) ;
#14921=CARTESIAN_POINT ( 'NONE',  ( 4.553261556744875094, 0.000000000000000000, 0.000000000000000000 ) ) ;
#14922=VERTEX_POINT ( 'NONE', #30343 ) ;
#14929=ORIENTED_EDGE ( 'NONE', *, *, #16258, .T. ) ;
#14933=CARTESIAN_POINT ( 'NONE',  ( 0.1157506346131639274, 9.908971581732375356, 42.99712713653383389 ) ) ;
#14947=LINE ( 'NONE', #34976, #16673 ) ;
#14948=EDGE_CURVE ( 'NONE', #54066, #12972, #58006, .T. ) ;
#14949=CARTESIAN_POINT ( 'NONE',  ( 0.8744876279028306332, 11.79038800009151089, 47.65854384249261244 ) ) ;
#14950=VERTEX_POINT ( 'NONE', #60087 ) ;
#14952=B_SPLINE_CURVE_WITH_KNOTS ( 'NONE', 3,
 ( #1801, #54414, #13624, #21545 ),
 .UNSPECIFIED., .F., .F.,
 ( 4, 4 ),
 ( 0.000000000000000000, 0.005013413432710151982 ),
 .UNSPECIFIED. ) ;
#14956=CARTESIAN_POINT ( 'NONE',  ( 0.6026112563231247332, 22.55952149237266013, 43.61890627857813740 ) ) ;
#14958=CARTESIAN_POINT ( 'NONE',  ( 2.299746137290199943, -24.30809607782931536, 42.58400876804762447 ) ) ;
#14961=DIRECTION ( 'NONE',  ( -1.000000000000000000, -0.000000000000000000, -0.000000000000000000 ) ) ;
#14975=B_SPLINE_CURVE_WITH_KNOTS ( 'NONE', 3,
 ( #46234, #60598, #49988, #45009 ),
 .UNSPECIFIED., .F., .F.,
 ( 4, 4 ),
 ( 0.000000000000000000, 0.004442905043737214836 ),
 .UNSPECIFIED. ) ;
#14977=CARTESIAN_POINT ( 'NONE',  ( -2.601141883200665639, 8.903211435101033189, -11.98032777561927986 ) ) ;
#14985=ORIENTED_EDGE ( 'NONE', *, *, #17762, .T. ) ;
#14990=CARTESIAN_POINT ( 'NONE',  ( 4.553261556744873317, -29.36425772793689859, 32.66925058691941075 ) ) ;
#14991=CARTESIAN_POINT ( 'NONE',  ( 0.3676999524040323597, 3.413584541508654091, 43.98065510995502336 ) ) ;
#14999=ORIENTED_EDGE ( 'NONE', *, *, #46529, .F. ) ;
#15004=ORIENTED_EDGE ( 'NONE', *, *, #52603, .T. ) ;
#15007=CARTESIAN_POINT ( 'NONE',  ( 3.678834586032787346, -26.95182293378241667, 40.89268406664441358 ) ) ;
#15008=ORIENTED_EDGE ( 'NONE', *, *, #55861, .T. ) ;
#15010=EDGE_CURVE ( 'NONE', #21977, #30486, #43077, .T. ) ;
#15013=CARTESIAN_POINT ( 'NONE',  ( 0.3676999524040323597, 24.55639947020961600, 36.64606156713607277 ) ) ;
#15019=( BOUNDED_SURFACE ( )  B_SPLINE_SURFACE ( 3, 1, ( 
 ( #42716, #23589 ),
 ( #14821, #33932 ),
 ( #23903, #14214 ),
 ( #53007, #13590 ) ),
 .UNSPECIFIED., .F., .F., .F. ) 
 B_SPLINE_SURFACE_WITH_KNOTS ( ( 4, 4 ),
 ( 2, 2 ),
 ( 0.000000000000000000, 1.000000000000000000 ),
 ( 0.000000000000000000, 1.000000000000000000 ),
 .UNSPECIFIED. ) 
 GEOMETRIC_REPRESENTATION_ITEM ( )  RATIONAL_B_SPLINE_SURFACE ( (
 ( 1.000000000000000000, 1.000000000000000000),
 ( 0.9953485035131437453, 0.8621029689291523912),
 ( 0.9953485035131437453, 0.8621029689291523912),
 ( 1.000000000000000000, 1.000000000000000000) ) ) 
 REPRESENTATION_ITEM ( '' )  SURFACE ( )  );
#15025=CARTESIAN_POINT ( 'NONE',  ( 0.1154773475650540254, -42.63511898549099044, 11.36618929717198512 ) ) ;
#15030=CARTESIAN_POINT ( 'NONE',  ( 4.975610109902397937, -5.269241389990889424, -48.62802178077758697 ) ) ;
#15035=CARTESIAN_POINT ( 'NONE',  ( 5.901764892641288895, -16.95277890151785627, -45.94120976809306001 ) ) ;
#15039=VECTOR ( 'NONE', #23502, 1000.000000000000227 ) ;
#15047=CARTESIAN_POINT ( 'NONE',  ( 0.8744876279028263033, -13.11369837310799547, -47.31153099783008997 ) ) ;
#15055=CARTESIAN_POINT ( 'NONE',  ( 0.5997462898726536595, -31.02483596213004091, -38.06587952047387091 ) ) ;
#15059=CARTESIAN_POINT ( 'NONE',  ( -2.739355103387247858, -7.512526911498964566, -12.89998086645948661 ) ) ;
#15064=FACE_OUTER_BOUND ( 'NONE', #28894, .T. ) ;
#15067=ORIENTED_EDGE ( 'NONE', *, *, #43459, .F. ) ;
#15069=CARTESIAN_POINT ( 'NONE',  ( 4.834790513006553603, -36.27562111512950338, 30.27653635467491355 ) ) ;
#15074=CARTESIAN_POINT ( 'NONE',  ( 0.5980271706414734822, 46.82647351461020691, 14.80981502339485623 ) ) ;
#15075=CARTESIAN_POINT ( 'NONE',  ( 0.1158816050234198758, -17.85553307869832551, 40.34999355366331741 ) ) ;
#15077=DIRECTION ( 'NONE',  ( 0.000000000000000000, 0.000000000000000000, -1.000000000000000000 ) ) ;
#15079=ORIENTED_EDGE ( 'NONE', *, *, #38507, .T. ) ;
#15085=CARTESIAN_POINT ( 'NONE',  ( 0.6039202388192952409, 49.01762936092972467, -2.972494690241308302 ) ) ;
#15088=EDGE_CURVE ( 'NONE', #58860, #47387, #36312, .T. ) ;
#15090=CARTESIAN_POINT ( 'NONE',  ( 0.1140933569871964148, -41.04033302048136278, 16.20620299921893093 ) ) ;
#15092=CARTESIAN_POINT ( 'NONE',  ( 4.553261556744875094, 38.16266689001181334, 21.75202109381179483 ) ) ;
#15100=CARTESIAN_POINT ( 'NONE',  ( 0.3676999524040323597, 34.11874447325018167, -27.96179284115914854 ) ) ;
#15102=CARTESIAN_POINT ( 'NONE',  ( 0.1158516988532803521, -43.76817641532991843, -5.593647478108881188 ) ) ;
#15107=CARTESIAN_POINT ( 'NONE',  ( 0.7242003506640003474, -39.83544447980661829, -28.70799605026916268 ) ) ;
#15110=CARTESIAN_POINT ( 'NONE',  ( 0.5987334308729319599, -7.239498256756843553, 48.57110840366055271 ) ) ;
#15114=CARTESIAN_POINT ( 'NONE',  ( -6.078457390727109555, 15.42941986619915440, -11.52074275513721702 ) ) ;
#15115=( BOUNDED_SURFACE ( )  B_SPLINE_SURFACE ( 3, 1, ( 
 ( #40164, #39530 ),
 ( #16315, #30715 ),
 ( #59523, #16631 ),
 ( #11955, #6256 ) ),
 .UNSPECIFIED., .F., .F., .F. ) 
 B_SPLINE_SURFACE_WITH_KNOTS ( ( 4, 4 ),
 ( 2, 2 ),
 ( 0.000000000000000000, 1.000000000000000000 ),
 ( 0.000000000000000000, 1.000000000000000000 ),
 .UNSPECIFIED. ) 
 GEOMETRIC_REPRESENTATION_ITEM ( )  RATIONAL_B_SPLINE_SURFACE ( (
 ( 1.000000000000000000, 1.000000000000000000),
 ( 0.9953485035131437453, 0.8621029689291523912),
 ( 0.9953485035131437453, 0.8621029689291523912),
 ( 1.000000000000000000, 1.000000000000000000) ) ) 
 REPRESENTATION_ITEM ( '' )  SURFACE ( )  );
#15125=CARTESIAN_POINT ( 'NONE',  ( -6.077587904424778920, 7.788877841491745002, 17.61049128685084142 ) ) ;
#15134=CARTESIAN_POINT ( 'NONE',  ( 4.975610109902397937, 48.43414999183897862, -6.825138951392602849 ) ) ;
#15137=ORIENTED_EDGE ( 'NONE', *, *, #17712, .T. ) ;
#15138=DIRECTION ( 'NONE',  ( 0.000000000000000000, 0.000000000000000000, -1.000000000000000000 ) ) ;
#15143=ORIENTED_EDGE ( 'NONE', *, *, #39922, .T. ) ;
#15144=CARTESIAN_POINT ( 'NONE',  ( 0.1157991065609915854, -1.332877529279917983, -44.10403386346468579 ) ) ;
#15152=CARTESIAN_POINT ( 'NONE',  ( 0.1135584504625007374, 37.21391936710485737, -23.70814749139775302 ) ) ;
#15158=CARTESIAN_POINT ( 'NONE',  ( 4.975610109902397937, 7.237810502494805398, -48.37420290059309025 ) ) ;
#15162=CARTESIAN_POINT ( 'NONE',  ( 4.553261556744873317, 43.53643125131393532, -5.841123155973635406 ) ) ;
#15174=CARTESIAN_POINT ( 'NONE',  ( 0.1147471544378675795, -7.348573952980992807, -43.50805269522889773 ) ) ;
#15176=FACE_OUTER_BOUND ( 'NONE', #31017, .T. ) ;
#15177=CARTESIAN_POINT ( 'NONE',  ( 0.8744876279028306332, -47.70753782033967383, -11.59055156152427557 ) ) ;
#15180=CARTESIAN_POINT ( 'NONE',  ( 0.5997462898726536595, 33.39998138387895921, -35.99990102348682797 ) ) ;
#15181=LINE ( 'NONE', #34285, #30667 ) ;
#15183=CARTESIAN_POINT ( 'NONE',  ( 0.7242486021783856032, 48.34643330280884044, -8.581016797036948418 ) ) ;
#15184=CARTESIAN_POINT ( 'NONE',  ( 0.6026777506516367566, -30.48164694038906930, 38.50215046511933537 ) ) ;
#15203=CARTESIAN_POINT ( 'NONE',  ( 0.1368894036331278763, -44.11864566353360573, 0.6375192066904099564 ) ) ;
#15209=CARTESIAN_POINT ( 'NONE',  ( 4.553261556744875094, 0.000000000000000000, 0.000000000000000000 ) ) ;
#15214=CARTESIAN_POINT ( 'NONE',  ( 0.5997462898726536595, -2.096122762664449635, -49.06279547180479739 ) ) ;
#15223=DIRECTION ( 'NONE',  ( 0.000000000000000000, 0.000000000000000000, 1.000000000000000000 ) ) ;
#15228=CARTESIAN_POINT ( 'NONE',  ( 0.6029443449137436017, 4.758762304982984581, -48.87631041013637656 ) ) ;
#15247=CARTESIAN_POINT ( 'NONE',  ( 0.5997462898726536595, -20.35457962188166192, -44.69052157405179315 ) ) ;
#15248=CARTESIAN_POINT ( 'NONE',  ( 3.221118495291108719, -16.06124188590834478, 40.94872316378246779 ) ) ;
#15252=CARTESIAN_POINT ( 'NONE',  ( 0.6008122571543327295, 23.09929608320648953, 43.33563280864464673 ) ) ;
#15264=LINE ( 'NONE', #54356, #38346 ) ;
#15265=ORIENTED_EDGE ( 'NONE', *, *, #48813, .T. ) ;
#15270=CARTESIAN_POINT ( 'NONE',  ( 0.1140933569871964842, -23.19718125549982801, 37.53452719674769611 ) ) ;
#15272=CARTESIAN_POINT ( 'NONE',  ( 4.553261556744875094, -24.94552653848424129, -36.15605442441715667 ) ) ;
#15275=VERTEX_POINT ( 'NONE', #29657 ) ;
#15279=EDGE_LOOP ( 'NONE', ( #49882, #42980, #30344, #45058 ) ) ;
#15280=EDGE_CURVE ( 'NONE', #17545, #34842, #11012, .T. ) ;
#15284=ORIENTED_EDGE ( 'NONE', *, *, #60880, .T. ) ;
#15286=ORIENTED_EDGE ( 'NONE', *, *, #27598, .F. ) ;
#15295=CARTESIAN_POINT ( 'NONE',  ( 0.8744876279028263033, -48.57046782678510510, -7.159588358748426806 ) ) ;
#15298=VERTEX_POINT ( 'NONE', #15886 ) ;
#15304=VECTOR ( 'NONE', #47661, 1000.000000000000114 ) ;
#15308=CARTESIAN_POINT ( 'NONE',  ( 0.8753041380234471980, 28.81806460335509001, -39.75748332565621723 ) ) ;
#15310=CARTESIAN_POINT ( 'NONE',  ( 0.2940135542859014239, 36.52812816767694670, -24.73734830690602138 ) ) ;
#15312=CARTESIAN_POINT ( 'NONE',  ( 0.3676999524040323597, 10.61898383218351860, -42.81574203134477585 ) ) ;
#15325=ORIENTED_EDGE ( 'NONE', *, *, #10573, .F. ) ;
#15330=CARTESIAN_POINT ( 'NONE',  ( 0.5997462898726536595, -25.90236585764231947, -41.72072714036939090 ) ) ;
#15331=CARTESIAN_POINT ( 'NONE',  ( -6.078726893082806448, 18.62537590944121391, -4.887679766589349661 ) ) ;
#15332=CARTESIAN_POINT ( 'NONE',  ( 0.7044674535452954967, -48.59206901384826693, -7.114320189892598734 ) ) ;
#15336=CARTESIAN_POINT ( 'NONE',  ( 0.1158816050234199174, 20.40407993419151822, -39.12308223215911340 ) ) ;
#15337=CARTESIAN_POINT ( 'NONE',  ( 4.335381028904201628, 26.25686719067146058, 41.35618179904649594 ) ) ;
#15348=CARTESIAN_POINT ( 'NONE',  ( 1.657374760986086049, 24.17973270432427313, -36.82704133649178146 ) ) ;
#15351=ORIENTED_EDGE ( 'NONE', *, *, #52354, .T. ) ;
#15355=VECTOR ( 'NONE', #9863, 1000.000000000000227 ) ;
#15357=DIRECTION ( 'NONE',  ( 0.000000000000000000, 0.000000000000000000, 1.000000000000000000 ) ) ;
#15362=EDGE_LOOP ( 'NONE', ( #13472, #14929, #17004, #58034 ) ) ;
#15363=ADVANCED_FACE ( 'NONE', ( #6132 ), #5927, .F. ) ;
#15364=CARTESIAN_POINT ( 'NONE',  ( -6.078075953587585900, -6.655346486686461560, 18.06935354098995461 ) ) ;
#15369=CARTESIAN_POINT ( 'NONE',  ( 0.1368894036331270714, -13.16414094522229838, -42.11373551583444907 ) ) ;
#15372=CARTESIAN_POINT ( 'NONE',  ( 0.5987334308729318488, 4.112662331024658613, -48.93515009807060778 ) ) ;
#15373=VERTEX_POINT ( 'NONE', #22734 ) ;
#15380=CARTESIAN_POINT ( 'NONE',  ( 4.553261556744875094, 0.000000000000000000, 0.000000000000000000 ) ) ;
#15383=CARTESIAN_POINT ( 'NONE',  ( 0.6000166863083090663, -45.32251430608278753, 18.91277818522110010 ) ) ;
#15385=CARTESIAN_POINT ( 'NONE',  ( 0.3676999524040323597, 3.413584541508654091, 43.98065510995502336 ) ) ;
#15387=CARTESIAN_POINT ( 'NONE',  ( 0.1129192098497455998, -18.30288010335110016, 40.14917642626692640 ) ) ;
#15393=CARTESIAN_POINT ( 'NONE',  ( 0.1155031312995260795, 25.10578313294615427, 36.28555202574827376 ) ) ;
#15394=ORIENTED_EDGE ( 'NONE', *, *, #13443, .F. ) ;
#15395=DIRECTION ( 'NONE',  ( 0.09722883295013592941, 0.9469132758617033740, 0.3064340092744473054 ) ) ;
#15402=CIRCLE ( 'NONE', #16367, 48.91267123290010943 ) ;
#15405=ADVANCED_FACE ( 'NONE', ( #60009 ), #42755, .F. ) ;
#15412=CARTESIAN_POINT ( 'NONE',  ( 0.3676999524040323597, -38.02468164711575582, -22.36233818182566324 ) ) ;
#15415=CARTESIAN_POINT ( 'NONE',  ( 2.706805983486679779, 18.87354163078242664, -39.75632703898686060 ) ) ;
#15427=ORIENTED_EDGE ( 'NONE', *, *, #6830, .F. ) ;
#15432=CARTESIAN_POINT ( 'NONE',  ( 0.6000166863083106206, -48.63754814943177252, -6.797969676319517873 ) ) ;
#15438=ORIENTED_EDGE ( 'NONE', *, *, #41923, .F. ) ;
#15443=CARTESIAN_POINT ( 'NONE',  ( 0.1157506346131639274, 43.29263408050130835, -8.525754756891059216 ) ) ;
#15449=CARTESIAN_POINT ( 'NONE',  ( 0.1135584504625008623, -0.9824315139179617962, -44.11334129779462643 ) ) ;
#15453=ORIENTED_EDGE ( 'NONE', *, *, #54161, .T. ) ;
#15454=CARTESIAN_POINT ( 'NONE',  ( 4.390527457369401532, -43.06122069908267491, -8.713013745743406702 ) ) ;
#15457=CARTESIAN_POINT ( 'NONE',  ( 0.6028777368367060907, -35.21566487464662742, -34.22567423364589700 ) ) ;
#15459=VERTEX_POINT ( 'NONE', #47171 ) ;
#15461=CARTESIAN_POINT ( 'NONE',  ( 3.678748215320120529, -3.416822541561816529, -48.85630090396691827 ) ) ;
#15464=CARTESIAN_POINT ( 'NONE',  ( -6.078726893082806448, -12.94836301907731801, -14.25250631976393656 ) ) ;
#15466=CARTESIAN_POINT ( 'NONE',  ( 4.694002226626921015, 12.64038892846058282, 43.80074587473810510 ) ) ;
#15476=B_SPLINE_CURVE_WITH_KNOTS ( 'NONE', 3,
 ( #5806, #24643, #53728, #24956, #39078, #58131 ),
 .UNSPECIFIED., .F., .F.,
 ( 4, 2, 4 ),
 ( 0.000000000000000000, 0.0002447195606305743666, 0.0004894391212611487333 ),
 .UNSPECIFIED. ) ;
#15479=CARTESIAN_POINT ( 'NONE',  ( 0.1154773475650540393, -35.25385042465135399, 26.53506473107669450 ) ) ;
#15483=CARTESIAN_POINT ( 'NONE',  ( 0.6021447746440204973, 32.82110281078899305, -36.52829518841669199 ) ) ;
#15490=CARTESIAN_POINT ( 'NONE',  ( 0.6016118706126977189, 49.02773421256183894, -2.798630516221145115 ) ) ;
#15491=CARTESIAN_POINT ( 'NONE',  ( 4.975610109902397937, -17.43163075979644816, -45.70106843599929647 ) ) ;
#15495=CARTESIAN_POINT ( 'NONE',  ( 2.185380717157383135, 43.82594162643527369, -4.255190198274171998 ) ) ;
#15497=ORIENTED_EDGE ( 'NONE', *, *, #4496, .F. ) ;
#15500=CARTESIAN_POINT ( 'NONE',  ( 5.901764892641307547, 7.858096707079341492, -48.33468509861078388 ) ) ;
#15512=CARTESIAN_POINT ( 'NONE',  ( 4.975610109902397937, 42.89797504594920241, 23.49921581872238718 ) ) ;
#15513=EDGE_CURVE ( 'NONE', #28003, #39250, #38498, .T. ) ;
#15514=CARTESIAN_POINT ( 'NONE',  ( 0.1149546198390367924, 15.49570923134082534, -41.31379382773940279 ) ) ;
#15518=CARTESIAN_POINT ( 'NONE',  ( 0.3676999524040323597, -40.57213187173838520, -17.31625533148287843 ) ) ;
#15519=ORIENTED_EDGE ( 'NONE', *, *, #12113, .F. ) ;
#15523=CARTESIAN_POINT ( 'NONE',  ( 0.1157991065609916270, -40.86881191294364868, -16.63377823472870531 ) ) ;
#15526=B_SPLINE_CURVE_WITH_KNOTS ( 'NONE', 3,
 ( #15775, #34889, #15461, #34574 ),
 .UNSPECIFIED., .F., .F.,
 ( 4, 4 ),
 ( 0.000000000000000000, 0.004442905043737216571 ),
 .UNSPECIFIED. ) ;
#15527=ORIENTED_EDGE ( 'NONE', *, *, #11620, .T. ) ;
#15528=DIRECTION ( 'NONE',  ( 0.000000000000000000, 0.000000000000000000, 1.000000000000000000 ) ) ;
#15534=CARTESIAN_POINT ( 'NONE',  ( 4.553261556744875094, -29.36425772793644029, -32.66925058691983708 ) ) ;
#15544=CARTESIAN_POINT ( 'NONE',  ( 0.3676999524040366896, -31.10876963919527682, 31.27610965031171020 ) ) ;
#15547=ORIENTED_EDGE ( 'NONE', *, *, #38718, .T. ) ;
#15568=VERTEX_POINT ( 'NONE', #14896 ) ;
#15586=ORIENTED_EDGE ( 'NONE', *, *, #16298, .T. ) ;
#15590=ORIENTED_EDGE ( 'NONE', *, *, #19840, .T. ) ;
#15592=( BOUNDED_SURFACE ( )  B_SPLINE_SURFACE ( 3, 1, ( 
 ( #49018, #6069 ),
 ( #44347, #1376 ),
 ( #20515, #27061 ),
 ( #17362, #3539 ) ),
 .UNSPECIFIED., .F., .F., .F. ) 
 B_SPLINE_SURFACE_WITH_KNOTS ( ( 4, 4 ),
 ( 2, 2 ),
 ( 0.000000000000000000, 1.000000000000000000 ),
 ( 0.000000000000000000, 1.000000000000000000 ),
 .UNSPECIFIED. ) 
 GEOMETRIC_REPRESENTATION_ITEM ( )  RATIONAL_B_SPLINE_SURFACE ( (
 ( 1.000000000000000000, 1.000000000000000000),
 ( 0.9953485035131437453, 0.8621029689291523912),
 ( 0.9953485035131437453, 0.8621029689291523912),
 ( 1.000000000000000000, 1.000000000000000000) ) ) 
 REPRESENTATION_ITEM ( '' )  SURFACE ( )  );
#15599=CARTESIAN_POINT ( 'NONE',  ( 4.335381028904216727, 26.25686719067205033, -41.35618179904614067 ) ) ;
#15602=CARTESIAN_POINT ( 'NONE',  ( 0.6039202388192953519, 4.888815891286212967, 48.86372061182098747 ) ) ;
#15608=ORIENTED_EDGE ( 'NONE', *, *, #30401, .F. ) ;
#15614=CARTESIAN_POINT ( 'NONE',  ( 0.6021448801613057400, -48.67017654873032484, -6.538734842641000355 ) ) ;
#15616=CARTESIAN_POINT ( 'NONE',  ( -6.078457390727109555, 16.78028475769473005, 9.445451523785720838 ) ) ;
#15618=CARTESIAN_POINT ( 'NONE',  ( 0.1129192098497447394, -35.64954734424924965, -26.00118385641864194 ) ) ;
#15621=AXIS2_PLACEMENT_3D ( 'NONE', #43314, #57981, #5357 ) ;
#15626=CARTESIAN_POINT ( 'NONE',  ( 3.894904216938897878, 31.16049771651687195, 31.00238240095667663 ) ) ;
#15635=EDGE_CURVE ( 'NONE', #2290, #35035, #13978, .T. ) ;
#15637=CARTESIAN_POINT ( 'NONE',  ( 0.6016118706126977189, -19.55889245893339279, -45.04443118259803214 ) ) ;
#15644=CARTESIAN_POINT ( 'NONE',  ( -2.739355103387247858, -9.100462108390344085, -11.83339158334450580 ) ) ;
#15647=CARTESIAN_POINT ( 'NONE',  ( -6.072942160501519915, 3.087637228657821975, 19.00712126107544719 ) ) ;
#15649=LINE ( 'NONE', #11563, #24856 ) ;
#15662=CARTESIAN_POINT ( 'NONE',  ( 2.359973842542475886, 40.29593983161778681, 17.73057042847576170 ) ) ;
#15666=CARTESIAN_POINT ( 'NONE',  ( 0.6028777368367059797, 28.16654571100842830, -40.22667687021567673 ) ) ;
#15667=B_SPLINE_CURVE_WITH_KNOTS ( 'NONE', 3,
 ( #14337, #8678, #33441, #9608, #28725, #32201 ),
 .UNSPECIFIED., .F., .F.,
 ( 4, 2, 4 ),
 ( 9.215718466126787689E-19, 0.0002293801035737121367, 0.0004587602071474233519 ),
 .UNSPECIFIED. ) ;
#15674=VECTOR ( 'NONE', #47372, 1000.000000000000114 ) ;
#15679=CARTESIAN_POINT ( 'NONE',  ( 2.299652685299202304, 48.83329552428664755, 4.426169121920126237 ) ) ;
#15681=VERTEX_POINT ( 'NONE', #6985 ) ;
#15685=CARTESIAN_POINT ( 'NONE',  ( 4.553261556744875094, 0.000000000000000000, 0.000000000000000000 ) ) ;
#15686=CARTESIAN_POINT ( 'NONE',  ( 0.1154773475650540393, -1.234467219940398319, 44.10691239169902644 ) ) ;
#15688=VERTEX_POINT ( 'NONE', #44949 ) ;
#15689=CARTESIAN_POINT ( 'NONE',  ( -6.078726893082806448, -17.35055002122458490, 8.351793533709011896 ) ) ;
#15690=CARTESIAN_POINT ( 'NONE',  ( 1.657374760986086715, -36.03312162084205283, -25.34767432152008482 ) ) ;
#15691=CARTESIAN_POINT ( 'NONE',  ( 0.1368894036331280983, -32.13611142736034054, -30.23461043657771441 ) ) ;
#15694=DIRECTION ( 'NONE',  ( 0.000000000000000000, 0.000000000000000000, 1.000000000000000000 ) ) ;
#15702=CARTESIAN_POINT ( 'NONE',  ( 4.975610109902397937, 45.11887670192734134, 18.88746601040093154 ) ) ;
#15703=CARTESIAN_POINT ( 'NONE',  ( 0.5997462898726536595, 48.09935696025624452, 9.899671214447447909 ) ) ;
#15709=CARTESIAN_POINT ( 'NONE',  ( 0.5997462898726536595, -30.20781297212564454, -38.71743361310750231 ) ) ;
#15712=B_SPLINE_CURVE_WITH_KNOTS ( 'NONE', 3,
 ( #39707, #45025, #39091, #40025, #58756, #35301, #54364, #58447, #34681, #25270, #11486, #19661, #30573, #29348, #25575, #58146, #15270, #53745, #24972 ),
 .UNSPECIFIED., .F., .F.,
 ( 4, 3, 3, 3, 3, 3, 4 ),
 ( 3.469552829456483146E-18, 0.0002612768053151673722, 0.0003919133833142922265, 0.0005225499612322564167, 0.0006531865391693380185, 0.0008112755173415141111, 0.0009693688056799736573 ),
 .UNSPECIFIED. ) ;
#15714=( LENGTH_UNIT ( ) NAMED_UNIT ( * ) SI_UNIT ( .MILLI., .METRE. ) );
#15717=ADVANCED_FACE ( 'NONE', ( #22276 ), #44416, .F. ) ;
#15719=CARTESIAN_POINT ( 'NONE',  ( 0.5997462898726536595, -7.321308210775074876, -48.55872811583048332 ) ) ;
#15721=EDGE_CURVE ( 'NONE', #43021, #54546, #51372, .T. ) ;
#15723=CARTESIAN_POINT ( 'NONE',  ( 4.553261556744875094, 38.16266689001181334, 21.75202109381179483 ) ) ;
#15726=CARTESIAN_POINT ( 'NONE',  ( 4.834790513006555379, -10.06429236341644362, 46.16599787882916672 ) ) ;
#15729=CARTESIAN_POINT ( 'NONE',  ( 0.1140933569871964287, 36.77173631030485268, 24.38830372964288529 ) ) ;
#15730=ORIENTED_EDGE ( 'NONE', *, *, #35236, .F. ) ;
#15732=CARTESIAN_POINT ( 'NONE',  ( 0.8744876279028306332, -6.955970791788286256, 48.60004650947653460 ) ) ;
#15736=CARTESIAN_POINT ( 'NONE',  ( 0.1158403557922069033, 4.199242128790555917, 43.92387360795505202 ) ) ;
#15739=LINE ( 'NONE', #1921, #1535 ) ;
#15742=CARTESIAN_POINT ( 'NONE',  ( 0.6029442701453592290, 11.01234799411597010, 47.85680115526702139 ) ) ;
#15746=ORIENTED_EDGE ( 'NONE', *, *, #56995, .T. ) ;
#15748=VERTEX_POINT ( 'NONE', #8455 ) ;
#15766=CARTESIAN_POINT ( 'NONE',  ( 0.8744876279028306332, 28.81338721758086052, 39.75095932715638014 ) ) ;
#15767=ORIENTED_EDGE ( 'NONE', *, *, #44729, .T. ) ;
#15768=CARTESIAN_POINT ( 'NONE',  ( 3.221118495291108719, -42.98720608046416913, -9.319953490090810533 ) ) ;
#15774=CARTESIAN_POINT ( 'NONE',  ( 4.553261556744873317, 6.787618719204111528, -43.39893775135914922 ) ) ;
#15775=CARTESIAN_POINT ( 'NONE',  ( 0.8744876279028306332, -2.462621419132613454, -49.03351451941336592 ) ) ;
#15777=CARTESIAN_POINT ( 'NONE',  ( -6.077587904424778920, -19.21610359950805247, 1.239912838430311970 ) ) ;
#15778=DIRECTION ( 'NONE',  ( 0.1011922191286468153, 0.3556331495180372615, 0.9291314211411113577 ) ) ;
#15782=CARTESIAN_POINT ( 'NONE',  ( 0.6000166863083090663, 16.46965316277442781, 46.26633772416364110 ) ) ;
#15784=EDGE_CURVE ( 'NONE', #59245, #57068, #42278, .T. ) ;
#15788=CIRCLE ( 'NONE', #23648, 48.91267123290010943 ) ;
#15794=CARTESIAN_POINT ( 'NONE',  ( 4.553261556744875094, 0.000000000000000000, 0.000000000000000000 ) ) ;
#15798=CARTESIAN_POINT ( 'NONE',  ( 0.6029443449137436017, 49.00930124176078095, -3.102890551997893542 ) ) ;
#15800=ORIENTED_EDGE ( 'NONE', *, *, #22432, .F. ) ;
#15801=ORIENTED_EDGE ( 'NONE', *, *, #56300, .F. ) ;
#15802=EDGE_CURVE ( 'NONE', #54760, #50250, #36189, .T. ) ;
#15808=EDGE_CURVE ( 'NONE', #31069, #13981, #54874, .T. ) ;
#15809=ORIENTED_EDGE ( 'NONE', *, *, #3643, .T. ) ;
#15817=CARTESIAN_POINT ( 'NONE',  ( 0.6000166863083090663, 44.01764848084249593, 21.77774331572116040 ) ) ;
#15821=CARTESIAN_POINT ( 'NONE',  ( -6.078726893082806448, -16.13637198556907748, 10.50768958487361537 ) ) ;
#15822=ADVANCED_FACE ( 'NONE', ( #56077 ), #44210, .F. ) ;
#15823=CARTESIAN_POINT ( 'NONE',  ( 0.1158816050234199313, 15.23361400778437336, -41.41109809660929386 ) ) ;
#15826=CARTESIAN_POINT ( 'NONE',  ( 0.2285344041767117251, 34.08191643308648366, 28.01649768517765082 ) ) ;
#15832=CARTESIAN_POINT ( 'NONE',  ( 0.5997462898726536595, -8.352924653000716404, 48.39194436975645175 ) ) ;
#15837=CARTESIAN_POINT ( 'NONE',  ( 0.6029442701453591180, -35.21567780871351516, 34.22573975286961456 ) ) ;
#15838=CARTESIAN_POINT ( 'NONE',  ( 0.8744876279028263033, 28.81338721758142896, -39.75095932715596092 ) ) ;
#15842=CARTESIAN_POINT ( 'NONE',  ( 4.553261556744873317, -25.31600221269608397, -35.89762663172042068 ) ) ;
#15848=ORIENTED_EDGE ( 'NONE', *, *, #28516, .T. ) ;
#15853=CARTESIAN_POINT ( 'NONE',  ( 0.1129192098497455998, 33.91039995638899995, -28.23183597612607798 ) ) ;
#15858=EDGE_CURVE ( 'NONE', #13508, #18777, #37308, .T. ) ;
#15860=DIRECTION ( 'NONE',  ( 0.1011922191286468153, -0.5046905544709855418, 0.8573491581704556497 ) ) ;
#15866=CARTESIAN_POINT ( 'NONE',  ( 0.6039202388192953519, 37.27969488251792995, -31.96541978944368267 ) ) ;
#15867=CARTESIAN_POINT ( 'NONE',  ( 0.6029442701453591180, 22.79128462898585994, 43.49830537065587777 ) ) ;
#15879=ORIENTED_EDGE ( 'NONE', *, *, #5639, .T. ) ;
#15886=CARTESIAN_POINT ( 'NONE',  ( 0.5997462898726536595, -1.051648045106814422, -49.09628974305016413 ) ) ;
#15888=B_SPLINE_CURVE_WITH_KNOTS ( 'NONE', 3,
 ( #52950, #42354, #37337, #28843, #61408, #632 ),
 .UNSPECIFIED., .F., .F.,
 ( 4, 2, 4 ),
 ( 0.000000000000000000, 0.0002447195606305751798, 0.0004894391212611503596 ),
 .UNSPECIFIED. ) ;
#15898=EDGE_LOOP ( 'NONE', ( #7086, #42866, #31719, #20632 ) ) ;
#15903=ORIENTED_EDGE ( 'NONE', *, *, #22502, .F. ) ;
#15917=EDGE_CURVE ( 'NONE', #45566, #51246, #18297, .T. ) ;
#15924=CARTESIAN_POINT ( 'NONE',  ( 0.8744876279028263033, -49.08725279547490317, -0.8897546699139439186 ) ) ;
#15927=VERTEX_POINT ( 'NONE', #10644 ) ;
#15931=CARTESIAN_POINT ( 'NONE',  ( 4.060580049360325461, 31.21837995092301554, 30.93348424602403668 ) ) ;
#15936=CARTESIAN_POINT ( 'NONE',  ( 0.8753041380234530822, 40.66072100792177935, -27.52896828776785654 ) ) ;
#15941=ORIENTED_EDGE ( 'NONE', *, *, #47662, .T. ) ;
#15943=CARTESIAN_POINT ( 'NONE',  ( 0.1119898979215349227, -38.71871422322526257, -21.16181648989621422 ) ) ;
#15945=CARTESIAN_POINT ( 'NONE',  ( 0.5980271706414734822, 41.53842981737961537, 26.20320764998614038 ) ) ;
#15958=CARTESIAN_POINT ( 'NONE',  ( 3.559346040607745287, -19.65740999566269664, -39.33213080681503726 ) ) ;
#15965=VECTOR ( 'NONE', #6683, 1000.000000000000000 ) ;
#15973=CARTESIAN_POINT ( 'NONE',  ( 0.6021447746440204973, -13.72175854280559193, 47.15139957182002206 ) ) ;
#15975=CARTESIAN_POINT ( 'NONE',  ( 3.727782113643637096, -43.91135458311394046, 2.137922959793808975 ) ) ;
#15988=ORIENTED_EDGE ( 'NONE', *, *, #47277, .T. ) ;
#15990=CARTESIAN_POINT ( 'NONE',  ( 0.3676999524040366896, 16.00695768809390884, 41.10629986868691077 ) ) ;
#15993=ADVANCED_FACE ( 'NONE', ( #50090 ), #12749, .F. ) ;
#15994=ORIENTED_EDGE ( 'NONE', *, *, #20163, .F. ) ;
#15998=CARTESIAN_POINT ( 'NONE',  ( -6.078075953587585900, 17.85074021576670233, -7.221235905047362458 ) ) ;
#16000=CARTESIAN_POINT ( 'NONE',  ( 4.975610109902397937, 0.000000000000000000, 0.000000000000000000 ) ) ;
#16001=LINE ( 'NONE', #35114, #39925 ) ;
#16007=EDGE_CURVE ( 'NONE', #55289, #57068, #35703, .T. ) ;
#16009=ORIENTED_EDGE ( 'NONE', *, *, #54642, .F. ) ;
#16011=CARTESIAN_POINT ( 'NONE',  ( 0.7044674535453004927, 36.84332507061654383, -32.47109669462652448 ) ) ;
#16016=ORIENTED_EDGE ( 'NONE', *, *, #5764, .F. ) ;
#16022=CARTESIAN_POINT ( 'NONE',  ( 1.112077966505211846, -8.069605668463317727, -43.33487959466437900 ) ) ;
#16027=CARTESIAN_POINT ( 'NONE',  ( 0.1368894036331274600, -27.00909305656406190, 34.89083286746241441 ) ) ;
#16028=EDGE_CURVE ( 'NONE', #6381, #55761, #34714, .T. ) ;
#16029=CARTESIAN_POINT ( 'NONE',  ( -6.057079549204054558, -1.840653143754341636, -19.16880870331085163 ) ) ;
#16031=( BOUNDED_SURFACE ( )  B_SPLINE_SURFACE ( 3, 1, ( 
 ( #41017, #36299 ),
 ( #51912, #37855 ),
 ( #56913, #37226 ),
 ( #46937, #46621 ) ),
 .UNSPECIFIED., .F., .F., .F. ) 
 B_SPLINE_SURFACE_WITH_KNOTS ( ( 4, 4 ),
 ( 2, 2 ),
 ( 0.000000000000000000, 1.000000000000000000 ),
 ( 0.000000000000000000, 1.000000000000000000 ),
 .UNSPECIFIED. ) 
 GEOMETRIC_REPRESENTATION_ITEM ( )  RATIONAL_B_SPLINE_SURFACE ( (
 ( 1.000000000000000000, 1.000000000000000000),
 ( 0.7211978278499968642, 0.9934217856018975334),
 ( 0.7211978278499968642, 0.9934217856018975334),
 ( 1.000000000000000000, 1.000000000000000000) ) ) 
 REPRESENTATION_ITEM ( '' )  SURFACE ( )  );
#16044=EDGE_LOOP ( 'NONE', ( #52310, #32371, #2246, #11128 ) ) ;
#16045=B_SPLINE_CURVE_WITH_KNOTS ( 'NONE', 3,
 ( #18339, #61216, #27724, #26477, #12402, #36212 ),
 .UNSPECIFIED., .F., .F.,
 ( 4, 2, 4 ),
 ( 0.000000000000000000, 0.0002447195606305733366, 0.0004894391212611466733 ),
 .UNSPECIFIED. ) ;
#16048=VERTEX_POINT ( 'NONE', #17199 ) ;
#16057=CARTESIAN_POINT ( 'NONE',  ( 4.553261556744875094, -29.36425772793644029, -32.66925058691983708 ) ) ;
#16058=CLOSED_SHELL ( 'NONE', ( #40991, #40127, #22764, #42448, #27007, #43945, #13288, #43538, #50797, #42562, #34538, #53402, #1505, #45288, #25320, #46623, #19460, #32230, #32534, #30968, #46795, #35161, #38036, #61514, #53877, #11702, #60588, #47824, #34250, #60049, #28858, #7794, #4786, #43308, #7700, #39258, #52688, #11331, #47394, #23497, #53474, #3559, #41955, #38159, #6474, #42712, #21694, #20109, #40348, #3465, #59549, #42186, #17867, #40470, #1892, #42048, #24975, #32394, #2388, #6751, #17981, #18142, #53384, #4145, #37549, #22125, #24983, #11567, #34269, #9036, #28245, #57827, #21023, #10993, #26515, #25406, #17985, #8060, #26166, #33090, #49207, #7586, #50913, #24469, #2868, #28648, #30976, #37807, #2038, #5734, #19470, #61921, #19128, #47544, #35634, #45116, #59081, #61870, #35149, #926, #19079, #45310, #47457, #60969, #41251, #13740, #19983, #44310, #23135, #58898, #25106, #31048, #47965, #18053, #58383, #10208, #16849, #48901, #54521, #46041, #60283, #27928, #55648, #45072, #8207, #24109, #44591, #56915, #22535, #55768, #19113, #60663, #11564, #51173, #10496, #49546, #60519, #36119, #18875, #40909, #9185, #58526, #40622, #21961, #4574, #47697, #27816, #19830, #19853, #44678, #53004, #41843, #47981, #44788, #18048, #4223, #10273, #31601, #25816, #21429, #16260, #47681, #34847, #12979, #5389, #13673, #52611, #48165, #32830, #2991, #9555, #58072, #41178, #51523, #32769, #2437, #51762, #53548, #59836, #18470, #34804, #47045, #46266, #23762, #32942, #18201, #54433, #42748, #7251, #27700, #5283, #23264, #15993, #32848, #16158, #54506, #34825, #36026, #53800, #14056, #49150, #38433, #49348, #58817, #1155, #8568, #45505, #7836, #9112, #5925, #15405, #31555, #20574, #39575, #36638, #6435, #15717, #50549, #28705, #46619, #6900, #42846, #53552, #19374, #30039, #13471, #33262, #21498, #47305, #15822, #61336, #28368, #53861, #15363, #20045, #41195, #59949, #19630, #44364, #18188, #10270, #9624, #47722, #3026, #42752, #38273, #38289, #46699, #16771, #13818, #25539, #31956, #53458, #37087, #55186, #6204, #35479, #39333, #40487, #1756, #52332, #17189, #14023, #5248, #33483, #8325, #61368, #28897, #10335, #4653, #29327, #6920, #17498, #50979, #41548, #29065, #49104, #29066, #30762, #43478, #60100, #44792, #60716, #26845, #46340, #61737, #2200, #28010, #54502, #46183, #1857, #7858, #38253, #29642, #28903, #14595, #7939, #8287, #25947, #36614, #245, #3917, #1131, #31996, #13808, #43948 ) ) ;
#16060=EDGE_CURVE ( 'NONE', #9752, #52483, #36164, .T. ) ;
#16062=EDGE_CURVE ( 'NONE', #28594, #54914, #14525, .T. ) ;
#16078=CARTESIAN_POINT ( 'NONE',  ( -2.739355103387248747, 11.53562761125299474, 9.475065306662248332 ) ) ;
#16083=CARTESIAN_POINT ( 'NONE',  ( 4.694002226626920127, 6.935496447963913624, -45.05755941533467279 ) ) ;
#16089=CARTESIAN_POINT ( 'NONE',  ( 0.9268187852002115479, -13.49168632951830737, -41.97295239668654432 ) ) ;
#16099=CARTESIAN_POINT ( 'NONE',  ( 0.8744876279028263033, -38.80702141274021955, -30.07266432244763621 ) ) ;
#16106=CARTESIAN_POINT ( 'NONE',  ( 0.6029442701453591180, 49.00093189689916073, -3.233248891398188718 ) ) ;
#16111=CARTESIAN_POINT ( 'NONE',  ( 0.7413678028165011646, 43.93608276952824809, -3.755891723600084831 ) ) ;
#16112=CARTESIAN_POINT ( 'NONE',  ( 0.5987334363312688534, -34.85272424572811900, -34.59552744392418333 ) ) ;
#16118=ORIENTED_EDGE ( 'NONE', *, *, #21428, .T. ) ;
#16120=CARTESIAN_POINT ( 'NONE',  ( 0.3676999524040366896, 29.04098611012985742, -33.20499524279568249 ) ) ;
#16122=CARTESIAN_POINT ( 'NONE',  ( 0.7413678028165013867, -40.51427950544401568, 17.40917137387654989 ) ) ;
#16125=( BOUNDED_SURFACE ( )  B_SPLINE_SURFACE ( 3, 1, ( 
 ( #11827, #6761 ),
 ( #7386, #45041 ),
 ( #12750, #21511 ),
 ( #30588, #40649 ) ),
 .UNSPECIFIED., .F., .F., .F. ) 
 B_SPLINE_SURFACE_WITH_KNOTS ( ( 4, 4 ),
 ( 2, 2 ),
 ( 0.000000000000000000, 1.000000000000000000 ),
 ( 0.000000000000000000, 1.000000000000000000 ),
 .UNSPECIFIED. ) 
 GEOMETRIC_REPRESENTATION_ITEM ( )  RATIONAL_B_SPLINE_SURFACE ( (
 ( 1.000000000000000000, 1.000000000000000000),
 ( 0.9953485035131437453, 0.8621029689291515030),
 ( 0.9953485035131437453, 0.8621029689291515030),
 ( 1.000000000000000000, 1.000000000000000000) ) ) 
 REPRESENTATION_ITEM ( '' )  SURFACE ( )  );
#16127=CARTESIAN_POINT ( 'NONE',  ( 0.1119898979215349644, 4.795286723730743716, 43.86304291187561688 ) ) ;
#16136=CARTESIAN_POINT ( 'NONE',  ( 0.08486401232817714080, 0.000000000000000000, 0.000000000000000000 ) ) ;
#16142=CARTESIAN_POINT ( 'NONE',  ( 0.5997462898726536595, -8.352924653000716404, 48.39194436975645175 ) ) ;
#16144=CARTESIAN_POINT ( 'NONE',  ( 5.901764892641288895, -48.86589420182303201, 3.180542610297211858 ) ) ;
#16151=ORIENTED_EDGE ( 'NONE', *, *, #19292, .F. ) ;
#16158=ADVANCED_FACE ( 'NONE', ( #34690 ), #9997, .F. ) ;
#16160=B_SPLINE_CURVE_WITH_KNOTS ( 'NONE', 3,
 ( #29534, #1319, #21382, #55808 ),
 .UNSPECIFIED., .F., .F.,
 ( 4, 4 ),
 ( 0.000000000000000000, 0.005013413432710148512 ),
 .UNSPECIFIED. ) ;
#16161=FACE_OUTER_BOUND ( 'NONE', #41120, .T. ) ;
#16167=CARTESIAN_POINT ( 'NONE',  ( 5.901764892641307547, -16.87177170878291221, -45.97102116384180448 ) ) ;
#16180=CARTESIAN_POINT ( 'NONE',  ( 0.08486401232817714080, 9.539392014169456147, -3.000000000000000000 ) ) ;
#16183=ORIENTED_EDGE ( 'NONE', *, *, #12026, .F. ) ;
#16184=CARTESIAN_POINT ( 'NONE',  ( -6.057079549204054558, 0.6087215340721632284, -19.24735538181013084 ) ) ;
#16194=CARTESIAN_POINT ( 'NONE',  ( 0.8744876279028263033, 21.91587810745035725, 43.93226988398016886 ) ) ;
#16196=CARTESIAN_POINT ( 'NONE',  ( 0.6016117650947689910, 37.61761104844107706, 31.56685592916568694 ) ) ;
#16198=CARTESIAN_POINT ( 'NONE',  ( 4.975610109902397937, 0.000000000000000000, 48.91267123290010943 ) ) ;
#16199=DIRECTION ( 'NONE',  ( -1.000000000000000000, -0.000000000000000000, -0.000000000000000000 ) ) ;
#16200=( BOUNDED_SURFACE ( )  B_SPLINE_SURFACE ( 3, 1, ( 
 ( #50210, #45850 ),
 ( #60516, #36443 ),
 ( #51426, #41769 ),
 ( #17632, #55827 ) ),
 .UNSPECIFIED., .F., .F., .F. ) 
 B_SPLINE_SURFACE_WITH_KNOTS ( ( 4, 4 ),
 ( 2, 2 ),
 ( 0.000000000000000000, 1.000000000000000000 ),
 ( 0.000000000000000000, 1.000000000000000000 ),
 .UNSPECIFIED. ) 
 GEOMETRIC_REPRESENTATION_ITEM ( )  RATIONAL_B_SPLINE_SURFACE ( (
 ( 1.000000000000000000, 1.000000000000000000),
 ( 0.9953485035131437453, 0.8621029689291523912),
 ( 0.9953485035131437453, 0.8621029689291523912),
 ( 1.000000000000000000, 1.000000000000000000) ) ) 
 REPRESENTATION_ITEM ( '' )  SURFACE ( )  );
#16202=CARTESIAN_POINT ( 'NONE',  ( 0.6000166863083106206, -13.47152005829798327, -47.22649287240508897 ) ) ;
#16212=CARTESIAN_POINT ( 'NONE',  ( 0.8744876279028306332, 49.04340454744548339, 2.257104511336577968 ) ) ;
#16213=CARTESIAN_POINT ( 'NONE',  ( 5.901764892641288895, -41.06410928599452603, -26.67827573115581430 ) ) ;
#16215=CARTESIAN_POINT ( 'NONE',  ( 0.1147471544378676211, 39.61889945511968847, -19.42408284677457075 ) ) ;
#16221=CARTESIAN_POINT ( 'NONE',  ( 0.5997462898726536595, 10.41743419021273631, 47.98988117339838055 ) ) ;
#16223=VERTEX_POINT ( 'NONE', #52538 ) ;
#16224=CARTESIAN_POINT ( 'NONE',  ( 0.2940135542859019235, 41.60821252483800947, -14.66278279111214822 ) ) ;
#16228=EDGE_LOOP ( 'NONE', ( #4075, #49035, #60662, #57700 ) ) ;
#16231=ORIENTED_EDGE ( 'NONE', *, *, #58797, .T. ) ;
#16242=VERTEX_POINT ( 'NONE', #34384 ) ;
#16243=CARTESIAN_POINT ( 'NONE',  ( 4.553261556744873317, -33.30082861731504096, 28.64601855797499042 ) ) ;
#16244=CARTESIAN_POINT ( 'NONE',  ( 0.6021447746440204973, -20.11649849682114777, -44.79807615641413321 ) ) ;
#16250=CARTESIAN_POINT ( 'NONE',  ( 0.6021448801613057400, 37.56148455560388300, -31.63346355690565304 ) ) ;
#16251=CARTESIAN_POINT ( 'NONE',  ( 0.1139756605157202229, 29.95793622539913414, 32.39563669400465784 ) ) ;
#16253=SURFACE_STYLE_FILL_AREA ( #12495 ) ;
#16254=CARTESIAN_POINT ( 'NONE',  ( 1.479689385636123067, -21.82878006710240015, 38.27647065822245764 ) ) ;
#16258=EDGE_CURVE ( 'NONE', #22153, #14826, #19732, .T. ) ;
#16260=ADVANCED_FACE ( 'NONE', ( #24048 ), #57155, .F. ) ;
#16263=CARTESIAN_POINT ( 'NONE',  ( 0.1129192098497447394, -38.68182264534125636, -21.22895156665819627 ) ) ;
#16268=CARTESIAN_POINT ( 'NONE',  ( 0.6027444965799114707, 28.20219763130657498, -40.20167365486376099 ) ) ;
#16270=CARTESIAN_POINT ( 'NONE',  ( -2.739355103387247858, 8.323596231104264831, 12.39214722042002848 ) ) ;
#16272=DIRECTION ( 'NONE',  ( -0.1011922191286467460, -0.9018493587347873319, 0.4200331759962215306 ) ) ;
#16283=CARTESIAN_POINT ( 'NONE',  ( 0.1147471544378675795, 20.68395129688062895, 38.97597140831149432 ) ) ;
#16289=ORIENTED_EDGE ( 'NONE', *, *, #11207, .F. ) ;
#16292=CARTESIAN_POINT ( 'NONE',  ( -6.078457390727109555, -17.35098001992631822, 8.350928294843967592 ) ) ;
#16297=CARTESIAN_POINT ( 'NONE',  ( -6.078726893082806448, -18.27395335922917141, -6.070969436048653911 ) ) ;
#16298=EDGE_CURVE ( 'NONE', #34962, #43681, #28201, .T. ) ;
#16304=VERTEX_POINT ( 'NONE', #49693 ) ;
#16305=LINE ( 'NONE', #49197, #44606 ) ;
#16306=CARTESIAN_POINT ( 'NONE',  ( 0.8753041380234530822, 36.80657072176735056, -32.50253343320360244 ) ) ;
#16312=CARTESIAN_POINT ( 'NONE',  ( 4.975610109902397937, 0.000000000000000000, 0.000000000000000000 ) ) ;
#16315=CARTESIAN_POINT ( 'NONE',  ( -6.078457390727109555, -18.27642172158497758, -6.063573211587741874 ) ) ;
#16320=CARTESIAN_POINT ( 'NONE',  ( 4.834790513006555379, -47.18049212391682090, -2.567197668549027423 ) ) ;
#16327=B_SPLINE_CURVE_WITH_KNOTS ( 'NONE', 3,
 ( #30036, #36535, #6199, #1830, #41238, #55601 ),
 .UNSPECIFIED., .F., .F.,
 ( 4, 2, 4 ),
 ( 1.843143693225357538E-18, 0.0002447193893791703586, 0.0004894387787583388740 ),
 .UNSPECIFIED. ) ;
#16330=CARTESIAN_POINT ( 'NONE',  ( 0.1158403557922069033, 36.95925186148238595, 24.10298755389733572 ) ) ;
#16333=CARTESIAN_POINT ( 'NONE',  ( 3.678834586032788234, 48.95863180854046703, -1.290248450541623182 ) ) ;
#16334=CARTESIAN_POINT ( 'NONE',  ( 3.678834586032788234, -44.67002089670381793, -20.07988054537172928 ) ) ;
#16335=ORIENTED_EDGE ( 'NONE', *, *, #56160, .T. ) ;
#16339=B_SPLINE_CURVE_WITH_KNOTS ( 'NONE', 3,
 ( #59021, #35250, #15826, #20829, #29910, #44057 ),
 .UNSPECIFIED., .F., .F.,
 ( 4, 2, 4 ),
 ( 0.000000000000000000, 0.0002293801035737105375, 0.0004587602071474210751 ),
 .UNSPECIFIED. ) ;
#16342=B_SPLINE_CURVE_WITH_KNOTS ( 'NONE', 3,
 ( #19276, #23351, #61836, #48083, #38394, #18979 ),
 .UNSPECIFIED., .F., .F.,
 ( 4, 2, 4 ),
 ( 5.421010862427522170E-19, 0.0002293801035737082065, 0.0004587602071474158709 ),
 .UNSPECIFIED. ) ;
#16351=CARTESIAN_POINT ( 'NONE',  ( -6.072942160501519027, 7.781335985898283347, 17.61405610765404717 ) ) ;
#16354=AXIS2_PLACEMENT_3D ( 'NONE', #46376, #17865, #3423 ) ;
#16358=EDGE_CURVE ( 'NONE', #33849, #45637, #27154, .T. ) ;
#16367=AXIS2_PLACEMENT_3D ( 'NONE', #53099, #5165, #44359 ) ;
#16373=CARTESIAN_POINT ( 'NONE',  ( 3.894904216938898323, 13.07376739574732660, -41.96666461083243860 ) ) ;
#16376=CARTESIAN_POINT ( 'NONE',  ( 0.6253024248130463203, 48.06489359206558021, 10.06032958709880099 ) ) ;
#16377=CARTESIAN_POINT ( 'NONE',  ( 3.727782113643637096, 7.686874865524217171, -43.28613785853096374 ) ) ;
#16385=B_SPLINE_CURVE_WITH_KNOTS ( 'NONE', 3,
 ( #50276, #39994, #10850, #1719 ),
 .UNSPECIFIED., .F., .F.,
 ( 4, 4 ),
 ( 0.000000000000000000, 0.005013413432710142441 ),
 .UNSPECIFIED. ) ;
#16386=CARTESIAN_POINT ( 'NONE',  ( 0.3676999524040366896, 16.00695768809390884, 41.10629986868691077 ) ) ;
#16388=CARTESIAN_POINT ( 'NONE',  ( 0.9268187852002115479, -41.22770443219307168, -15.62148264923511576 ) ) ;
#16392=CARTESIAN_POINT ( 'NONE',  ( 0.6000166863083090663, -48.77118664543507975, -5.761495891223787247 ) ) ;
#16403=CARTESIAN_POINT ( 'NONE',  ( 0.5980271706414711508, 11.60998973146016766, -47.72061798926175413 ) ) ;
#16406=CARTESIAN_POINT ( 'NONE',  ( 0.6026112563231247332, 48.16826574472209899, 9.558199100774150025 ) ) ;
#16410=ORIENTED_EDGE ( 'NONE', *, *, #47959, .F. ) ;
#16417=CARTESIAN_POINT ( 'NONE',  ( 4.553261556744875094, -29.69864478935419072, 32.36556910513705532 ) ) ;
#16418=CARTESIAN_POINT ( 'NONE',  ( 4.335381028904216727, 8.818319717467909769, -48.18707383754342999 ) ) ;
#16426=ORIENTED_EDGE ( 'NONE', *, *, #20926, .T. ) ;
#16431=ORIENTED_EDGE ( 'NONE', *, *, #35461, .F. ) ;
#16432=CARTESIAN_POINT ( 'NONE',  ( 0.3676999524040323597, 43.44964275340426951, -7.620966337964178550 ) ) ;
#16442=CARTESIAN_POINT ( 'NONE',  ( 0.6028777368367060907, -35.33680725117163490, 34.10058478390973136 ) ) ;
#16444=DIRECTION ( 'NONE',  ( 0.1011922191286467876, -0.9655114622251689260, -0.2398911234281835836 ) ) ;
#16446=ORIENTED_EDGE ( 'NONE', *, *, #14014, .T. ) ;
#16455=CARTESIAN_POINT ( 'NONE',  ( 0.2940133293163015304, -42.46217173550956403, -11.96680914371648896 ) ) ;
#16458=CARTESIAN_POINT ( 'NONE',  ( 0.5997462898726536595, -14.47257175146244457, -46.92649887902442885 ) ) ;
#16463=CARTESIAN_POINT ( 'NONE',  ( 4.975610109902397937, -48.11736577406850301, -8.784561349451310619 ) ) ;
#16464=CARTESIAN_POINT ( 'NONE',  ( -6.077587904424778920, -4.290907484552072049, -18.77189746277518623 ) ) ;
#16465=( BOUNDED_SURFACE ( )  B_SPLINE_SURFACE ( 3, 1, ( 
 ( #58, #52072 ),
 ( #15114, #19208 ),
 ( #38623, #14504 ),
 ( #33305, #5059 ) ),
 .UNSPECIFIED., .F., .F., .F. ) 
 B_SPLINE_SURFACE_WITH_KNOTS ( ( 4, 4 ),
 ( 2, 2 ),
 ( 0.000000000000000000, 1.000000000000000000 ),
 ( 0.000000000000000000, 1.000000000000000000 ),
 .UNSPECIFIED. ) 
 GEOMETRIC_REPRESENTATION_ITEM ( )  RATIONAL_B_SPLINE_SURFACE ( (
 ( 1.000000000000000000, 1.000000000000000000),
 ( 0.9953485035131437453, 0.8621029689291523912),
 ( 0.9953485035131437453, 0.8621029689291523912),
 ( 1.000000000000000000, 1.000000000000000000) ) ) 
 REPRESENTATION_ITEM ( '' )  SURFACE ( )  );
#16467=ORIENTED_EDGE ( 'NONE', *, *, #60018, .T. ) ;
#16469=CARTESIAN_POINT ( 'NONE',  ( 4.694002226626920127, 7.615834493546986828, 44.94756763622514484 ) ) ;
#16470=CARTESIAN_POINT ( 'NONE',  ( 4.975610109902397937, -43.81605102859474954, 21.73943604138237973 ) ) ;
#16471=CARTESIAN_POINT ( 'NONE',  ( 0.1158516988532803799, 44.03032832662167806, -2.876168681196155319 ) ) ;
#16475=CARTESIAN_POINT ( 'NONE',  ( 0.3676999524040323597, -13.34038000160386339, 42.04741186726771929 ) ) ;
#16479=EDGE_CURVE ( 'NONE', #41130, #7712, #22723, .T. ) ;
#16480=DIRECTION ( 'NONE',  ( 0.000000000000000000, 0.000000000000000000, 1.000000000000000000 ) ) ;
#16481=EDGE_CURVE ( 'NONE', #47629, #51544, #57089, .T. ) ;
#16489=( BOUNDED_SURFACE ( )  B_SPLINE_SURFACE ( 3, 1, ( 
 ( #46065, #3107 ),
 ( #22238, #17534 ),
 ( #14083, #4019 ),
 ( #33186, #37905 ) ),
 .UNSPECIFIED., .F., .F., .F. ) 
 B_SPLINE_SURFACE_WITH_KNOTS ( ( 4, 4 ),
 ( 2, 2 ),
 ( 0.000000000000000000, 1.000000000000000000 ),
 ( 0.000000000000000000, 1.000000000000000000 ),
 .UNSPECIFIED. ) 
 GEOMETRIC_REPRESENTATION_ITEM ( )  RATIONAL_B_SPLINE_SURFACE ( (
 ( 1.000000000000000000, 1.000000000000000000),
 ( 0.9953485035131437453, 0.8621029689291515030),
 ( 0.9953485035131437453, 0.8621029689291515030),
 ( 1.000000000000000000, 1.000000000000000000) ) ) 
 REPRESENTATION_ITEM ( '' )  SURFACE ( )  );
#16491=CARTESIAN_POINT ( 'NONE',  ( 1.830465331921978134, 44.02103255007548199, -1.588945909584584593 ) ) ;
#16494=VERTEX_POINT ( 'NONE', #46769 ) ;
#16500=CARTESIAN_POINT ( 'NONE',  ( 0.6039202388192953519, 48.16848798300492263, -9.558267535495215128 ) ) ;
#16502=VERTEX_POINT ( 'NONE', #23550 ) ;
#16503=CIRCLE ( 'NONE', #25522, 43.92652462719577500 ) ;
#16513=ORIENTED_EDGE ( 'NONE', *, *, #15280, .F. ) ;
#16517=CARTESIAN_POINT ( 'NONE',  ( -6.063463321072276813, 16.78636876910481845, 9.436009539370578736 ) ) ;
#16518=ORIENTED_EDGE ( 'NONE', *, *, #9612, .F. ) ;
#16520=CARTESIAN_POINT ( 'NONE',  ( 0.1129192098497447394, 39.54191224844646513, -19.58032082273713570 ) ) ;
#16521=EDGE_LOOP ( 'NONE', ( #29108, #33495, #39431, #47266 ) ) ;
#16522=CARTESIAN_POINT ( 'NONE',  ( 4.553261556744875094, 0.000000000000000000, 0.000000000000000000 ) ) ;
#16532=CARTESIAN_POINT ( 'NONE',  ( 0.1157506346131639274, 43.32810245082073664, 8.343632171543594822 ) ) ;
#16539=CARTESIAN_POINT ( 'NONE',  ( 3.050102900204245682, 30.89180545305748993, 31.32286074145379473 ) ) ;
#16550=CARTESIAN_POINT ( 'NONE',  ( 4.975610109902397937, 42.33317580307156192, -24.50207406657668230 ) ) ;
#16552=CARTESIAN_POINT ( 'NONE',  ( 0.5997462898726536595, 44.46857747280011353, 20.83500054451363326 ) ) ;
#16555=CARTESIAN_POINT ( 'NONE',  ( 0.3676999524040323597, 24.55639947020961600, 36.64606156713607277 ) ) ;
#16557=CARTESIAN_POINT ( 'NONE',  ( 0.1156495703730067576, -12.68516895305341308, -42.26144154975737877 ) ) ;
#16559=CARTESIAN_POINT ( 'NONE',  ( 0.1365634738349441879, 30.13243411101788993, -32.23195672261324773 ) ) ;
#16565=CARTESIAN_POINT ( 'NONE',  ( 0.1129192098497447394, -17.41650932123218354, 40.54154647825593827 ) ) ;
#16566=B_SPLINE_CURVE_WITH_KNOTS ( 'NONE', 3,
 ( #59858, #16976, #26974, #30416 ),
 .UNSPECIFIED., .F., .F.,
 ( 4, 4 ),
 ( 0.000000000000000000, 0.004442905043737217438 ),
 .UNSPECIFIED. ) ;
#16580=CARTESIAN_POINT ( 'NONE',  ( 0.6029443449137436017, 28.13086200025576389, -40.25163526002264547 ) ) ;
#16582=B_SPLINE_CURVE_WITH_KNOTS ( 'NONE', 3,
 ( #29202, #43028, #53603, #48317 ),
 .UNSPECIFIED., .F., .F.,
 ( 4, 4 ),
 ( 0.000000000000000000, 0.005013413432710148512 ),
 .UNSPECIFIED. ) ;
#16583=LINE ( 'NONE', #16270, #3503 ) ;
#16586=CARTESIAN_POINT ( 'NONE',  ( -6.072942160501519915, -16.14637491494715960, -10.49279464179992516 ) ) ;
#16588=CARTESIAN_POINT ( 'NONE',  ( 0.5997462898726536595, 48.97040376101512749, 3.667585803694950464 ) ) ;
#16592=CARTESIAN_POINT ( 'NONE',  ( 0.6039202388192953519, -35.15506827346180785, 34.28826165814228943 ) ) ;
#16593=ORIENTED_EDGE ( 'NONE', *, *, #50017, .T. ) ;
#16599=CARTESIAN_POINT ( 'NONE',  ( 4.694002226626921015, 1.805541223688327701, -45.55244002614676191 ) ) ;
#16606=CARTESIAN_POINT ( 'NONE',  ( -6.078457390727109555, -16.13585499094672926, 10.50850582854895698 ) ) ;
#16607=CIRCLE ( 'NONE', #48604, 48.91267123290010943 ) ;
#16614=CARTESIAN_POINT ( 'NONE',  ( -6.063463321072278589, 19.09660126457254492, 2.477957348582926045 ) ) ;
#16625=ORIENTED_EDGE ( 'NONE', *, *, #23256, .T. ) ;
#16628=FACE_OUTER_BOUND ( 'NONE', #20067, .T. ) ;
#16629=CARTESIAN_POINT ( 'NONE',  ( 0.8744876279028306332, -26.20733431478126008, -41.51536677536140729 ) ) ;
#16630=SURFACE_SIDE_STYLE ('',( #25399 ) ) ;
#16631=CARTESIAN_POINT ( 'NONE',  ( 0.7044674535452954967, 46.33602660604208978, 16.27191940660552660 ) ) ;
#16637=CARTESIAN_POINT ( 'NONE',  ( 0.5980271706414711508, 23.33483692714806068, -43.21498152753358823 ) ) ;
#16638=CIRCLE ( 'NONE', #25653, 43.92652462719577500 ) ;
#16639=CONICAL_SURFACE ( 'NONE', #33688, 48.91267123290010943, 0.04450589592585339760 ) ;
#16644=CARTESIAN_POINT ( 'NONE',  ( 4.335381028904216727, 6.815065961880201861, 48.51094436928195819 ) ) ;
#16648=CARTESIAN_POINT ( 'NONE',  ( 0.6029443449137436017, -45.53481268790790182, 18.38804969159247449 ) ) ;
#16651=CARTESIAN_POINT ( 'NONE',  ( 3.050102900204245682, -3.218072654074529027, -43.87561119313505031 ) ) ;
#16653=CARTESIAN_POINT ( 'NONE',  ( 3.894904216938898323, -41.89961406944992461, 13.28708671257003537 ) ) ;
#16660=VERTEX_POINT ( 'NONE', #50557 ) ;
#16664=CARTESIAN_POINT ( 'NONE',  ( 0.6029443199889047422, 10.92745038804929791, 47.87617852200740742 ) ) ;
#16669=CARTESIAN_POINT ( 'NONE',  ( -6.078726893082806448, 19.25601281685051802, -0.003415553934477524867 ) ) ;
#16673=VECTOR ( 'NONE', #15860, 1000.000000000000114 ) ;
#16674=ORIENTED_EDGE ( 'NONE', *, *, #38884, .T. ) ;
#16675=CARTESIAN_POINT ( 'NONE',  ( 0.1158816050234198897, 15.24427584951536296, 41.40717444029529304 ) ) ;
#16676=CARTESIAN_POINT ( 'NONE',  ( 3.240649175237395152, -30.30232522355354874, -31.89097056289822518 ) ) ;
#16693=CARTESIAN_POINT ( 'NONE',  ( 3.050102900204245682, 8.016424753797352309, -43.25693219987711302 ) ) ;
#16697=ORIENTED_EDGE ( 'NONE', *, *, #2826, .T. ) ;
#16701=CARTESIAN_POINT ( 'NONE',  ( 0.7044674535452954967, 49.05595398932693740, -2.305667150293843282 ) ) ;
#16708=CARTESIAN_POINT ( 'NONE',  ( -6.063463321072276813, -12.93474753578269798, 14.26578980165603383 ) ) ;
#16712=CARTESIAN_POINT ( 'NONE',  ( 3.559346040607745287, 41.03794546218089323, -15.78978510889415077 ) ) ;
#16719=CARTESIAN_POINT ( 'NONE',  ( 0.6008122571543323964, 48.28333758046749580, 8.959568212583292279 ) ) ;
#16723=CARTESIAN_POINT ( 'NONE',  ( 0.5997462898726536595, 17.44942740672471260, -45.90282249842328355 ) ) ;
#16724=B_SPLINE_CURVE_WITH_KNOTS ( 'NONE', 3,
 ( #30285, #25284, #44430, #16830 ),
 .UNSPECIFIED., .F., .F.,
 ( 4, 4 ),
 ( 0.000000000000000000, 0.005013413432710150247 ),
 .UNSPECIFIED. ) ;
#16731=CARTESIAN_POINT ( 'NONE',  ( 0.6000166863083106206, -31.02657807334564666, 38.06803035050592854 ) ) ;
#16739=CARTESIAN_POINT ( 'NONE',  ( 0.6000166863083090663, 46.77044519531233391, -14.97828220927684839 ) ) ;
#16743=CARTESIAN_POINT ( 'NONE',  ( 4.975610109902397937, -32.45573888811600227, -36.59336579715246529 ) ) ;
#16749=ORIENTED_EDGE ( 'NONE', *, *, #44109, .T. ) ;
#16750=B_SPLINE_CURVE_WITH_KNOTS ( 'NONE', 3,
 ( #38342, #37413, #56793, #24213, #14531, #52095, #9192, #4462, #28299, #23915, #13923, #383, #33634, #47725, #42130, #38049, #4773, #4163, #56486, #23601, #52404, #23001, #43350, #33333, #23300 ),
 .UNSPECIFIED., .F., .F.,
 ( 4, 3, 3, 3, 3, 3, 3, 3, 4 ),
 ( 6.992893892674702526E-18, 0.0005656085177311382306, 0.001131215744874499839, 0.001696821861372765482, 0.002262427090022498151, 0.002828031679238744191, 0.003393635864401604429, 0.003977030878808129888, 0.004561030005651157265 ),
 .UNSPECIFIED. ) ;
#16751=CARTESIAN_POINT ( 'NONE',  ( 0.6039202388192953519, 4.542059820466915809, -48.89717175293773010 ) ) ;
#16752=CARTESIAN_POINT ( 'NONE',  ( 0.2940133293163014749, -40.58327630480741277, -17.29850380656375108 ) ) ;
#16755=CARTESIAN_POINT ( 'NONE',  ( 0.6029443449137436017, -7.880500877275125937, 48.47099384071466943 ) ) ;
#16756=CARTESIAN_POINT ( 'NONE',  ( -6.078075953587585900, 15.43522972334815258, -11.51298647765233518 ) ) ;
#16757=CARTESIAN_POINT ( 'NONE',  ( 2.706805983486679779, -43.82831923521022333, -3.981776781319652514 ) ) ;
#16764=FACE_OUTER_BOUND ( 'NONE', #4585, .T. ) ;
#16771=ADVANCED_FACE ( 'NONE', ( #42426 ), #10723, .F. ) ;
#16774=CARTESIAN_POINT ( 'NONE',  ( 0.1368894036331286812, -11.94180260692783335, 42.47651911845537853 ) ) ;
#16785=CARTESIAN_POINT ( 'NONE',  ( 3.240649175237394708, 35.83975900205959420, 25.51032324514801175 ) ) ;
#16790=CARTESIAN_POINT ( 'NONE',  ( 0.6253024248130445439, 33.51950167461898644, -35.88714581717047736 ) ) ;
#16793=CARTESIAN_POINT ( 'NONE',  ( 4.553261556744873317, 7.233533384970671776, 43.32684572631789166 ) ) ;
#16801=CARTESIAN_POINT ( 'NONE',  ( 2.879087469061463178, 35.90367940211508824, -25.43673489608120164 ) ) ;
#16805=ORIENTED_EDGE ( 'NONE', *, *, #12884, .T. ) ;
#16808=B_SPLINE_CURVE_WITH_KNOTS ( 'NONE', 3,
 ( #18839, #18212, #38261, #37641 ),
 .UNSPECIFIED., .F., .F.,
 ( 4, 4 ),
 ( 0.000000000000000000, 0.005013413432710148512 ),
 .UNSPECIFIED. ) ;
#16810=LINE ( 'NONE', #26495, #51785 ) ;
#16816=EDGE_CURVE ( 'NONE', #26055, #5134, #18926, .T. ) ;
#16830=CARTESIAN_POINT ( 'NONE',  ( 4.975610109902397937, -22.11219452748616021, 43.62912170003406942 ) ) ;
#16831=ORIENTED_EDGE ( 'NONE', *, *, #5571, .F. ) ;
#16835=CARTESIAN_POINT ( 'NONE',  ( -6.057079549204054558, 17.85280408805624219, -7.218629876453069194 ) ) ;
#16836=CARTESIAN_POINT ( 'NONE',  ( 0.6253024248130475415, 11.59571641818049059, -47.71774919426502493 ) ) ;
#16840=ORIENTED_EDGE ( 'NONE', *, *, #47112, .T. ) ;
#16844=VERTEX_POINT ( 'NONE', #58017 ) ;
#16849=ADVANCED_FACE ( 'NONE', ( #57097 ), #55522, .F. ) ;
#16855=ORIENTED_EDGE ( 'NONE', *, *, #12365, .F. ) ;
#16856=CARTESIAN_POINT ( 'NONE',  ( 0.1129192098497455998, -27.13044910148877165, -34.79785222304216319 ) ) ;
#16861=ORIENTED_EDGE ( 'NONE', *, *, #39638, .T. ) ;
#16863=CARTESIAN_POINT ( 'NONE',  ( 0.7413678028165008316, 30.33017393467367739, 32.00885253898809424 ) ) ;
#16868=ORIENTED_EDGE ( 'NONE', *, *, #47859, .F. ) ;
#16873=CARTESIAN_POINT ( 'NONE',  ( 0.3676999524040323597, 44.06746933160595603, -2.002181318164867552 ) ) ;
#16874=CARTESIAN_POINT ( 'NONE',  ( 0.6026777506516367566, 44.31962571317131250, 21.14987393063190879 ) ) ;
#16878=CARTESIAN_POINT ( 'NONE',  ( 0.6024113833632039894, 4.498702367898188115, 48.90095649479604134 ) ) ;
#16883=B_SPLINE_CURVE_WITH_KNOTS ( 'NONE', 3,
 ( #50747, #7206, #45468, #60757, #21640, #26959 ),
 .UNSPECIFIED., .F., .F.,
 ( 4, 2, 4 ),
 ( 1.870625823323990238E-17, 0.0002293755540694317793, 0.0004587511081388448561 ),
 .UNSPECIFIED. ) ;
#16885=B_SPLINE_CURVE_WITH_KNOTS ( 'NONE', 3,
 ( #53096, #9892, #61254, #61559, #5162, #4237, #24293, #18680, #33712, #14606, #43427, #14918, #57784, #19609, #19001, #38730, #61861, #52790, #47190 ),
 .UNSPECIFIED., .F., .F.,
 ( 4, 3, 3, 3, 3, 3, 4 ),
 ( 5.204329244184724719E-18, 0.0002612768053151714380, 0.0003919133833142906002, 0.0005225499612322623798, 0.0006531865391693369343, 0.0008112755173415195321, 0.0009693688056799705131 ),
 .UNSPECIFIED. ) ;
#16887=VECTOR ( 'NONE', #43071, 1000.000000000000000 ) ;
#16898=CARTESIAN_POINT ( 'NONE',  ( 0.6016117650947689910, -47.58864192223926182, -12.11908471137122234 ) ) ;
#16904=CARTESIAN_POINT ( 'NONE',  ( 0.6000166863083090663, -35.63988196839337519, -33.78790160675033860 ) ) ;
#16906=EDGE_LOOP ( 'NONE', ( #30058, #32365, #28446, #18138 ) ) ;
#16909=ORIENTED_EDGE ( 'NONE', *, *, #40054, .F. ) ;
#16913=ORIENTED_EDGE ( 'NONE', *, *, #26243, .F. ) ;
#16936=CARTESIAN_POINT ( 'NONE',  ( 4.335381028904216727, -41.60039470203984280, 25.86820458205096784 ) ) ;
#16944=CARTESIAN_POINT ( 'NONE',  ( 3.390910168358336918, -34.03117032279242693, 27.85635624044769898 ) ) ;
#16945=CARTESIAN_POINT ( 'NONE',  ( 2.299652685299201860, 46.11347781897552522, 16.66819991171828619 ) ) ;
#16955=CARTESIAN_POINT ( 'NONE',  ( 0.5997462898726536595, 11.43624519451647714, 47.75734421002918140 ) ) ;
#16960=CARTESIAN_POINT ( 'NONE',  ( 0.8744876279028263033, 33.66006955981258386, -35.74003032466635688 ) ) ;
#16963=VECTOR ( 'NONE', #28241, 1000.000000000000114 ) ;
#16968=DIRECTION ( 'NONE',  ( -1.000000000000000000, -0.000000000000000000, -0.000000000000000000 ) ) ;
#16971=CARTESIAN_POINT ( 'NONE',  ( -6.078726893082806448, -11.01948708261742738, 15.79129335123464983 ) ) ;
#16972=ORIENTED_EDGE ( 'NONE', *, *, #3725, .T. ) ;
#16976=CARTESIAN_POINT ( 'NONE',  ( 2.299746137290199943, 15.71953357350441216, -46.44542606024415221 ) ) ;
#16980=CARTESIAN_POINT ( 'NONE',  ( 0.6028777368367060907, 44.28197450755376252, -21.22843760203353014 ) ) ;
#16981=VERTEX_POINT ( 'NONE', #2242 ) ;
#16984=ORIENTED_EDGE ( 'NONE', *, *, #22281, .F. ) ;
#16992=CARTESIAN_POINT ( 'NONE',  ( -6.079354080745853928, 16.77752703747123064, 9.450266755763248483 ) ) ;
#16998=CARTESIAN_POINT ( 'NONE',  ( -6.077587904424778920, -14.66646125808257395, 12.47761738310216550 ) ) ;
#16999=CARTESIAN_POINT ( 'NONE',  ( 3.678748215320119197, -43.55036755802045434, -22.40487223486901414 ) ) ;
#17002=EDGE_CURVE ( 'NONE', #55634, #26582, #38022, .T. ) ;
#17004=ORIENTED_EDGE ( 'NONE', *, *, #20916, .T. ) ;
#17005=CARTESIAN_POINT ( 'NONE',  ( 4.834790513006553603, -35.67803047646607695, -30.97850032271963272 ) ) ;
#17006=CARTESIAN_POINT ( 'NONE',  ( 0.1154773475650540115, -12.38201431068792679, 42.35126151197906808 ) ) ;
#17009=CARTESIAN_POINT ( 'NONE',  ( 0.3676999524040366896, 19.66859742988788184, -39.48540057367844724 ) ) ;
#17010=CARTESIAN_POINT ( 'NONE',  ( 4.553261556744875094, -20.11719049292643646, -39.04917684785361587 ) ) ;
#17016=CARTESIAN_POINT ( 'NONE',  ( 0.7413678028165008316, 42.13455360898415591, 13.00636320967101511 ) ) ;
#17021=B_SPLINE_CURVE_WITH_KNOTS ( 'NONE', 3,
 ( #29971, #39709, #39093, #58758, #49080, #38468, #24974, #1143, #43481, #29658, #524, #25272, #57523, #19663, #58149, #33769, #34081, #33459, #44415 ),
 .UNSPECIFIED., .F., .F.,
 ( 4, 3, 3, 3, 3, 3, 4 ),
 ( 1.734776414728241573E-18, 0.0002612768053151691612, 0.0003919133833142924433, 0.0005225499612322612956, 0.0006531865391693340069, 0.0008112755173415185563, 0.0009693688056799734405 ),
 .UNSPECIFIED. ) ;
#17026=CARTESIAN_POINT ( 'NONE',  ( -6.078726893082806448, 19.09748444646205456, 2.465791776663210033 ) ) ;
#17030=CARTESIAN_POINT ( 'NONE',  ( 2.009741617377216460, 41.34405726916381951, -15.17145365965789772 ) ) ;
#17035=CARTESIAN_POINT ( 'NONE',  ( 0.3676999524040366896, 43.96170928169366476, -3.649479463524768263 ) ) ;
#17036=FACE_OUTER_BOUND ( 'NONE', #50778, .T. ) ;
#17042=CARTESIAN_POINT ( 'NONE',  ( 2.879087469061463178, 2.498337803474706131, -43.93017169330331484 ) ) ;
#17046=CARTESIAN_POINT ( 'NONE',  ( 0.5987334308729317378, 36.99765834705322476, -32.29142584966560747 ) ) ;
#17047=DIRECTION ( 'NONE',  ( 0.1011922191286467876, 0.3314939457937465250, -0.9380148712520033349 ) ) ;
#17055=CARTESIAN_POINT ( 'NONE',  ( 0.7044674535452954967, 46.86672925371332354, -14.67352758780377009 ) ) ;
#17058=B_SPLINE_CURVE_WITH_KNOTS ( 'NONE', 3,
 ( #55668, #12798, #23718, #13099, #8363, #3968 ),
 .UNSPECIFIED., .F., .F.,
 ( 4, 2, 4 ),
 ( 0.000000000000000000, 0.0002293801035737084775, 0.0004587602071474169551 ),
 .UNSPECIFIED. ) ;
#17062=EDGE_CURVE ( 'NONE', #20594, #27771, #54375, .T. ) ;
#17065=CARTESIAN_POINT ( 'NONE',  ( 0.8753041380234530822, -0.6841799139051543133, 49.09857661601188283 ) ) ;
#17071=CARTESIAN_POINT ( 'NONE',  ( 0.8744876279028306332, 41.62483489565916983, 26.03311679935014666 ) ) ;
#17082=CARTESIAN_POINT ( 'NONE',  ( 0.8744876279028306332, -48.57046782678520458, 7.159588358747709158 ) ) ;
#17094=CARTESIAN_POINT ( 'NONE',  ( 2.648799415243708655, 46.95584109391743510, 14.13033794544112354 ) ) ;
#17096=CARTESIAN_POINT ( 'NONE',  ( 0.6029443449137434907, 41.18007799215122589, -26.75333090558397586 ) ) ;
#17118=CARTESIAN_POINT ( 'NONE',  ( 5.901764892641307547, 13.97448418306336926, -46.93298689894976405 ) ) ;
#17123=ORIENTED_EDGE ( 'NONE', *, *, #18060, .F. ) ;
#17130=CARTESIAN_POINT ( 'NONE',  ( 0.8744876279028306332, -0.6840263623749832655, 49.09055060105833235 ) ) ;
#17132=( BOUNDED_SURFACE ( )  B_SPLINE_SURFACE ( 3, 1, ( 
 ( #55673, #60079 ),
 ( #41613, #18105 ),
 ( #13724, #55366 ),
 ( #17798, #12489 ) ),
 .UNSPECIFIED., .F., .F., .F. ) 
 B_SPLINE_SURFACE_WITH_KNOTS ( ( 4, 4 ),
 ( 2, 2 ),
 ( 0.000000000000000000, 1.000000000000000000 ),
 ( 0.000000000000000000, 1.000000000000000000 ),
 .UNSPECIFIED. ) 
 GEOMETRIC_REPRESENTATION_ITEM ( )  RATIONAL_B_SPLINE_SURFACE ( (
 ( 1.000000000000000000, 1.000000000000000000),
 ( 0.9754377213608244057, 0.9999580625633939235),
 ( 0.9754377213608244057, 0.9999580625633939235),
 ( 1.000000000000000000, 1.000000000000000000) ) ) 
 REPRESENTATION_ITEM ( '' )  SURFACE ( )  );
#17136=EDGE_LOOP ( 'NONE', ( #34197, #32308, #45035, #31144 ) ) ;
#17142=CARTESIAN_POINT ( 'NONE',  ( -6.078726893082806448, -18.27395335922917141, -6.070969436048653911 ) ) ;
#17144=ORIENTED_EDGE ( 'NONE', *, *, #39913, .T. ) ;
#17146=DIRECTION ( 'NONE',  ( 0.000000000000000000, 0.000000000000000000, -1.000000000000000000 ) ) ;
#17155=CARTESIAN_POINT ( 'NONE',  ( 0.6029442701453591180, -48.71537682882689069, -6.193325890317136206 ) ) ;
#17158=CARTESIAN_POINT ( 'NONE',  ( 0.1155031312995260795, 43.27794838057445048, 8.600047470807512084 ) ) ;
#17160=CARTESIAN_POINT ( 'NONE',  ( 4.335381028904216727, 0.5556724879607355394, 48.98416147848679003 ) ) ;
#17163=ORIENTED_EDGE ( 'NONE', *, *, #36184, .T. ) ;
#17164=CARTESIAN_POINT ( 'NONE',  ( 4.975610109902397937, 48.58133226360775581, 5.683622315980952244 ) ) ;
#17170=EDGE_LOOP ( 'NONE', ( #34605, #11921, #4371, #14437 ) ) ;
#17172=CARTESIAN_POINT ( 'NONE',  ( 4.553261556744875094, -33.59363643963393997, 28.30206982864213217 ) ) ;
#17175=CARTESIAN_POINT ( 'NONE',  ( 2.648799415243708655, 43.56092747588142799, -22.51584021817966885 ) ) ;
#17179=VECTOR ( 'NONE', #51635, 1000.000000000000114 ) ;
#17185=CARTESIAN_POINT ( 'NONE',  ( 0.3676999524040323597, 43.96170928169360081, 3.649479463525401535 ) ) ;
#17189=ADVANCED_FACE ( 'NONE', ( #57319 ), #8316, .F. ) ;
#17193=ORIENTED_EDGE ( 'NONE', *, *, #57768, .T. ) ;
#17195=EDGE_CURVE ( 'NONE', #40357, #19147, #25071, .T. ) ;
#17199=CARTESIAN_POINT ( 'NONE',  ( 4.553261556744873317, -25.31600221269608397, -35.89762663172042068 ) ) ;
#17201=ORIENTED_EDGE ( 'NONE', *, *, #48309, .F. ) ;
#17216=CARTESIAN_POINT ( 'NONE',  ( 0.1158403557922069033, 20.37552838888686679, 39.13793747832765035 ) ) ;
#17224=VERTEX_POINT ( 'NONE', #40434 ) ;
#17227=CARTESIAN_POINT ( 'NONE',  ( 0.6016118706126976079, -25.15846823153664147, -42.17348137190825241 ) ) ;
#17230=ORIENTED_EDGE ( 'NONE', *, *, #26170, .T. ) ;
#17235=VERTEX_POINT ( 'NONE', #49185 ) ;
#17236=B_SPLINE_CURVE_WITH_KNOTS ( 'NONE', 3,
 ( #45483, #26351, #1916, #11650, #11977, #40800 ),
 .UNSPECIFIED., .F., .F.,
 ( 4, 2, 4 ),
 ( 1.951563910473907981E-18, 0.0002447193893791694912, 0.0004894387787583370309 ),
 .UNSPECIFIED. ) ;
#17237=ORIENTED_EDGE ( 'NONE', *, *, #43887, .T. ) ;
#17243=CARTESIAN_POINT ( 'NONE',  ( -6.078726893082806448, -16.14009859332537999, -10.50196451462564262 ) ) ;
#17244=CARTESIAN_POINT ( 'NONE',  ( 0.5549461598389364703, -34.81405122074062319, 27.07765745160486404 ) ) ;
#17248=LINE ( 'NONE', #59837, #43389 ) ;
#17262=CARTESIAN_POINT ( 'NONE',  ( 4.553261556744875094, 0.000000000000000000, 0.000000000000000000 ) ) ;
#17264=EDGE_CURVE ( 'NONE', #22365, #17224, #41666, .T. ) ;
#17266=EDGE_CURVE ( 'NONE', #10962, #17686, #3234, .T. ) ;
#17268=CARTESIAN_POINT ( 'NONE',  ( 0.8753041380234524160, 40.66072100792177935, -27.52896828776786009 ) ) ;
#17271=CARTESIAN_POINT ( 'NONE',  ( 0.5549461598389364703, -2.290644651554962774, -44.04509782651307859 ) ) ;
#17272=CARTESIAN_POINT ( 'NONE',  ( 4.975610109902397937, 0.000000000000000000, 0.000000000000000000 ) ) ;
#17273=CARTESIAN_POINT ( 'NONE',  ( 1.296416391601052709, -42.33482010800442197, 12.25032164880019891 ) ) ;
#17277=CARTESIAN_POINT ( 'NONE',  ( 0.6026112563231247332, 44.31956384428061568, -21.14987601753119861 ) ) ;
#17280=CARTESIAN_POINT ( 'NONE',  ( 0.7948884756798509921, -45.17791574701932689, -19.22640302696720482 ) ) ;
#17281=FACE_OUTER_BOUND ( 'NONE', #14515, .T. ) ;
#17282=CARTESIAN_POINT ( 'NONE',  ( 2.359973842542475886, -11.07206836914077108, 42.60921492660445864 ) ) ;
#17289=EDGE_CURVE ( 'NONE', #53243, #41130, #2205, .T. ) ;
#17290=ORIENTED_EDGE ( 'NONE', *, *, #57194, .F. ) ;
#17291=CARTESIAN_POINT ( 'NONE',  ( 0.8753041380234465318, -49.09527960836077654, -0.8898584437169343442 ) ) ;
#17295=CARTESIAN_POINT ( 'NONE',  ( 1.657374760986086271, -0.1743100015788275059, 44.05519337462489915 ) ) ;
#17299=CARTESIAN_POINT ( 'NONE',  ( 2.359973842542475442, -37.59610043656226708, 22.90565708720059490 ) ) ;
#17302=CARTESIAN_POINT ( 'NONE',  ( 4.975610109902397937, 2.142807115709095100, 48.86571174967821918 ) ) ;
#17307=EDGE_CURVE ( 'NONE', #33349, #12356, #54257, .T. ) ;
#17308=DIRECTION ( 'NONE',  ( 0.000000000000000000, 0.000000000000000000, 1.000000000000000000 ) ) ;
#17311=CARTESIAN_POINT ( 'NONE',  ( 0.6039202388192952409, -1.748061966039296866, 49.07655236680626132 ) ) ;
#17314=ORIENTED_EDGE ( 'NONE', *, *, #6330, .T. ) ;
#17315=ORIENTED_EDGE ( 'NONE', *, *, #40584, .F. ) ;
#17317=CARTESIAN_POINT ( 'NONE',  ( 0.9268187852002115479, 42.14386952154099220, 12.94791854546337539 ) ) ;
#17319=CARTESIAN_POINT ( 'NONE',  ( 0.8753041380234530822, 46.31375555491767670, -16.31485134079719401 ) ) ;
#17325=CARTESIAN_POINT ( 'NONE',  ( -6.078075953587585900, 19.09727103821293070, 2.467673629183867678 ) ) ;
#17328=CARTESIAN_POINT ( 'NONE',  ( 1.657374760986086493, 41.40460839256266468, -15.05153982523958334 ) ) ;
#17334=CARTESIAN_POINT ( 'NONE',  ( 0.5997462898726536595, 17.44942740672405534, 45.90282249842351803 ) ) ;
#17339=B_SPLINE_CURVE_WITH_KNOTS ( 'NONE', 3,
 ( #51288, #57750, #33674, #23957, #27491, #28960, #47458, #4507, #23646, #18969, #57133, #29259, #14267, #52443, #118, #19269 ),
 .UNSPECIFIED., .F., .F.,
 ( 4, 3, 3, 3, 3, 4 ),
 ( 2.194378057379452319E-17, 0.0002612764279487740844, 0.0003919131003184803835, 0.0005225497727000661232, 0.0007837925190632462217, 0.001045051706266716734 ),
 .UNSPECIFIED. ) ;
#17343=EDGE_CURVE ( 'NONE', #17964, #43366, #46884, .T. ) ;
#17344=EDGE_LOOP ( 'NONE', ( #61640, #47038, #59009, #2298 ) ) ;
#17346=CARTESIAN_POINT ( 'NONE',  ( 4.694002226626920127, -16.06750747807276980, -42.66286411960886937 ) ) ;
#17352=ORIENTED_EDGE ( 'NONE', *, *, #12473, .T. ) ;
#17354=EDGE_CURVE ( 'NONE', #8818, #55634, #55719, .T. ) ;
#17358=EDGE_CURVE ( 'NONE', #9740, #24079, #22542, .T. ) ;
#17359=CARTESIAN_POINT ( 'NONE',  ( 0.3676999524040323597, -17.09834788623527047, -40.66444494744902727 ) ) ;
#17362=CARTESIAN_POINT ( 'NONE',  ( -6.077587904424778920, 5.484810954822209261, 18.45840919970604688 ) ) ;
#17365=VERTEX_POINT ( 'NONE', #8120 ) ;
#17368=CARTESIAN_POINT ( 'NONE',  ( 0.6008122571543323964, -48.64681258932709795, 6.711346762327411675 ) ) ;
#17374=CARTESIAN_POINT ( 'NONE',  ( 0.8753041380234471980, -48.80600061351585595, 5.395612290228920749 ) ) ;
#17375=CARTESIAN_POINT ( 'NONE',  ( -6.077587904424778920, 18.62472241188256206, -4.890371813497390363 ) ) ;
#17378=ORIENTED_EDGE ( 'NONE', *, *, #25249, .T. ) ;
#17380=CARTESIAN_POINT ( 'NONE',  ( 0.2940135542859003137, 30.25014503988288084, 32.11182451617268185 ) ) ;
#17385=CARTESIAN_POINT ( 'NONE',  ( -6.063463321072276813, 15.42324870294179995, -11.53012800998644494 ) ) ;
#17386=CARTESIAN_POINT ( 'NONE',  ( 50.15577769773999961, 12.80000000000000071, -3.000000000000000000 ) ) ;
#17391=CARTESIAN_POINT ( 'NONE',  ( 0.8753041380234524160, 46.87455897190329068, 14.62580080072680921 ) ) ;
#17395=VERTEX_POINT ( 'NONE', #29083 ) ;
#17403=B_SPLINE_CURVE_WITH_KNOTS ( 'NONE', 3,
 ( #2036, #54039, #1119, #44686 ),
 .UNSPECIFIED., .F., .F.,
 ( 4, 4 ),
 ( 2.189128766608093472E-17, 0.004559932413162187670 ),
 .UNSPECIFIED. ) ;
#17405=CARTESIAN_POINT ( 'NONE',  ( 0.5997462898726536595, -2.096122762664449635, -49.06279547180479739 ) ) ;
#17406=CARTESIAN_POINT ( 'NONE',  ( 2.533389852662419894, 36.00264103935801074, -25.32311927714972200 ) ) ;
#17408=CARTESIAN_POINT ( 'NONE',  ( 0.6027444965799114707, -1.704510300802369427, 49.07782758560019687 ) ) ;
#17418=CARTESIAN_POINT ( 'NONE',  ( 4.335381028904216727, 14.90794766671208471, -46.66379693114267013 ) ) ;
#17420=EDGE_CURVE ( 'NONE', #855, #41374, #11698, .T. ) ;
#17424=CARTESIAN_POINT ( 'NONE',  ( 4.060580049360325461, 38.04379863422499852, 22.00311523029749239 ) ) ;
#17426=VERTEX_POINT ( 'NONE', #47583 ) ;
#17430=CARTESIAN_POINT ( 'NONE',  ( 0.5997462898726536595, 48.09935696025637952, -9.899671214446758682 ) ) ;
#17432=DIRECTION ( 'NONE',  ( 0.000000000000000000, 0.000000000000000000, 1.000000000000000000 ) ) ;
#17433=CARTESIAN_POINT ( 'NONE',  ( 0.8744876279028306332, -24.68559978112762110, 42.43785119236699188 ) ) ;
#17436=DIRECTION ( 'NONE',  ( 0.000000000000000000, 0.000000000000000000, -1.000000000000000000 ) ) ;
#17437=ORIENTED_EDGE ( 'NONE', *, *, #34754, .F. ) ;
#17438=CARTESIAN_POINT ( 'NONE',  ( -6.063463321072278589, 17.85520303107530538, -7.211946838305800966 ) ) ;
#17441=CARTESIAN_POINT ( 'NONE',  ( -6.077587904424778920, 16.78120357693980935, 9.443898977818069085 ) ) ;
#17446=CARTESIAN_POINT ( 'NONE',  ( -6.078726893082806448, -14.66019907464911043, 12.48489504803213812 ) ) ;
#17448=CARTESIAN_POINT ( 'NONE',  ( -6.079354080745853928, 12.00499765711163036, 15.05566293794153232 ) ) ;
#17451=ORIENTED_EDGE ( 'NONE', *, *, #2546, .F. ) ;
#17454=DIRECTION ( 'NONE',  ( -0.1011922191286467321, -0.3556331495180506952, 0.9291314211411062507 ) ) ;
#17460=ORIENTED_EDGE ( 'NONE', *, *, #37026, .T. ) ;
#17472=CARTESIAN_POINT ( 'NONE',  ( 0.7948878604505671408, -48.79909643919308593, -5.417271824151775661 ) ) ;
#17475=CARTESIAN_POINT ( 'NONE',  ( -6.077587904424778920, -17.35179747939703887, 8.349320069797363075 ) ) ;
#17483=( BOUNDED_SURFACE ( )  B_SPLINE_SURFACE ( 3, 1, ( 
 ( #33060, #28034 ),
 ( #4194, #37771 ),
 ( #18640, #56827 ),
 ( #38078, #28333 ) ),
 .UNSPECIFIED., .F., .F., .F. ) 
 B_SPLINE_SURFACE_WITH_KNOTS ( ( 4, 4 ),
 ( 2, 2 ),
 ( 0.000000000000000000, 1.000000000000000000 ),
 ( 0.000000000000000000, 1.000000000000000000 ),
 .UNSPECIFIED. ) 
 GEOMETRIC_REPRESENTATION_ITEM ( )  RATIONAL_B_SPLINE_SURFACE ( (
 ( 1.000000000000000000, 1.000000000000000000),
 ( 0.9754377213608244057, 0.9999580625633939235),
 ( 0.9754377213608244057, 0.9999580625633939235),
 ( 1.000000000000000000, 1.000000000000000000) ) ) 
 REPRESENTATION_ITEM ( '' )  SURFACE ( )  );
#17494=CARTESIAN_POINT ( 'NONE',  ( 4.060580049360325461, 17.32852353021683101, 40.38799285210804157 ) ) ;
#17498=ADVANCED_FACE ( 'NONE', ( #44750 ), #46056, .F. ) ;
#17501=CARTESIAN_POINT ( 'NONE',  ( 4.975610109902397937, -17.43163075979644816, -45.70106843599929647 ) ) ;
#17504=CARTESIAN_POINT ( 'NONE',  ( 0.6029443449137436017, -45.50214841125133347, -18.46873108645500494 ) ) ;
#17507=EDGE_CURVE ( 'NONE', #30486, #52564, #29692, .T. ) ;
#17512=VERTEX_POINT ( 'NONE', #1176 ) ;
#17515=ORIENTED_EDGE ( 'NONE', *, *, #60803, .F. ) ;
#17517=ORIENTED_EDGE ( 'NONE', *, *, #46428, .F. ) ;
#17522=ORIENTED_EDGE ( 'NONE', *, *, #25992, .F. ) ;
#17526=VERTEX_POINT ( 'NONE', #6471 ) ;
#17531=CARTESIAN_POINT ( 'NONE',  ( 4.553261556744875094, 1.182159483579356074, 43.91061448874314976 ) ) ;
#17534=CARTESIAN_POINT ( 'NONE',  ( 0.7044674535453004927, 3.876803250506410947, -48.95684956538534038 ) ) ;
#17545=VERTEX_POINT ( 'NONE', #10291 ) ;
#17547=CARTESIAN_POINT ( 'NONE',  ( 4.390527457369401532, -33.66034041506548391, 28.23414280212042371 ) ) ;
#17552=ORIENTED_EDGE ( 'NONE', *, *, #41420, .T. ) ;
#17554=FACE_OUTER_BOUND ( 'NONE', #47474, .T. ) ;
#17556=B_SPLINE_CURVE_WITH_KNOTS ( 'NONE', 3,
 ( #1681, #50471, #34616, #25502, #7542, #26666, #17588, #36403, #22286, #6367, #53996, #53682, #50772, #17282, #21981, #44048, #12593, #34934, #29590, #10813, #31685, #46112, #24912, #60781, #12901 ),
 .UNSPECIFIED., .F., .F.,
 ( 4, 3, 3, 3, 3, 3, 3, 3, 4 ),
 ( 4.670885906470169154E-18, 0.0005656085177311400737, 0.001131215744874499622, 0.001696821861372766567, 0.002262427090022498151, 0.002828031679238746359, 0.003393635864401605730, 0.003977030878808132490, 0.004561030005651159867 ),
 .UNSPECIFIED. ) ;
#17557=CARTESIAN_POINT ( 'NONE',  ( 4.553261556744875094, -43.15908619232990873, 8.175135770534621926 ) ) ;
#17560=EDGE_CURVE ( 'NONE', #21995, #33629, #34114, .T. ) ;
#17562=DIRECTION ( 'NONE',  ( 0.000000000000000000, 0.000000000000000000, -1.000000000000000000 ) ) ;
#17563=CARTESIAN_POINT ( 'NONE',  ( 5.901764892641288895, 47.35677775444521131, -12.46302804922470386 ) ) ;
#17564=EDGE_CURVE ( 'NONE', #54294, #29266, #8676, .T. ) ;
#17566=CARTESIAN_POINT ( 'NONE',  ( -6.078075953587585900, -1.854308114362783311, -19.16655200248976243 ) ) ;
#17574=CARTESIAN_POINT ( 'NONE',  ( 4.335381028904201628, -48.94118403004391382, -2.125406643849441224 ) ) ;
#17584=ORIENTED_EDGE ( 'NONE', *, *, #47334, .F. ) ;
#17585=CARTESIAN_POINT ( 'NONE',  ( 0.1155031312995260795, 4.404628064233996554, -43.90376845041404152 ) ) ;
#17588=CARTESIAN_POINT ( 'NONE',  ( 3.559346040607745287, -10.52814864373571524, 42.69178337429104886 ) ) ;
#17592=ORIENTED_EDGE ( 'NONE', *, *, #26720, .F. ) ;
#17593=CARTESIAN_POINT ( 'NONE',  ( -6.077587904424778920, 7.788877841491745002, 17.61049128685084142 ) ) ;
#17596=ORIENTED_EDGE ( 'NONE', *, *, #7977, .F. ) ;
#17602=CARTESIAN_POINT ( 'NONE',  ( 0.1155031312995260795, 15.08069845605273329, 41.46702505135155548 ) ) ;
#17604=CARTESIAN_POINT ( 'NONE',  ( 1.296416391601053153, -37.84290377757003654, 22.58809438083998700 ) ) ;
#17610=EDGE_CURVE ( 'NONE', #14671, #58860, #5653, .T. ) ;
#17612=CARTESIAN_POINT ( 'NONE',  ( 0.1147471544378677322, -12.25660023001551124, 42.38782772536036703 ) ) ;
#17613=CARTESIAN_POINT ( 'NONE',  ( 0.7413678028165009426, 14.35015966441118529, -41.69603109860877765 ) ) ;
#17616=CARTESIAN_POINT ( 'NONE',  ( 0.3676999524040323597, 42.11837424242189343, -13.11461530118710428 ) ) ;
#17617=CARTESIAN_POINT ( 'NONE',  ( 0.5997462898726536595, 28.52220283460625438, 39.97543715340569292 ) ) ;
#17621=ORIENTED_EDGE ( 'NONE', *, *, #37692, .F. ) ;
#17632=CARTESIAN_POINT ( 'NONE',  ( -6.077587904424778920, -19.21689618909966413, -1.227567615774088017 ) ) ;
#17642=CARTESIAN_POINT ( 'NONE',  ( 0.6029443449137436017, -47.51238410865360606, 12.41422145344172101 ) ) ;
#17645=B_SPLINE_CURVE_WITH_KNOTS ( 'NONE', 3,
 ( #13436, #51013, #8105, #3388 ),
 .UNSPECIFIED., .F., .F.,
 ( 4, 4 ),
 ( 0.000000000000000000, 0.005013413432710149380 ),
 .UNSPECIFIED. ) ;
#17647=CARTESIAN_POINT ( 'NONE',  ( -6.078726893082806448, 13.83492043373111180, -13.39361854993076406 ) ) ;
#17649=CARTESIAN_POINT ( 'NONE',  ( 0.5987334308729317378, 44.50372324553362802, 20.76009450495541486 ) ) ;
#17656=EDGE_CURVE ( 'NONE', #61378, #4827, #55335, .T. ) ;
#17664=CARTESIAN_POINT ( 'NONE',  ( 0.1129192098497455998, -17.41650932123162931, -40.54154647825617275 ) ) ;
#17669=CIRCLE ( 'NONE', #2624, 48.91267123290010943 ) ;
#17671=CARTESIAN_POINT ( 'NONE',  ( 0.1129192098497455998, 39.54191224844618802, 19.58032082273768637 ) ) ;
#17676=CARTESIAN_POINT ( 'NONE',  ( 0.5987334308729318488, -30.14260565354317123, 38.76836636982163498 ) ) ;
#17677=CARTESIAN_POINT ( 'NONE',  ( 0.5997462898726536595, -48.63480578518795738, -6.797594896826151256 ) ) ;
#17679=B_SPLINE_CURVE_WITH_KNOTS ( 'NONE', 3,
 ( #51561, #61270, #5407, #43362, #51879, #18388, #43677, #34567, #22768, #24537, #28086, #32804, #57717, #717, #38972, #3946, #58030, #15152, #5097 ),
 .UNSPECIFIED., .F., .F.,
 ( 4, 3, 3, 3, 3, 3, 4 ),
 ( 1.355252715606880543E-20, 0.0002612768053151719259, 0.0003919133833142912507, 0.0005225499612322561998, 0.0006531865391693348743, 0.0008112755173415194237, 0.0009693688056799674773 ),
 .UNSPECIFIED. ) ;
#17680=ORIENTED_EDGE ( 'NONE', *, *, #29634, .F. ) ;
#17681=CARTESIAN_POINT ( 'NONE',  ( -6.077587904424778920, 12.00112336472187025, -15.05885318935865236 ) ) ;
#17685=CARTESIAN_POINT ( 'NONE',  ( 4.335381028904201628, -9.909170555161033178, 47.97463065593183273 ) ) ;
#17686=VERTEX_POINT ( 'NONE', #3330 ) ;
#17691=CARTESIAN_POINT ( 'NONE',  ( 0.5980271706414711508, -34.78940872470953849, -34.66621241824330468 ) ) ;
#17698=CARTESIAN_POINT ( 'NONE',  ( 0.7948878604505658085, -14.79943965969628117, -46.81533117534708310 ) ) ;
#17703=CIRCLE ( 'NONE', #42705, 10.00000000000000000 ) ;
#17704=CARTESIAN_POINT ( 'NONE',  ( 0.6021447746440204973, 41.01325366509355064, -27.00840911440690206 ) ) ;
#17706=EDGE_CURVE ( 'NONE', #15748, #59402, #27434, .T. ) ;
#17712=EDGE_CURVE ( 'NONE', #15568, #27320, #3452, .T. ) ;
#17715=CARTESIAN_POINT ( 'NONE',  ( 4.553261556744875094, -24.94552653848424129, -36.15605442441715667 ) ) ;
#17724=EDGE_LOOP ( 'NONE', ( #38967, #4478, #27600, #57288 ) ) ;
#17725=CARTESIAN_POINT ( 'NONE',  ( 1.112077966505211624, -18.79777896220841882, -39.87071395418583819 ) ) ;
#17727=CARTESIAN_POINT ( 'NONE',  ( 3.678834586032786458, -9.636421247177533900, 48.01824398262914428 ) ) ;
#17728=ORIENTED_EDGE ( 'NONE', *, *, #120, .F. ) ;
#17732=ORIENTED_EDGE ( 'NONE', *, *, #26461, .F. ) ;
#17733=VERTEX_POINT ( 'NONE', #48047 ) ;
#17736=CARTESIAN_POINT ( 'NONE',  ( 2.009741617377216460, 37.63911818071238002, 22.86483894982449527 ) ) ;
#17739=CARTESIAN_POINT ( 'NONE',  ( 0.6021447746440204973, 49.02259406747356962, 2.885551937531610545 ) ) ;
#17750=CARTESIAN_POINT ( 'NONE',  ( 0.8744876279028263033, -20.68330519280349122, 44.52584571550372061 ) ) ;
#17752=CARTESIAN_POINT ( 'NONE',  ( 3.894904216938897878, 38.58700858884896689, -21.05153440109051388 ) ) ;
#17762=EDGE_CURVE ( 'NONE', #41953, #37050, #17679, .T. ) ;
#17764=CARTESIAN_POINT ( 'NONE',  ( 3.221118495291109163, 43.49601572552855089, 6.546604896152265596 ) ) ;
#17768=CARTESIAN_POINT ( 'NONE',  ( 0.1152339509894530906, -43.73278499344712600, 5.863975372745715120 ) ) ;
#17770=CARTESIAN_POINT ( 'NONE',  ( 0.1129192098497455998, 43.21532672376827833, 8.909956450124401073 ) ) ;
#17773=( BOUNDED_SURFACE ( )  B_SPLINE_SURFACE ( 3, 1, ( 
 ( #28621, #57114 ),
 ( #29240, #23624 ),
 ( #9516, #33045 ),
 ( #14857, #53344 ) ),
 .UNSPECIFIED., .F., .F., .F. ) 
 B_SPLINE_SURFACE_WITH_KNOTS ( ( 4, 4 ),
 ( 2, 2 ),
 ( 0.000000000000000000, 1.000000000000000000 ),
 ( 0.000000000000000000, 1.000000000000000000 ),
 .UNSPECIFIED. ) 
 GEOMETRIC_REPRESENTATION_ITEM ( )  RATIONAL_B_SPLINE_SURFACE ( (
 ( 1.000000000000000000, 1.000000000000000000),
 ( 0.7211978278499970862, 0.9934217856018976445),
 ( 0.7211978278499970862, 0.9934217856018976445),
 ( 1.000000000000000000, 1.000000000000000000) ) ) 
 REPRESENTATION_ITEM ( '' )  SURFACE ( )  );
#17777=CARTESIAN_POINT ( 'NONE',  ( 0.7948884756798499929, -38.82350056502001223, -30.05718630341241848 ) ) ;
#17787=CARTESIAN_POINT ( 'NONE',  ( -6.063463321072278589, -18.28058862190286149, 6.053142334046474282 ) ) ;
#17789=EDGE_CURVE ( 'NONE', #8183, #45251, #53232, .T. ) ;
#17792=CARTESIAN_POINT ( 'NONE',  ( 4.975610109902397937, 34.73360008816130318, 34.43873447229810836 ) ) ;
#17794=B_SPLINE_CURVE_WITH_KNOTS ( 'NONE', 3,
 ( #58004, #36332, #10425, #59480 ),
 .UNSPECIFIED., .F., .F.,
 ( 4, 4 ),
 ( 2.170598744017606518E-17, 0.004559932413162187670 ),
 .UNSPECIFIED. ) ;
#17796=B_SPLINE_CURVE_WITH_KNOTS ( 'NONE', 3,
 ( #32849, #43412, #46328, #22813 ),
 .UNSPECIFIED., .F., .F.,
 ( 4, 4 ),
 ( 0.000000000000000000, 0.005013413432710145043 ),
 .UNSPECIFIED. ) ;
#17798=CARTESIAN_POINT ( 'NONE',  ( -6.078726893082806448, 13.83492043373091995, 13.39361854993096124 ) ) ;
#17804=CARTESIAN_POINT ( 'NONE',  ( 3.559346040607745287, 17.09700346547288063, 40.51077330838793245 ) ) ;
#17806=LINE ( 'NONE', #27197, #56479 ) ;
#17808=CARTESIAN_POINT ( 'NONE',  ( 1.296416391601052265, 32.82713958318685599, -29.40554847069044442 ) ) ;
#17821=EDGE_CURVE ( 'NONE', #61623, #18115, #42994, .T. ) ;
#17822=CARTESIAN_POINT ( 'NONE',  ( 3.390910168358336474, -25.85228378503758506, 35.57747264255177555 ) ) ;
#17825=CARTESIAN_POINT ( 'NONE',  ( -6.072942160501519915, 12.01744408475423320, 15.04610248399318451 ) ) ;
#17827=EDGE_LOOP ( 'NONE', ( #60870, #49932, #25691, #4321 ) ) ;
#17831=CARTESIAN_POINT ( 'NONE',  ( 0.8744876279028306332, -43.20725972823464645, -23.31271664041680580 ) ) ;
#17838=EDGE_LOOP ( 'NONE', ( #49745, #58718, #2918, #30829 ) ) ;
#17841=CARTESIAN_POINT ( 'NONE',  ( 0.2940133293163016970, 25.89542274635558172, -35.71648961426042490 ) ) ;
#17846=CARTESIAN_POINT ( 'NONE',  ( 1.830465331921977912, 42.17827523781150489, -12.70311591074435142 ) ) ;
#17849=CARTESIAN_POINT ( 'NONE',  ( 0.3676999524040366896, 5.056646555325087000, 43.82215089355334925 ) ) ;
#17851=LINE ( 'NONE', #40754, #34795 ) ;
#17852=CARTESIAN_POINT ( 'NONE',  ( 0.6000166863083090663, 48.30184070261004337, -8.874438937089866641 ) ) ;
#17855=( BOUNDED_SURFACE ( )  B_SPLINE_SURFACE ( 3, 1, ( 
 ( #41604, #8361 ),
 ( #17787, #13097 ),
 ( #51278, #3657 ),
 ( #22788, #48440 ) ),
 .UNSPECIFIED., .F., .F., .F. ) 
 B_SPLINE_SURFACE_WITH_KNOTS ( ( 4, 4 ),
 ( 2, 2 ),
 ( 0.000000000000000000, 1.000000000000000000 ),
 ( 0.000000000000000000, 1.000000000000000000 ),
 .UNSPECIFIED. ) 
 GEOMETRIC_REPRESENTATION_ITEM ( )  RATIONAL_B_SPLINE_SURFACE ( (
 ( 1.000000000000000000, 1.000000000000000000),
 ( 0.7211978278499968642, 0.9934217856018975334),
 ( 0.7211978278499968642, 0.9934217856018975334),
 ( 1.000000000000000000, 1.000000000000000000) ) ) 
 REPRESENTATION_ITEM ( '' )  SURFACE ( )  );
#17858=CARTESIAN_POINT ( 'NONE',  ( 3.240649175237396484, 21.95100081562274497, -38.12372595366539940 ) ) ;
#17865=DIRECTION ( 'NONE',  ( -1.000000000000000000, -0.000000000000000000, -0.000000000000000000 ) ) ;
#17867=ADVANCED_FACE ( 'NONE', ( #30771 ), #48400, .F. ) ;
#17869=CARTESIAN_POINT ( 'NONE',  ( 3.727782113643637096, -43.27745144898557328, 7.735630031656845595 ) ) ;
#17871=DIRECTION ( 'NONE',  ( 0.000000000000000000, 0.000000000000000000, 1.000000000000000000 ) ) ;
#17876=CARTESIAN_POINT ( 'NONE',  ( 4.975610109902397937, 42.33317580307156192, -24.50207406657668230 ) ) ;
#17882=CARTESIAN_POINT ( 'NONE',  ( 0.6016118706126977189, -49.10631034723315480, -0.3483372864810193592 ) ) ;
#17888=ORIENTED_EDGE ( 'NONE', *, *, #30145, .T. ) ;
#17892=CARTESIAN_POINT ( 'NONE',  ( 0.1365634738349413291, 44.06882432424109908, -2.191196545822806652 ) ) ;
#17896=EDGE_CURVE ( 'NONE', #17512, #22171, #1322, .T. ) ;
#17899=B_SPLINE_CURVE_WITH_KNOTS ( 'NONE', 3,
 ( #14111, #34139, #14717, #24408 ),
 .UNSPECIFIED., .F., .F.,
 ( 4, 4 ),
 ( 0.000000000000000000, 0.004442905043737215703 ),
 .UNSPECIFIED. ) ;
#17903=CARTESIAN_POINT ( 'NONE',  ( 0.1158516988532803382, 4.187934451109883049, -43.92497426141537886 ) ) ;
#17906=CARTESIAN_POINT ( 'NONE',  ( -6.072942160501519915, -19.21577577016807226, 1.248248308487570402 ) ) ;
#17907=VERTEX_POINT ( 'NONE', #35811 ) ;
#17911=ORIENTED_EDGE ( 'NONE', *, *, #29414, .T. ) ;
#17913=VERTEX_POINT ( 'NONE', #17010 ) ;
#17914=CARTESIAN_POINT ( 'NONE',  ( -4.915099999999998914, 1.224646799147353256E-15, -10.00000000000000000 ) ) ;
#17921=CARTESIAN_POINT ( 'NONE',  ( 0.1152809850208375703, 15.03117900825671782, 41.48504477653962397 ) ) ;
#17922=CARTESIAN_POINT ( 'NONE',  ( -6.072942160501519915, -11.00492040199085864, 15.80176854769318595 ) ) ;
#17924=CARTESIAN_POINT ( 'NONE',  ( -6.078726893082806448, 3.076629396955071538, 19.00863995194059086 ) ) ;
#17928=CARTESIAN_POINT ( 'NONE',  ( -2.739355103387248747, -2.122549901524039218, 14.77641190771823965 ) ) ;
#17933=ORIENTED_EDGE ( 'NONE', *, *, #5521, .T. ) ;
#17936=CARTESIAN_POINT ( 'NONE',  ( 0.6000166863083106206, 48.10206967781400778, 9.900220927796519632 ) ) ;
#17939=ORIENTED_EDGE ( 'NONE', *, *, #12400, .F. ) ;
#17940=PLANE ( 'NONE',  #5896 ) ;
#17946=CARTESIAN_POINT ( 'NONE',  ( 2.648799415243708655, 48.82680556394809201, -4.523330820314529710 ) ) ;
#17948=DIRECTION ( 'NONE',  ( 0.000000000000000000, 0.000000000000000000, -1.000000000000000000 ) ) ;
#17961=CARTESIAN_POINT ( 'NONE',  ( 0.6026112563231247332, -47.54525502191918918, 12.28778742511749478 ) ) ;
#17964=VERTEX_POINT ( 'NONE', #17616 ) ;
#17965=CARTESIAN_POINT ( 'NONE',  ( 0.6008123274975392114, -39.61436965115080255, 29.02165171558021228 ) ) ;
#17966=CARTESIAN_POINT ( 'NONE',  ( 0.8753041380234471980, 44.61941359694289844, -20.49990873486824583 ) ) ;
#17971=CARTESIAN_POINT ( 'NONE',  ( 2.009741617377216460, -30.66706143059037615, 31.60752158641105680 ) ) ;
#17972=CARTESIAN_POINT ( 'NONE',  ( -6.078075953587585900, 15.42887869085103425, 11.52149628260751690 ) ) ;
#17976=VERTEX_POINT ( 'NONE', #42067 ) ;
#17977=ORIENTED_EDGE ( 'NONE', *, *, #12884, .F. ) ;
#17981=ADVANCED_FACE ( 'NONE', ( #46754 ), #54791, .F. ) ;
#17983=CYLINDRICAL_SURFACE ( 'NONE', #41006, 10.00000000000000000 ) ;
#17985=ADVANCED_FACE ( 'NONE', ( #61421 ), #48044, .F. ) ;
#17986=ORIENTED_EDGE ( 'NONE', *, *, #49360, .F. ) ;
#17989=CARTESIAN_POINT ( 'NONE',  ( 2.299652685299201860, -48.77886880766101285, 4.990358975379336925 ) ) ;
#17990=EDGE_CURVE ( 'NONE', #34487, #1986, #36428, .T. ) ;
#18000=CARTESIAN_POINT ( 'NONE',  ( 0.5980271706414734822, -31.16543947089364863, -37.95740540958678366 ) ) ;
#18001=DIRECTION ( 'NONE',  ( 0.1011922191286468015, 0.4487230644346660857, -0.8879232772217329206 ) ) ;
#18004=FACE_OUTER_BOUND ( 'NONE', #21237, .T. ) ;
#18012=CARTESIAN_POINT ( 'NONE',  ( 4.834790513006553603, 7.995814508776146745, -46.56883390493718622 ) ) ;
#18016=CARTESIAN_POINT ( 'NONE',  ( 0.1156495703730067437, -17.98529708537768812, -40.29233229761928925 ) ) ;
#18023=ORIENTED_EDGE ( 'NONE', *, *, #47688, .T. ) ;
#18024=CONICAL_SURFACE ( 'NONE', #48927, 43.92652462719577500, 1.486293639869522343 ) ;
#18028=CARTESIAN_POINT ( 'NONE',  ( 0.6026112563231247332, -39.25096069177133984, -29.51106707113837402 ) ) ;
#18034=( BOUNDED_SURFACE ( )  B_SPLINE_SURFACE ( 3, 1, ( 
 ( #13207, #8474 ),
 ( #3770, #56397 ),
 ( #13513, #51704 ),
 ( #24129, #24752 ) ),
 .UNSPECIFIED., .F., .F., .F. ) 
 B_SPLINE_SURFACE_WITH_KNOTS ( ( 4, 4 ),
 ( 2, 2 ),
 ( 0.000000000000000000, 1.000000000000000000 ),
 ( 0.000000000000000000, 1.000000000000000000 ),
 .UNSPECIFIED. ) 
 GEOMETRIC_REPRESENTATION_ITEM ( )  RATIONAL_B_SPLINE_SURFACE ( (
 ( 1.000000000000000000, 1.000000000000000000),
 ( 0.7211978278499970862, 0.9934217856018976445),
 ( 0.7211978278499970862, 0.9934217856018976445),
 ( 1.000000000000000000, 1.000000000000000000) ) ) 
 REPRESENTATION_ITEM ( '' )  SURFACE ( )  );
#18036=CARTESIAN_POINT ( 'NONE',  ( 0.6026777506516367566, -1.399865435252327872, 49.08754187571837946 ) ) ;
#18041=CARTESIAN_POINT ( 'NONE',  ( 0.1156495703730067853, -6.907609969323758037, 43.58013168569789286 ) ) ;
#18045=ORIENTED_EDGE ( 'NONE', *, *, #55566, .T. ) ;
#18048=ADVANCED_FACE ( 'NONE', ( #57960 ), #52411, .F. ) ;
#18049=( BOUNDED_SURFACE ( )  B_SPLINE_SURFACE ( 3, 1, ( 
 ( #23414, #23725 ),
 ( #13723, #42853 ),
 ( #61300, #43160 ),
 ( #32833, #23114 ) ),
 .UNSPECIFIED., .F., .F., .F. ) 
 B_SPLINE_SURFACE_WITH_KNOTS ( ( 4, 4 ),
 ( 2, 2 ),
 ( 0.000000000000000000, 1.000000000000000000 ),
 ( 0.000000000000000000, 1.000000000000000000 ),
 .UNSPECIFIED. ) 
 GEOMETRIC_REPRESENTATION_ITEM ( )  RATIONAL_B_SPLINE_SURFACE ( (
 ( 1.000000000000000000, 1.000000000000000000),
 ( 0.9953485035131437453, 0.8621029689291515030),
 ( 0.9953485035131437453, 0.8621029689291515030),
 ( 1.000000000000000000, 1.000000000000000000) ) ) 
 REPRESENTATION_ITEM ( '' )  SURFACE ( )  );
#18052=EDGE_CURVE ( 'NONE', #2310, #45554, #9748, .T. ) ;
#18053=ADVANCED_FACE ( 'NONE', ( #52345 ), #12025, .F. ) ;
#18056=CARTESIAN_POINT ( 'NONE',  ( 2.881901170002227897, 8.474399077991585715E-12, -49.00591519830774700 ) ) ;
#18057=CARTESIAN_POINT ( 'NONE',  ( 0.1147471544378676767, -42.75889291922428015, -10.89170623894889189 ) ) ;
#18058=CARTESIAN_POINT ( 'NONE',  ( 0.8753041380234465318, 17.79089796329371964, -45.76704357430848802 ) ) ;
#18060=EDGE_CURVE ( 'NONE', #48571, #43165, #13142, .T. ) ;
#18064=CARTESIAN_POINT ( 'NONE',  ( 0.7044674535452954967, -43.19749584530718778, 23.36191506502784421 ) ) ;
#18065=CARTESIAN_POINT ( 'NONE',  ( 1.296416391601052709, 39.21237564904568274, -20.11708154863144316 ) ) ;
#18071=FACE_OUTER_BOUND ( 'NONE', #60323, .T. ) ;
#18073=EDGE_LOOP ( 'NONE', ( #58395, #45522, #34717, #30437 ) ) ;
#18075=EDGE_LOOP ( 'NONE', ( #19117, #26623, #18211, #16855 ) ) ;
#18080=ORIENTED_EDGE ( 'NONE', *, *, #24546, .T. ) ;
#18082=CARTESIAN_POINT ( 'NONE',  ( -6.077587904424778920, 19.25606354205735116, 0.006185319731012296589 ) ) ;
#18089=EDGE_CURVE ( 'NONE', #25770, #11233, #30388, .T. ) ;
#18105=CARTESIAN_POINT ( 'NONE',  ( 0.6039202388192953519, -35.39742030259981931, -34.03801329058565983 ) ) ;
#18115=VERTEX_POINT ( 'NONE', #15703 ) ;
#18118=( BOUNDED_SURFACE ( )  B_SPLINE_SURFACE ( 3, 1, ( 
 ( #14263, #22405 ),
 ( #41533, #60597 ),
 ( #14876, #19883 ),
 ( #10470, #29254 ) ),
 .UNSPECIFIED., .F., .F., .F. ) 
 B_SPLINE_SURFACE_WITH_KNOTS ( ( 4, 4 ),
 ( 2, 2 ),
 ( 0.000000000000000000, 1.000000000000000000 ),
 ( 0.000000000000000000, 1.000000000000000000 ),
 .UNSPECIFIED. ) 
 GEOMETRIC_REPRESENTATION_ITEM ( )  RATIONAL_B_SPLINE_SURFACE ( (
 ( 1.000000000000000000, 1.000000000000000000),
 ( 0.9754377213608244057, 0.9999580625633939235),
 ( 0.9754377213608244057, 0.9999580625633939235),
 ( 1.000000000000000000, 1.000000000000000000) ) ) 
 REPRESENTATION_ITEM ( '' )  SURFACE ( )  );
#18121=CARTESIAN_POINT ( 'NONE',  ( 2.185380717157383135, 28.52207511433232057, -33.54565596675051609 ) ) ;
#18122=CARTESIAN_POINT ( 'NONE',  ( 0.6026112563231247332, -45.45287008515247607, -18.58971747839269284 ) ) ;
#18123=ORIENTED_EDGE ( 'NONE', *, *, #55497, .F. ) ;
#18124=EDGE_CURVE ( 'NONE', #32624, #52129, #45994, .T. ) ;
#18126=B_SPLINE_CURVE_WITH_KNOTS ( 'NONE', 3,
 ( #22647, #51132, #13256, #32055 ),
 .UNSPECIFIED., .F., .F.,
 ( 4, 4 ),
 ( 2.194270917860438266E-17, 0.004559932413162187670 ),
 .UNSPECIFIED. ) ;
#18128=B_SPLINE_CURVE_WITH_KNOTS ( 'NONE', 3,
 ( #24491, #44254, #20419, #58600, #40475, #49528, #55455, #2531, #30730, #16651, #49224, #60158, #45181, #6583, #25729, #11972, #1910, #58923, #26346, #54516, #36085, #55148, #44870, #17271, #21035 ),
 .UNSPECIFIED., .F., .F.,
 ( 4, 3, 3, 3, 3, 3, 3, 3, 4 ),
 ( 5.057544569639794935E-18, 0.0005656085177311401821, 0.001131215744874499622, 0.001696821861372766567, 0.002262427090022498585, 0.002828031679238746359, 0.003393635864401605730, 0.003977030878808131623, 0.004561030005651158133 ),
 .UNSPECIFIED. ) ;
#18129=ORIENTED_EDGE ( 'NONE', *, *, #14948, .F. ) ;
#18134=CARTESIAN_POINT ( 'NONE',  ( 0.7242003506640004584, 17.72439838236845588, 45.79145527398227955 ) ) ;
#18138=ORIENTED_EDGE ( 'NONE', *, *, #44294, .F. ) ;
#18142=ADVANCED_FACE ( 'NONE', ( #49505 ), #12784, .F. ) ;
#18147=CARTESIAN_POINT ( 'NONE',  ( -2.601141883200665639, 13.24771294992759607, 6.877029087164693522 ) ) ;
#18157=CARTESIAN_POINT ( 'NONE',  ( 3.727782113643637096, 6.344544998048565532, 43.50315534158083608 ) ) ;
#18159=CARTESIAN_POINT ( 'NONE',  ( -6.078457390727109555, -18.90008989325098199, 3.685256173529869006 ) ) ;
#18171=CARTESIAN_POINT ( 'NONE',  ( 4.834790513006553603, 38.14091330549818792, -27.89014293880282835 ) ) ;
#18173=CARTESIAN_POINT ( 'NONE',  ( 4.390527457369402420, 42.57725424673462555, -10.83340931736345958 ) ) ;
#18175=CARTESIAN_POINT ( 'NONE',  ( 0.5549461598389368033, -43.62161577359375997, 6.509403411047773425 ) ) ;
#18179=CARTESIAN_POINT ( 'NONE',  ( -6.078726893082806448, -19.21623043802544828, -1.237145513439781075 ) ) ;
#18182=FACE_OUTER_BOUND ( 'NONE', #51567, .T. ) ;
#18183=LINE ( 'NONE', #55445, #839 ) ;
#18188=ADVANCED_FACE ( 'NONE', ( #11617 ), #44052, .F. ) ;
#18194=CARTESIAN_POINT ( 'NONE',  ( 4.975610109902397937, -46.59897809419034331, -14.86555238512655919 ) ) ;
#18200=AXIS2_PLACEMENT_3D ( 'NONE', #47087, #24180, #47379 ) ;
#18201=ADVANCED_FACE ( 'NONE', ( #35745 ), #18416, .F. ) ;
#18207=CARTESIAN_POINT ( 'NONE',  ( 0.5997462898726536595, 23.17609050332868037, 43.29457771044576475 ) ) ;
#18208=ORIENTED_EDGE ( 'NONE', *, *, #11040, .F. ) ;
#18211=ORIENTED_EDGE ( 'NONE', *, *, #58835, .F. ) ;
#18212=CARTESIAN_POINT ( 'NONE',  ( 4.694002226626920127, -10.47998749083556191, -44.36726984656667128 ) ) ;
#18217=B_SPLINE_CURVE_WITH_KNOTS ( 'NONE', 3,
 ( #49783, #54775, #58859, #30665, #31605, #31296 ),
 .UNSPECIFIED., .F., .F.,
 ( 4, 2, 4 ),
 ( 1.910620358896493634E-17, 0.0002293755540694311288, 0.0004587511081388431214 ),
 .UNSPECIFIED. ) ;
#18220=( BOUNDED_SURFACE ( )  B_SPLINE_SURFACE ( 3, 1, ( 
 ( #26007, #59193 ),
 ( #35421, #6239 ),
 ( #49189, #53869 ),
 ( #30078, #26310 ) ),
 .UNSPECIFIED., .F., .F., .F. ) 
 B_SPLINE_SURFACE_WITH_KNOTS ( ( 4, 4 ),
 ( 2, 2 ),
 ( 0.000000000000000000, 1.000000000000000000 ),
 ( 0.000000000000000000, 1.000000000000000000 ),
 .UNSPECIFIED. ) 
 GEOMETRIC_REPRESENTATION_ITEM ( )  RATIONAL_B_SPLINE_SURFACE ( (
 ( 1.000000000000000000, 1.000000000000000000),
 ( 0.7211978278499970862, 0.9934217856018976445),
 ( 0.7211978278499970862, 0.9934217856018976445),
 ( 1.000000000000000000, 1.000000000000000000) ) ) 
 REPRESENTATION_ITEM ( '' )  SURFACE ( )  );
#18243=PLANE ( 'NONE',  #13971 ) ;
#18250=CARTESIAN_POINT ( 'NONE',  ( 0.6000166863083090663, -25.90381862410858460, -41.72308308835457069 ) ) ;
#18263=CARTESIAN_POINT ( 'NONE',  ( 2.706805983486679335, -21.38196053433432198, 38.46541143713302802 ) ) ;
#18267=CARTESIAN_POINT ( 'NONE',  ( 0.5997462898726536595, -47.36625756029543055, 12.96106765957438789 ) ) ;
#18272=CARTESIAN_POINT ( 'NONE',  ( 2.648799415243696664, 44.76338677751291328, -20.01890774983441545 ) ) ;
#18275=ORIENTED_EDGE ( 'NONE', *, *, #23611, .F. ) ;
#18278=CARTESIAN_POINT ( 'NONE',  ( 0.1365634738349408572, 43.18335443710246579, 9.058726134663299234 ) ) ;
#18280=VERTEX_POINT ( 'NONE', #60427 ) ;
#18281=ORIENTED_EDGE ( 'NONE', *, *, #50552, .T. ) ;
#18283=DIRECTION ( 'NONE',  ( 0.000000000000000000, 0.000000000000000000, 1.000000000000000000 ) ) ;
#18289=ORIENTED_EDGE ( 'NONE', *, *, #2318, .T. ) ;
#18296=EDGE_CURVE ( 'NONE', #27020, #20580, #49733, .T. ) ;
#18297=B_SPLINE_CURVE_WITH_KNOTS ( 'NONE', 3,
 ( #19739, #39798, #29121, #5293, #28813, #43555, #48533, #25044, #39474, #44490, #4982, #598, #47936, #15662, #53528, #38862, #24114, #58531, #5590, #52923, #34764, #58222, #48240, #34151, #52608 ),
 .UNSPECIFIED., .F., .F.,
 ( 4, 3, 3, 3, 3, 3, 3, 3, 4 ),
 ( 5.553824967135426632E-18, 0.0005656085177311407242, 0.001131215744874500707, 0.001696821861372765916, 0.002262427090022498151, 0.002828031679238745492, 0.003393635864401604862, 0.003977030878808131623, 0.004561030005651159000 ),
 .UNSPECIFIED. ) ;
#18300=EDGE_LOOP ( 'NONE', ( #42494, #38339, #9119, #37561 ) ) ;
#18301=CARTESIAN_POINT ( 'NONE',  ( 0.7044674535453004927, -0.7321618212258587111, 49.10465010442948852 ) ) ;
#18308=CARTESIAN_POINT ( 'NONE',  ( 0.3676999524040366896, -43.84864779214676389, -4.821480075983068048 ) ) ;
#18313=VECTOR ( 'NONE', #41479, 1000.000000000000000 ) ;
#18317=CARTESIAN_POINT ( 'NONE',  ( 4.553261556744875094, 40.80044851610500700, -16.27461110774390818 ) ) ;
#18318=CARTESIAN_POINT ( 'NONE',  ( -6.078726893082806448, 13.83492043373091995, 13.39361854993096124 ) ) ;
#18323=EDGE_CURVE ( 'NONE', #30839, #32393, #60933, .T. ) ;
#18335=EDGE_CURVE ( 'NONE', #3780, #52994, #56971, .T. ) ;
#18337=ORIENTED_EDGE ( 'NONE', *, *, #269, .F. ) ;
#18339=CARTESIAN_POINT ( 'NONE',  ( 0.5997462898726536595, 32.62638226927734308, -36.70246327105708417 ) ) ;
#18349=CARTESIAN_POINT ( 'NONE',  ( 0.6039202388192953519, -42.70269169458240555, 24.24961514924382655 ) ) ;
#18354=CARTESIAN_POINT ( 'NONE',  ( 0.7044674535453004927, -7.005514063659647128, 48.60787483026567912 ) ) ;
#18358=VECTOR ( 'NONE', #39389, 1000.000000000000114 ) ;
#18362=ORIENTED_EDGE ( 'NONE', *, *, #48926, .F. ) ;
#18364=CARTESIAN_POINT ( 'NONE',  ( 0.7242003506640013466, -20.62185031759747389, -44.56176571461944746 ) ) ;
#18367=EDGE_CURVE ( 'NONE', #35355, #18514, #1126, .T. ) ;
#18369=EDGE_CURVE ( 'NONE', #40746, #60982, #37596, .T. ) ;
#18375=CARTESIAN_POINT ( 'NONE',  ( 0.7044674535453004927, 44.60554499456272026, 20.54624244354541673 ) ) ;
#18377=B_SPLINE_CURVE_WITH_KNOTS ( 'NONE', 3,
 ( #39584, #54247, #38659, #57714 ),
 .UNSPECIFIED., .F., .F.,
 ( 4, 4 ),
 ( 0.000000000000000000, 0.005013413432710142441 ),
 .UNSPECIFIED. ) ;
#18378=ORIENTED_EDGE ( 'NONE', *, *, #25168, .T. ) ;
#18382=CARTESIAN_POINT ( 'NONE',  ( 0.6039202388192952409, 16.79650288729614616, 46.14586875990139703 ) ) ;
#18388=CARTESIAN_POINT ( 'NONE',  ( 0.1156495703730067715, 36.90540492852111498, -24.18540965733181736 ) ) ;
#18389=EDGE_LOOP ( 'NONE', ( #54253, #25615, #49485, #31408 ) ) ;
#18416=( BOUNDED_SURFACE ( )  B_SPLINE_SURFACE ( 3, 1, ( 
 ( #20700, #16306 ),
 ( #58893, #16011 ),
 ( #35433, #49818 ),
 ( #31024, #6879 ) ),
 .UNSPECIFIED., .F., .F., .F. ) 
 B_SPLINE_SURFACE_WITH_KNOTS ( ( 4, 4 ),
 ( 2, 2 ),
 ( 0.000000000000000000, 1.000000000000000000 ),
 ( 0.000000000000000000, 1.000000000000000000 ),
 .UNSPECIFIED. ) 
 GEOMETRIC_REPRESENTATION_ITEM ( )  RATIONAL_B_SPLINE_SURFACE ( (
 ( 1.000000000000000000, 1.000000000000000000),
 ( 0.9953485035131437453, 0.8621029689291515030),
 ( 0.9953485035131437453, 0.8621029689291515030),
 ( 1.000000000000000000, 1.000000000000000000) ) ) 
 REPRESENTATION_ITEM ( '' )  SURFACE ( )  );
#18425=CARTESIAN_POINT ( 'NONE',  ( 1.657374760986085827, 32.73027908137574826, -29.48930786755600408 ) ) ;
#18429=CARTESIAN_POINT ( 'NONE',  ( 1.479689385636123067, 28.74311660336230645, -33.39786060802713052 ) ) ;
#18430=CARTESIAN_POINT ( 'NONE',  ( 1.830465331921978134, -18.95265478904632062, 39.76396524902450835 ) ) ;
#18431=ORIENTED_EDGE ( 'NONE', *, *, #28422, .F. ) ;
#18435=ORIENTED_EDGE ( 'NONE', *, *, #56390, .F. ) ;
#18436=EDGE_CURVE ( 'NONE', #40643, #19013, #58646, .T. ) ;
#18446=CARTESIAN_POINT ( 'NONE',  ( -6.078457390727109555, 19.09737280526037040, -2.466751502362881876 ) ) ;
#18454=CARTESIAN_POINT ( 'NONE',  ( 0.5997462898726536595, -43.04230894295718457, -23.64130434225950950 ) ) ;
#18468=CARTESIAN_POINT ( 'NONE',  ( 0.2940135542859019235, -42.46217170869496726, 11.96680920181833763 ) ) ;
#18469=AXIS2_PLACEMENT_3D ( 'NONE', #15380, #1551, #34483 ) ;
#18470=ADVANCED_FACE ( 'NONE', ( #10615 ), #9244, .F. ) ;
#18471=VERTEX_POINT ( 'NONE', #5569 ) ;
#18472=EDGE_CURVE ( 'NONE', #61919, #10554, #47406, .T. ) ;
#18473=CARTESIAN_POINT ( 'NONE',  ( -6.057079549204054558, 7.787131596469658135, -17.61226313109710517 ) ) ;
#18493=CIRCLE ( 'NONE', #12512, 43.92652462719577500 ) ;
#18496=( BOUNDED_SURFACE ( )  B_SPLINE_SURFACE ( 3, 1, ( 
 ( #19568, #29562 ),
 ( #53357, #10467 ),
 ( #33981, #38997 ),
 ( #26034, #53055 ) ),
 .UNSPECIFIED., .F., .F., .F. ) 
 B_SPLINE_SURFACE_WITH_KNOTS ( ( 4, 4 ),
 ( 2, 2 ),
 ( 0.000000000000000000, 1.000000000000000000 ),
 ( 0.000000000000000000, 1.000000000000000000 ),
 .UNSPECIFIED. ) 
 GEOMETRIC_REPRESENTATION_ITEM ( )  RATIONAL_B_SPLINE_SURFACE ( (
 ( 1.000000000000000000, 1.000000000000000000),
 ( 0.7211978278499968642, 0.9934217856018975334),
 ( 0.7211978278499968642, 0.9934217856018975334),
 ( 1.000000000000000000, 1.000000000000000000) ) ) 
 REPRESENTATION_ITEM ( '' )  SURFACE ( )  );
#18501=( BOUNDED_SURFACE ( )  B_SPLINE_SURFACE ( 3, 1, ( 
 ( #39959, #6066 ),
 ( #60172, #45804 ),
 ( #25201, #59014 ),
 ( #44642, #29900 ) ),
 .UNSPECIFIED., .F., .F., .F. ) 
 B_SPLINE_SURFACE_WITH_KNOTS ( ( 4, 4 ),
 ( 2, 2 ),
 ( 0.000000000000000000, 1.000000000000000000 ),
 ( 0.000000000000000000, 1.000000000000000000 ),
 .UNSPECIFIED. ) 
 GEOMETRIC_REPRESENTATION_ITEM ( )  RATIONAL_B_SPLINE_SURFACE ( (
 ( 1.000000000000000000, 1.000000000000000000),
 ( 0.9953485035131437453, 0.8621029689291515030),
 ( 0.9953485035131437453, 0.8621029689291515030),
 ( 1.000000000000000000, 1.000000000000000000) ) ) 
 REPRESENTATION_ITEM ( '' )  SURFACE ( )  );
#18505=ORIENTED_EDGE ( 'NONE', *, *, #21420, .T. ) ;
#18506=CARTESIAN_POINT ( 'NONE',  ( -2.601141883200665639, -11.68881050534876387, -9.282625514337903283 ) ) ;
#18510=FACE_OUTER_BOUND ( 'NONE', #10742, .T. ) ;
#18514=VERTEX_POINT ( 'NONE', #25627 ) ;
#18522=CARTESIAN_POINT ( 'NONE',  ( -6.079354080745853928, -1.850179728782696875, 19.16689307684904264 ) ) ;
#18526=CARTESIAN_POINT ( 'NONE',  ( 0.8753041380234524160, -47.71532843791157319, -11.59248721954040739 ) ) ;
#18528=FACE_OUTER_BOUND ( 'NONE', #7312, .T. ) ;
#18535=CARTESIAN_POINT ( 'NONE',  ( 0.6027444965799114707, 46.64666970468664431, -15.35013750261902743 ) ) ;
#18545=EDGE_CURVE ( 'NONE', #3481, #56877, #44502, .T. ) ;
#18548=B_SPLINE_CURVE_WITH_KNOTS ( 'NONE', 3,
 ( #59606, #40541, #12037, #26407 ),
 .UNSPECIFIED., .F., .F.,
 ( 4, 4 ),
 ( 0.001844835322069226938, 0.004559932413162187670 ),
 .UNSPECIFIED. ) ;
#18556=CARTESIAN_POINT ( 'NONE',  ( 4.975610109902397937, 0.000000000000000000, 0.000000000000000000 ) ) ;
#18558=EDGE_CURVE ( 'NONE', #18600, #51070, #2731, .T. ) ;
#18560=CARTESIAN_POINT ( 'NONE',  ( 0.8744876279028263033, 16.11801507201566253, 46.37412684372363714 ) ) ;
#18561=B_SPLINE_CURVE_WITH_KNOTS ( 'NONE', 3,
 ( #30309, #6787, #49417, #1793, #54406, #59425, #16532, #53189, #8050, #50958, #26854, #60654, #17158, #50342, #22160, #27163, #46289, #45991, #17770 ),
 .UNSPECIFIED., .F., .F.,
 ( 4, 3, 3, 3, 3, 3, 4 ),
 ( 3.469552829456483146E-18, 0.0002612768053151726306, 0.0003919133833142900581, 0.0005225499612322590188, 0.0006531865391693349827, 0.0008112755173415182311, 0.0009693688056799727899 ),
 .UNSPECIFIED. ) ;
#18564=CARTESIAN_POINT ( 'NONE',  ( 3.221118495291109607, -21.16578580483263750, 38.55866868715381202 ) ) ;
#18565=B_SPLINE_CURVE_WITH_KNOTS ( 'NONE', 3,
 ( #23440, #47254, #41960, #18134, #51938, #61625 ),
 .UNSPECIFIED., .F., .F.,
 ( 4, 2, 4 ),
 ( 0.000000000000000000, 0.0002447195606305753424, 0.0004894391212611506848 ),
 .UNSPECIFIED. ) ;
#18569=CARTESIAN_POINT ( 'NONE',  ( 0.8744876279028306332, -39.87136468799875644, -28.64654129726831044 ) ) ;
#18572=CARTESIAN_POINT ( 'NONE',  ( 0.6029443199889047422, -39.35533208240347136, 29.37167817027392402 ) ) ;
#18575=ORIENTED_EDGE ( 'NONE', *, *, #49230, .F. ) ;
#18581=UNCERTAINTY_MEASURE_WITH_UNIT (LENGTH_MEASURE( 1.000000000000000082E-05 ), #15714, 'distance_accuracy_value', 'NONE');
#18586=DIRECTION ( 'NONE',  ( -1.000000000000000000, 0.000000000000000000, 0.000000000000000000 ) ) ;
#18598=ORIENTED_EDGE ( 'NONE', *, *, #49471, .T. ) ;
#18600=VERTEX_POINT ( 'NONE', #41596 ) ;
#18609=FACE_OUTER_BOUND ( 'NONE', #37917, .T. ) ;
#18615=ORIENTED_EDGE ( 'NONE', *, *, #19186, .F. ) ;
#18618=CARTESIAN_POINT ( 'NONE',  ( -6.078457390727109555, 13.83560117034693526, 13.39293288613821176 ) ) ;
#18619=EDGE_CURVE ( 'NONE', #60972, #36056, #35981, .T. ) ;
#18624=CARTESIAN_POINT ( 'NONE',  ( -6.063463321072276813, 17.85520303107520235, 7.211946838306062091 ) ) ;
#18628=DIRECTION ( 'NONE',  ( 0.09722883295013595717, 0.2288279796715356751, -0.9685991481322898666 ) ) ;
#18629=CARTESIAN_POINT ( 'NONE',  ( 4.694002226626921015, -41.22189368134375087, 19.46895612944177500 ) ) ;
#18633=CARTESIAN_POINT ( 'NONE',  ( 0.8744876279028306332, -14.81965677137948489, -46.80521149998148900 ) ) ;
#18636=CARTESIAN_POINT ( 'NONE',  ( -6.072942160501519915, -4.299083787220544295, -18.77024349547649251 ) ) ;
#18637=LINE ( 'NONE', #57734, #44886 ) ;
#18638=ORIENTED_EDGE ( 'NONE', *, *, #4871, .T. ) ;
#18640=CARTESIAN_POINT ( 'NONE',  ( -6.079354080745853928, 0.6183512803180944983, 19.24605406160678456 ) ) ;
#18641=CARTESIAN_POINT ( 'NONE',  ( 0.1155031312995260795, -35.26066340436319280, -26.52597309838059658 ) ) ;
#18642=CARTESIAN_POINT ( 'NONE',  ( 0.6029443449137434907, -39.32931611637160785, -29.40653722902179368 ) ) ;
#18645=CARTESIAN_POINT ( 'NONE',  ( 1.479689385636123067, -23.83924572570610323, -37.05771456116924867 ) ) ;
#18648=CARTESIAN_POINT ( 'NONE',  ( 4.975610109902397937, 0.000000000000000000, 0.000000000000000000 ) ) ;
#18649=CIRCLE ( 'NONE', #26639, 48.91267123290010943 ) ;
#18667=AXIS2_PLACEMENT_3D ( 'NONE', #28876, #6899, #40171 ) ;
#18668=CARTESIAN_POINT ( 'NONE',  ( 0.6252788684277226228, -20.50349297004706983, -44.62119571684401365 ) ) ;
#18675=ORIENTED_EDGE ( 'NONE', *, *, #46081, .T. ) ;
#18680=CARTESIAN_POINT ( 'NONE',  ( 0.1158516988532803521, 41.86075703818062976, -13.95059780164302765 ) ) ;
#18687=CARTESIAN_POINT ( 'NONE',  ( 0.7044674535452954967, 37.93506595837585138, -31.18867572604804650 ) ) ;
#18688=LINE ( 'NONE', #27770, #12182 ) ;
#18689=EDGE_CURVE ( 'NONE', #56737, #47174, #37006, .T. ) ;
#18694=CARTESIAN_POINT ( 'NONE',  ( 2.879087469061463178, 43.48727737615701017, 6.705101281305238636 ) ) ;
#18704=CARTESIAN_POINT ( 'NONE',  ( 0.1368894036331274322, -43.67490804582807584, 6.274052367632553917 ) ) ;
#18711=CARTESIAN_POINT ( 'NONE',  ( 0.3676999524040366896, -17.09834788623584600, 40.66444494744877858 ) ) ;
#18715=B_SPLINE_CURVE_WITH_KNOTS ( 'NONE', 3,
 ( #37184, #32164, #46895, #46577 ),
 .UNSPECIFIED., .F., .F.,
 ( 4, 4 ),
 ( 2.189128766608093472E-17, 0.004559932413162185935 ),
 .UNSPECIFIED. ) ;
#18731=CARTESIAN_POINT ( 'NONE',  ( 4.553261556744875094, 1.633632119647590697, -43.89613664004262716 ) ) ;
#18732=FACE_OUTER_BOUND ( 'NONE', #33645, .T. ) ;
#18734=CARTESIAN_POINT ( 'NONE',  ( 2.706805983486679335, 32.41343978096548994, -29.76818830371574620 ) ) ;
#18736=ORIENTED_EDGE ( 'NONE', *, *, #55214, .F. ) ;
#18744=CARTESIAN_POINT ( 'NONE',  ( 5.901764892641307547, -4.659217859063449652, -48.74713485305021266 ) ) ;
#18752=ORIENTED_EDGE ( 'NONE', *, *, #27779, .F. ) ;
#18756=CARTESIAN_POINT ( 'NONE',  ( 0.3676999524040366896, 42.11837424242170158, 13.11461530118771179 ) ) ;
#18757=DIRECTION ( 'NONE',  ( 0.09722883295013597105, -0.2904161885395503129, 0.9519479983052198113 ) ) ;
#18758=EDGE_LOOP ( 'NONE', ( #25109, #27480, #27310, #11729 ) ) ;
#18762=CARTESIAN_POINT ( 'NONE',  ( 4.553261556744873317, -39.67390170502044100, -18.85526688551536623 ) ) ;
#18767=( BOUNDED_SURFACE ( )  B_SPLINE_SURFACE ( 3, 1, ( 
 ( #25381, #26006 ),
 ( #54478, #34183 ),
 ( #54171, #39202 ),
 ( #20691, #30076 ) ),
 .UNSPECIFIED., .F., .F., .F. ) 
 B_SPLINE_SURFACE_WITH_KNOTS ( ( 4, 4 ),
 ( 2, 2 ),
 ( 0.000000000000000000, 1.000000000000000000 ),
 ( 0.000000000000000000, 1.000000000000000000 ),
 .UNSPECIFIED. ) 
 GEOMETRIC_REPRESENTATION_ITEM ( )  RATIONAL_B_SPLINE_SURFACE ( (
 ( 1.000000000000000000, 1.000000000000000000),
 ( 0.9953485035131437453, 0.8621029689291515030),
 ( 0.9953485035131437453, 0.8621029689291515030),
 ( 1.000000000000000000, 1.000000000000000000) ) ) 
 REPRESENTATION_ITEM ( '' )  SURFACE ( )  );
#18775=CARTESIAN_POINT ( 'NONE',  ( 4.694002226626921015, -30.39302829899101965, -33.97864921186342713 ) ) ;
#18776=CARTESIAN_POINT ( 'NONE',  ( 0.2940133293163011974, -43.64383948024472915, -6.438619805569689269 ) ) ;
#18777=VERTEX_POINT ( 'NONE', #29321 ) ;
#18780=CARTESIAN_POINT ( 'NONE',  ( 0.1129192098497447394, -38.20615368646970467, 22.07354996983974260 ) ) ;
#18788=CARTESIAN_POINT ( 'NONE',  ( 4.975610109902397937, 48.43414999183897862, -6.825138951392602849 ) ) ;
#18792=VECTOR ( 'NONE', #38514, 1000.000000000000114 ) ;
#18794=CARTESIAN_POINT ( 'NONE',  ( 4.553261556744875094, -41.75933753256810377, 13.62707946203756393 ) ) ;
#18796=CARTESIAN_POINT ( 'NONE',  ( 2.879087469061463178, -39.15901799926898263, -20.06671338601083932 ) ) ;
#18802=VERTEX_POINT ( 'NONE', #5798 ) ;
#18803=CARTESIAN_POINT ( 'NONE',  ( 0.8744876279028263033, -31.30103973185235233, 37.82320666052117275 ) ) ;
#18811=B_SPLINE_CURVE_WITH_KNOTS ( 'NONE', 3,
 ( #44265, #14512, #24197, #38947 ),
 .UNSPECIFIED., .F., .F.,
 ( 4, 4 ),
 ( 0.000000000000000000, 0.004442905043737215703 ),
 .UNSPECIFIED. ) ;
#18815=ORIENTED_EDGE ( 'NONE', *, *, #48095, .F. ) ;
#18817=CARTESIAN_POINT ( 'NONE',  ( 2.879087469061462734, 23.73415476983658934, -37.05120206072701450 ) ) ;
#18820=ORIENTED_EDGE ( 'NONE', *, *, #47769, .T. ) ;
#18828=CARTESIAN_POINT ( 'NONE',  ( 0.5980271706414734822, -45.78139539622846144, -17.77956912908339859 ) ) ;
#18831=EDGE_CURVE ( 'NONE', #61591, #13981, #51780, .T. ) ;
#18839=CARTESIAN_POINT ( 'NONE',  ( 4.553261556744873317, -9.994631851593151595, -42.77437199977056537 ) ) ;
#18853=CARTESIAN_POINT ( 'NONE',  ( 0.1157506346131639274, -22.95291453873705478, -37.68427223630924061 ) ) ;
#18854=ORIENTED_EDGE ( 'NONE', *, *, #46654, .T. ) ;
#18857=CARTESIAN_POINT ( 'NONE',  ( 0.1156495703730067715, -31.79125611521524419, -30.59834943012220876 ) ) ;
#18858=EDGE_LOOP ( 'NONE', ( #56236, #46298, #57189, #2389 ) ) ;
#18860=EDGE_LOOP ( 'NONE', ( #25081, #55789, #28891, #14271 ) ) ;
#18866=DIRECTION ( 'NONE',  ( -1.000000000000000000, -0.000000000000000000, -0.000000000000000000 ) ) ;
#18870=CARTESIAN_POINT ( 'NONE',  ( 4.834790513006553603, -21.44535528597671004, -42.10327870347644108 ) ) ;
#18874=CARTESIAN_POINT ( 'NONE',  ( 0.6000166863083106206, -39.66797998683833271, -28.95297645272843923 ) ) ;
#18875=ADVANCED_FACE ( 'NONE', ( #11460 ), #54051, .F. ) ;
#18881=DIRECTION ( 'NONE',  ( 0.1011922191286468153, -0.7235494112461594574, -0.6828150439710272135 ) ) ;
#18882=EDGE_CURVE ( 'NONE', #17395, #18471, #19021, .T. ) ;
#18886=CARTESIAN_POINT ( 'NONE',  ( 4.975610109902397937, 14.46773809681547718, 46.72401910687614190 ) ) ;
#18894=AXIS2_PLACEMENT_3D ( 'NONE', #38603, #28868, #47679 ) ;
#18902=ORIENTED_EDGE ( 'NONE', *, *, #19256, .T. ) ;
#18907=CARTESIAN_POINT ( 'NONE',  ( 4.975610109902397937, -23.13264022976583334, 43.09675583078141869 ) ) ;
#18915=CARTESIAN_POINT ( 'NONE',  ( -6.072942160501519915, -8.919639966878049719, -17.06587780192662507 ) ) ;
#18916=B_SPLINE_CURVE_WITH_KNOTS ( 'NONE', 3,
 ( #44708, #59073, #49378, #30268, #35617, #48763 ),
 .UNSPECIFIED., .F., .F.,
 ( 4, 2, 4 ),
 ( 5.421010862427522170E-19, 0.0002293801035737097786, 0.0004587602071474190151 ),
 .UNSPECIFIED. ) ;
#18917=VERTEX_POINT ( 'NONE', #49976 ) ;
#18923=CARTESIAN_POINT ( 'NONE',  ( -6.078726893082806448, -16.13637198556892827, -10.50768958487384808 ) ) ;
#18925=CARTESIAN_POINT ( 'NONE',  ( 0.6027444965799114707, 46.56435540091575831, 15.59805507057365936 ) ) ;
#18926=LINE ( 'NONE', #13924, #52251 ) ;
#18935=CIRCLE ( 'NONE', #26926, 48.91267123290010943 ) ;
#18952=EDGE_CURVE ( 'NONE', #44276, #28569, #53374, .T. ) ;
#18958=LINE ( 'NONE', #9223, #59915 ) ;
#18959=CARTESIAN_POINT ( 'NONE',  ( 4.553261556744873317, 17.98701270972406618, 40.07501640179154379 ) ) ;
#18969=CARTESIAN_POINT ( 'NONE',  ( 0.6029443199889047422, 48.20182254088276608, -9.387328991339774831 ) ) ;
#18975=ORIENTED_EDGE ( 'NONE', *, *, #51209, .T. ) ;
#18979=CARTESIAN_POINT ( 'NONE',  ( 0.1129192098497447394, 14.78321943369649283, -41.57412910645673776 ) ) ;
#18986=ORIENTED_EDGE ( 'NONE', *, *, #59946, .T. ) ;
#18997=EDGE_LOOP ( 'NONE', ( #43022, #14999, #3230, #22512 ) ) ;
#19001=CARTESIAN_POINT ( 'NONE',  ( 0.1149546198390367924, 41.96184135302931395, -13.64369580745698762 ) ) ;
#19002=CARTESIAN_POINT ( 'NONE',  ( 0.1129192098497447394, -35.06977877439262414, 26.77802092202325213 ) ) ;
#19008=CARTESIAN_POINT ( 'NONE',  ( 0.1129192098497447394, -44.12161472487018443, 0.4846667466135898827 ) ) ;
#19013=VERTEX_POINT ( 'NONE', #33359 ) ;
#19014=CARTESIAN_POINT ( 'NONE',  ( 4.553261556744873317, -14.95853073564509828, 41.30111286702087625 ) ) ;
#19015=CARTESIAN_POINT ( 'NONE',  ( 0.6027444965799114707, -25.56852311693717894, 41.92599601090104500 ) ) ;
#19021=B_SPLINE_CURVE_WITH_KNOTS ( 'NONE', 3,
 ( #46524, #35590, #16785, #59357 ),
 .UNSPECIFIED., .F., .F.,
 ( 4, 4 ),
 ( 2.308109569601360422E-17, 0.004559932413162185935 ),
 .UNSPECIFIED. ) ;
#19023=CARTESIAN_POINT ( 'NONE',  ( 0.6253024248130472085, -0.8873488924062337135, -49.09844029458358250 ) ) ;
#19025=CARTESIAN_POINT ( 'NONE',  ( 0.5980271706414711508, 22.09347986454737622, 43.86259671196521026 ) ) ;
#19027=B_SPLINE_CURVE_WITH_KNOTS ( 'NONE', 3,
 ( #42288, #13779, #3407, #36657, #60418, #56345, #32886, #51338, #60731, #56656, #41363, #46987, #27545, #51648, #41984, #3110 ),
 .UNSPECIFIED., .F., .F.,
 ( 4, 3, 3, 3, 3, 4 ),
 ( 5.057544569639795705E-18, 0.0005656085177311398569, 0.001131215744874500056, 0.001696821861372766350, 0.002262427090022499018, 0.002715792992282060631 ),
 .UNSPECIFIED. ) ;
#19031=EDGE_CURVE ( 'NONE', #2992, #54794, #39221, .T. ) ;
#19032=CARTESIAN_POINT ( 'NONE',  ( 3.050102900204245682, -16.13753096457668335, 40.92682914110729087 ) ) ;
#19063=CARTESIAN_POINT ( 'NONE',  ( -6.077587904424778920, 0.6110050725289616347, 19.24636833782608392 ) ) ;
#19071=ORIENTED_EDGE ( 'NONE', *, *, #9612, .T. ) ;
#19079=ADVANCED_FACE ( 'NONE', ( #33660 ), #5564, .F. ) ;
#19080=VERTEX_POINT ( 'NONE', #28945 ) ;
#19082=CARTESIAN_POINT ( 'NONE',  ( 0.6029443199889047422, -7.837561479521124141, -48.47793592872049118 ) ) ;
#19086=EDGE_LOOP ( 'NONE', ( #14548, #1292, #16183, #39678 ) ) ;
#19087=VERTEX_POINT ( 'NONE', #60905 ) ;
#19091=CARTESIAN_POINT ( 'NONE',  ( 0.9268187852002115479, -28.25673427553589434, -33.84244821212526944 ) ) ;
#19095=DIRECTION ( 'NONE',  ( -0.1011922191286467598, 0.4144321176143397900, -0.9044369268652812099 ) ) ;
#19099=CARTESIAN_POINT ( 'NONE',  ( -6.077587904424778920, -6.656176160390447905, -18.06907137391903717 ) ) ;
#19104=EDGE_LOOP ( 'NONE', ( #13273, #4772, #37632, #49374 ) ) ;
#19110=CARTESIAN_POINT ( 'NONE',  ( 0.9268187852002115479, -38.89159468621753035, -20.76531231818109191 ) ) ;
#19111=DIRECTION ( 'NONE',  ( 0.000000000000000000, 0.000000000000000000, 1.000000000000000000 ) ) ;
#19113=ADVANCED_FACE ( 'NONE', ( #56514 ), #39272, .F. ) ;
#19117=ORIENTED_EDGE ( 'NONE', *, *, #55497, .T. ) ;
#19118=CARTESIAN_POINT ( 'NONE',  ( 0.6039202388192953519, 49.01762936092966783, 2.972494690241990423 ) ) ;
#19119=CARTESIAN_POINT ( 'NONE',  ( 50.15577769773999961, 12.80000000000000071, -3.000000000000000000 ) ) ;
#19127=B_SPLINE_CURVE_WITH_KNOTS ( 'NONE', 3,
 ( #49184, #15069, #58877, #53555 ),
 .UNSPECIFIED., .F., .F.,
 ( 4, 4 ),
 ( 0.000000000000000000, 0.005013413432710141573 ),
 .UNSPECIFIED. ) ;
#19128=ADVANCED_FACE ( 'NONE', ( #34896 ), #11640, .F. ) ;
#19129=CARTESIAN_POINT ( 'NONE',  ( -6.072942160501519915, -12.95676005301696421, -14.24522836663435577 ) ) ;
#19130=ORIENTED_EDGE ( 'NONE', *, *, #57338, .T. ) ;
#19136=CARTESIAN_POINT ( 'NONE',  ( 1.542467486220083783, -0.2257246335812510551, -44.06061125825107894 ) ) ;
#19140=ORIENTED_EDGE ( 'NONE', *, *, #39638, .F. ) ;
#19143=ORIENTED_EDGE ( 'NONE', *, *, #53944, .T. ) ;
#19144=CARTESIAN_POINT ( 'NONE',  ( 0.6252788684277206244, -31.15129425738415847, -37.96104842155354220 ) ) ;
#19146=CARTESIAN_POINT ( 'NONE',  ( 0.8744876279028306332, -38.80702141274064587, 30.07266432244707843 ) ) ;
#19147=VERTEX_POINT ( 'NONE', #48360 ) ;
#19149=DIRECTION ( 'NONE',  ( 0.000000000000000000, -1.000000000000000000, 0.000000000000000000 ) ) ;
#19161=CARTESIAN_POINT ( 'NONE',  ( 0.1157991065609915715, -22.80398465254558360, -37.77460323423880340 ) ) ;
#19171=ORIENTED_EDGE ( 'NONE', *, *, #43459, .T. ) ;
#19174=CARTESIAN_POINT ( 'NONE',  ( 4.975610109902397937, 0.000000000000000000, 0.000000000000000000 ) ) ;
#19176=ORIENTED_EDGE ( 'NONE', *, *, #34562, .F. ) ;
#19177=CARTESIAN_POINT ( 'NONE',  ( 0.1156495703730067437, -40.84808789472971569, 16.68462371692890756 ) ) ;
#19186=EDGE_CURVE ( 'NONE', #16242, #27767, #14863, .T. ) ;
#19189=CARTESIAN_POINT ( 'NONE',  ( 4.975610109902397937, -48.84566763821283786, -2.559328059280381318 ) ) ;
#19192=CARTESIAN_POINT ( 'NONE',  ( 0.1152339509894530906, 39.85093012247246946, 18.94323253378521699 ) ) ;
#19195=CARTESIAN_POINT ( 'NONE',  ( 0.3676999524040366896, -17.09834788623584600, 40.66444494744877858 ) ) ;
#19199=CARTESIAN_POINT ( 'NONE',  ( -6.079354080745853928, 19.09774425860446811, -2.463558296672129888 ) ) ;
#19207=CARTESIAN_POINT ( 'NONE',  ( 4.694002226626921015, -38.39382765324710789, 24.58045503197395476 ) ) ;
#19208=CARTESIAN_POINT ( 'NONE',  ( 0.5980271706414711508, -39.77423938000287507, 28.81074668563609009 ) ) ;
#19231=CARTESIAN_POINT ( 'NONE',  ( 0.6008122571543325074, 46.74120789342043025, 15.06034644785334109 ) ) ;
#19234=ORIENTED_EDGE ( 'NONE', *, *, #51350, .F. ) ;
#19237=B_SPLINE_CURVE_WITH_KNOTS ( 'NONE', 3,
 ( #1692, #59022, #40576, #30831, #16752, #15518 ),
 .UNSPECIFIED., .F., .F.,
 ( 4, 2, 4 ),
 ( 1.870830531855975817E-17, 0.0002293755540694300988, 0.0004587511081388414950 ),
 .UNSPECIFIED. ) ;
#19242=CARTESIAN_POINT ( 'NONE',  ( -6.057079549204054558, 11.99988366729700573, 15.06101002825099400 ) ) ;
#19243=CARTESIAN_POINT ( 'NONE',  ( 0.6008122571543322854, -35.57793373092638234, -33.84915334100880102 ) ) ;
#19248=CARTESIAN_POINT ( 'NONE',  ( 1.830465331921977912, -32.48963746129035002, 29.74557973064752403 ) ) ;
#19250=DIRECTION ( 'NONE',  ( -1.000000000000000000, -0.000000000000000000, -0.000000000000000000 ) ) ;
#19252=CARTESIAN_POINT ( 'NONE',  ( 0.6016117650947689910, -42.61630575986080771, 24.40085116602604387 ) ) ;
#19254=CARTESIAN_POINT ( 'NONE',  ( 4.553261556744873317, 1.633632119646958980, 43.89613664004264848 ) ) ;
#19256=EDGE_CURVE ( 'NONE', #13969, #8619, #34722, .T. ) ;
#19262=CARTESIAN_POINT ( 'NONE',  ( 0.6027444965799114707, 41.08494361130553330, 26.89918073739952931 ) ) ;
#19263=CARTESIAN_POINT ( 'NONE',  ( 0.1129192098497455998, -35.64954734424960492, 26.00118385641814456 ) ) ;
#19264=CARTESIAN_POINT ( 'NONE',  ( 0.1365634738349410515, -27.00966719914814362, -34.89040695398243486 ) ) ;
#19269=CARTESIAN_POINT ( 'NONE',  ( 0.5997462898726536595, 48.09935696025637952, -9.899671214446758682 ) ) ;
#19275=CARTESIAN_POINT ( 'NONE',  ( 4.553261556744873317, 42.54662847375970358, 10.92355122382355148 ) ) ;
#19276=CARTESIAN_POINT ( 'NONE',  ( 0.3676999524040366896, 14.45783756353458216, -41.67639039443420756 ) ) ;
#19280=CARTESIAN_POINT ( 'NONE',  ( -6.077587904424778920, -18.89978312007036720, 3.687033958106935128 ) ) ;
#19285=ORIENTED_EDGE ( 'NONE', *, *, #40054, .T. ) ;
#19287=LINE ( 'NONE', #28978, #47303 ) ;
#19288=CARTESIAN_POINT ( 'NONE',  ( 0.5987334308729318488, -20.42989745030504523, -44.65626716083365011 ) ) ;
#19292=EDGE_CURVE ( 'NONE', #48331, #61199, #45170, .T. ) ;
#19293=CARTESIAN_POINT ( 'NONE',  ( 0.1135584504625007374, 33.31662552165888513, 28.93016619352194851 ) ) ;
#19300=CARTESIAN_POINT ( 'NONE',  ( 0.7948884756798508811, -39.86121518214929438, 28.66674325420559200 ) ) ;
#19301=CARTESIAN_POINT ( 'NONE',  ( 0.1158516988532803521, -40.91787788753845234, -16.51270504833438935 ) ) ;
#19309=CARTESIAN_POINT ( 'NONE',  ( 4.553261556744873317, -20.11719049292697648, 39.04917684785332455 ) ) ;
#19310=ORIENTED_EDGE ( 'NONE', *, *, #27576, .T. ) ;
#19312=CARTESIAN_POINT ( 'NONE',  ( 0.6024113833632039894, -25.64285567226712814, 41.88061391708750847 ) ) ;
#19322=CARTESIAN_POINT ( 'NONE',  ( -6.078726893082806448, -8.909671472910670076, -17.07078778245227824 ) ) ;
#19326=EDGE_CURVE ( 'NONE', #11136, #7783, #24280, .T. ) ;
#19332=CARTESIAN_POINT ( 'NONE',  ( 4.553261556744873317, 38.38432632180467863, 21.35844232721216684 ) ) ;
#19335=AXIS2_PLACEMENT_3D ( 'NONE', #43574, #11276, #58238 ) ;
#19336=CARTESIAN_POINT ( 'NONE',  ( -6.077587904424778920, 5.484810954822209261, 18.45840919970604688 ) ) ;
#19339=EDGE_CURVE ( 'NONE', #13969, #31069, #30811, .T. ) ;
#19342=CARTESIAN_POINT ( 'NONE',  ( 4.975610109902397937, 42.89797504594955058, -23.49921581872176191 ) ) ;
#19345=VERTEX_POINT ( 'NONE', #23793 ) ;
#19350=DIRECTION ( 'NONE',  ( 0.09722883295013595717, 0.9469132758617077039, -0.3064340092744340383 ) ) ;
#19355=VERTEX_POINT ( 'NONE', #33206 ) ;
#19356=CARTESIAN_POINT ( 'NONE',  ( 4.553261556744875094, 0.000000000000000000, 0.000000000000000000 ) ) ;
#19358=CARTESIAN_POINT ( 'NONE',  ( 4.335381028904216727, -3.692956800736317824, -48.84791620665349399 ) ) ;
#19364=CARTESIAN_POINT ( 'NONE',  ( 0.7044674535453004927, 23.45856740197648449, 43.14508475200662474 ) ) ;
#19373=CARTESIAN_POINT ( 'NONE',  ( 0.1129192098497455998, 39.96249028893973332, -18.70698152272436587 ) ) ;
#19374=ADVANCED_FACE ( 'NONE', ( #57577 ), #27697, .F. ) ;
#19378=CARTESIAN_POINT ( 'NONE',  ( 0.6028777368367060907, -7.751577361373165331, -48.49178154823474785 ) ) ;
#19379=ORIENTED_EDGE ( 'NONE', *, *, #13420, .T. ) ;
#19391=CARTESIAN_POINT ( 'NONE',  ( 0.2940133293163021966, -28.13058116957257582, 33.98398082391366870 ) ) ;
#19394=ORIENTED_EDGE ( 'NONE', *, *, #18882, .F. ) ;
#19396=CARTESIAN_POINT ( 'NONE',  ( -6.078726893082806448, -18.90156862012333860, 3.677600436084480062 ) ) ;
#19398=CARTESIAN_POINT ( 'NONE',  ( 2.648799415243696664, 43.56092747588109404, 22.51584021818029768 ) ) ;
#19399=B_SPLINE_CURVE_WITH_KNOTS ( 'NONE', 3,
 ( #29112, #44481, #5284, #24412 ),
 .UNSPECIFIED., .F., .F.,
 ( 4, 4 ),
 ( 0.000000000000000000, 0.004444103432399267029 ),
 .UNSPECIFIED. ) ;
#19403=( BOUNDED_SURFACE ( )  B_SPLINE_SURFACE ( 3, 1, ( 
 ( #40575, #61102 ),
 ( #18522, #16751 ),
 ( #32316, #37647 ),
 ( #51710, #51392 ) ),
 .UNSPECIFIED., .F., .F., .F. ) 
 B_SPLINE_SURFACE_WITH_KNOTS ( ( 4, 4 ),
 ( 2, 2 ),
 ( 0.000000000000000000, 1.000000000000000000 ),
 ( 0.000000000000000000, 1.000000000000000000 ),
 .UNSPECIFIED. ) 
 GEOMETRIC_REPRESENTATION_ITEM ( )  RATIONAL_B_SPLINE_SURFACE ( (
 ( 1.000000000000000000, 1.000000000000000000),
 ( 0.9754377213608244057, 0.9999580625633939235),
 ( 0.9754377213608244057, 0.9999580625633939235),
 ( 1.000000000000000000, 1.000000000000000000) ) ) 
 REPRESENTATION_ITEM ( '' )  SURFACE ( )  );
#19414=VERTEX_POINT ( 'NONE', #33514 ) ;
#19415=CARTESIAN_POINT ( 'NONE',  ( 0.8753041380234471980, 48.93739466471249955, 4.033575498629939027 ) ) ;
#19416=CARTESIAN_POINT ( 'NONE',  ( 2.648799415243696664, -24.22471848649487214, -42.63426412569674540 ) ) ;
#19417=CARTESIAN_POINT ( 'NONE',  ( -6.078726893082806448, 3.069885851706565916, -19.00973019603939917 ) ) ;
#19427=CARTESIAN_POINT ( 'NONE',  ( 0.8753041380234524160, 33.66554281472423327, 35.74590263041275762 ) ) ;
#19430=ORIENTED_EDGE ( 'NONE', *, *, #18472, .F. ) ;
#19439=CARTESIAN_POINT ( 'NONE',  ( -6.077587904424778920, -6.656176160390709917, 18.06907137391894125 ) ) ;
#19443=CARTESIAN_POINT ( 'NONE',  ( 0.6000166863083090663, -14.47337940799722134, 46.92914627628139357 ) ) ;
#19450=CARTESIAN_POINT ( 'NONE',  ( -2.601141883200665639, 9.698805021789150160, 11.34586306187000382 ) ) ;
#19452=VECTOR ( 'NONE', #40903, 1000.000000000000114 ) ;
#19456=CARTESIAN_POINT ( 'NONE',  ( 0.5997462898726536595, -1.051648045107538954, 49.09628974305014992 ) ) ;
#19460=ADVANCED_FACE ( 'NONE', ( #30634 ), #56437, .F. ) ;
#19468=ORIENTED_EDGE ( 'NONE', *, *, #38884, .F. ) ;
#19470=ADVANCED_FACE ( 'NONE', ( #35683 ), #3199, .F. ) ;
#19471=CARTESIAN_POINT ( 'NONE',  ( 0.1145239942831223490, 24.97564404501438062, 36.37530323229500340 ) ) ;
#19478=ORIENTED_EDGE ( 'NONE', *, *, #15802, .F. ) ;
#19480=LINE ( 'NONE', #38596, #42825 ) ;
#19490=CARTESIAN_POINT ( 'NONE',  ( 0.1129192098497455998, 33.91039995638899995, -28.23183597612607798 ) ) ;
#19493=CARTESIAN_POINT ( 'NONE',  ( 0.1140933569871965536, 39.58854792274839696, 19.48581082357515015 ) ) ;
#19504=CARTESIAN_POINT ( 'NONE',  ( 1.112077966505211846, 19.45195591732835538, -39.55567893639127419 ) ) ;
#19506=ORIENTED_EDGE ( 'NONE', *, *, #53686, .T. ) ;
#19509=CARTESIAN_POINT ( 'NONE',  ( 3.559346040607745287, 26.81358697290394488, 34.84912961880832682 ) ) ;
#19519=EDGE_CURVE ( 'NONE', #59488, #34766, #35992, .T. ) ;
#19526=CARTESIAN_POINT ( 'NONE',  ( 0.3676999524040366896, -7.853951980431815194, -43.40813312746713848 ) ) ;
#19532=CARTESIAN_POINT ( 'NONE',  ( 0.6039202388192953519, 41.25132197622554742, 26.64380130654712175 ) ) ;
#19535=CARTESIAN_POINT ( 'NONE',  ( -6.078075953587585900, -14.66587681219991524, -12.47827037599814481 ) ) ;
#19541=DIRECTION ( 'NONE',  ( 1.000000000000000000, 0.000000000000000000, 0.000000000000000000 ) ) ;
#19542=CARTESIAN_POINT ( 'NONE',  ( 4.553261556744875094, 0.000000000000000000, 0.000000000000000000 ) ) ;
#19552=ORIENTED_EDGE ( 'NONE', *, *, #22881, .T. ) ;
#19555=CARTESIAN_POINT ( 'NONE',  ( 4.694002226626921015, 36.32786722402781265, 27.54216466437490496 ) ) ;
#19558=CARTESIAN_POINT ( 'NONE',  ( 4.553261556744875094, 12.28162544311214432, 42.17465165592641796 ) ) ;
#19568=CARTESIAN_POINT ( 'NONE',  ( -6.057079549204054558, 16.77479338118040886, 9.457142175014846330 ) ) ;
#19575=CARTESIAN_POINT ( 'NONE',  ( 0.6021447746440204973, 22.48211463121051068, -43.65885546825062846 ) ) ;
#19578=CARTESIAN_POINT ( 'NONE',  ( 4.834790513006555379, -39.84947630189435586, -25.38914294317831022 ) ) ;
#19596=CARTESIAN_POINT ( 'NONE',  ( 4.553261556744875094, -39.67390170502071811, 18.85526688551479424 ) ) ;
#19604=VERTEX_POINT ( 'NONE', #51281 ) ;
#19609=CARTESIAN_POINT ( 'NONE',  ( 0.1152809850208375703, 41.94550343259623304, -13.69379510127901867 ) ) ;
#19612=CARTESIAN_POINT ( 'NONE',  ( 0.6253024248130470975, -39.76151138891634673, 28.81781462024348173 ) ) ;
#19622=CARTESIAN_POINT ( 'NONE',  ( 4.975610109902397937, 2.142807115709095100, 48.86571174967821918 ) ) ;
#19623=VERTEX_POINT ( 'NONE', #42847 ) ;
#19625=CARTESIAN_POINT ( 'NONE',  ( 4.553261556744873317, 40.80044851610476542, 16.27461110774448372 ) ) ;
#19630=ADVANCED_FACE ( 'NONE', ( #189 ), #37264, .F. ) ;
#19631=DIRECTION ( 'NONE',  ( 0.000000000000000000, 0.000000000000000000, 1.000000000000000000 ) ) ;
#19649=CARTESIAN_POINT ( 'NONE',  ( 4.975610109902397937, -48.77192499014908833, -3.707929326867496655 ) ) ;
#19658=CARTESIAN_POINT ( 'NONE',  ( -6.078457390727109555, 18.62514245781370548, -4.888617336594570872 ) ) ;
#19661=CARTESIAN_POINT ( 'NONE',  ( 0.1156867017252034835, -22.98040861868942386, 37.66754076115470440 ) ) ;
#19663=CARTESIAN_POINT ( 'NONE',  ( 0.1152809850208375564, 10.03408747456458627, -42.96815531347071726 ) ) ;
#19671=EDGE_LOOP ( 'NONE', ( #12735, #45150, #51168, #14695 ) ) ;
#19685=ORIENTED_EDGE ( 'NONE', *, *, #45653, .F. ) ;
#19686=CARTESIAN_POINT ( 'NONE',  ( 4.834790513006553603, 47.24803566211424055, 0.4609414235700721174 ) ) ;
#19695=CARTESIAN_POINT ( 'NONE',  ( 0.1365634738349405242, 10.43816654247781806, -42.87082106578719021 ) ) ;
#19701=AXIS2_PLACEMENT_3D ( 'NONE', #29102, #38842, #5272 ) ;
#19703=EDGE_LOOP ( 'NONE', ( #58647, #34157, #55336, #33415 ) ) ;
#19705=CARTESIAN_POINT ( 'NONE',  ( 0.3676999524040366896, 25.91024933382758277, 35.70167450949220722 ) ) ;
#19712=CARTESIAN_POINT ( 'NONE',  ( 0.1365634738349406074, -42.83729192637484573, 10.57492506062288307 ) ) ;
#19715=CARTESIAN_POINT ( 'NONE',  ( 0.2940133293163009753, -32.24540449752910831, 30.10771393461770984 ) ) ;
#19723=CARTESIAN_POINT ( 'NONE',  ( 0.1156867017252034557, 29.57210022659650051, 32.74803345948146927 ) ) ;
#19724=CARTESIAN_POINT ( 'NONE',  ( 4.834790513006553603, -4.995710817785154134, 46.98544683568995595 ) ) ;
#19726=AXIS2_PLACEMENT_3D ( 'NONE', #5834, #38796, #58462 ) ;
#19732=B_SPLINE_CURVE_WITH_KNOTS ( 'NONE', 3,
 ( #20285, #43176, #39400, #6753 ),
 .UNSPECIFIED., .F., .F.,
 ( 4, 4 ),
 ( 0.000000000000000000, 0.005013413432710141573 ),
 .UNSPECIFIED. ) ;
#19736=VECTOR ( 'NONE', #22971, 1000.000000000000114 ) ;
#19738=CARTESIAN_POINT ( 'NONE',  ( 1.112077966505211846, 24.35052357902559450, -36.74346644719130239 ) ) ;
#19739=CARTESIAN_POINT ( 'NONE',  ( 4.553261556744875094, 40.63093864075490558, 16.69330377710913993 ) ) ;
#19741=VERTEX_POINT ( 'NONE', #8148 ) ;
#19742=CARTESIAN_POINT ( 'NONE',  ( 0.8744876279028263033, 32.34273794994744833, 36.93639603806145288 ) ) ;
#19743=DIRECTION ( 'NONE',  ( -1.000000000000000000, -0.000000000000000000, -0.000000000000000000 ) ) ;
#19749=EDGE_CURVE ( 'NONE', #59488, #4551, #9173, .T. ) ;
#19757=CARTESIAN_POINT ( 'NONE',  ( 0.1129192098497447394, 29.30421273086510681, -32.98810246148386227 ) ) ;
#19758=CARTESIAN_POINT ( 'NONE',  ( 2.299746137290199943, -49.01654327427706193, 1.288341230832333428 ) ) ;
#19764=CARTESIAN_POINT ( 'NONE',  ( 4.694002226626921015, 45.58690636503205695, -0.3445860007819027127 ) ) ;
#19767=( BOUNDED_SURFACE ( )  B_SPLINE_SURFACE ( 3, 1, ( 
 ( #3083, #51622 ),
 ( #17825, #61324 ),
 ( #41639, #32545 ),
 ( #22214, #22521 ) ),
 .UNSPECIFIED., .F., .F., .F. ) 
 B_SPLINE_SURFACE_WITH_KNOTS ( ( 4, 4 ),
 ( 2, 2 ),
 ( 0.000000000000000000, 1.000000000000000000 ),
 ( 0.000000000000000000, 1.000000000000000000 ),
 .UNSPECIFIED. ) 
 GEOMETRIC_REPRESENTATION_ITEM ( )  RATIONAL_B_SPLINE_SURFACE ( (
 ( 1.000000000000000000, 1.000000000000000000),
 ( 0.7211978278499970862, 0.9934217856018976445),
 ( 0.7211978278499970862, 0.9934217856018976445),
 ( 1.000000000000000000, 1.000000000000000000) ) ) 
 REPRESENTATION_ITEM ( '' )  SURFACE ( )  );
#19771=VECTOR ( 'NONE', #55251, 1000.000000000000114 ) ;
#19781=ORIENTED_EDGE ( 'NONE', *, *, #55935, .T. ) ;
#19787=CARTESIAN_POINT ( 'NONE',  ( 0.1140933569871965259, 25.55436557308794931, -35.97115997908439766 ) ) ;
#19791=CARTESIAN_POINT ( 'NONE',  ( 0.1129192098497447394, -42.80154921430116843, -10.72283417016740259 ) ) ;
#19796=CARTESIAN_POINT ( 'NONE',  ( -6.078726893082806448, 15.43407385306362301, 11.51448676958282391 ) ) ;
#19800=EDGE_CURVE ( 'NONE', #46169, #55636, #30677, .T. ) ;
#19801=B_SPLINE_CURVE_WITH_KNOTS ( 'NONE', 3,
 ( #10978, #34165, #15679, #43573 ),
 .UNSPECIFIED., .F., .F.,
 ( 4, 4 ),
 ( 0.000000000000000000, 0.004444103432399267029 ),
 .UNSPECIFIED. ) ;
#19809=EDGE_CURVE ( 'NONE', #1366, #3780, #1726, .T. ) ;
#19811=CARTESIAN_POINT ( 'NONE',  ( 0.5980271706414711508, -45.25597162979951804, -19.07737599054031463 ) ) ;
#19821=FACE_OUTER_BOUND ( 'NONE', #11648, .T. ) ;
#19823=ORIENTED_EDGE ( 'NONE', *, *, #2524, .F. ) ;
#19825=CARTESIAN_POINT ( 'NONE',  ( 0.7948878604505658085, 37.94263140573792015, 31.16176133190687736 ) ) ;
#19830=ADVANCED_FACE ( 'NONE', ( #23180 ), #41290, .F. ) ;
#19832=EDGE_LOOP ( 'NONE', ( #17621, #4692, #34098, #55093 ) ) ;
#19840=EDGE_CURVE ( 'NONE', #5480, #3927, #57939, .T. ) ;
#19847=CARTESIAN_POINT ( 'NONE',  ( 4.834790513006555379, 29.81904690970609551, 36.65260948856339951 ) ) ;
#19850=VERTEX_POINT ( 'NONE', #5277 ) ;
#19853=ADVANCED_FACE ( 'NONE', ( #61066 ), #9613, .F. ) ;
#19855=CARTESIAN_POINT ( 'NONE',  ( 0.6000166863083106206, -25.01014854877413995, -42.26483113981061024 ) ) ;
#19856=ORIENTED_EDGE ( 'NONE', *, *, #47323, .F. ) ;
#19863=ORIENTED_EDGE ( 'NONE', *, *, #38632, .F. ) ;
#19869=CARTESIAN_POINT ( 'NONE',  ( 0.1158816050234199174, -31.69261404977700280, 30.70049276472673228 ) ) ;
#19870=( BOUNDED_SURFACE ( )  B_SPLINE_SURFACE ( 3, 1, ( 
 ( #48078, #43086 ),
 ( #39010, #29264 ),
 ( #24260, #52141 ),
 ( #28342, #757 ) ),
 .UNSPECIFIED., .F., .F., .F. ) 
 B_SPLINE_SURFACE_WITH_KNOTS ( ( 4, 4 ),
 ( 2, 2 ),
 ( 0.000000000000000000, 1.000000000000000000 ),
 ( 0.000000000000000000, 1.000000000000000000 ),
 .UNSPECIFIED. ) 
 GEOMETRIC_REPRESENTATION_ITEM ( )  RATIONAL_B_SPLINE_SURFACE ( (
 ( 1.000000000000000000, 1.000000000000000000),
 ( 0.9953485035131437453, 0.8621029689291523912),
 ( 0.9953485035131437453, 0.8621029689291523912),
 ( 1.000000000000000000, 1.000000000000000000) ) ) 
 REPRESENTATION_ITEM ( '' )  SURFACE ( )  );
#19875=B_SPLINE_CURVE_WITH_KNOTS ( 'NONE', 3,
 ( #7156, #49169, #20366, #11273 ),
 .UNSPECIFIED., .F., .F.,
 ( 4, 4 ),
 ( 2.165753205240583906E-17, 0.004559932413162187670 ),
 .UNSPECIFIED. ) ;
#19876=ORIENTED_EDGE ( 'NONE', *, *, #51828, .F. ) ;
#19883=CARTESIAN_POINT ( 'NONE',  ( 0.6039202388192952409, -20.03711874569821205, 44.83388880322316794 ) ) ;
#19888=EDGE_CURVE ( 'NONE', #56636, #59488, #12985, .T. ) ;
#19891=CARTESIAN_POINT ( 'NONE',  ( 0.5997462898726536595, 22.24958391914565681, -43.77793560195825506 ) ) ;
#19892=CARTESIAN_POINT ( 'NONE',  ( 0.6026112563231247332, -30.75395997435152751, 38.28491792860723564 ) ) ;
#19897=CARTESIAN_POINT ( 'NONE',  ( -2.739355103387248747, -9.511660422586917463, -11.50547187021943429 ) ) ;
#19899=ORIENTED_EDGE ( 'NONE', *, *, #55256, .T. ) ;
#19903=EDGE_CURVE ( 'NONE', #55806, #8492, #31595, .T. ) ;
#19904=CARTESIAN_POINT ( 'NONE',  ( 0.1157506346131639274, 41.90541932839798278, 13.81580582933776036 ) ) ;
#19910=B_SPLINE_CURVE_WITH_KNOTS ( 'NONE', 3,
 ( #37480, #8629, #56555, #22744, #46885, #23061, #41878, #13671, #41562, #45640, #2692, #55937, #17739, #12748, #56243, #46566 ),
 .UNSPECIFIED., .F., .F.,
 ( 4, 3, 3, 3, 3, 4 ),
 ( 2.081781105835003771E-17, 0.0002612764279487743012, 0.0003919131003184794619, 0.0005225497727000646053, 0.0007837925190632457880, 0.001045051706266715216 ),
 .UNSPECIFIED. ) ;
#19918=CARTESIAN_POINT ( 'NONE',  ( 0.2279481005628791745, 14.52238209920514933, 41.66057975157808357 ) ) ;
#19924=ORIENTED_EDGE ( 'NONE', *, *, #51418, .F. ) ;
#19926=CARTESIAN_POINT ( 'NONE',  ( 3.559346040607745287, 43.96414470145123943, 0.7643704676690852295 ) ) ;
#19931=CARTESIAN_POINT ( 'NONE',  ( -2.601141883200665639, 14.91765895884289428, -0.5088011959921571181 ) ) ;
#19933=CARTESIAN_POINT ( 'NONE',  ( 50.15577769773999961, 0.000000000000000000, 0.000000000000000000 ) ) ;
#19934=CARTESIAN_POINT ( 'NONE',  ( 4.553261556744875094, 0.000000000000000000, 0.000000000000000000 ) ) ;
#19937=EDGE_CURVE ( 'NONE', #36320, #43985, #29717, .T. ) ;
#19939=CARTESIAN_POINT ( 'NONE',  ( 0.6026777506516367566, 4.542038867869873542, -48.89699656993237653 ) ) ;
#19949=CARTESIAN_POINT ( 'NONE',  ( 0.1145239942831223490, 33.80898014942432894, -28.35310109953591251 ) ) ;
#19955=CARTESIAN_POINT ( 'NONE',  ( 3.894904216938897878, -15.73571937194873804, 41.04280044445649622 ) ) ;
#19956=ORIENTED_EDGE ( 'NONE', *, *, #36382, .F. ) ;
#19959=CARTESIAN_POINT ( 'NONE',  ( 4.975610109902397937, 42.89797504594920241, 23.49921581872238718 ) ) ;
#19963=CARTESIAN_POINT ( 'NONE',  ( 0.6026112563231247332, -20.03700257410760699, 44.83368736507640762 ) ) ;
#19978=CARTESIAN_POINT ( 'NONE',  ( 2.299746137290199943, -26.51152743748404816, -41.24827572902495376 ) ) ;
#19982=CARTESIAN_POINT ( 'NONE',  ( 0.3676999524040323597, -22.15802448779959377, -38.14410221935904843 ) ) ;
#19983=ADVANCED_FACE ( 'NONE', ( #60078 ), #13661, .F. ) ;
#19985=CARTESIAN_POINT ( 'NONE',  ( 2.648799415243708655, -2.956030660111293784, -48.94669903094671781 ) ) ;
#19991=ORIENTED_EDGE ( 'NONE', *, *, #50593, .T. ) ;
#19994=CARTESIAN_POINT ( 'NONE',  ( -6.078075953587585900, -8.901949479772877538, -17.07484903906055962 ) ) ;
#20001=DIRECTION ( 'NONE',  ( 0.09722883295013597105, 0.8382159563662602286, -0.5366009360187049548 ) ) ;
#20012=CARTESIAN_POINT ( 'NONE',  ( -6.077587904424778920, -11.01164173315302008, 15.79682777441765751 ) ) ;
#20014=CARTESIAN_POINT ( 'NONE',  ( 3.678834586032788234, 12.69316164127655000, -47.30217772129290665 ) ) ;
#20019=CARTESIAN_POINT ( 'NONE',  ( 4.975610109902397937, -48.84566763821283786, -2.559328059280381318 ) ) ;
#20022=ORIENTED_EDGE ( 'NONE', *, *, #52376, .T. ) ;
#20026=B_SPLINE_CURVE_WITH_KNOTS ( 'NONE', 3,
 ( #6278, #57671, #24183, #43323, #1286, #48307, #58601, #20420, #39547, #5970, #353, #15415, #10095, #24808, #33916, #34840, #49225, #25413, #10718, #34527, #19504, #53907, #38936, #44560, #52992 ),
 .UNSPECIFIED., .F., .F.,
 ( 4, 3, 3, 3, 3, 3, 3, 3, 4 ),
 ( 6.254634441385501517E-18, 0.0005656085177311400737, 0.001131215744874499189, 0.001696821861372766133, 0.002262427090022496850, 0.002828031679238745058, 0.003393635864401603995, 0.003977030878808130755, 0.004561030005651158133 ),
 .UNSPECIFIED. ) ;
#20027=CARTESIAN_POINT ( 'NONE',  ( 0.6000166863083090663, -19.40010892967620038, -45.11606427011504650 ) ) ;
#20031=ORIENTED_EDGE ( 'NONE', *, *, #33478, .F. ) ;
#20034=CARTESIAN_POINT ( 'NONE',  ( 0.1119899015040011631, -42.82020505619818351, 10.64853732386031915 ) ) ;
#20035=CARTESIAN_POINT ( 'NONE',  ( 0.6026112563231247332, -19.71849761537919932, -44.97468006219157388 ) ) ;
#20036=FACE_OUTER_BOUND ( 'NONE', #22458, .T. ) ;
#20038=CARTESIAN_POINT ( 'NONE',  ( -6.078075953587585900, 19.09862890096249544, 2.457142313838565961 ) ) ;
#20039=CARTESIAN_POINT ( 'NONE',  ( 0.6029443199889047422, 37.39262245022165132, -31.83283569130437130 ) ) ;
#20042=CARTESIAN_POINT ( 'NONE',  ( 4.335381028904201628, -5.712845112847932505, -48.65306001045518514 ) ) ;
#20044=CARTESIAN_POINT ( 'NONE',  ( 0.8744876279028306332, 3.827863332835647281, -48.94586308039347955 ) ) ;
#20045=ADVANCED_FACE ( 'NONE', ( #50370 ), #16031, .F. ) ;
#20049=CARTESIAN_POINT ( 'NONE',  ( 4.975610109902397937, 0.000000000000000000, 0.000000000000000000 ) ) ;
#20051=CARTESIAN_POINT ( 'NONE',  ( 4.553261556744873317, -39.67390170502044100, -18.85526688551536623 ) ) ;
#20054=ORIENTED_EDGE ( 'NONE', *, *, #24473, .T. ) ;
#20062=CARTESIAN_POINT ( 'NONE',  ( -2.601141883200662974, -14.31801740503249931, 4.217796232462521111 ) ) ;
#20065=B_SPLINE_CURVE_WITH_KNOTS ( 'NONE', 3,
 ( #25806, #59001, #48382, #14892, #33998, #53982, #39016, #25489, #11107, #30190, #58677, #53071, #6052, #762, #15495, #24581, #44627, #39943, #20807, #1359, #44329, #11406, #16111, #29578, #49602 ),
 .UNSPECIFIED., .F., .F.,
 ( 4, 3, 3, 3, 3, 3, 3, 3, 4 ),
 ( 5.057544569639794935E-18, 0.0005656085177311390979, 0.001131215744874498972, 0.001696821861372765482, 0.002262427090022497284, 0.002828031679238745058, 0.003393635864401603561, 0.003977030878808130755, 0.004561030005651157265 ),
 .UNSPECIFIED. ) ;
#20067=EDGE_LOOP ( 'NONE', ( #31536, #42599, #8054, #8633 ) ) ;
#20069=ORIENTED_EDGE ( 'NONE', *, *, #41420, .F. ) ;
#20070=CARTESIAN_POINT ( 'NONE',  ( 0.1129192098497447394, -13.01845098534572820, -42.16007260106777466 ) ) ;
#20085=FACE_OUTER_BOUND ( 'NONE', #21367, .T. ) ;
#20087=ORIENTED_EDGE ( 'NONE', *, *, #19749, .F. ) ;
#20105=CARTESIAN_POINT ( 'NONE',  ( 4.553261556744875094, -9.554252317234240621, -42.87488575474295516 ) ) ;
#20109=ADVANCED_FACE ( 'NONE', ( #57205 ), #18049, .F. ) ;
#20111=CARTESIAN_POINT ( 'NONE',  ( 0.7044674535452954967, 32.38853019898860452, 36.91592927667010571 ) ) ;
#20124=EDGE_CURVE ( 'NONE', #41574, #25523, #33164, .T. ) ;
#20126=CARTESIAN_POINT ( 'NONE',  ( 1.479689385636123067, 26.16456136252788767, 35.45418979435581974 ) ) ;
#20129=ORIENTED_EDGE ( 'NONE', *, *, #18124, .F. ) ;
#20132=( BOUNDED_SURFACE ( )  B_SPLINE_SURFACE ( 3, 1, ( 
 ( #40304, #31483 ),
 ( #35591, #11159 ),
 ( #54651, #2969 ),
 ( #49977, #25547 ) ),
 .UNSPECIFIED., .F., .F., .F. ) 
 B_SPLINE_SURFACE_WITH_KNOTS ( ( 4, 4 ),
 ( 2, 2 ),
 ( 0.000000000000000000, 1.000000000000000000 ),
 ( 0.000000000000000000, 1.000000000000000000 ),
 .UNSPECIFIED. ) 
 GEOMETRIC_REPRESENTATION_ITEM ( )  RATIONAL_B_SPLINE_SURFACE ( (
 ( 1.000000000000000000, 1.000000000000000000),
 ( 0.9953485035131437453, 0.8621029689291515030),
 ( 0.9953485035131437453, 0.8621029689291515030),
 ( 1.000000000000000000, 1.000000000000000000) ) ) 
 REPRESENTATION_ITEM ( '' )  SURFACE ( )  );
#20142=ORIENTED_EDGE ( 'NONE', *, *, #45446, .F. ) ;
#20148=CARTESIAN_POINT ( 'NONE',  ( 0.1156495703730067437, 43.28422450877429384, -8.568480723272513089 ) ) ;
#20152=EDGE_CURVE ( 'NONE', #27210, #14390, #50999, .T. ) ;
#20155=CARTESIAN_POINT ( 'NONE',  ( 4.553261556744875094, 0.000000000000000000, 0.000000000000000000 ) ) ;
#20158=CARTESIAN_POINT ( 'NONE',  ( -6.079354080745853928, -6.649248899792496559, 18.07153685541909027 ) ) ;
#20159=FACE_OUTER_BOUND ( 'NONE', #50724, .T. ) ;
#20162=DIRECTION ( 'NONE',  ( -1.000000000000000000, -0.000000000000000000, -0.000000000000000000 ) ) ;
#20163=EDGE_CURVE ( 'NONE', #21722, #54914, #11700, .T. ) ;
#20164=CARTESIAN_POINT ( 'NONE',  ( -6.078726893082806448, 9.985094725776445301, -16.46486940689149137 ) ) ;
#20166=ORIENTED_EDGE ( 'NONE', *, *, #22301, .F. ) ;
#20167=VERTEX_POINT ( 'NONE', #58137 ) ;
#20169=FACE_OUTER_BOUND ( 'NONE', #8875, .T. ) ;
#20174=CARTESIAN_POINT ( 'NONE',  ( 0.1129192098497447394, 15.69290830752478882, 41.23935519181615206 ) ) ;
#20176=CARTESIAN_POINT ( 'NONE',  ( 0.8744876279028306332, -19.05609938969034545, 45.24616145519679122 ) ) ;
#20185=CARTESIAN_POINT ( 'NONE',  ( 0.3676999524040323597, -42.87209381266892194, 10.38913641457044434 ) ) ;
#20186=CARTESIAN_POINT ( 'NONE',  ( 0.6000166863083090663, 23.17738933882538177, -43.29702189694987879 ) ) ;
#20192=CARTESIAN_POINT ( 'NONE',  ( 4.553261556744875094, -15.38244134641827898, 41.14510984366961566 ) ) ;
#20201=CARTESIAN_POINT ( 'NONE',  ( 0.1119898979215350615, -43.83035652836955620, -5.085386401035962400 ) ) ;
#20226=CARTESIAN_POINT ( 'NONE',  ( 0.1149546198390367369, -40.79590554332651209, -16.81192005462792949 ) ) ;
#20229=CARTESIAN_POINT ( 'NONE',  ( 0.8744876279028306332, 48.92939099258504143, -4.032957658373305776 ) ) ;
#20248=B_SPLINE_CURVE_WITH_KNOTS ( 'NONE', 3,
 ( #12604, #41730, #31694, #22297 ),
 .UNSPECIFIED., .F., .F.,
 ( 4, 4 ),
 ( 0.002122961284640939757, 0.004442905043737215703 ),
 .UNSPECIFIED. ) ;
#20255=ORIENTED_EDGE ( 'NONE', *, *, #46945, .T. ) ;
#20256=CARTESIAN_POINT ( 'NONE',  ( 50.15577769773999961, 0.000000000000000000, 0.000000000000000000 ) ) ;
#20263=CARTESIAN_POINT ( 'NONE',  ( 0.6026777506516368677, 22.86838944615219305, 43.45783191527546307 ) ) ;
#20265=CARTESIAN_POINT ( 'NONE',  ( 0.6029443199889047422, -19.87783894042105715, 44.90444477903142229 ) ) ;
#20271=CARTESIAN_POINT ( 'NONE',  ( -2.739355103387248747, -3.994689410813206276, 14.38367211327322615 ) ) ;
#20285=CARTESIAN_POINT ( 'NONE',  ( 4.975610109902397937, 30.94437158899635776, -37.88001153774755636 ) ) ;
#20287=ORIENTED_EDGE ( 'NONE', *, *, #18367, .T. ) ;
#20291=CARTESIAN_POINT ( 'NONE',  ( -6.078457390727109555, -8.902764005229702349, -17.07440494145240351 ) ) ;
#20297=CARTESIAN_POINT ( 'NONE',  ( 0.7948884756798507700, -48.57723108478376162, -7.138015461994420718 ) ) ;
#20301=CARTESIAN_POINT ( 'NONE',  ( -6.077587904424778920, 9.976910903713122281, -16.46988980574249695 ) ) ;
#20304=ORIENTED_EDGE ( 'NONE', *, *, #49627, .T. ) ;
#20306=ORIENTED_EDGE ( 'NONE', *, *, #35991, .T. ) ;
#20307=EDGE_CURVE ( 'NONE', #6110, #4631, #49555, .T. ) ;
#20311=CARTESIAN_POINT ( 'NONE',  ( 0.6008123274975391004, -30.27644390292597265, -38.66382670858426707 ) ) ;
#20323=CARTESIAN_POINT ( 'NONE',  ( -6.077587904424778920, 7.800189710370596607, 17.60548385805284255 ) ) ;
#20327=CARTESIAN_POINT ( 'NONE',  ( -6.078075953587585900, -16.14115596471642178, 10.50039324834243359 ) ) ;
#20335=CARTESIAN_POINT ( 'NONE',  ( 2.185380717157383135, 11.19526193201791919, 42.58504330561036255 ) ) ;
#20339=CARTESIAN_POINT ( 'NONE',  ( 0.1157506346131639274, 29.73331724943256305, 32.60169482016893028 ) ) ;
#20343=CARTESIAN_POINT ( 'NONE',  ( 2.706805983486680223, -19.31528737462589973, -39.54359350078559743 ) ) ;
#20350=CARTESIAN_POINT ( 'NONE',  ( 1.830465331921978800, -41.27772401688780946, 15.37938736959416453 ) ) ;
#20357=CARTESIAN_POINT ( 'NONE',  ( 0.6008123274975389894, 28.45128422543073299, -40.02597877731679432 ) ) ;
#20361=ORIENTED_EDGE ( 'NONE', *, *, #24185, .T. ) ;
#20366=CARTESIAN_POINT ( 'NONE',  ( 3.240649175237396484, -28.83388502998269587, 33.22456909390083979 ) ) ;
#20368=CARTESIAN_POINT ( 'NONE',  ( 0.1135584504625007513, 29.98315275015343673, -32.37225051330565861 ) ) ;
#20369=CARTESIAN_POINT ( 'NONE',  ( 0.1154773475650540948, 20.56842169694548872, 39.03695248021728759 ) ) ;
#20372=ORIENTED_EDGE ( 'NONE', *, *, #26576, .T. ) ;
#20377=ORIENTED_EDGE ( 'NONE', *, *, #54399, .F. ) ;
#20379=CARTESIAN_POINT ( 'NONE',  ( 4.553261556744875094, -36.69060082144763868, -24.15241969627107110 ) ) ;
#20381=CARTESIAN_POINT ( 'NONE',  ( 0.2279481005628790080, -6.290797834582413373, -43.66840218827940845 ) ) ;
#20387=AXIS2_PLACEMENT_3D ( 'NONE', #16312, #2189, #21324 ) ;
#20394=CARTESIAN_POINT ( 'NONE',  ( 0.5980271706414734822, -14.64360625457663545, -46.87871626551421400 ) ) ;
#20396=CARTESIAN_POINT ( 'NONE',  ( -6.077587904424778920, 15.43577113102541887, -11.51229738082424348 ) ) ;
#20400=EDGE_CURVE ( 'NONE', #8721, #8500, #31497, .T. ) ;
#20406=CARTESIAN_POINT ( 'NONE',  ( 2.879087469061463178, -8.726460098500798068, -43.12714424736063989 ) ) ;
#20408=CARTESIAN_POINT ( 'NONE',  ( 2.299746137290199943, 18.13766869742548238, 45.55552998164515088 ) ) ;
#20410=CARTESIAN_POINT ( 'NONE',  ( -6.077587904424778920, -12.95044751835525609, -14.25068175450762809 ) ) ;
#20414=( BOUNDED_SURFACE ( )  B_SPLINE_SURFACE ( 3, 1, ( 
 ( #61914, #56922 ),
 ( #33146, #14657 ),
 ( #33767, #47238 ),
 ( #14046, #24039 ) ),
 .UNSPECIFIED., .F., .F., .F. ) 
 B_SPLINE_SURFACE_WITH_KNOTS ( ( 4, 4 ),
 ( 2, 2 ),
 ( 0.000000000000000000, 1.000000000000000000 ),
 ( 0.000000000000000000, 1.000000000000000000 ),
 .UNSPECIFIED. ) 
 GEOMETRIC_REPRESENTATION_ITEM ( )  RATIONAL_B_SPLINE_SURFACE ( (
 ( 1.000000000000000000, 1.000000000000000000),
 ( 0.7211978278499968642, 0.9934217856018975334),
 ( 0.7211978278499968642, 0.9934217856018975334),
 ( 1.000000000000000000, 1.000000000000000000) ) ) 
 REPRESENTATION_ITEM ( '' )  SURFACE ( )  );
#20417=CARTESIAN_POINT ( 'NONE',  ( 3.678834586032788234, 15.16700106520579716, 46.56795516571884264 ) ) ;
#20419=CARTESIAN_POINT ( 'NONE',  ( 4.226256110419179812, -3.807882442703405257, -43.77587556279986813 ) ) ;
#20420=CARTESIAN_POINT ( 'NONE',  ( 3.390910168358336474, 18.57460499532419007, -39.86328117204245558 ) ) ;
#20423=CARTESIAN_POINT ( 'NONE',  ( 0.1154773475650540671, 4.415934506188623487, 43.90265541494242996 ) ) ;
#20430=CARTESIAN_POINT ( 'NONE',  ( 0.6027444965799114707, 10.80005187744475492, 47.90508736378573218 ) ) ;
#20432=ORIENTED_EDGE ( 'NONE', *, *, #7555, .F. ) ;
#20433=CARTESIAN_POINT ( 'NONE',  ( 0.8744876279028263033, -48.79802643035343834, 5.394688766001209501 ) ) ;
#20434=ORIENTED_EDGE ( 'NONE', *, *, #34496, .F. ) ;
#20435=CARTESIAN_POINT ( 'NONE',  ( 4.553261556744873317, 27.21079963941887314, -34.48350256002191117 ) ) ;
#20438=ORIENTED_EDGE ( 'NONE', *, *, #45215, .F. ) ;
#20444=CARTESIAN_POINT ( 'NONE',  ( 3.240649175237395596, 30.90334817137453172, -31.30891229660418773 ) ) ;
#20451=CARTESIAN_POINT ( 'NONE',  ( -6.079354080745853928, 7.795569227098915199, 17.60744318956248833 ) ) ;
#20454=FACE_OUTER_BOUND ( 'NONE', #30394, .T. ) ;
#20456=DIRECTION ( 'NONE',  ( 0.09722883295013594329, 0.8299705264940797633, -0.5492681305103133127 ) ) ;
#20460=CARTESIAN_POINT ( 'NONE',  ( 0.6029443199889047422, -35.27629250736205080, -34.16315015904468311 ) ) ;
#20461=ORIENTED_EDGE ( 'NONE', *, *, #2524, .T. ) ;
#20469=CARTESIAN_POINT ( 'NONE',  ( 4.553261556744875094, 17.57396821678876364, 40.25785894628445760 ) ) ;
#20478=CARTESIAN_POINT ( 'NONE',  ( 0.1140933569871964842, -6.667546420828093900, -43.61758561417639157 ) ) ;
#20482=CARTESIAN_POINT ( 'NONE',  ( 4.553261556744873317, 40.63093864075514006, -16.69330377710856084 ) ) ;
#20483=CARTESIAN_POINT ( 'NONE',  ( 0.5997462898726536595, 32.62638226927734308, -36.70246327105708417 ) ) ;
#20486=CARTESIAN_POINT ( 'NONE',  ( 0.1368894036331285147, 44.06884517012258584, 2.190481977807497760 ) ) ;
#20487=CARTESIAN_POINT ( 'NONE',  ( 0.5997462898726536595, -30.20781297212619165, 38.71743361310707598 ) ) ;
#20503=EDGE_CURVE ( 'NONE', #1834, #26558, #40490, .T. ) ;
#20505=VECTOR ( 'NONE', #48454, 1000.000000000000227 ) ;
#20506=ORIENTED_EDGE ( 'NONE', *, *, #2997, .T. ) ;
#20510=CARTESIAN_POINT ( 'NONE',  ( -6.078726893082806448, -17.35055002122446410, -8.351793533709264139 ) ) ;
#20511=CARTESIAN_POINT ( 'NONE',  ( 0.6000166863083106206, 32.62822748873757916, -36.70452632376071023 ) ) ;
#20512=CARTESIAN_POINT ( 'NONE',  ( 4.553261556744875094, 0.000000000000000000, 0.000000000000000000 ) ) ;
#20515=CARTESIAN_POINT ( 'NONE',  ( -6.078075953587585900, 5.483964907265256095, 18.45863762965780808 ) ) ;
#20517=CARTESIAN_POINT ( 'NONE',  ( 0.1152339509894530906, 15.02909110027396800, -41.48576998387410697 ) ) ;
#20526=CARTESIAN_POINT ( 'NONE',  ( 0.8744876279028306332, -47.25615711918273121, 13.31186180466906954 ) ) ;
#20537=FACE_OUTER_BOUND ( 'NONE', #14328, .T. ) ;
#20538=ORIENTED_EDGE ( 'NONE', *, *, #23994, .T. ) ;
#20542=CARTESIAN_POINT ( 'NONE',  ( 4.553261556744873317, 35.33793455049254106, 26.09156851415302825 ) ) ;
#20558=CARTESIAN_POINT ( 'NONE',  ( 0.6252788684277198472, 48.95677309978731273, -3.831279007016552995 ) ) ;
#20559=CARTESIAN_POINT ( 'NONE',  ( 0.1157991065609915993, 44.03865309785810922, -2.745796580996492597 ) ) ;
#20566=CARTESIAN_POINT ( 'NONE',  ( 0.3676999524040323597, -43.63756228305270213, -6.458617600968101335 ) ) ;
#20573=DIRECTION ( 'NONE',  ( 0.09722883295013594329, 0.08804304236305897369, -0.9913601649928300841 ) ) ;
#20574=ADVANCED_FACE ( 'NONE', ( #21716 ), #31205, .F. ) ;
#20580=VERTEX_POINT ( 'NONE', #6652 ) ;
#20584=EDGE_CURVE ( 'NONE', #42039, #3844, #36059, .T. ) ;
#20594=VERTEX_POINT ( 'NONE', #54587 ) ;
#20597=CARTESIAN_POINT ( 'NONE',  ( 0.2285344041767085332, -6.290293047543402238, 43.66844837719201422 ) ) ;
#20604=CARTESIAN_POINT ( 'NONE',  ( -6.057079549204054558, 9.975405573751451982, -16.47187040802916513 ) ) ;
#20612=CARTESIAN_POINT ( 'NONE',  ( 0.6029443449137436017, -30.58394248115737923, -38.42085371634249924 ) ) ;
#20622=CARTESIAN_POINT ( 'NONE',  ( 0.1129192098497447394, -23.28677643606880565, -37.47903188453118162 ) ) ;
#20632=ORIENTED_EDGE ( 'NONE', *, *, #3143, .F. ) ;
#20635=CARTESIAN_POINT ( 'NONE',  ( -6.078726893082806448, 18.62710865126535253, -4.881072071038842886 ) ) ;
#20636=CARTESIAN_POINT ( 'NONE',  ( 1.112077966505211624, 10.82950106662251244, 42.72882202654990635 ) ) ;
#20641=CARTESIAN_POINT ( 'NONE',  ( 0.1158816050234199174, 29.66892107124847655, 32.66033012345694431 ) ) ;
#20648=DIRECTION ( 'NONE',  ( 0.09722883295013598492, -0.9880289017988314049, 0.1197724645039495717 ) ) ;
#20657=CARTESIAN_POINT ( 'NONE',  ( 0.1156867017252034419, -38.38474613842218730, -21.76129755239952601 ) ) ;
#20662=ORIENTED_EDGE ( 'NONE', *, *, #11739, .T. ) ;
#20665=B_SPLINE_CURVE_WITH_KNOTS ( 'NONE', 3,
 ( #58315, #35178, #34552, #48952, #53321, #11356 ),
 .UNSPECIFIED., .F., .F.,
 ( 4, 2, 4 ),
 ( 5.421010862427522170E-19, 0.0002293801035737084233, 0.0004587602071474163046 ),
 .UNSPECIFIED. ) ;
#20668=B_SPLINE_CURVE_WITH_KNOTS ( 'NONE', 3,
 ( #12209, #50393, #45721, #2771, #35087, #54454 ),
 .UNSPECIFIED., .F., .F.,
 ( 4, 2, 4 ),
 ( 1.867239236438689166E-17, 0.0002293755540694308577, 0.0004587511081388430129 ),
 .UNSPECIFIED. ) ;
#20669=CARTESIAN_POINT ( 'NONE',  ( -2.601141883200665639, 13.63649176842545607, -6.069721552019776922 ) ) ;
#20672=ORIENTED_EDGE ( 'NONE', *, *, #329, .T. ) ;
#20678=CARTESIAN_POINT ( 'NONE',  ( 0.1152809850208375703, 29.82811608494973399, -32.51505456419408091 ) ) ;
#20680=ORIENTED_EDGE ( 'NONE', *, *, #35608, .F. ) ;
#20681=EDGE_LOOP ( 'NONE', ( #57308, #24674, #33811, #20087 ) ) ;
#20683=CARTESIAN_POINT ( 'NONE',  ( 0.6039202388192953519, -45.45307514328658272, 18.58982713388518704 ) ) ;
#20691=CARTESIAN_POINT ( 'NONE',  ( -6.078726893082806448, -11.01948708261742738, 15.79129335123464983 ) ) ;
#20698=CARTESIAN_POINT ( 'NONE',  ( 0.1158816050234199035, 25.24882932350766396, 36.18616668144803583 ) ) ;
#20700=CARTESIAN_POINT ( 'NONE',  ( -6.077587904424778920, -14.66646125808257395, 12.47761738310216550 ) ) ;
#20705=ORIENTED_EDGE ( 'NONE', *, *, #27870, .F. ) ;
#20715=AXIS2_PLACEMENT_3D ( 'NONE', #27583, #60773, #47313 ) ;
#20719=CARTESIAN_POINT ( 'NONE',  ( 0.3676999524040366896, -26.85386693986640338, 34.99743438737744583 ) ) ;
#20724=CARTESIAN_POINT ( 'NONE',  ( -6.078075953587585900, 17.85074021576659931, 7.221235905047625359 ) ) ;
#20737=EDGE_LOOP ( 'NONE', ( #41817, #45342, #28826, #12521 ) ) ;
#20743=CARTESIAN_POINT ( 'NONE',  ( 0.5997462898726536595, 11.43624519451647714, 47.75734421002918140 ) ) ;
#20744=CONICAL_SURFACE ( 'NONE', #23739, 43.92652462719577500, 1.486293639869522343 ) ;
#20752=CARTESIAN_POINT ( 'NONE',  ( 0.6253024248130496510, 41.52618082144132217, -26.21107654795206088 ) ) ;
#20753=ORIENTED_EDGE ( 'NONE', *, *, #2112, .T. ) ;
#20754=CARTESIAN_POINT ( 'NONE',  ( 0.1119899015040011075, 37.28332007608033649, -23.59905405513218213 ) ) ;
#20755=CARTESIAN_POINT ( 'NONE',  ( 4.553261556744875094, -29.69864478935419072, 32.36556910513705532 ) ) ;
#20757=CARTESIAN_POINT ( 'NONE',  ( 1.830465331921977246, 34.32868985341965384, -27.60284602764924600 ) ) ;
#20763=AXIS2_PLACEMENT_3D ( 'NONE', #39840, #5944, #53568 ) ;
#20765=( BOUNDED_SURFACE ( )  B_SPLINE_SURFACE ( 3, 1, ( 
 ( #22071, #13000 ),
 ( #22685, #7962 ),
 ( #42133, #18000 ),
 ( #55247, #36806 ) ),
 .UNSPECIFIED., .F., .F., .F. ) 
 B_SPLINE_SURFACE_WITH_KNOTS ( ( 4, 4 ),
 ( 2, 2 ),
 ( 0.000000000000000000, 1.000000000000000000 ),
 ( 0.000000000000000000, 1.000000000000000000 ),
 .UNSPECIFIED. ) 
 GEOMETRIC_REPRESENTATION_ITEM ( )  RATIONAL_B_SPLINE_SURFACE ( (
 ( 1.000000000000000000, 1.000000000000000000),
 ( 0.9953485035131437453, 0.8621029689291515030),
 ( 0.9953485035131437453, 0.8621029689291515030),
 ( 1.000000000000000000, 1.000000000000000000) ) ) 
 REPRESENTATION_ITEM ( '' )  SURFACE ( )  );
#20769=ORIENTED_EDGE ( 'NONE', *, *, #39159, .T. ) ;
#20776=LINE ( 'NONE', #34887, #51901 ) ;
#20777=CARTESIAN_POINT ( 'NONE',  ( 3.894904216938897878, 42.36413768828274584, 11.72195249966583752 ) ) ;
#20782=B_SPLINE_CURVE_WITH_KNOTS ( 'NONE', 3,
 ( #61937, #5537, #24676, #4932 ),
 .UNSPECIFIED., .F., .F.,
 ( 4, 4 ),
 ( 0.000000000000000000, 0.004444103432399267029 ),
 .UNSPECIFIED. ) ;
#20784=CARTESIAN_POINT ( 'NONE',  ( -6.077587904424778920, -6.656176160390447905, -18.06907137391903717 ) ) ;
#20790=VECTOR ( 'NONE', #52333, 1000.000000000000114 ) ;
#20792=CARTESIAN_POINT ( 'NONE',  ( 4.553261556744875094, 0.000000000000000000, 0.000000000000000000 ) ) ;
#20801=CARTESIAN_POINT ( 'NONE',  ( 0.6024113833632039894, 49.02002248349460700, -2.929038207082721001 ) ) ;
#20807=CARTESIAN_POINT ( 'NONE',  ( 1.479689385636123067, 43.88190798430054684, -3.995246791510194129 ) ) ;
#20810=EDGE_LOOP ( 'NONE', ( #43365, #42573, #41957, #30774 ) ) ;
#20814=CARTESIAN_POINT ( 'NONE',  ( 0.8753041380234524160, 48.36002538446245325, 8.511537621788880514 ) ) ;
#20817=CARTESIAN_POINT ( 'NONE',  ( 0.7413678028165008316, 28.94854816926588015, -33.26360850331690244 ) ) ;
#20818=CARTESIAN_POINT ( 'NONE',  ( 0.5549461598389363592, -40.54382484153107669, 17.36133527946660848 ) ) ;
#20819=CARTESIAN_POINT ( 'NONE',  ( -6.078075953587585900, -18.27338415406089212, 6.072775790793892625 ) ) ;
#20820=FACE_OUTER_BOUND ( 'NONE', #45362, .T. ) ;
#20821=VERTEX_POINT ( 'NONE', #25344 ) ;
#20823=CARTESIAN_POINT ( 'NONE',  ( 0.1365634738349413013, -2.050550585729402631, 44.07559258726546858 ) ) ;
#20829=CARTESIAN_POINT ( 'NONE',  ( 0.1368894036331288200, 34.00722248154819738, 28.11352245830850549 ) ) ;
#20834=CARTESIAN_POINT ( 'NONE',  ( 0.6028777368367060907, -7.923479829246307560, 48.46398969035256954 ) ) ;
#20835=CARTESIAN_POINT ( 'NONE',  ( -6.078726893082806448, 15.43407385306378998, -11.51448676958260187 ) ) ;
#20842=ORIENTED_EDGE ( 'NONE', *, *, #27426, .F. ) ;
#20847=CARTESIAN_POINT ( 'NONE',  ( 0.1158516988532803799, 9.866537107317912003, 43.00690182218099977 ) ) ;
#20855=CARTESIAN_POINT ( 'NONE',  ( 3.240649175237396040, -36.31843312004634328, 24.82410790144071910 ) ) ;
#20859=CYLINDRICAL_SURFACE ( 'NONE', #3606, 10.00000000000000000 ) ;
#20861=( BOUNDED_SURFACE ( )  B_SPLINE_SURFACE ( 3, 1, ( 
 ( #30558, #40312 ),
 ( #2043, #45610 ),
 ( #59368, #2664 ),
 ( #59682, #21173 ) ),
 .UNSPECIFIED., .F., .F., .F. ) 
 B_SPLINE_SURFACE_WITH_KNOTS ( ( 4, 4 ),
 ( 2, 2 ),
 ( 0.000000000000000000, 1.000000000000000000 ),
 ( 0.000000000000000000, 1.000000000000000000 ),
 .UNSPECIFIED. ) 
 GEOMETRIC_REPRESENTATION_ITEM ( )  RATIONAL_B_SPLINE_SURFACE ( (
 ( 1.000000000000000000, 1.000000000000000000),
 ( 0.9754377213608244057, 0.9999580625633939235),
 ( 0.9754377213608244057, 0.9999580625633939235),
 ( 1.000000000000000000, 1.000000000000000000) ) ) 
 REPRESENTATION_ITEM ( '' )  SURFACE ( )  );
#20866=CARTESIAN_POINT ( 'NONE',  ( -6.063463321072276813, -14.67303933398442695, -12.47086080360196014 ) ) ;
#20872=EDGE_CURVE ( 'NONE', #52483, #2209, #53216, .T. ) ;
#20873=LINE ( 'NONE', #6732, #35464 ) ;
#20874=CARTESIAN_POINT ( 'NONE',  ( 0.5997462898726536595, -25.90236585764290922, 41.72072714036901431 ) ) ;
#20879=CARTESIAN_POINT ( 'NONE',  ( 4.975610109902397937, -4.123593823332411645, 48.73854102369035957 ) ) ;
#20883=VERTEX_POINT ( 'NONE', #55069 ) ;
#20886=EDGE_CURVE ( 'NONE', #1157, #54460, #2392, .T. ) ;
#20893=EDGE_CURVE ( 'NONE', #60938, #34351, #17806, .T. ) ;
#20895=DIRECTION ( 'NONE',  ( 0.1011922191286468431, 0.6592733245820293631, -0.7450629626295874885 ) ) ;
#20903=CARTESIAN_POINT ( 'NONE',  ( -6.078726893082806448, -18.27610589745688330, -6.064486333867170842 ) ) ;
#20911=VERTEX_POINT ( 'NONE', #8379 ) ;
#20912=CARTESIAN_POINT ( 'NONE',  ( 0.1129192098497455998, 44.06201484046248140, -2.343210614524073421 ) ) ;
#20915=CARTESIAN_POINT ( 'NONE',  ( 0.6016117650947689910, -30.88963369689275851, -38.17566743773167559 ) ) ;
#20916=EDGE_CURVE ( 'NONE', #14826, #988, #51463, .T. ) ;
#20919=CARTESIAN_POINT ( 'NONE',  ( 0.7044674535452954967, -42.37103341363646791, -24.82938280085530636 ) ) ;
#20923=CARTESIAN_POINT ( 'NONE',  ( 0.5997462898726536595, 40.86908001809362645, -27.22627276398607421 ) ) ;
#20926=EDGE_CURVE ( 'NONE', #4535, #13345, #13117, .T. ) ;
#20929=CARTESIAN_POINT ( 'NONE',  ( 0.8753041380234524160, 48.01981714478404939, -10.25843502950054287 ) ) ;
#20934=CARTESIAN_POINT ( 'NONE',  ( -6.078457390727109555, -16.14063570603411080, 10.50116136637299391 ) ) ;
#20942=CARTESIAN_POINT ( 'NONE',  ( 0.6029442701453591180, -19.95751149647216138, -44.86917605691526489 ) ) ;
#20943=CARTESIAN_POINT ( 'NONE',  ( 0.1365634738349411625, -38.12893165387313843, -22.20466596365546508 ) ) ;
#20944=CARTESIAN_POINT ( 'NONE',  ( -6.057079549204054558, -4.276794256740572564, -18.77605554916285868 ) ) ;
#20945=CARTESIAN_POINT ( 'NONE',  ( -6.078726893082806448, 19.09835798914749816, 2.459016752095430025 ) ) ;
#20949=CARTESIAN_POINT ( 'NONE',  ( 0.1158516988532803521, 20.36546015188544700, -39.14320109079942966 ) ) ;
#20952=CARTESIAN_POINT ( 'NONE',  ( 0.1140933569871964842, 29.38290660318237002, 32.91800038933968153 ) ) ;
#20957=CARTESIAN_POINT ( 'NONE',  ( 0.1147471544378676211, -6.735538612062173414, 43.60716349498859046 ) ) ;
#20960=EDGE_CURVE ( 'NONE', #60741, #42039, #7443, .T. ) ;
#20961=( BOUNDED_SURFACE ( )  B_SPLINE_SURFACE ( 3, 1, ( 
 ( #8273, #46518 ),
 ( #41833, #3258 ),
 ( #2648, #7978 ),
 ( #45594, #46837 ) ),
 .UNSPECIFIED., .F., .F., .F. ) 
 B_SPLINE_SURFACE_WITH_KNOTS ( ( 4, 4 ),
 ( 2, 2 ),
 ( 0.000000000000000000, 1.000000000000000000 ),
 ( 0.000000000000000000, 1.000000000000000000 ),
 .UNSPECIFIED. ) 
 GEOMETRIC_REPRESENTATION_ITEM ( )  RATIONAL_B_SPLINE_SURFACE ( (
 ( 1.000000000000000000, 1.000000000000000000),
 ( 0.9953485035131437453, 0.8621029689291523912),
 ( 0.9953485035131437453, 0.8621029689291523912),
 ( 1.000000000000000000, 1.000000000000000000) ) ) 
 REPRESENTATION_ITEM ( '' )  SURFACE ( )  );
#20965=CARTESIAN_POINT ( 'NONE',  ( 0.1158403557922069033, -38.42759882943639838, -21.68547798384251379 ) ) ;
#20969=CARTESIAN_POINT ( 'NONE',  ( 4.694002226626921015, -15.42074131724369934, -42.90088004543483891 ) ) ;
#20976=CARTESIAN_POINT ( 'NONE',  ( 4.975610109902397937, -11.44439439467595143, 47.55497076097179843 ) ) ;
#20986=ORIENTED_EDGE ( 'NONE', *, *, #61650, .T. ) ;
#20989=ORIENTED_EDGE ( 'NONE', *, *, #18831, .F. ) ;
#20994=CARTESIAN_POINT ( 'NONE',  ( 0.3676999524040366896, -32.25712563511761743, -30.09033780274121739 ) ) ;
#20997=EDGE_CURVE ( 'NONE', #31990, #44428, #34484, .T. ) ;
#20999=CARTESIAN_POINT ( 'NONE',  ( 2.648799415243708655, -42.02883204265824446, 25.26053721557843446 ) ) ;
#21002=DIRECTION ( 'NONE',  ( 0.1011922191286468292, -0.9882612224441065241, -0.1144547552577001859 ) ) ;
#21006=CARTESIAN_POINT ( 'NONE',  ( 4.975610109902397937, 38.85236532789244279, 29.71435874397685595 ) ) ;
#21010=CARTESIAN_POINT ( 'NONE',  ( 4.694002226626920127, -34.48859517587359846, 29.81311077765690598 ) ) ;
#21023=ADVANCED_FACE ( 'NONE', ( #18732 ), #20414, .F. ) ;
#21027=CARTESIAN_POINT ( 'NONE',  ( 4.975610109902397937, -48.84566763821283786, -2.559328059280381318 ) ) ;
#21030=CARTESIAN_POINT ( 'NONE',  ( 0.1129192098497455998, -43.69739906996312584, -6.122834499277253428 ) ) ;
#21033=CARTESIAN_POINT ( 'NONE',  ( 0.6021447746440204973, -45.41982514268575954, 18.67031395280587347 ) ) ;
#21035=CARTESIAN_POINT ( 'NONE',  ( 0.3676999524040366896, -2.238562284875889041, -44.05609404179596567 ) ) ;
#21038=CARTESIAN_POINT ( 'NONE',  ( 2.533389852662419894, -42.14803637618723542, 12.68832382015906113 ) ) ;
#21044=ORIENTED_EDGE ( 'NONE', *, *, #27430, .T. ) ;
#21057=ORIENTED_EDGE ( 'NONE', *, *, #13368, .T. ) ;
#21062=CARTESIAN_POINT ( 'NONE',  ( 4.553261556744873317, 31.39705178283683296, -30.72075365562339755 ) ) ;
#21066=ORIENTED_EDGE ( 'NONE', *, *, #44418, .T. ) ;
#21067=EDGE_LOOP ( 'NONE', ( #58864, #20434, #51341, #42937 ) ) ;
#21070=CARTESIAN_POINT ( 'NONE',  ( 0.6000166863083106206, 16.46965316277509217, -46.26633772416342083 ) ) ;
#21073=CARTESIAN_POINT ( 'NONE',  ( 3.559346040607745287, -43.00729280057031190, -9.154400445031974698 ) ) ;
#21074=CARTESIAN_POINT ( 'NONE',  ( 0.7948884756798507700, 48.02008973275257375, 10.23570352533436889 ) ) ;
#21077=EDGE_CURVE ( 'NONE', #13041, #14464, #18493, .T. ) ;
#21085=B_SPLINE_CURVE_WITH_KNOTS ( 'NONE', 3,
 ( #30111, #54205, #53903, #1587, #6274, #25410, #58920, #11325, #16648, #6580, #25727, #44865, #21033, #53292, #49844, #10404 ),
 .UNSPECIFIED., .F., .F.,
 ( 4, 3, 3, 3, 3, 4 ),
 ( 2.194378057379452319E-17, 0.0002612764279487760359, 0.0003919131003184782693, 0.0005225497727000641716, 0.0007837925190632482816, 0.001045051706266712614 ),
 .UNSPECIFIED. ) ;
#21087=B_SPLINE_CURVE_WITH_KNOTS ( 'NONE', 3,
 ( #29767, #48879, #1554, #20381, #49186, #10368 ),
 .UNSPECIFIED., .F., .F.,
 ( 4, 2, 4 ),
 ( 1.823721537572523311E-17, 0.0002293755540694312101, 0.0004587511081388441513 ),
 .UNSPECIFIED. ) ;
#21088=CARTESIAN_POINT ( 'NONE',  ( 0.7413678028165007206, -41.21466309768522507, -15.67921036004513091 ) ) ;
#21091=CARTESIAN_POINT ( 'NONE',  ( -4.915099999999998914, 0.000000000000000000, 0.000000000000000000 ) ) ;
#21092=EDGE_CURVE ( 'NONE', #7236, #40034, #28738, .T. ) ;
#21093=CARTESIAN_POINT ( 'NONE',  ( -6.078457390727109555, 19.09737280526033487, 2.466751502363165649 ) ) ;
#21094=CARTESIAN_POINT ( 'NONE',  ( 0.6029442701453591180, 41.20385451604330029, 26.71680366696238096 ) ) ;
#21102=CARTESIAN_POINT ( 'NONE',  ( -6.078457390727109555, -4.280596808181184265, 18.77421108870614930 ) ) ;
#21106=ORIENTED_EDGE ( 'NONE', *, *, #21884, .T. ) ;
#21111=ORIENTED_EDGE ( 'NONE', *, *, #5545, .F. ) ;
#21113=CARTESIAN_POINT ( 'NONE',  ( 0.8744876279028306332, 36.80052600666260787, -32.49725120702428427 ) ) ;
#21116=B_SPLINE_CURVE_WITH_KNOTS ( 'NONE', 3,
 ( #39240, #14496, #11028, #10717 ),
 .UNSPECIFIED., .F., .F.,
 ( 4, 4 ),
 ( 0.000000000000000000, 0.004444103432399268763 ),
 .UNSPECIFIED. ) ;
#21123=ORIENTED_EDGE ( 'NONE', *, *, #21633, .T. ) ;
#21130=ORIENTED_EDGE ( 'NONE', *, *, #12857, .T. ) ;
#21131=ORIENTED_EDGE ( 'NONE', *, *, #17896, .T. ) ;
#21133=CARTESIAN_POINT ( 'NONE',  ( 0.6252788684277204023, -19.24757281514202489, 45.17715431387276226 ) ) ;
#21136=CARTESIAN_POINT ( 'NONE',  ( 0.6021448801613057400, -8.095331285689143286, 48.43559383348046055 ) ) ;
#21141=CARTESIAN_POINT ( 'NONE',  ( 2.881901169982995725, 1.330622528702777754E-16, 49.00591519830862808 ) ) ;
#21143=VECTOR ( 'NONE', #9391, 1000.000000000000000 ) ;
#21144=VECTOR ( 'NONE', #53058, 1000.000000000000000 ) ;
#21149=CARTESIAN_POINT ( 'NONE',  ( -6.077587904424778920, 18.62786028128793347, 4.878405757493543327 ) ) ;
#21155=EDGE_CURVE ( 'NONE', #40746, #60883, #15712, .T. ) ;
#21158=CARTESIAN_POINT ( 'NONE',  ( 0.8744876279028306332, -14.81965677137948489, -46.80521149998148900 ) ) ;
#21159=CARTESIAN_POINT ( 'NONE',  ( 0.5549461598389366923, 21.17425125324409407, 38.68938845899861434 ) ) ;
#21163=CARTESIAN_POINT ( 'NONE',  ( 4.335381028904216727, 48.70445384730881244, -5.256712194871631105 ) ) ;
#21173=CARTESIAN_POINT ( 'NONE',  ( 0.6000166863083106206, -47.36892948402866210, -12.96179004788979228 ) ) ;
#21183=ORIENTED_EDGE ( 'NONE', *, *, #363, .F. ) ;
#21193=ORIENTED_EDGE ( 'NONE', *, *, #45871, .F. ) ;
#21194=EDGE_CURVE ( 'NONE', #60883, #49846, #38781, .T. ) ;
#21197=CARTESIAN_POINT ( 'NONE',  ( 0.5997462898726536595, 40.86908001809322855, 27.22627276398666041 ) ) ;
#21203=ORIENTED_EDGE ( 'NONE', *, *, #32130, .T. ) ;
#21204=CARTESIAN_POINT ( 'NONE',  ( 0.6039202388192953519, -14.13938383033847224, -47.02809306943408529 ) ) ;
#21213=CARTESIAN_POINT ( 'NONE',  ( 0.8753041380234471980, -42.34096624980154644, -24.86726573039640087 ) ) ;
#21235=MECHANICAL_DESIGN_GEOMETRIC_PRESENTATION_REPRESENTATION('',(#60208),#47226);
#21237=EDGE_LOOP ( 'NONE', ( #1607, #15519, #951, #22364 ) ) ;
#21240=CARTESIAN_POINT ( 'NONE',  ( 2.706805983486680223, 30.79179577033409743, 31.44266888414198036 ) ) ;
#21241=CARTESIAN_POINT ( 'NONE',  ( 0.6026777506516367566, 33.14375390931751042, 36.23586576081520860 ) ) ;
#21244=CARTESIAN_POINT ( 'NONE',  ( 4.975610109902397937, 47.16372689271652519, 12.96272628450595832 ) ) ;
#21247=CARTESIAN_POINT ( 'NONE',  ( 0.08486401232817714080, 0.000000000000000000, 0.000000000000000000 ) ) ;
#21250=CARTESIAN_POINT ( 'NONE',  ( 0.6008123274975391004, 44.05373908824402918, 21.69844749062424683 ) ) ;
#21251=EDGE_CURVE ( 'NONE', #45554, #55549, #59524, .T. ) ;
#21256=B_SPLINE_CURVE_WITH_KNOTS ( 'NONE', 3,
 ( #57185, #56587, #13704, #32812, #51890, #8984, #28094, #24943, #53118, #6102, #34647, #53715, #811, #58118, #34969, #19949, #24630, #43769, #15853 ),
 .UNSPECIFIED., .F., .F.,
 ( 4, 3, 3, 3, 3, 3, 4 ),
 ( 3.469685171791681197E-18, 0.0002612768053151711127, 0.0003919133833142872392, 0.0005225499612322589103, 0.0006531865391693350911, 0.0008112755173415149785, 0.0009693688056799732236 ),
 .UNSPECIFIED. ) ;
#21266=ORIENTED_EDGE ( 'NONE', *, *, #40779, .F. ) ;
#21269=CARTESIAN_POINT ( 'NONE',  ( 0.1156495703730067853, -38.51293032282120521, -21.53362837936490237 ) ) ;
#21270=CARTESIAN_POINT ( 'NONE',  ( 0.6008123274975391004, -45.35345026050291750, -18.83133294874649977 ) ) ;
#21275=CARTESIAN_POINT ( 'NONE',  ( 4.975610109902397937, -16.35148546628888866, -46.09857188876371481 ) ) ;
#21277=VECTOR ( 'NONE', #22271, 1000.000000000000000 ) ;
#21280=CARTESIAN_POINT ( 'NONE',  ( 0.6026777506516367566, -13.80536265409133101, 47.12704481108740850 ) ) ;
#21284=EDGE_CURVE ( 'NONE', #60643, #55418, #56067, .T. ) ;
#21289=VERTEX_POINT ( 'NONE', #60612 ) ;
#21293=CARTESIAN_POINT ( 'NONE',  ( 0.1145239942831223490, 20.11902381989014899, 39.27047696730160453 ) ) ;
#21294=ORIENTED_EDGE ( 'NONE', *, *, #1194, .T. ) ;
#21295=ORIENTED_EDGE ( 'NONE', *, *, #38727, .F. ) ;
#21300=ORIENTED_EDGE ( 'NONE', *, *, #43591, .F. ) ;
#21314=CARTESIAN_POINT ( 'NONE',  ( -6.077587904424778920, 13.82827771187084664, -13.40055061993000685 ) ) ;
#21317=CARTESIAN_POINT ( 'NONE',  ( -6.077587904424778920, -16.14165210942803341, -10.49967087922893150 ) ) ;
#21320=CARTESIAN_POINT ( 'NONE',  ( 4.975610109902397937, 45.55079628452109830, 17.82061629079735354 ) ) ;
#21322=CARTESIAN_POINT ( 'NONE',  ( 1.830465331921976802, 26.20437692621130665, -35.40772070873008914 ) ) ;
#21324=DIRECTION ( 'NONE',  ( 0.000000000000000000, 0.000000000000000000, 1.000000000000000000 ) ) ;
#21326=EDGE_CURVE ( 'NONE', #32638, #759, #36690, .T. ) ;
#21334=CARTESIAN_POINT ( 'NONE',  ( 0.1152339509894530906, -35.22763790827196573, 26.56983661709124434 ) ) ;
#21343=CARTESIAN_POINT ( 'NONE',  ( 0.8744876279028263033, -31.30103973185235233, 37.82320666052117275 ) ) ;
#21344=B_SPLINE_CURVE_WITH_KNOTS ( 'NONE', 3,
 ( #26709, #19764, #39501, #38887 ),
 .UNSPECIFIED., .F., .F.,
 ( 4, 4 ),
 ( 0.000000000000000000, 0.005013413432710155451 ),
 .UNSPECIFIED. ) ;
#21346=CARTESIAN_POINT ( 'NONE',  ( 4.060580049360325461, -41.86530176281380733, 13.37027309622913407 ) ) ;
#21348=EDGE_CURVE ( 'NONE', #50534, #27996, #7060, .T. ) ;
#21352=CARTESIAN_POINT ( 'NONE',  ( 4.553261556744875094, 0.000000000000000000, 0.000000000000000000 ) ) ;
#21354=CARTESIAN_POINT ( 'NONE',  ( 0.1119899015040011631, 3.677941833846906317, 43.97083183269729290 ) ) ;
#21359=CARTESIAN_POINT ( 'NONE',  ( 0.6021448801613057400, 10.67258200247132294, 47.93367430134552620 ) ) ;
#21363=CARTESIAN_POINT ( 'NONE',  ( 0.8744876279028263033, -39.87136468799916145, 28.64654129726773846 ) ) ;
#21367=EDGE_LOOP ( 'NONE', ( #58459, #20705, #18123, #28768 ) ) ;
#21371=EDGE_CURVE ( 'NONE', #47629, #10066, #2057, .T. ) ;
#21381=CARTESIAN_POINT ( 'NONE',  ( 0.6039202388192953519, 16.79650288729678920, -46.14586875990116965 ) ) ;
#21382=CARTESIAN_POINT ( 'NONE',  ( 4.694002226626921015, 6.935496447963269695, 45.05755941533480069 ) ) ;
#21391=CARTESIAN_POINT ( 'NONE',  ( 0.5549461598389366923, 42.12604207101915677, 13.06193993622417970 ) ) ;
#21393=CARTESIAN_POINT ( 'NONE',  ( 0.7242003506640004584, -49.09522258624797075, 0.8190197389533786509 ) ) ;
#21396=CARTESIAN_POINT ( 'NONE',  ( 1.479689385636123067, -13.65972076154995207, -41.89267088625614122 ) ) ;
#21400=CARTESIAN_POINT ( 'NONE',  ( 0.8753041380234471980, 33.66554281472474486, -35.74590263041226734 ) ) ;
#21406=CARTESIAN_POINT ( 'NONE',  ( 2.299746137290198611, 44.72136981280802814, 20.10672573424628240 ) ) ;
#21411=CARTESIAN_POINT ( 'NONE',  ( 1.830465331921976357, 28.68895279831538403, 33.42633756806781520 ) ) ;
#21415=VERTEX_POINT ( 'NONE', #43095 ) ;
#21420=EDGE_CURVE ( 'NONE', #25523, #4961, #52503, .T. ) ;
#21422=CARTESIAN_POINT ( 'NONE',  ( 4.060580049360325461, -29.91699279630384467, 32.19380742293636644 ) ) ;
#21428=EDGE_CURVE ( 'NONE', #46672, #41724, #30497, .T. ) ;
#21429=ADVANCED_FACE ( 'NONE', ( #47784 ), #40933, .F. ) ;
#21430=CARTESIAN_POINT ( 'NONE',  ( 0.8744876279028263033, -20.68330519280349122, 44.52584571550372061 ) ) ;
#21434=CARTESIAN_POINT ( 'NONE',  ( 0.1119899015040013990, -17.34614229840122590, -40.57182095440284542 ) ) ;
#21438=ORIENTED_EDGE ( 'NONE', *, *, #120, .T. ) ;
#21439=ORIENTED_EDGE ( 'NONE', *, *, #33831, .F. ) ;
#21446=CARTESIAN_POINT ( 'NONE',  ( 3.221118495291109163, -43.82609091211070051, -3.746354898452465498 ) ) ;
#21466=EDGE_CURVE ( 'NONE', #51708, #4904, #6669, .T. ) ;
#21470=CARTESIAN_POINT ( 'NONE',  ( 0.6029442701453592290, 41.10881650023822687, -26.86280758051954365 ) ) ;
#21473=CARTESIAN_POINT ( 'NONE',  ( -6.063463321072278589, 15.42324870294163830, 11.53012800998666698 ) ) ;
#21479=CARTESIAN_POINT ( 'NONE',  ( 3.678748215320120085, 24.27640525275985794, 42.53550237511316112 ) ) ;
#21481=CARTESIAN_POINT ( 'NONE',  ( 3.894904216938897878, 35.57819931341702357, -25.81309873089577067 ) ) ;
#21498=ADVANCED_FACE ( 'NONE', ( #10801 ), #6463, .F. ) ;
#21507=CARTESIAN_POINT ( 'NONE',  ( 0.5980271706414711508, -26.05568637495964524, 41.63112357805641039 ) ) ;
#21511=CARTESIAN_POINT ( 'NONE',  ( 0.5980271706414734822, 28.66946741852817837, 39.87619441194977554 ) ) ;
#21519=CARTESIAN_POINT ( 'NONE',  ( 0.5987334363312691865, 11.51672169166321424, -47.73811923346844566 ) ) ;
#21533=B_SPLINE_CURVE_WITH_KNOTS ( 'NONE', 3,
 ( #27775, #3632, #37196, #14622 ),
 .UNSPECIFIED., .F., .F.,
 ( 4, 4 ),
 ( 0.000000000000000000, 0.004444103432399267029 ),
 .UNSPECIFIED. ) ;
#21534=CARTESIAN_POINT ( 'NONE',  ( 0.1145239942831223490, -43.80251030910497434, 5.318418122470812470 ) ) ;
#21536=CARTESIAN_POINT ( 'NONE',  ( 0.1157506346131639274, -27.58342920138327869, -34.43973131856737524 ) ) ;
#21539=B_SPLINE_CURVE_WITH_KNOTS ( 'NONE', 3,
 ( #48000, #5048, #31045, #50157 ),
 .UNSPECIFIED., .F., .F.,
 ( 4, 4 ),
 ( 0.000000000000000000, 0.005013413432710146778 ),
 .UNSPECIFIED. ) ;
#21540=ORIENTED_EDGE ( 'NONE', *, *, #14513, .T. ) ;
#21545=CARTESIAN_POINT ( 'NONE',  ( 4.975610109902397937, -37.61482235126130291, -31.26618855282533360 ) ) ;
#21549=CARTESIAN_POINT ( 'NONE',  ( -2.601141883200662974, 14.01836437022357451, -5.126488842573914795 ) ) ;
#21550=CONICAL_SURFACE ( 'NONE', #56545, 44.12552607296456131, 0.04450589592585061510 ) ;
#21559=CARTESIAN_POINT ( 'NONE',  ( 0.6026112563231247332, 44.16843500053740712, 21.46369829520319783 ) ) ;
#21561=CARTESIAN_POINT ( 'NONE',  ( 3.240649175237396040, -10.75352374005706402, -42.65708199783103538 ) ) ;
#21562=CARTESIAN_POINT ( 'NONE',  ( 0.6039202388192953519, -47.45712035475610691, 12.62479467093167074 ) ) ;
#21564=CARTESIAN_POINT ( 'NONE',  ( 0.1154773475650540393, -12.72687235669186911, -42.24890945412192877 ) ) ;
#21567=CARTESIAN_POINT ( 'NONE',  ( 0.1119899015040010798, 30.07795574961987484, -32.28432880077288303 ) ) ;
#21571=CARTESIAN_POINT ( 'NONE',  ( 2.533389852662419894, 16.67687449783081277, 40.73490381377152403 ) ) ;
#21572=B_SPLINE_CURVE_WITH_KNOTS ( 'NONE', 3,
 ( #11033, #57674, #33920, #29194 ),
 .UNSPECIFIED., .F., .F.,
 ( 4, 4 ),
 ( 2.173710443588397387E-17, 0.004559932413162187670 ),
 .UNSPECIFIED. ) ;
#21573=CARTESIAN_POINT ( 'NONE',  ( 0.5997462898726536595, 40.86908001809322855, 27.22627276398666041 ) ) ;
#21587=CARTESIAN_POINT ( 'NONE',  ( 0.6027444965799114707, -14.09757999337120005, 47.04037366154675226 ) ) ;
#21588=ORIENTED_EDGE ( 'NONE', *, *, #37118, .F. ) ;
#21589=CARTESIAN_POINT ( 'NONE',  ( -6.063463321072276813, -16.14731216720862506, -10.49212858547712557 ) ) ;
#21590=EDGE_LOOP ( 'NONE', ( #49294, #7934, #19924, #16151 ) ) ;
#21593=CIRCLE ( 'NONE', #41602, 43.92652462719577500 ) ;
#21595=CARTESIAN_POINT ( 'NONE',  ( 2.648799415243708655, -26.59464913125692220, -41.19759824158361283 ) ) ;
#21596=VERTEX_POINT ( 'NONE', #57762 ) ;
#21602=CARTESIAN_POINT ( 'NONE',  ( 0.3676999524040323597, 5.056646555325726489, -43.82215089355327109 ) ) ;
#21608=LINE ( 'NONE', #12230, #49404 ) ;
#21627=ORIENTED_EDGE ( 'NONE', *, *, #47893, .T. ) ;
#21630=CARTESIAN_POINT ( 'NONE',  ( 0.2279481005628795909, 39.41468212403272986, 19.82388256962714834 ) ) ;
#21631=DIRECTION ( 'NONE',  ( 0.000000000000000000, 0.000000000000000000, 1.000000000000000000 ) ) ;
#21633=EDGE_CURVE ( 'NONE', #5027, #6245, #1363, .T. ) ;
#21640=CARTESIAN_POINT ( 'NONE',  ( 0.2940133293163010308, 9.030615628137779183, 43.18203944876707823 ) ) ;
#21641=AXIS2_PLACEMENT_3D ( 'NONE', #51171, #31459, #32401 ) ;
#21650=CARTESIAN_POINT ( 'NONE',  ( 0.6000166863083106206, 27.66667954482629099, -40.57558779207448652 ) ) ;
#21655=CARTESIAN_POINT ( 'NONE',  ( 0.3676999524040323597, -18.60775935196367925, 39.99627326667132365 ) ) ;
#21659=CARTESIAN_POINT ( 'NONE',  ( 0.3676999524040323597, 16.00695768809450215, -41.10629986868669761 ) ) ;
#21660=EDGE_CURVE ( 'NONE', #49921, #31310, #58944, .T. ) ;
#21664=ORIENTED_EDGE ( 'NONE', *, *, #33254, .T. ) ;
#21665=CARTESIAN_POINT ( 'NONE',  ( 0.5980271706414734822, 11.60998973145947311, 47.72061798926192466 ) ) ;
#21667=VERTEX_POINT ( 'NONE', #26421 ) ;
#21669=ORIENTED_EDGE ( 'NONE', *, *, #28861, .F. ) ;
#21670=CARTESIAN_POINT ( 'NONE',  ( 0.3676999524040323597, -13.34038000160386339, 42.04741186726771929 ) ) ;
#21671=EDGE_CURVE ( 'NONE', #8492, #29973, #41793, .T. ) ;
#21673=DIRECTION ( 'NONE',  ( 0.09722883295013595717, 0.2140925343086520494, 0.9719624173786006738 ) ) ;
#21675=ORIENTED_EDGE ( 'NONE', *, *, #50786, .F. ) ;
#21678=CARTESIAN_POINT ( 'NONE',  ( -6.072942160501519027, -14.67202460315916923, 12.47140153845237620 ) ) ;
#21688=CARTESIAN_POINT ( 'NONE',  ( 1.479689385636123067, 14.10936131825397233, -41.74337993572934380 ) ) ;
#21694=ADVANCED_FACE ( 'NONE', ( #11730 ), #51679, .F. ) ;
#21699=CARTESIAN_POINT ( 'NONE',  ( 1.112077966505211402, 42.15317579919562974, 12.88953432714551184 ) ) ;
#21704=CARTESIAN_POINT ( 'NONE',  ( 3.221118495291108275, -14.31435738594796803, -41.59159280779119428 ) ) ;
#21714=CARTESIAN_POINT ( 'NONE',  ( 3.678748215320120973, 47.03014671954850456, 13.66667896151895256 ) ) ;
#21716=FACE_OUTER_BOUND ( 'NONE', #39740, .T. ) ;
#21721=CARTESIAN_POINT ( 'NONE',  ( 4.553261556744875094, 0.000000000000000000, 0.000000000000000000 ) ) ;
#21722=VERTEX_POINT ( 'NONE', #59310 ) ;
#21723=VERTEX_POINT ( 'NONE', #6984 ) ;
#21726=CARTESIAN_POINT ( 'NONE',  ( 0.6027444965799114707, 17.08250209178403267, -46.04048911742398786 ) ) ;
#21732=CARTESIAN_POINT ( 'NONE',  ( 0.6000166863083106206, -30.20952222014459565, 38.71961065066439289 ) ) ;
#21734=EDGE_CURVE ( 'NONE', #45974, #24292, #48526, .T. ) ;
#21735=UNCERTAINTY_MEASURE_WITH_UNIT (LENGTH_MEASURE( 1.000000000000000082E-05 ), #11246, 'distance_accuracy_value', 'NONE');
#21737=VERTEX_POINT ( 'NONE', #27352 ) ;
#21754=CARTESIAN_POINT ( 'NONE',  ( 0.6024113833632038784, -48.73164146766168159, 6.063743807924546481 ) ) ;
#21755=DIRECTION ( 'NONE',  ( 0.000000000000000000, 0.000000000000000000, 1.000000000000000000 ) ) ;
#21758=ORIENTED_EDGE ( 'NONE', *, *, #38146, .F. ) ;
#21759=CARTESIAN_POINT ( 'NONE',  ( -6.057079549204054558, 19.09779050476951667, -2.470957088998842810 ) ) ;
#21761=CARTESIAN_POINT ( 'NONE',  ( 0.1139756605157200703, -31.97198000184581801, -30.40966481986596293 ) ) ;
#21767=CARTESIAN_POINT ( 'NONE',  ( 0.7948878604505665857, -48.57723113705768014, 7.138015295254673376 ) ) ;
#21785=CARTESIAN_POINT ( 'NONE',  ( 0.9268187852002115479, -32.35242309955501838, -29.95121120248737512 ) ) ;
#21786=EDGE_CURVE ( 'NONE', #10837, #9740, #28336, .T. ) ;
#21788=EDGE_CURVE ( 'NONE', #57221, #20594, #2921, .T. ) ;
#21789=CARTESIAN_POINT ( 'NONE',  ( 0.2940133293163010864, 36.52812821143385946, 24.73734826021361854 ) ) ;
#21790=EDGE_LOOP ( 'NONE', ( #35803, #57882, #13990, #50114 ) ) ;
#21804=DIRECTION ( 'NONE',  ( -0.1011922191286467460, -0.7491372366378198366, -0.6546400044837399346 ) ) ;
#21808=CARTESIAN_POINT ( 'NONE',  ( 4.975610109902397937, 0.000000000000000000, 0.000000000000000000 ) ) ;
#21814=ORIENTED_EDGE ( 'NONE', *, *, #23611, .T. ) ;
#21816=VECTOR ( 'NONE', #9958, 1000.000000000000114 ) ;
#21821=CARTESIAN_POINT ( 'NONE',  ( 0.1129192098497447394, -42.80154921430116843, -10.72283417016740259 ) ) ;
#21825=CARTESIAN_POINT ( 'NONE',  ( 0.1119898979215349644, 29.24697001900925741, -33.03900805046971811 ) ) ;
#21829=VECTOR ( 'NONE', #61505, 1000.000000000000114 ) ;
#21836=ORIENTED_EDGE ( 'NONE', *, *, #19749, .T. ) ;
#21838=CARTESIAN_POINT ( 'NONE',  ( 0.1139756605157204450, 39.58051477185625089, -19.50225807669184164 ) ) ;
#21839=ORIENTED_EDGE ( 'NONE', *, *, #45305, .F. ) ;
#21853=VERTEX_POINT ( 'NONE', #58293 ) ;
#21858=DIRECTION ( 'NONE',  ( 0.000000000000000000, 0.000000000000000000, 1.000000000000000000 ) ) ;
#21860=CARTESIAN_POINT ( 'NONE',  ( 0.1119899015040012741, 33.23178756756905727, 29.02773851433260788 ) ) ;
#21867=CIRCLE ( 'NONE', #10821, 43.92652462719577500 ) ;
#21869=CARTESIAN_POINT ( 'NONE',  ( -6.078726893082806448, 16.77644806189609739, 9.452239506869414498 ) ) ;
#21872=CARTESIAN_POINT ( 'NONE',  ( -2.739355103387248747, 7.136887160706232969, 13.11153723277188732 ) ) ;
#21884=EDGE_CURVE ( 'NONE', #17235, #35184, #47765, .T. ) ;
#21888=EDGE_CURVE ( 'NONE', #3087, #46201, #21572, .T. ) ;
#21896=CARTESIAN_POINT ( 'NONE',  ( 0.1155031312995260795, -38.36323999597067314, -21.79916167065524846 ) ) ;
#21902=ORIENTED_EDGE ( 'NONE', *, *, #30895, .T. ) ;
#21916=ORIENTED_EDGE ( 'NONE', *, *, #43960, .T. ) ;
#21917=CARTESIAN_POINT ( 'NONE',  ( 0.1145239942831223490, -1.740630560447053554, 44.08985921906205618 ) ) ;
#21918=B_SPLINE_CURVE_WITH_KNOTS ( 'NONE', 3,
 ( #34829, #11020, #33140, #50749 ),
 .UNSPECIFIED., .F., .F.,
 ( 4, 4 ),
 ( 2.175771182130668512E-17, 0.004559932413162187670 ),
 .UNSPECIFIED. ) ;
#21923=CARTESIAN_POINT ( 'NONE',  ( -6.078726893082806448, -16.13637198556907748, 10.50768958487361537 ) ) ;
#21925=CARTESIAN_POINT ( 'NONE',  ( 4.975610109902397937, 0.000000000000000000, 0.000000000000000000 ) ) ;
#21928=CARTESIAN_POINT ( 'NONE',  ( 3.559346040607745287, 6.262100278120851016, 43.52259621907622034 ) ) ;
#21930=CARTESIAN_POINT ( 'NONE',  ( -6.063463321072278589, 16.78636876910494991, -9.436009539370331822 ) ) ;
#21931=ORIENTED_EDGE ( 'NONE', *, *, #47323, .T. ) ;
#21934=DIRECTION ( 'NONE',  ( 0.000000000000000000, 0.000000000000000000, -1.000000000000000000 ) ) ;
#21936=DIRECTION ( 'NONE',  ( -0.1011922191286467460, 0.5046905544709733293, 0.8573491581704628661 ) ) ;
#21937=VERTEX_POINT ( 'NONE', #1594 ) ;
#21953=FACE_OUTER_BOUND ( 'NONE', #49509, .T. ) ;
#21961=ADVANCED_FACE ( 'NONE', ( #55153 ), #23342, .F. ) ;
#21972=CARTESIAN_POINT ( 'NONE',  ( 4.226256110419178924, -41.83098940882571526, 13.45345959468784081 ) ) ;
#21977=VERTEX_POINT ( 'NONE', #60163 ) ;
#21981=CARTESIAN_POINT ( 'NONE',  ( 2.185380717157383135, -11.14258708398306297, 42.59885627740553815 ) ) ;
#21982=EDGE_LOOP ( 'NONE', ( #681, #32604, #21300, #11935 ) ) ;
#21986=CARTESIAN_POINT ( 'NONE',  ( 5.901764892641307547, -22.61189840244690785, -43.43608543684728573 ) ) ;
#21987=ORIENTED_EDGE ( 'NONE', *, *, #48039, .F. ) ;
#21988=CARTESIAN_POINT ( 'NONE',  ( 0.2279481005628811452, -13.27919661951364994, 42.07334576918279367 ) ) ;
#21990=CARTESIAN_POINT ( 'NONE',  ( -6.078726893082806448, 16.77980020642702641, 9.446287434813308792 ) ) ;
#21994=CARTESIAN_POINT ( 'NONE',  ( 0.5980271706414734822, 37.84660806146489875, 31.29989618327069323 ) ) ;
#21995=VERTEX_POINT ( 'NONE', #39871 ) ;
#21999=CARTESIAN_POINT ( 'NONE',  ( 4.390527457369402420, -36.99449152968317378, 23.69795208638966599 ) ) ;
#22000=CARTESIAN_POINT ( 'NONE',  ( 0.7044674535452954967, -7.005514063658970336, -48.60787483026575018 ) ) ;
#22007=VERTEX_POINT ( 'NONE', #45185 ) ;
#22010=CARTESIAN_POINT ( 'NONE',  ( 0.3676999524040366896, 9.009680404096547690, -43.18305503711933113 ) ) ;
#22017=CARTESIAN_POINT ( 'NONE',  ( 2.359973842542475886, 42.23244574406162144, 12.43207227727508624 ) ) ;
#22019=CARTESIAN_POINT ( 'NONE',  ( 4.553261556744875094, 0.000000000000000000, 0.000000000000000000 ) ) ;
#22020=CARTESIAN_POINT ( 'NONE',  ( 0.2940135542859004802, -18.59037419722897866, -40.00798090254521355 ) ) ;
#22027=CARTESIAN_POINT ( 'NONE',  ( 0.8753041380234530822, -48.80600061351578489, -5.395612290229643726 ) ) ;
#22029=CARTESIAN_POINT ( 'NONE',  ( -6.078075953587585900, 7.789670135765894621, -17.61011679186406909 ) ) ;
#22033=DIRECTION ( 'NONE',  ( 0.000000000000000000, 0.000000000000000000, 1.000000000000000000 ) ) ;
#22035=CARTESIAN_POINT ( 'NONE',  ( 0.7242003506639987931, -38.85571581871069213, 30.02074320102056149 ) ) ;
#22038=CARTESIAN_POINT ( 'NONE',  ( 0.6016118706126977189, -47.58863909114165125, 12.11909585063984629 ) ) ;
#22039=DIRECTION ( 'NONE',  ( -1.000000000000000000, -0.000000000000000000, -0.000000000000000000 ) ) ;
#22044=LINE ( 'NONE', #42098, #19736 ) ;
#22045=ORIENTED_EDGE ( 'NONE', *, *, #49421, .T. ) ;
#22047=CARTESIAN_POINT ( 'NONE',  ( -6.078726893082806448, 12.00325722817150620, -15.05708661006732108 ) ) ;
#22064=ORIENTED_EDGE ( 'NONE', *, *, #48521, .F. ) ;
#22069=CARTESIAN_POINT ( 'NONE',  ( -6.078075953587585900, 9.986729131371225421, 16.46391252114020887 ) ) ;
#22071=CARTESIAN_POINT ( 'NONE',  ( -6.077587904424778920, 12.00112336472165353, 15.05885318935882644 ) ) ;
#22074=LINE ( 'NONE', #2947, #48907 ) ;
#22076=VERTEX_POINT ( 'NONE', #30734 ) ;
#22119=VERTEX_POINT ( 'NONE', #51072 ) ;
#22121=CARTESIAN_POINT ( 'NONE',  ( 2.879087469061463178, 37.79288285606617848, 22.53441106865315646 ) ) ;
#22125=ADVANCED_FACE ( 'NONE', ( #51691 ), #56069, .F. ) ;
#22128=CARTESIAN_POINT ( 'NONE',  ( 0.1140933569871965536, -42.58338260172239131, -11.55878351208433230 ) ) ;
#22130=CARTESIAN_POINT ( 'NONE',  ( 0.2285344041767134737, 33.09684643513740099, -29.17361695683942102 ) ) ;
#22136=CARTESIAN_POINT ( 'NONE',  ( 0.6252788684277231779, 22.10253682748975734, -43.85113678073950894 ) ) ;
#22137=CARTESIAN_POINT ( 'NONE',  ( 0.3676999524040323597, -32.25712563511804376, 30.09033780274075198 ) ) ;
#22141=CARTESIAN_POINT ( 'NONE',  ( 2.185380717157383135, 39.02616721911296338, -20.39063695064556114 ) ) ;
#22146=CARTESIAN_POINT ( 'NONE',  ( 0.1155031312995260795, 39.82731631370493375, -18.99280147266069108 ) ) ;
#22153=VERTEX_POINT ( 'NONE', #38550 ) ;
#22155=CARTESIAN_POINT ( 'NONE',  ( -2.601141883200662974, 3.756714151559825687, 14.44584806277771705 ) ) ;
#22159=ORIENTED_EDGE ( 'NONE', *, *, #40341, .T. ) ;
#22160=CARTESIAN_POINT ( 'NONE',  ( 0.1149546198390366814, 43.25733823727443195, 8.703404715929053737 ) ) ;
#22162=( BOUNDED_SURFACE ( )  B_SPLINE_SURFACE ( 3, 1, ( 
 ( #9322, #18744 ),
 ( #24356, #19358 ),
 ( #33152, #19985 ),
 ( #19063, #33777 ) ),
 .UNSPECIFIED., .F., .F., .F. ) 
 B_SPLINE_SURFACE_WITH_KNOTS ( ( 4, 4 ),
 ( 2, 2 ),
 ( 0.000000000000000000, 1.000000000000000000 ),
 ( 0.000000000000000000, 1.000000000000000000 ),
 .UNSPECIFIED. ) 
 GEOMETRIC_REPRESENTATION_ITEM ( )  RATIONAL_B_SPLINE_SURFACE ( (
 ( 1.000000000000000000, 1.000000000000000000),
 ( 0.7211978278499968642, 0.9934217856018975334),
 ( 0.7211978278499968642, 0.9934217856018975334),
 ( 1.000000000000000000, 1.000000000000000000) ) ) 
 REPRESENTATION_ITEM ( '' )  SURFACE ( )  );
#22165=ORIENTED_EDGE ( 'NONE', *, *, #25591, .F. ) ;
#22166=CARTESIAN_POINT ( 'NONE',  ( 0.6253024248130467644, -38.93995934748834031, -29.91861951082636040 ) ) ;
#22171=VERTEX_POINT ( 'NONE', #39172 ) ;
#22178=CARTESIAN_POINT ( 'NONE',  ( 0.1119899015040013573, -38.16786807883124055, -22.13989960477330499 ) ) ;
#22182=CIRCLE ( 'NONE', #33190, 48.91267123290010943 ) ;
#22190=CARTESIAN_POINT ( 'NONE',  ( 0.6008123274975391004, 23.09929101554148900, -43.33563551787122492 ) ) ;
#22191=CARTESIAN_POINT ( 'NONE',  ( 5.901764892641288895, 45.40663509823448152, 18.33654701669480147 ) ) ;
#22196=DIRECTION ( 'NONE',  ( 0.09722883295013594329, -0.7930735330831515384, 0.6013159944373356325 ) ) ;
#22198=ORIENTED_EDGE ( 'NONE', *, *, #43085, .T. ) ;
#22199=B_SPLINE_CURVE_WITH_KNOTS ( 'NONE', 3,
 ( #37515, #14628, #5185, #19023, #57184, #38140 ),
 .UNSPECIFIED., .F., .F.,
 ( 4, 2, 4 ),
 ( 2.279404534222591916E-18, 0.0002447193893791696538, 0.0004894387787583370309 ),
 .UNSPECIFIED. ) ;
#22200=CARTESIAN_POINT ( 'NONE',  ( 2.009741617377216460, -32.57420985222115206, -29.63823426127985528 ) ) ;
#22205=CARTESIAN_POINT ( 'NONE',  ( 1.479689385636123067, -40.38744186525652680, 17.61926175661785976 ) ) ;
#22213=EDGE_CURVE ( 'NONE', #21596, #1942, #31479, .T. ) ;
#22214=CARTESIAN_POINT ( 'NONE',  ( -6.057079549204054558, 12.01317374117813230, 15.05041154799451242 ) ) ;
#22216=ORIENTED_EDGE ( 'NONE', *, *, #42055, .T. ) ;
#22222=CARTESIAN_POINT ( 'NONE',  ( 4.694002226626920127, 1.116723307533209475, -45.57452907601510361 ) ) ;
#22233=DIRECTION ( 'NONE',  ( 0.09722883295013598492, -0.4097642837406538785, 0.9069949205004753656 ) ) ;
#22235=CARTESIAN_POINT ( 'NONE',  ( 3.240649175237396484, 42.29049807985159504, -12.11522552640768779 ) ) ;
#22238=CARTESIAN_POINT ( 'NONE',  ( -6.078075953587585900, -1.854308114363064419, 19.16655200248973401 ) ) ;
#22243=ORIENTED_EDGE ( 'NONE', *, *, #7051, .F. ) ;
#22244=CARTESIAN_POINT ( 'NONE',  ( 0.7044674535452954967, 44.60554499456301158, -20.54624244354476659 ) ) ;
#22248=CARTESIAN_POINT ( 'NONE',  ( 0.1129192098497455998, 14.78321943369591196, 41.57412910645692961 ) ) ;
#22255=CARTESIAN_POINT ( 'NONE',  ( 4.975610109902397937, 30.94437158899580353, 37.88001153774800400 ) ) ;
#22257=CARTESIAN_POINT ( 'NONE',  ( 2.879087469061463178, -43.38468303210888166, 7.339683575388114001 ) ) ;
#22267=CARTESIAN_POINT ( 'NONE',  ( 0.6029442701453591180, -49.10740919470779176, 0.08710534889204829545 ) ) ;
#22271=DIRECTION ( 'NONE',  ( -0.1011922191286467598, -0.2088217057275243982, -0.9727042870291398025 ) ) ;
#22272=CARTESIAN_POINT ( 'NONE',  ( 5.901764892641307547, 39.27045567455346742, -29.25444886769549413 ) ) ;
#22276=FACE_OUTER_BOUND ( 'NONE', #3124, .T. ) ;
#22279=CARTESIAN_POINT ( 'NONE',  ( 0.6000166863083090663, -13.47152005829862098, 47.22649287240490423 ) ) ;
#22281=EDGE_CURVE ( 'NONE', #28495, #35248, #33065, .T. ) ;
#22282=VERTEX_POINT ( 'NONE', #15047 ) ;
#22286=CARTESIAN_POINT ( 'NONE',  ( 3.221118495291109163, -10.69297281925443244, 42.66640073815035095 ) ) ;
#22297=CARTESIAN_POINT ( 'NONE',  ( 4.975610109902397937, 0.9924324126403755164, 48.90260202733708894 ) ) ;
#22298=CARTESIAN_POINT ( 'NONE',  ( 1.296416391601052487, -0.3014346417254653576, 44.07058555582086257 ) ) ;
#22300=CARTESIAN_POINT ( 'NONE',  ( 0.1152339509894530906, 15.44841342848934040, 41.33145549091772608 ) ) ;
#22301=EDGE_CURVE ( 'NONE', #38660, #27238, #36066, .T. ) ;
#22303=CARTESIAN_POINT ( 'NONE',  ( 1.657374760986086493, -37.76384079651226955, 22.68882490451896317 ) ) ;
#22304=FACE_OUTER_BOUND ( 'NONE', #22810, .T. ) ;
#22313=CARTESIAN_POINT ( 'NONE',  ( 2.879087469061463178, 13.55971874537538824, -41.85971457534910911 ) ) ;
#22325=EDGE_CURVE ( 'NONE', #53301, #6381, #55083, .T. ) ;
#22337=CARTESIAN_POINT ( 'NONE',  ( 0.6029443199889047422, 16.96000599311128454, 46.08574441807392930 ) ) ;
#22338=CARTESIAN_POINT ( 'NONE',  ( 0.6008122571543325074, -47.38919495537865600, 12.87706301710256440 ) ) ;
#22340=ORIENTED_EDGE ( 'NONE', *, *, #44998, .T. ) ;
#22341=VERTEX_POINT ( 'NONE', #31290 ) ;
#22342=FACE_OUTER_BOUND ( 'NONE', #61542, .T. ) ;
#22346=ORIENTED_EDGE ( 'NONE', *, *, #55566, .F. ) ;
#22349=CIRCLE ( 'NONE', #16354, 43.92652462719577500 ) ;
#22352=( BOUNDED_SURFACE ( )  B_SPLINE_SURFACE ( 3, 1, ( 
 ( #47628, #28818 ),
 ( #33853, #43562 ),
 ( #14432, #29431 ),
 ( #48248, #53231 ) ),
 .UNSPECIFIED., .F., .F., .F. ) 
 B_SPLINE_SURFACE_WITH_KNOTS ( ( 4, 4 ),
 ( 2, 2 ),
 ( 0.000000000000000000, 1.000000000000000000 ),
 ( 0.000000000000000000, 1.000000000000000000 ),
 .UNSPECIFIED. ) 
 GEOMETRIC_REPRESENTATION_ITEM ( )  RATIONAL_B_SPLINE_SURFACE ( (
 ( 1.000000000000000000, 1.000000000000000000),
 ( 0.7211978278499968642, 0.9934217856018975334),
 ( 0.7211978278499968642, 0.9934217856018975334),
 ( 1.000000000000000000, 1.000000000000000000) ) ) 
 REPRESENTATION_ITEM ( '' )  SURFACE ( )  );
#22356=CARTESIAN_POINT ( 'NONE',  ( 0.1129192098497447394, 39.96249028893947752, 18.70698152272492365 ) ) ;
#22359=CARTESIAN_POINT ( 'NONE',  ( 0.2279481005628783974, -17.16174681686966963, -40.64453140665511910 ) ) ;
#22360=VECTOR ( 'NONE', #35025, 1000.000000000000227 ) ;
#22361=CARTESIAN_POINT ( 'NONE',  ( 0.5980271706414734822, -42.44486003424520959, 24.70795619866194315 ) ) ;
#22364=ORIENTED_EDGE ( 'NONE', *, *, #32537, .F. ) ;
#22365=VERTEX_POINT ( 'NONE', #30660 ) ;
#22371=CARTESIAN_POINT ( 'NONE',  ( 0.6252788684277222897, -30.07747058975758492, 38.81739422083782642 ) ) ;
#22374=B_SPLINE_CURVE_WITH_KNOTS ( 'NONE', 3,
 ( #40683, #59750, #25316, #54731 ),
 .UNSPECIFIED., .F., .F.,
 ( 4, 4 ),
 ( 0.000000000000000000, 0.004442905043737214836 ),
 .UNSPECIFIED. ) ;
#22377=CARTESIAN_POINT ( 'NONE',  ( 2.648799415243696664, 6.085982952329662687, -48.65673925360751895 ) ) ;
#22384=B_SPLINE_CURVE_WITH_KNOTS ( 'NONE', 3,
 ( #52361, #9454, #28563, #19192, #43006, #24486, #38929, #43624, #58282, #48298, #34832, #5962, #43942, #14488, #53286, #980, #19493, #9769, #667 ),
 .UNSPECIFIED., .F., .F.,
 ( 4, 3, 3, 3, 3, 3, 4 ),
 ( 0.000000000000000000, 0.0002612768053151725764, 0.0003919133833142917386, 0.0005225499612322563082, 0.0006531865391693363922, 0.0008112755173415148700, 0.0009693688056799733320 ),
 .UNSPECIFIED. ) ;
#22391=CARTESIAN_POINT ( 'NONE',  ( 0.6024113833632039894, -42.89465211219818030, 23.90796288424339977 ) ) ;
#22395=FACE_OUTER_BOUND ( 'NONE', #6147, .T. ) ;
#22403=VECTOR ( 'NONE', #13773, 1000.000000000000000 ) ;
#22405=CARTESIAN_POINT ( 'NONE',  ( 0.6000166863083106206, -19.40010892967683986, 45.11606427011477649 ) ) ;
#22409=CARTESIAN_POINT ( 'NONE',  ( 0.5987334308729319599, -2.178790671009264379, -49.05930877806629553 ) ) ;
#22411=CARTESIAN_POINT ( 'NONE',  ( 1.479689385636123067, 36.27458947416105417, -25.01475572034986072 ) ) ;
#22429=CARTESIAN_POINT ( 'NONE',  ( 2.706805983486680223, 37.76032296520254761, 22.60385194791702901 ) ) ;
#22432=EDGE_CURVE ( 'NONE', #60557, #28087, #4597, .T. ) ;
#22433=CARTESIAN_POINT ( 'NONE',  ( 4.390527457369401532, -43.86299345468695066, 2.494622581215259149 ) ) ;
#22434=B_SPLINE_CURVE_WITH_KNOTS ( 'NONE', 3,
 ( #59790, #25656, #11257, #2135 ),
 .UNSPECIFIED., .F., .F.,
 ( 4, 4 ),
 ( 0.000000000000000000, 0.004442905043737215703 ),
 .UNSPECIFIED. ) ;
#22438=CARTESIAN_POINT ( 'NONE',  ( 0.5980271706414711508, 27.52111707190132961, 40.67723390247133608 ) ) ;
#22439=CARTESIAN_POINT ( 'NONE',  ( 0.1156867017252034557, 33.51703926206629802, 28.69757631543633991 ) ) ;
#22444=CARTESIAN_POINT ( 'NONE',  ( 0.7948884756798525464, -20.66454828366466501, 44.53846751777887647 ) ) ;
#22446=CARTESIAN_POINT ( 'NONE',  ( 1.834102595619085285, 39.10291415957683370, -20.27707693644353171 ) ) ;
#22448=EDGE_CURVE ( 'NONE', #37659, #6381, #7611, .T. ) ;
#22457=CARTESIAN_POINT ( 'NONE',  ( 2.299652685299200083, -40.05308401807694452, 28.28484020635476170 ) ) ;
#22458=EDGE_LOOP ( 'NONE', ( #2687, #18736, #35193, #17515 ) ) ;
#22459=CARTESIAN_POINT ( 'NONE',  ( 3.727782113643637096, 43.51027460820039749, 6.295536468401055075 ) ) ;
#22466=ORIENTED_EDGE ( 'NONE', *, *, #3210, .T. ) ;
#22474=EDGE_CURVE ( 'NONE', #10386, #61727, #38278, .T. ) ;
#22475=CARTESIAN_POINT ( 'NONE',  ( 0.5987334308729322929, -48.77819069500445437, -5.678998071095664457 ) ) ;
#22479=CARTESIAN_POINT ( 'NONE',  ( 5.901764892641307547, 42.68902166415596611, -23.99247583716404719 ) ) ;
#22480=B_SPLINE_CURVE_WITH_KNOTS ( 'NONE', 3,
 ( #29750, #40126, #16283, #1236, #20369, #35406, #46051, #2151, #45425, #17216, #36637, #40422, #26288, #59485, #41047, #21293, #30998, #36337, #49794 ),
 .UNSPECIFIED., .F., .F.,
 ( 4, 3, 3, 3, 3, 3, 4 ),
 ( 3.469552829456483146E-18, 0.0002612768053151735522, 0.0003919133833142943407, 0.0005225499612322647650, 0.0006531865391693365006, 0.0008112755173415180142, 0.0009693688056799728983 ),
 .UNSPECIFIED. ) ;
#22485=DIRECTION ( 'NONE',  ( 0.09722883295013595717, 0.9754357953229587652, 0.1976652808305532638 ) ) ;
#22488=CARTESIAN_POINT ( 'NONE',  ( 4.975610109902397937, -48.84566763821283786, 2.559328059280373768 ) ) ;
#22493=CARTESIAN_POINT ( 'NONE',  ( 4.975610109902397937, 19.27143522741655701, 44.95621415792550124 ) ) ;
#22497=CARTESIAN_POINT ( 'NONE',  ( 1.112077966505212068, 16.20463149544202253, 40.99317312950392989 ) ) ;
#22501=CARTESIAN_POINT ( 'NONE',  ( 0.9268187852002115479, 32.91938759995093022, -29.32692027732920437 ) ) ;
#22502=EDGE_CURVE ( 'NONE', #43289, #12977, #24831, .T. ) ;
#22508=B_SPLINE_CURVE_WITH_KNOTS ( 'NONE', 3,
 ( #51967, #24090, #46677, #3722 ),
 .UNSPECIFIED., .F., .F.,
 ( 4, 4 ),
 ( 0.000000000000000000, 0.004444103432399267896 ),
 .UNSPECIFIED. ) ;
#22510=CARTESIAN_POINT ( 'NONE',  ( 3.894904216938897878, 27.86699861404660439, -33.99345114460909656 ) ) ;
#22512=ORIENTED_EDGE ( 'NONE', *, *, #53281, .F. ) ;
#22516=ORIENTED_EDGE ( 'NONE', *, *, #9504, .T. ) ;
#22518=CARTESIAN_POINT ( 'NONE',  ( 4.553261556744875094, -25.31600221269659201, 35.89762663172006540 ) ) ;
#22521=CARTESIAN_POINT ( 'NONE',  ( 5.901764892641288895, -28.05153439369972901, -40.13854613210049394 ) ) ;
#22529=( BOUNDED_SURFACE ( )  B_SPLINE_SURFACE ( 3, 1, ( 
 ( #8394, #51006 ),
 ( #46960, #61020 ),
 ( #32541, #51620 ),
 ( #31919, #12827 ) ),
 .UNSPECIFIED., .F., .F., .F. ) 
 B_SPLINE_SURFACE_WITH_KNOTS ( ( 4, 4 ),
 ( 2, 2 ),
 ( 0.000000000000000000, 1.000000000000000000 ),
 ( 0.000000000000000000, 1.000000000000000000 ),
 .UNSPECIFIED. ) 
 GEOMETRIC_REPRESENTATION_ITEM ( )  RATIONAL_B_SPLINE_SURFACE ( (
 ( 1.000000000000000000, 1.000000000000000000),
 ( 0.9953485035131437453, 0.8621029689291515030),
 ( 0.9953485035131437453, 0.8621029689291515030),
 ( 1.000000000000000000, 1.000000000000000000) ) ) 
 REPRESENTATION_ITEM ( '' )  SURFACE ( )  );
#22532=CARTESIAN_POINT ( 'NONE',  ( -6.072942160501519027, 13.84283391500593119, -13.38581755032474874 ) ) ;
#22535=ADVANCED_FACE ( 'NONE', ( #34011 ), #13284, .F. ) ;
#22538=LINE ( 'NONE', #51951, #38702 ) ;
#22542=LINE ( 'NONE', #60726, #11265 ) ;
#22544=ORIENTED_EDGE ( 'NONE', *, *, #46152, .T. ) ;
#22545=CARTESIAN_POINT ( 'NONE',  ( 4.390527457369401532, 6.694952568920494507, 43.42076630747694566 ) ) ;
#22551=CARTESIAN_POINT ( 'NONE',  ( 4.553261556744875094, 0.000000000000000000, 0.000000000000000000 ) ) ;
#22552=CARTESIAN_POINT ( 'NONE',  ( 1.830465331921976579, 32.72788206612836603, 29.48324594314511771 ) ) ;
#22553=CARTESIAN_POINT ( 'NONE',  ( 4.553261556744873317, -3.993093339917161977, 43.74465420371208069 ) ) ;
#22556=VERTEX_POINT ( 'NONE', #49310 ) ;
#22559=CARTESIAN_POINT ( 'NONE',  ( 2.299652685299200527, 32.00015747886172335, 37.15200729686356595 ) ) ;
#22574=DIRECTION ( 'NONE',  ( 1.000000000000000000, 0.000000000000000000, 0.000000000000000000 ) ) ;
#22577=B_SPLINE_CURVE_WITH_KNOTS ( 'NONE', 3,
 ( #27114, #8931, #27413, #51211, #55913, #60924, #17408, #46544, #45941, #13037, #32132, #18036, #23345, #36531, #3589, #37153 ),
 .UNSPECIFIED., .F., .F.,
 ( 4, 3, 3, 3, 3, 4 ),
 ( 2.081781105835003463E-17, 0.0002612764279487748975, 0.0003919131003184791909, 0.0005225497727000653642, 0.0007837925190632464385, 0.001045051706266716517 ),
 .UNSPECIFIED. ) ;
#22578=VECTOR ( 'NONE', #37720, 1000.000000000000114 ) ;
#22582=CARTESIAN_POINT ( 'NONE',  ( 2.648799415243696664, -49.01629645596155171, -1.385692978581185342 ) ) ;
#22585=CARTESIAN_POINT ( 'NONE',  ( -2.601141883200665639, 10.36212650428638682, -10.74345204199070380 ) ) ;
#22587=ORIENTED_EDGE ( 'NONE', *, *, #50182, .F. ) ;
#22593=CARTESIAN_POINT ( 'NONE',  ( 0.6000166863083106206, -49.10753961887881758, -0.5225268306040948829 ) ) ;
#22604=CARTESIAN_POINT ( 'NONE',  ( -2.739355103387247858, 3.064916856561431313, 14.61005994557799781 ) ) ;
#22615=ORIENTED_EDGE ( 'NONE', *, *, #19031, .T. ) ;
#22617=VERTEX_POINT ( 'NONE', #21430 ) ;
#22623=CARTESIAN_POINT ( 'NONE',  ( 0.6039202388192952409, 48.16848798300480183, 9.558267535495888367 ) ) ;
#22631=CARTESIAN_POINT ( 'NONE',  ( -6.078726893082806448, -18.27610589745697567, 6.064486333866907053 ) ) ;
#22634=CARTESIAN_POINT ( 'NONE',  ( 1.555521457401304097, -0.4925839501666971487, 49.06288516100940456 ) ) ;
#22638=FACE_OUTER_BOUND ( 'NONE', #30386, .T. ) ;
#22641=CARTESIAN_POINT ( 'NONE',  ( -2.739355103387247858, -13.73625580088950748, -5.844898931850437407 ) ) ;
#22646=CARTESIAN_POINT ( 'NONE',  ( 4.553261556744875094, 12.71466023209559104, -42.04612920360213479 ) ) ;
#22647=CARTESIAN_POINT ( 'NONE',  ( 0.3676999524040323597, -17.09834788623527047, -40.66444494744902727 ) ) ;
#22655=CARTESIAN_POINT ( 'NONE',  ( 0.5997462898726536595, 48.09935696025637952, -9.899671214446758682 ) ) ;
#22656=FACE_OUTER_BOUND ( 'NONE', #56872, .T. ) ;
#22661=CARTESIAN_POINT ( 'NONE',  ( 1.479689385636123067, -30.82386906365282542, 31.48766331778968919 ) ) ;
#22662=CARTESIAN_POINT ( 'NONE',  ( 0.2940133293163004202, 43.14164474393039228, 9.221661366941855675 ) ) ;
#22670=CIRCLE ( 'NONE', #9647, 48.91267123290010943 ) ;
#22685=CARTESIAN_POINT ( 'NONE',  ( -6.078075953587585900, 12.00179475453279387, 15.05828997320761786 ) ) ;
#22686=CARTESIAN_POINT ( 'NONE',  ( 0.7242486021783849370, -2.392220701665511040, 49.04374315331669720 ) ) ;
#22689=CARTESIAN_POINT ( 'NONE',  ( -6.057079549204054558, -1.840653143754622523, 19.16880870331082320 ) ) ;
#22694=CARTESIAN_POINT ( 'NONE',  ( 0.1129192098497455998, 30.02178898772931603, -32.33641869102712718 ) ) ;
#22696=VERTEX_POINT ( 'NONE', #7302 ) ;
#22711=B_SPLINE_CURVE_WITH_KNOTS ( 'NONE', 3,
 ( #22518, #9024, #41637, #28133, #9330, #14060, #27517, #17822, #33160, #42264, #37249, #13752, #27829, #51934, #56318, #36946, #56013, #47249, #13132, #41956, #56939, #4299, #3687, #23437, #3081 ),
 .UNSPECIFIED., .F., .F.,
 ( 4, 3, 3, 3, 3, 3, 3, 3, 4 ),
 ( 6.254634441385501517E-18, 0.0005656085177311398569, 0.001131215744874499406, 0.001696821861372766783, 0.002262427090022500319, 0.002828031679238746793, 0.003393635864401604862, 0.003977030878808132490, 0.004561030005651160735 ),
 .UNSPECIFIED. ) ;
#22712=AXIS2_PLACEMENT_3D ( 'NONE', #53271, #10383, #9436 ) ;
#22716=CARTESIAN_POINT ( 'NONE',  ( 0.1158816050234199313, -35.36510507486345745, -26.38657583600091527 ) ) ;
#22717=CARTESIAN_POINT ( 'NONE',  ( 0.5997462898726536595, -39.66574928371219499, -28.95133786038212875 ) ) ;
#22722=( BOUNDED_SURFACE ( )  B_SPLINE_SURFACE ( 3, 1, ( 
 ( #49045, #58117 ),
 ( #53420, #34346 ),
 ( #1409, #1716 ),
 ( #49349, #491 ) ),
 .UNSPECIFIED., .F., .F., .F. ) 
 B_SPLINE_SURFACE_WITH_KNOTS ( ( 4, 4 ),
 ( 2, 2 ),
 ( 0.000000000000000000, 1.000000000000000000 ),
 ( 0.000000000000000000, 1.000000000000000000 ),
 .UNSPECIFIED. ) 
 GEOMETRIC_REPRESENTATION_ITEM ( )  RATIONAL_B_SPLINE_SURFACE ( (
 ( 1.000000000000000000, 1.000000000000000000),
 ( 0.7211978278499968642, 0.9934217856018975334),
 ( 0.7211978278499968642, 0.9934217856018975334),
 ( 1.000000000000000000, 1.000000000000000000) ) ) 
 REPRESENTATION_ITEM ( '' )  SURFACE ( )  );
#22723=B_SPLINE_CURVE_WITH_KNOTS ( 'NONE', 3,
 ( #27025, #46154, #35206, #35825 ),
 .UNSPECIFIED., .F., .F.,
 ( 4, 4 ),
 ( 0.000000000000000000, 0.005013413432710148512 ),
 .UNSPECIFIED. ) ;
#22729=CARTESIAN_POINT ( 'NONE',  ( 0.1135584504625009039, -7.468331181319575407, 43.48765435731597506 ) ) ;
#22734=CARTESIAN_POINT ( 'NONE',  ( 0.8744876279028306332, 5.599149760997630842, 48.77498920895230583 ) ) ;
#22737=ORIENTED_EDGE ( 'NONE', *, *, #8240, .T. ) ;
#22743=CARTESIAN_POINT ( 'NONE',  ( 3.894904216938897878, -43.89961190414321379, 2.224501549068497841 ) ) ;
#22744=CARTESIAN_POINT ( 'NONE',  ( 0.6021448801613057400, 48.98911663091443103, 3.406991392652731765 ) ) ;
#22746=CARTESIAN_POINT ( 'NONE',  ( 0.5997462898726536595, -25.00873172704263325, 42.26245340191598387 ) ) ;
#22748=ORIENTED_EDGE ( 'NONE', *, *, #26650, .T. ) ;
#22749=CARTESIAN_POINT ( 'NONE',  ( 4.834790513006553603, 45.81970208965029201, -11.53881455523394095 ) ) ;
#22750=FACE_OUTER_BOUND ( 'NONE', #57893, .T. ) ;
#22752=CARTESIAN_POINT ( 'NONE',  ( 0.6253024248130503171, -20.50354113282875090, 44.62117242332436717 ) ) ;
#22754=CARTESIAN_POINT ( 'NONE',  ( 4.226256110419178924, 38.48784581281913120, -21.20172103098821736 ) ) ;
#22757=EDGE_LOOP ( 'NONE', ( #46138, #48319, #26068, #31129 ) ) ;
#22759=CARTESIAN_POINT ( 'NONE',  ( 0.1145239942831223490, -44.12299651911310860, -0.3265867097808889952 ) ) ;
#22760=CARTESIAN_POINT ( 'NONE',  ( 0.5980271706414711508, -47.32398142236174010, -13.13354579607594275 ) ) ;
#22762=ORIENTED_EDGE ( 'NONE', *, *, #34391, .T. ) ;
#22764=ADVANCED_FACE ( 'NONE', ( #41799 ), #17983, .F. ) ;
#22766=CARTESIAN_POINT ( 'NONE',  ( 2.533389852662419894, 43.47932600038843276, 6.855562871534678138 ) ) ;
#22768=CARTESIAN_POINT ( 'NONE',  ( 0.1158816050234198619, 36.97683962690370407, -24.07603315563850543 ) ) ;
#22770=CARTESIAN_POINT ( 'NONE',  ( 0.7242003506639993482, -8.644113737957038524, -48.33519392545445470 ) ) ;
#22778=CARTESIAN_POINT ( 'NONE',  ( 0.8744876279028263033, -43.20725972823498040, 23.31271664041618052 ) ) ;
#22785=ORIENTED_EDGE ( 'NONE', *, *, #49749, .T. ) ;
#22787=FACE_OUTER_BOUND ( 'NONE', #8778, .T. ) ;
#22788=CARTESIAN_POINT ( 'NONE',  ( -6.077587904424778920, -18.27702681447052768, 6.061873655649367088 ) ) ;
#22796=CARTESIAN_POINT ( 'NONE',  ( 0.1147471544378676628, -12.85192855149397317, -42.21113740448768681 ) ) ;
#22800=DIRECTION ( 'NONE',  ( 0.1011922191286468292, 0.9018493587347812257, 0.4200331759962346312 ) ) ;
#22802=AXIS2_PLACEMENT_3D ( 'NONE', #28320, #47139, #4182 ) ;
#22807=DIRECTION ( 'NONE',  ( 0.1011922191286468153, 0.5585841627631871198, -0.8232520075274455396 ) ) ;
#22809=CARTESIAN_POINT ( 'NONE',  ( 0.5549461598389361372, 33.00765054922539576, -29.25256742043379532 ) ) ;
#22810=EDGE_LOOP ( 'NONE', ( #31383, #15800, #22159, #48725 ) ) ;
#22811=B_SPLINE_CURVE_WITH_KNOTS ( 'NONE', 3,
 ( #9368, #47914, #4641, #23789, #59132, #59762 ),
 .UNSPECIFIED., .F., .F.,
 ( 4, 2, 4 ),
 ( 0.000000000000000000, 0.0002447195606305743666, 0.0004894391212611487333 ),
 .UNSPECIFIED. ) ;
#22813=CARTESIAN_POINT ( 'NONE',  ( 4.975610109902397937, 47.45567470742089000, 11.84940273605495520 ) ) ;
#22819=CARTESIAN_POINT ( 'NONE',  ( 0.8744876279028263033, -48.57046782678510510, -7.159588358748426806 ) ) ;
#22823=ORIENTED_EDGE ( 'NONE', *, *, #7063, .F. ) ;
#22827=CARTESIAN_POINT ( 'NONE',  ( 0.1129192098497447394, -27.13044910148925837, 34.79785222304180081 ) ) ;
#22831=EDGE_CURVE ( 'NONE', #33142, #14421, #41156, .T. ) ;
#22841=FACE_OUTER_BOUND ( 'NONE', #52448, .T. ) ;
#22846=CARTESIAN_POINT ( 'NONE',  ( 4.390527457369401532, -29.29850356886337082, -32.73809745928922865 ) ) ;
#22850=CARTESIAN_POINT ( 'NONE',  ( 0.8753041380234465318, 48.36002538446257404, -8.511537621788184182 ) ) ;
#22853=CARTESIAN_POINT ( 'NONE',  ( 0.7242003506639999033, 11.72319998681805409, 47.68205381687218392 ) ) ;
#22859=EDGE_CURVE ( 'NONE', #1548, #21722, #40384, .T. ) ;
#22868=CARTESIAN_POINT ( 'NONE',  ( 1.112077966505211402, -43.57125842763898760, 6.676508380916812868 ) ) ;
#22878=VECTOR ( 'NONE', #30794, 1000.000000000000000 ) ;
#22879=CARTESIAN_POINT ( 'NONE',  ( -6.077587904424778920, 0.6233693561568425245, 19.24597183931575373 ) ) ;
#22881=EDGE_CURVE ( 'NONE', #51544, #34106, #13517, .T. ) ;
#22882=DIRECTION ( 'NONE',  ( 0.1011922191286468015, 0.2088217057275386090, -0.9727042870291366938 ) ) ;
#22891=CARTESIAN_POINT ( 'NONE',  ( 0.1129192098497447394, -6.563350895509266536, 43.63340707310824484 ) ) ;
#22892=CARTESIAN_POINT ( 'NONE',  ( 1.834102595619085729, 24.12078293692350428, -36.85628271227993480 ) ) ;
#22893=DIRECTION ( 'NONE',  ( 1.000000000000000000, 0.000000000000000000, 0.000000000000000000 ) ) ;
#22901=ORIENTED_EDGE ( 'NONE', *, *, #51226, .T. ) ;
#22903=DIRECTION ( 'NONE',  ( 0.000000000000000000, 0.000000000000000000, 1.000000000000000000 ) ) ;
#22908=ORIENTED_EDGE ( 'NONE', *, *, #43419, .T. ) ;
#22912=EDGE_CURVE ( 'NONE', #59245, #30839, #53565, .T. ) ;
#22920=CARTESIAN_POINT ( 'NONE',  ( 0.7242003506640004584, 40.69931820417237844, -27.46956810438689800 ) ) ;
#22921=EDGE_CURVE ( 'NONE', #17913, #46201, #41977, .T. ) ;
#22925=CARTESIAN_POINT ( 'NONE',  ( 2.648799415243708655, -47.76469914295812913, -11.09283458239118580 ) ) ;
#22932=ORIENTED_EDGE ( 'NONE', *, *, #33275, .T. ) ;
#22943=AXIS2_PLACEMENT_3D ( 'NONE', #20512, #7865, #31374 ) ;
#22956=FACE_OUTER_BOUND ( 'NONE', #32450, .T. ) ;
#22961=CARTESIAN_POINT ( 'NONE',  ( 2.879087469061463622, -21.31151173680148503, 38.49572890952385507 ) ) ;
#22966=CARTESIAN_POINT ( 'NONE',  ( 0.6008123274975392114, -47.61009137730950158, 12.03468945185942651 ) ) ;
#22969=CARTESIAN_POINT ( 'NONE',  ( 0.5997462898726536595, -39.66574928371259290, 28.95133786038155321 ) ) ;
#22971=DIRECTION ( 'NONE',  ( 0.09722883295013592941, 0.6635018476521751252, -0.7418300696286881379 ) ) ;
#22972=ORIENTED_EDGE ( 'NONE', *, *, #38218, .F. ) ;
#22982=VECTOR ( 'NONE', #54860, 1000.000000000000000 ) ;
#22984=CARTESIAN_POINT ( 'NONE',  ( 4.975610109902397937, 48.90928568712960356, 0.5754830253899292369 ) ) ;
#22987=DIRECTION ( 'NONE',  ( 1.000000000000000000, 0.000000000000000000, 0.000000000000000000 ) ) ;
#22990=CARTESIAN_POINT ( 'NONE',  ( 4.553261556744873317, -14.95853073564509828, 41.30111286702087625 ) ) ;
#22991=CARTESIAN_POINT ( 'NONE',  ( 2.299746137290199943, -31.56858058830529146, -37.51940907484834753 ) ) ;
#22996=ORIENTED_EDGE ( 'NONE', *, *, #889, .T. ) ;
#22999=CARTESIAN_POINT ( 'NONE',  ( 0.5980271706414734822, -0.8742700727941912220, 49.10483575658797406 ) ) ;
#23001=CARTESIAN_POINT ( 'NONE',  ( 0.9268187852002115479, 34.20493226694245692, 27.81684636191718241 ) ) ;
#23004=EDGE_CURVE ( 'NONE', #24004, #3087, #40446, .T. ) ;
#23005=CARTESIAN_POINT ( 'NONE',  ( 0.8744876279028306332, 16.11801507201633399, -46.37412684372340266 ) ) ;
#23008=CARTESIAN_POINT ( 'NONE',  ( 0.8753041380234471980, -31.30612550145435335, 37.82941757363136048 ) ) ;
#23017=FACE_OUTER_BOUND ( 'NONE', #42504, .T. ) ;
#23020=CARTESIAN_POINT ( 'NONE',  ( 4.335381028904201628, -44.56680861641509495, -20.33608658056349228 ) ) ;
#23024=CARTESIAN_POINT ( 'NONE',  ( 0.3676999524040323597, -38.83470403830501994, 20.92406140260764857 ) ) ;
#23029=CARTESIAN_POINT ( 'NONE',  ( 0.1119898979215349921, -22.39193976382053819, 38.02055157234389071 ) ) ;
#23034=FACE_OUTER_BOUND ( 'NONE', #43648, .T. ) ;
#23036=CARTESIAN_POINT ( 'NONE',  ( 2.299746137290199055, 9.651167162349302941, -48.07427909070013783 ) ) ;
#23037=CARTESIAN_POINT ( 'NONE',  ( 4.553261556744873317, -24.94552653848474222, 36.15605442441679429 ) ) ;
#23039=FACE_OUTER_BOUND ( 'NONE', #50184, .T. ) ;
#23051=CARTESIAN_POINT ( 'NONE',  ( 0.6008123274975391004, 11.35154294343716863, -47.77757867412034898 ) ) ;
#23054=B_SPLINE_CURVE_WITH_KNOTS ( 'NONE', 3,
 ( #56359, #37602, #3733, #4643, #42302, #13173, #37289, #51974, #8143, #42919, #18796, #32584, #51353, #52276, #47600, #9066, #37922, #8758, #38223, #61971, #56978, #19110, #47289, #13794, #28173 ),
 .UNSPECIFIED., .F., .F.,
 ( 4, 3, 3, 3, 3, 3, 3, 3, 4 ),
 ( 6.254634441385501517E-18, 0.0005656085177311386642, 0.001131215744874498972, 0.001696821861372766350, 0.002262427090022497717, 0.002828031679238744624, 0.003393635864401602694, 0.003977030878808130755, 0.004561030005651157265 ),
 .UNSPECIFIED. ) ;
#23058=CARTESIAN_POINT ( 'NONE',  ( 0.7413678028165006095, 37.45741361428792970, 23.26861098343432843 ) ) ;
#23061=CARTESIAN_POINT ( 'NONE',  ( 0.6026112563231247332, 48.99508032062211527, 3.320105311582033814 ) ) ;
#23074=ORIENTED_EDGE ( 'NONE', *, *, #26576, .F. ) ;
#23075=ORIENTED_EDGE ( 'NONE', *, *, #34113, .T. ) ;
#23078=CARTESIAN_POINT ( 'NONE',  ( -6.078726893082806448, -6.647148524917478873, -18.07233957617019371 ) ) ;
#23083=CARTESIAN_POINT ( 'NONE',  ( 4.390527457369401532, 43.53099151023969426, 5.936170041707031331 ) ) ;
#23089=CARTESIAN_POINT ( 'NONE',  ( 0.1140933569871964981, -27.80654152114252753, 34.25997954927705536 ) ) ;
#23094=LINE ( 'NONE', #32494, #49484 ) ;
#23096=CARTESIAN_POINT ( 'NONE',  ( -2.601141883200665639, -0.9259886695528269929, 14.89758277215630677 ) ) ;
#23097=( BOUNDED_SURFACE ( )  B_SPLINE_SURFACE ( 3, 1, ( 
 ( #42352, #52328 ),
 ( #46739, #61406 ),
 ( #43831, #37652 ),
 ( #13845, #32949 ) ),
 .UNSPECIFIED., .F., .F., .F. ) 
 B_SPLINE_SURFACE_WITH_KNOTS ( ( 4, 4 ),
 ( 2, 2 ),
 ( 0.000000000000000000, 1.000000000000000000 ),
 ( 0.000000000000000000, 1.000000000000000000 ),
 .UNSPECIFIED. ) 
 GEOMETRIC_REPRESENTATION_ITEM ( )  RATIONAL_B_SPLINE_SURFACE ( (
 ( 1.000000000000000000, 1.000000000000000000),
 ( 0.9754377213608244057, 0.9999580625633939235),
 ( 0.9754377213608244057, 0.9999580625633939235),
 ( 1.000000000000000000, 1.000000000000000000) ) ) 
 REPRESENTATION_ITEM ( '' )  SURFACE ( )  );
#23099=VERTEX_POINT ( 'NONE', #22553 ) ;
#23102=ORIENTED_EDGE ( 'NONE', *, *, #5792, .T. ) ;
#23105=CARTESIAN_POINT ( 'NONE',  ( 0.3676999524040366896, -34.85286720109691316, 27.04123205746257241 ) ) ;
#23108=CARTESIAN_POINT ( 'NONE',  ( 2.648799415243696664, -12.61806922346143089, -47.38461556625244953 ) ) ;
#23114=CARTESIAN_POINT ( 'NONE',  ( 0.6000166863083090663, -30.20952222014459210, 38.71961065066439289 ) ) ;
#23123=CONICAL_SURFACE ( 'NONE', #31113, 43.92652462719577500, 1.486293639869522343 ) ;
#23127=CARTESIAN_POINT ( 'NONE',  ( 4.226256110419179812, 27.71872288846495991, -34.09544913063436411 ) ) ;
#23135=ADVANCED_FACE ( 'NONE', ( #4330 ), #2461, .F. ) ;
#23140=FACE_OUTER_BOUND ( 'NONE', #12659, .T. ) ;
#23143=EDGE_LOOP ( 'NONE', ( #49072, #33096, #8411, #43349 ) ) ;
#23145=CARTESIAN_POINT ( 'NONE',  ( 0.8753041380234465318, -48.80600061351585595, 5.395612290228925190 ) ) ;
#23160=CARTESIAN_POINT ( 'NONE',  ( 0.1129192098497455998, -27.13044910148877165, -34.79785222304216319 ) ) ;
#23163=ORIENTED_EDGE ( 'NONE', *, *, #59745, .T. ) ;
#23165=ORIENTED_EDGE ( 'NONE', *, *, #14785, .F. ) ;
#23167=CARTESIAN_POINT ( 'NONE',  ( 5.901764892641288895, 13.97448418306270490, 46.93298689894995590 ) ) ;
#23170=CARTESIAN_POINT ( 'NONE',  ( 3.240649175237397372, -37.40057439548368734, -23.16164830674929576 ) ) ;
#23174=CARTESIAN_POINT ( 'NONE',  ( 0.9268187852002115479, 43.07451267043047238, -9.398972875455658738 ) ) ;
#23176=CARTESIAN_POINT ( 'NONE',  ( 3.390910168358336918, -41.46266722896311308, -14.66098096287914743 ) ) ;
#23180=FACE_OUTER_BOUND ( 'NONE', #17724, .T. ) ;
#23182=CARTESIAN_POINT ( 'NONE',  ( 0.6000166863083106206, -7.321729200003417759, 48.56146376737702752 ) ) ;
#23187=CARTESIAN_POINT ( 'NONE',  ( 0.6028777368367059797, -49.10735432294857361, -0.08706728120422242700 ) ) ;
#23195=CARTESIAN_POINT ( 'NONE',  ( 4.553261556744875094, 0.000000000000000000, 0.000000000000000000 ) ) ;
#23197=ORIENTED_EDGE ( 'NONE', *, *, #28516, .F. ) ;
#23199=CARTESIAN_POINT ( 'NONE',  ( 0.5997462898726536595, 44.46857747280041195, -20.83500054451300088 ) ) ;
#23208=ORIENTED_EDGE ( 'NONE', *, *, #27943, .T. ) ;
#23216=ORIENTED_EDGE ( 'NONE', *, *, #44649, .T. ) ;
#23224=FACE_OUTER_BOUND ( 'NONE', #48500, .T. ) ;
#23230=CARTESIAN_POINT ( 'NONE',  ( 0.1140933569871965397, -31.43159979652969227, -30.96779753735644292 ) ) ;
#23235=VERTEX_POINT ( 'NONE', #10613 ) ;
#23244=CARTESIAN_POINT ( 'NONE',  ( 4.975610109902397937, -22.11219452748553138, -43.62912170003438916 ) ) ;
#23250=CARTESIAN_POINT ( 'NONE',  ( -6.063463321072278589, 5.464110623309939463, 18.46520911269897880 ) ) ;
#23254=LINE ( 'NONE', #22641, #24219 ) ;
#23256=EDGE_CURVE ( 'NONE', #2406, #55928, #10931, .T. ) ;
#23257=CARTESIAN_POINT ( 'NONE',  ( 5.901764892641307547, -10.93876531158323040, 47.73190631954460628 ) ) ;
#23261=CARTESIAN_POINT ( 'NONE',  ( 4.390527457369401532, -20.60499138400743036, 38.80231522336777772 ) ) ;
#23264=ADVANCED_FACE ( 'NONE', ( #61963 ), #53316, .F. ) ;
#23267=CARTESIAN_POINT ( 'NONE',  ( 4.694002226626921015, -38.01786027345620056, -25.15804188871017999 ) ) ;
#23269=FACE_OUTER_BOUND ( 'NONE', #2998, .T. ) ;
#23275=CARTESIAN_POINT ( 'NONE',  ( 1.657374760986086493, -30.77364477053859559, 31.52575510259740454 ) ) ;
#23291=CARTESIAN_POINT ( 'NONE',  ( 4.694002226626921015, 18.13772657221498719, 41.82472529781519199 ) ) ;
#23293=CARTESIAN_POINT ( 'NONE',  ( 0.6000166863083106206, -45.32251430608251752, -18.91277818522173959 ) ) ;
#23299=VERTEX_POINT ( 'NONE', #34124 ) ;
#23300=CARTESIAN_POINT ( 'NONE',  ( 0.3676999524040366896, 34.11874447324979087, 27.96179284115963171 ) ) ;
#23317=CARTESIAN_POINT ( 'NONE',  ( -6.078075953587585900, 13.83625866740996813, 13.39227838478794652 ) ) ;
#23320=CARTESIAN_POINT ( 'NONE',  ( -6.077587904424778920, 17.85108912406241899, 7.220432014686572586 ) ) ;
#23323=CARTESIAN_POINT ( 'NONE',  ( 4.553261556744873317, -43.82122302957819215, 3.039733214543990591 ) ) ;
#23330=CARTESIAN_POINT ( 'NONE',  ( 0.2285344041767104206, -22.21790586462361361, 38.11647713635377244 ) ) ;
#23334=CARTESIAN_POINT ( 'NONE',  ( 0.2940133293163013639, -35.83075917510851127, 25.73707921488799855 ) ) ;
#23336=CARTESIAN_POINT ( 'NONE',  ( 0.6016118706126976079, -39.14612183274096679, -29.65016357864037033 ) ) ;
#23337=CARTESIAN_POINT ( 'NONE',  ( 3.559346040607745287, -24.52570418190676094, -36.49548076027481613 ) ) ;
#23338=VECTOR ( 'NONE', #9319, 1000.000000000000114 ) ;
#23342=( BOUNDED_SURFACE ( )  B_SPLINE_SURFACE ( 3, 1, ( 
 ( #6912, #41106 ),
 ( #59229, #54522 ),
 ( #54843, #1915 ),
 ( #11332, #55458 ) ),
 .UNSPECIFIED., .F., .F., .F. ) 
 B_SPLINE_SURFACE_WITH_KNOTS ( ( 4, 4 ),
 ( 2, 2 ),
 ( 0.000000000000000000, 1.000000000000000000 ),
 ( 0.000000000000000000, 1.000000000000000000 ),
 .UNSPECIFIED. ) 
 GEOMETRIC_REPRESENTATION_ITEM ( )  RATIONAL_B_SPLINE_SURFACE ( (
 ( 1.000000000000000000, 1.000000000000000000),
 ( 0.9953485035131437453, 0.8621029689291515030),
 ( 0.9953485035131437453, 0.8621029689291515030),
 ( 1.000000000000000000, 1.000000000000000000) ) ) 
 REPRESENTATION_ITEM ( '' )  SURFACE ( )  );
#23345=CARTESIAN_POINT ( 'NONE',  ( 0.6021447746440204973, -1.312817911176840546, 49.08989354460427990 ) ) ;
#23350=CARTESIAN_POINT ( 'NONE',  ( 0.1158816050234199174, -7.036604598242554687, 43.55947930167616278 ) ) ;
#23351=CARTESIAN_POINT ( 'NONE',  ( 0.2940135542859019235, 14.47847097612530298, -41.67270601826714227 ) ) ;
#23357=CARTESIAN_POINT ( 'NONE',  ( 0.8753041380234524160, 16.12068986424834449, -46.38169559399161557 ) ) ;
#23363=CARTESIAN_POINT ( 'NONE',  ( 3.559346040607745287, -39.94197359654808821, 18.38665349525692960 ) ) ;
#23364=CARTESIAN_POINT ( 'NONE',  ( 0.8753041380234524160, 41.63161868429038037, 26.03740873433498848 ) ) ;
#23368=ORIENTED_EDGE ( 'NONE', *, *, #60245, .F. ) ;
#23375=CARTESIAN_POINT ( 'NONE',  ( 0.6253024248130488738, 23.32030274153287763, -43.21582704821111776 ) ) ;
#23379=CARTESIAN_POINT ( 'NONE',  ( 0.1157991065609915854, -44.12409475290455418, -0.08141114419867848118 ) ) ;
#23382=EDGE_CURVE ( 'NONE', #23759, #38660, #22374, .T. ) ;
#23386=CARTESIAN_POINT ( 'NONE',  ( 2.009741617377216460, 43.46874900317952495, 7.069083230633559367 ) ) ;
#23389=ORIENTED_EDGE ( 'NONE', *, *, #50619, .F. ) ;
#23392=DIRECTION ( 'NONE',  ( -0.1011922191286467460, -0.9481578383257858178, 0.3012587731655177459 ) ) ;
#23396=CARTESIAN_POINT ( 'NONE',  ( 0.3676999524040323597, 19.66859742988730986, 39.48540057367873857 ) ) ;
#23400=ORIENTED_EDGE ( 'NONE', *, *, #12329, .F. ) ;
#23409=CARTESIAN_POINT ( 'NONE',  ( -6.079354080745853928, -4.285997663762476151, -18.77293741731390853 ) ) ;
#23414=CARTESIAN_POINT ( 'NONE',  ( -6.077587904424778920, 12.01079512011154193, -15.05114022181160927 ) ) ;
#23420=EDGE_CURVE ( 'NONE', #19355, #7571, #13090, .T. ) ;
#23436=VERTEX_POINT ( 'NONE', #3341 ) ;
#23437=CARTESIAN_POINT ( 'NONE',  ( 0.5549461598389364703, -26.80708097326903072, 35.02282263266913986 ) ) ;
#23440=CARTESIAN_POINT ( 'NONE',  ( 0.5997462898726536595, 17.44942740672405534, 45.90282249842351803 ) ) ;
#23442=ORIENTED_EDGE ( 'NONE', *, *, #15010, .T. ) ;
#23445=CARTESIAN_POINT ( 'NONE',  ( 0.6252788684277218456, -43.12018560342360018, -23.49667901427708472 ) ) ;
#23448=FACE_OUTER_BOUND ( 'NONE', #38121, .T. ) ;
#23456=CARTESIAN_POINT ( 'NONE',  ( 2.533389852662419894, -28.66318653646339953, -33.40467436317140937 ) ) ;
#23466=CARTESIAN_POINT ( 'NONE',  ( 4.694002226626920127, 45.16857381419794848, -6.171281150416436212 ) ) ;
#23482=CARTESIAN_POINT ( 'NONE',  ( 0.6039202388192953519, 22.55960655125616299, -43.61912269981493750 ) ) ;
#23489=CARTESIAN_POINT ( 'NONE',  ( -6.077587904424778920, -12.95044751835525609, -14.25068175450762809 ) ) ;
#23490=ORIENTED_EDGE ( 'NONE', *, *, #50720, .F. ) ;
#23491=CARTESIAN_POINT ( 'NONE',  ( 5.901764892641288895, -48.87142464753282667, -3.094401454271686447 ) ) ;
#23497=ADVANCED_FACE ( 'NONE', ( #29624 ), #76, .F. ) ;
#23500=( BOUNDED_SURFACE ( )  B_SPLINE_SURFACE ( 3, 1, ( 
 ( #16464, #26167 ),
 ( #18636, #43070 ),
 ( #42454, #32117 ),
 ( #57122, #57422 ) ),
 .UNSPECIFIED., .F., .F., .F. ) 
 B_SPLINE_SURFACE_WITH_KNOTS ( ( 4, 4 ),
 ( 2, 2 ),
 ( 0.000000000000000000, 1.000000000000000000 ),
 ( 0.000000000000000000, 1.000000000000000000 ),
 .UNSPECIFIED. ) 
 GEOMETRIC_REPRESENTATION_ITEM ( )  RATIONAL_B_SPLINE_SURFACE ( (
 ( 1.000000000000000000, 1.000000000000000000),
 ( 0.7211978278499970862, 0.9934217856018976445),
 ( 0.7211978278499970862, 0.9934217856018976445),
 ( 1.000000000000000000, 1.000000000000000000) ) ) 
 REPRESENTATION_ITEM ( '' )  SURFACE ( )  );
#23501=ORIENTED_EDGE ( 'NONE', *, *, #18436, .T. ) ;
#23502=DIRECTION ( 'NONE',  ( -0.1011922191286467598, 0.7895409829358833731, 0.6052975888374734215 ) ) ;
#23513=ORIENTED_EDGE ( 'NONE', *, *, #605, .T. ) ;
#23515=VECTOR ( 'NONE', #5406, 1000.000000000000114 ) ;
#23519=CARTESIAN_POINT ( 'NONE',  ( 0.1129192098497455998, -0.9297496242496093855, -44.11448008785053787 ) ) ;
#23530=EDGE_CURVE ( 'NONE', #61531, #19087, #32826, .T. ) ;
#23531=B_SPLINE_CURVE_WITH_KNOTS ( 'NONE', 3,
 ( #32319, #27610, #46126, #22300, #40821, #46427, #45819, #3172, #16675, #50486, #41735, #60486, #17602, #17921, #2863, #55795, #37041, #42969, #23839 ),
 .UNSPECIFIED., .F., .F.,
 ( 4, 3, 3, 3, 3, 3, 4 ),
 ( 1.355252715606880543E-20, 0.0002612768053151702996, 0.0003919133833142921181, 0.0005225499612322598861, 0.0006531865391693344406, 0.0008112755173415187732, 0.0009693688056799728983 ),
 .UNSPECIFIED. ) ;
#23538=CARTESIAN_POINT ( 'NONE',  ( 0.7044674535453004927, 33.63530026269737050, 35.78364569253805882 ) ) ;
#23540=DIRECTION ( 'NONE',  ( 0.000000000000000000, 0.000000000000000000, 1.000000000000000000 ) ) ;
#23547=CARTESIAN_POINT ( 'NONE',  ( -6.078726893082806448, 9.979253153318763836, 16.46841060244423360 ) ) ;
#23549=VECTOR ( 'NONE', #37411, 1000.000000000000114 ) ;
#23550=CARTESIAN_POINT ( 'NONE',  ( 0.8744876279028263033, -45.16590161814997373, -19.24555484778471026 ) ) ;
#23558=VECTOR ( 'NONE', #15778, 1000.000000000000114 ) ;
#23560=CARTESIAN_POINT ( 'NONE',  ( 0.5997462898726536595, -42.52950339524468859, -24.55184251941555118 ) ) ;
#23566=CARTESIAN_POINT ( 'NONE',  ( 0.1139756605157203478, 37.19545956418076571, 23.73716511094820092 ) ) ;
#23568=EDGE_LOOP ( 'NONE', ( #52271, #9737, #47648, #49736 ) ) ;
#23569=CARTESIAN_POINT ( 'NONE',  ( 0.6008122571543325074, -39.09350205120696131, 29.71956675050282470 ) ) ;
#23576=B_SPLINE_CURVE_WITH_KNOTS ( 'NONE', 3,
 ( #31978, #41096, #51059, #8153 ),
 .UNSPECIFIED., .F., .F.,
 ( 4, 4 ),
 ( 0.000000000000000000, 0.004442905043737213969 ),
 .UNSPECIFIED. ) ;
#23578=ORIENTED_EDGE ( 'NONE', *, *, #56692, .T. ) ;
#23581=CARTESIAN_POINT ( 'NONE',  ( 0.5997462898726536595, 37.72933316221968170, 31.43324751403423534 ) ) ;
#23582=ORIENTED_EDGE ( 'NONE', *, *, #51323, .T. ) ;
#23587=CARTESIAN_POINT ( 'NONE',  ( 4.975610109902397937, -23.13264022976521161, -43.09675583078175265 ) ) ;
#23589=CARTESIAN_POINT ( 'NONE',  ( 0.6000166863083090663, 33.40185771989303731, -36.00193581695955913 ) ) ;
#23590=CARTESIAN_POINT ( 'NONE',  ( 0.8753041380234471980, 21.91949880997691480, 43.93943445007457171 ) ) ;
#23601=CARTESIAN_POINT ( 'NONE',  ( 1.296416391601052931, 34.26782981329887434, 27.71323174880446416 ) ) ;
#23611=EDGE_CURVE ( 'NONE', #10962, #16304, #16385, .T. ) ;
#23624=CARTESIAN_POINT ( 'NONE',  ( 2.648799415243696664, -43.38879977521501985, 22.84577679475794199 ) ) ;
#23626=CARTESIAN_POINT ( 'NONE',  ( 0.1129192098497455998, -17.41650932123162931, -40.54154647825617275 ) ) ;
#23629=( BOUNDED_SURFACE ( )  B_SPLINE_SURFACE ( 3, 1, ( 
 ( #7950, #2934 ),
 ( #12063, #46187 ),
 ( #36172, #22361 ),
 ( #31138, #50246 ) ),
 .UNSPECIFIED., .F., .F., .F. ) 
 B_SPLINE_SURFACE_WITH_KNOTS ( ( 4, 4 ),
 ( 2, 2 ),
 ( 0.000000000000000000, 1.000000000000000000 ),
 ( 0.000000000000000000, 1.000000000000000000 ),
 .UNSPECIFIED. ) 
 GEOMETRIC_REPRESENTATION_ITEM ( )  RATIONAL_B_SPLINE_SURFACE ( (
 ( 1.000000000000000000, 1.000000000000000000),
 ( 0.9953485035131437453, 0.8621029689291515030),
 ( 0.9953485035131437453, 0.8621029689291515030),
 ( 1.000000000000000000, 1.000000000000000000) ) ) 
 REPRESENTATION_ITEM ( '' )  SURFACE ( )  );
#23631=DIRECTION ( 'NONE',  ( -1.000000000000000000, -0.000000000000000000, -0.000000000000000000 ) ) ;
#23638=CARTESIAN_POINT ( 'NONE',  ( 0.3676999524040323597, 19.66859742988730986, 39.48540057367873857 ) ) ;
#23644=DIRECTION ( 'NONE',  ( 0.000000000000000000, 0.000000000000000000, -1.000000000000000000 ) ) ;
#23646=CARTESIAN_POINT ( 'NONE',  ( 0.6029443449137436017, 48.21014671922638684, -9.344586202395333885 ) ) ;
#23648=AXIS2_PLACEMENT_3D ( 'NONE', #16000, #49493, #15694 ) ;
#23652=ORIENTED_EDGE ( 'NONE', *, *, #58391, .F. ) ;
#23653=CARTESIAN_POINT ( 'NONE',  ( 0.3676999524040366896, 42.11837424242170158, 13.11461530118771179 ) ) ;
#23655=AXIS2_PLACEMENT_3D ( 'NONE', #28769, #61339, #37269 ) ;
#23656=CARTESIAN_POINT ( 'NONE',  ( 3.678748215320120085, -48.30244781633944484, 8.092363637979213209 ) ) ;
#23657=EDGE_CURVE ( 'NONE', #8619, #52291, #35045, .T. ) ;
#23662=ORIENTED_EDGE ( 'NONE', *, *, #404, .T. ) ;
#23667=CARTESIAN_POINT ( 'NONE',  ( 2.533389852662419894, -40.17945474350555912, 17.97392411935152978 ) ) ;
#23668=CARTESIAN_POINT ( 'NONE',  ( 4.834790513006553603, 29.09828987666518429, 37.22739404226336291 ) ) ;
#23670=CARTESIAN_POINT ( 'NONE',  ( 0.8744876279028306332, 48.01195819035234535, -10.25679877482985169 ) ) ;
#23672=VERTEX_POINT ( 'NONE', #50891 ) ;
#23681=ORIENTED_EDGE ( 'NONE', *, *, #53944, .F. ) ;
#23682=VERTEX_POINT ( 'NONE', #3885 ) ;
#23683=CARTESIAN_POINT ( 'NONE',  ( 0.1156495703730067576, -44.12396594495942281, 0.1363177139302391427 ) ) ;
#23688=CARTESIAN_POINT ( 'NONE',  ( 0.6008122571543325074, 4.281854884450230436, -48.92055058167095893 ) ) ;
#23692=CARTESIAN_POINT ( 'NONE',  ( 4.694002226626920127, -15.42074131724428376, 42.90088004543460443 ) ) ;
#23694=EDGE_CURVE ( 'NONE', #29824, #32705, #42591, .T. ) ;
#23697=CIRCLE ( 'NONE', #3681, 43.92652462719577500 ) ;
#23699=CARTESIAN_POINT ( 'NONE',  ( 0.1129192098497447394, -27.13044910148925837, 34.79785222304180081 ) ) ;
#23704=CARTESIAN_POINT ( 'NONE',  ( 4.553261556744873317, -43.07273893850290136, 8.618510669437750238 ) ) ;
#23707=CARTESIAN_POINT ( 'NONE',  ( 0.3676999524040323597, -7.853951980432424484, 43.40813312746703190 ) ) ;
#23708=B_SPLINE_CURVE_WITH_KNOTS ( 'NONE', 3,
 ( #49350, #2342, #20855, #30857 ),
 .UNSPECIFIED., .F., .F.,
 ( 4, 4 ),
 ( 2.183987964099527011E-17, 0.004559932413162188537 ),
 .UNSPECIFIED. ) ;
#23711=VECTOR ( 'NONE', #4132, 1000.000000000000114 ) ;
#23713=CARTESIAN_POINT ( 'NONE',  ( 3.559346040607745287, -15.90101677405797531, 40.99497465657363904 ) ) ;
#23718=CARTESIAN_POINT ( 'NONE',  ( 0.2285344041767119194, 19.73012571914551572, -39.46166886235511839 ) ) ;
#23725=CARTESIAN_POINT ( 'NONE',  ( 0.8753041380234530822, -29.91468680897855492, 38.93905290314216927 ) ) ;
#23738=CARTESIAN_POINT ( 'NONE',  ( -2.601141883200662974, -9.652501068366079906, -11.38528219213649173 ) ) ;
#23739=AXIS2_PLACEMENT_3D ( 'NONE', #43596, #38899, #15077 ) ;
#23744=B_SPLINE_CURVE_WITH_KNOTS ( 'NONE', 3,
 ( #18056, #50926, #3303, #46565 ),
 .UNSPECIFIED., .F., .F.,
 ( 4, 4 ),
 ( 0.002320612883253031153, 0.004444103432399267896 ),
 .UNSPECIFIED. ) ;
#23754=CARTESIAN_POINT ( 'NONE',  ( 4.975610109902397937, -44.31543648230385202, -20.70245146161840211 ) ) ;
#23759=VERTEX_POINT ( 'NONE', #18633 ) ;
#23762=ADVANCED_FACE ( 'NONE', ( #52122 ), #4094, .F. ) ;
#23769=CARTESIAN_POINT ( 'NONE',  ( 2.359973842542475442, -28.61238109696261844, -33.45844501160621576 ) ) ;
#23776=ORIENTED_EDGE ( 'NONE', *, *, #38954, .T. ) ;
#23777=CARTESIAN_POINT ( 'NONE',  ( 0.7948884756798503259, -49.09120184641267315, -0.8674940201074746726 ) ) ;
#23780=CARTESIAN_POINT ( 'NONE',  ( 0.5997462898726536595, 37.72933316222010802, -31.43324751403371664 ) ) ;
#23789=CARTESIAN_POINT ( 'NONE',  ( 0.7242003506639987931, -34.69774349674525382, 34.74303196844081754 ) ) ;
#23793=CARTESIAN_POINT ( 'NONE',  ( 0.8744876279028263033, -48.79802643035343834, 5.394688766001209501 ) ) ;
#23798=CARTESIAN_POINT ( 'NONE',  ( 2.299652685299199195, -31.56856304606662889, 37.51942899438463286 ) ) ;
#23799=CARTESIAN_POINT ( 'NONE',  ( -6.063463321072276813, 9.995861580987984496, 16.45913739335079384 ) ) ;
#23805=VECTOR ( 'NONE', #13091, 1000.000000000000227 ) ;
#23809=CARTESIAN_POINT ( 'NONE',  ( -6.057079549204054558, -12.95277456599821164, -14.24980217905386404 ) ) ;
#23810=VERTEX_POINT ( 'NONE', #43374 ) ;
#23813=CARTESIAN_POINT ( 'NONE',  ( 0.7242486021783853811, -42.37565498843926548, -24.80555031993310777 ) ) ;
#23820=CARTESIAN_POINT ( 'NONE',  ( 0.1158816050234199035, 4.231281718317980278, -43.92081848423808310 ) ) ;
#23821=CARTESIAN_POINT ( 'NONE',  ( 4.694002226626920127, 32.98704702821290624, 31.46648216443339408 ) ) ;
#23822=CARTESIAN_POINT ( 'NONE',  ( -6.063463321072276813, -19.21612852159696061, 1.249342675544900638 ) ) ;
#23826=CIRCLE ( 'NONE', #50821, 48.91267123290010943 ) ;
#23827=ORIENTED_EDGE ( 'NONE', *, *, #32836, .T. ) ;
#23831=CARTESIAN_POINT ( 'NONE',  ( 3.678834586032787346, 47.68471048368242293, 11.17053068192113763 ) ) ;
#23835=CARTESIAN_POINT ( 'NONE',  ( 0.2940133293163008643, -43.84964716027407405, 4.842416080585272731 ) ) ;
#23839=CARTESIAN_POINT ( 'NONE',  ( 0.1129192098497455998, 14.78321943369591196, 41.57412910645692961 ) ) ;
#23846=CARTESIAN_POINT ( 'NONE',  ( 0.1139756605157203895, -17.49650554526767365, 40.50712916758530469 ) ) ;
#23856=CARTESIAN_POINT ( 'NONE',  ( -6.063463321072278589, 15.44190279603010119, -11.50513322467096344 ) ) ;
#23864=B_SPLINE_CURVE_WITH_KNOTS ( 'NONE', 3,
 ( #17792, #2433, #11557, #6812 ),
 .UNSPECIFIED., .F., .F.,
 ( 4, 4 ),
 ( 0.000000000000000000, 0.005013413432710140706 ),
 .UNSPECIFIED. ) ;
#23870=AXIS2_PLACEMENT_3D ( 'NONE', #20155, #19541, #57709 ) ;
#23874=CARTESIAN_POINT ( 'NONE',  ( 0.1152809850208375286, -43.73310776251593524, -5.861788798815898538 ) ) ;
#23878=( BOUNDED_SURFACE ( )  B_SPLINE_SURFACE ( 3, 1, ( 
 ( #28484, #51361 ),
 ( #28183, #4347 ),
 ( #32282, #8446 ),
 ( #22879, #47611 ) ),
 .UNSPECIFIED., .F., .F., .F. ) 
 B_SPLINE_SURFACE_WITH_KNOTS ( ( 4, 4 ),
 ( 2, 2 ),
 ( 0.000000000000000000, 1.000000000000000000 ),
 ( 0.000000000000000000, 1.000000000000000000 ),
 .UNSPECIFIED. ) 
 GEOMETRIC_REPRESENTATION_ITEM ( )  RATIONAL_B_SPLINE_SURFACE ( (
 ( 1.000000000000000000, 1.000000000000000000),
 ( 0.9953485035131437453, 0.8621029689291523912),
 ( 0.9953485035131437453, 0.8621029689291523912),
 ( 1.000000000000000000, 1.000000000000000000) ) ) 
 REPRESENTATION_ITEM ( '' )  SURFACE ( )  );
#23888=EDGE_LOOP ( 'NONE', ( #30800, #45118 ) ) ;
#23897=CARTESIAN_POINT ( 'NONE',  ( 4.694002226626921015, -21.39119943673082247, 40.25793534328533241 ) ) ;
#23903=CARTESIAN_POINT ( 'NONE',  ( -6.078075953587585900, -12.94192373113803463, 14.25839347137474888 ) ) ;
#23906=ORIENTED_EDGE ( 'NONE', *, *, #8550, .F. ) ;
#23915=CARTESIAN_POINT ( 'NONE',  ( 3.050102900204245682, 34.64366268476908317, 27.11534408710312505 ) ) ;
#23926=ORIENTED_EDGE ( 'NONE', *, *, #21888, .F. ) ;
#23927=CARTESIAN_POINT ( 'NONE',  ( 0.7948878604505656975, 41.61600051860138194, 26.05392769112145857 ) ) ;
#23928=CARTESIAN_POINT ( 'NONE',  ( 0.5980271706414734822, -24.85837266090920394, 42.35694218771019592 ) ) ;
#23931=EDGE_LOOP ( 'NONE', ( #49947, #34729, #7480, #20377 ) ) ;
#23933=DIRECTION ( 'NONE',  ( 0.000000000000000000, 0.000000000000000000, -1.000000000000000000 ) ) ;
#23937=CARTESIAN_POINT ( 'NONE',  ( 4.975610109902397937, -48.77192499014914517, 3.707929326866768349 ) ) ;
#23940=CARTESIAN_POINT ( 'NONE',  ( 0.6029443449137436017, -42.80956090170459305, 24.05994666217235078 ) ) ;
#23946=CARTESIAN_POINT ( 'NONE',  ( -2.739355103387248747, -13.73625580088958920, 5.844898931850249113 ) ) ;
#23951=CARTESIAN_POINT ( 'NONE',  ( 2.299746137290199499, -47.74024417197872339, -11.18706503449364575 ) ) ;
#23952=DIRECTION ( 'NONE',  ( 1.000000000000000000, 0.000000000000000000, 0.000000000000000000 ) ) ;
#23957=CARTESIAN_POINT ( 'NONE',  ( 0.6021448801613057400, 48.25111984599001858, -9.130748722577767040 ) ) ;
#23967=EDGE_CURVE ( 'NONE', #16223, #34962, #29035, .T. ) ;
#23975=EDGE_CURVE ( 'NONE', #14042, #60263, #32272, .T. ) ;
#23976=VECTOR ( 'NONE', #21936, 1000.000000000000114 ) ;
#23981=EDGE_CURVE ( 'NONE', #35321, #8818, #23054, .T. ) ;
#23983=CARTESIAN_POINT ( 'NONE',  ( 4.226256110419178924, 43.93923658072332472, 0.4132053852653991832 ) ) ;
#23984=ORIENTED_EDGE ( 'NONE', *, *, #20400, .T. ) ;
#23994=EDGE_CURVE ( 'NONE', #44906, #8488, #33205, .T. ) ;
#23998=EDGE_LOOP ( 'NONE', ( #10968, #34328, #7459, #2959 ) ) ;
#24003=CIRCLE ( 'NONE', #58999, 10.00000000000000000 ) ;
#24004=VERTEX_POINT ( 'NONE', #4337 ) ;
#24007=CARTESIAN_POINT ( 'NONE',  ( 4.975610109902397937, 0.000000000000000000, 0.000000000000000000 ) ) ;
#24014=CARTESIAN_POINT ( 'NONE',  ( -6.072942160501519915, 13.82262479916552778, -13.40668512162922532 ) ) ;
#24017=CARTESIAN_POINT ( 'NONE',  ( 0.6039202388192953519, -13.80541670804789511, 47.12721275830073608 ) ) ;
#24018=CARTESIAN_POINT ( 'NONE',  ( 0.7413678028165011646, -16.99214960714165912, 40.69094424437406587 ) ) ;
#24020=ORIENTED_EDGE ( 'NONE', *, *, #53999, .T. ) ;
#24032=CARTESIAN_POINT ( 'NONE',  ( 4.694002226626921015, 42.38457918174925254, -16.78785927484989671 ) ) ;
#24033=EDGE_LOOP ( 'NONE', ( #17933, #27290, #6395, #3686 ) ) ;
#24037=CARTESIAN_POINT ( 'NONE',  ( -2.601141883200665639, 1.878577531912080545, -14.80764579283228777 ) ) ;
#24038=EDGE_CURVE ( 'NONE', #45127, #34420, #55977, .T. ) ;
#24039=CARTESIAN_POINT ( 'NONE',  ( 0.8753041380234524160, -6.957149426674410719, 48.60798699522440813 ) ) ;
#24048=FACE_OUTER_BOUND ( 'NONE', #55873, .T. ) ;
#24054=FACE_OUTER_BOUND ( 'NONE', #41942, .T. ) ;
#24071=CARTESIAN_POINT ( 'NONE',  ( 0.5997462898726536595, -14.47257175146309649, 46.92649887902422279 ) ) ;
#24074=VERTEX_POINT ( 'NONE', #1501 ) ;
#24078=CARTESIAN_POINT ( 'NONE',  ( 0.1365634738349412458, -43.67502418020411881, -6.273346991983733467 ) ) ;
#24079=VERTEX_POINT ( 'NONE', #15330 ) ;
#24090=CARTESIAN_POINT ( 'NONE',  ( 3.678834586032787346, 6.540082731167337293, -48.53699297955983383 ) ) ;
#24091=CARTESIAN_POINT ( 'NONE',  ( 1.830465331921976579, -37.76032919508905650, -22.68333297725216013 ) ) ;
#24094=CARTESIAN_POINT ( 'NONE',  ( 0.2940133293163014194, -42.87040773915203573, 10.41002833122450433 ) ) ;
#24099=CARTESIAN_POINT ( 'NONE',  ( 0.08486401232817714080, 5.403818426594913263E-15, -44.12552607296456131 ) ) ;
#24100=AXIS2_PLACEMENT_3D ( 'NONE', #9683, #28795, #17948 ) ;
#24102=CARTESIAN_POINT ( 'NONE',  ( 3.678834586032787346, -31.95978921216147128, 37.11043307673141101 ) ) ;
#24103=CARTESIAN_POINT ( 'NONE',  ( 0.8744876279028263033, 48.92939099258497038, 4.032957658374010101 ) ) ;
#24104=CARTESIAN_POINT ( 'NONE',  ( -6.078726893082806448, 3.076629396955338436, -19.00863995194055178 ) ) ;
#24109=ADVANCED_FACE ( 'NONE', ( #20036 ), #30449, .F. ) ;
#24110=ORIENTED_EDGE ( 'NONE', *, *, #13225, .T. ) ;
#24112=EDGE_CURVE ( 'NONE', #48331, #51387, #9988, .T. ) ;
#24114=CARTESIAN_POINT ( 'NONE',  ( 1.834102595619085507, 40.23352532279152882, 17.92933866482468730 ) ) ;
#24115=CARTESIAN_POINT ( 'NONE',  ( 4.553261556744875094, 17.98701270972463817, -40.07501640179128799 ) ) ;
#24120=B_SPLINE_CURVE_WITH_KNOTS ( 'NONE', 3,
 ( #28410, #57204, #193, #48152, #47850, #4275 ),
 .UNSPECIFIED., .F., .F.,
 ( 4, 2, 4 ),
 ( 3.252606517456513302E-18, 0.0002447193893791697623, 0.0004894387787583362719 ),
 .UNSPECIFIED. ) ;
#24122=DIRECTION ( 'NONE',  ( -1.000000000000000000, -0.000000000000000000, -0.000000000000000000 ) ) ;
#24124=VERTEX_POINT ( 'NONE', #53206 ) ;
#24126=EDGE_LOOP ( 'NONE', ( #41624, #25741, #15284, #16749 ) ) ;
#24129=CARTESIAN_POINT ( 'NONE',  ( -6.057079549204054558, -8.899553672604941568, 17.07715361318045666 ) ) ;
#24134=CARTESIAN_POINT ( 'NONE',  ( 0.3676999524040323597, -43.84864779214683495, 4.821480075982420566 ) ) ;
#24144=CARTESIAN_POINT ( 'NONE',  ( 0.1158403557922069033, -17.89533752146796530, 40.33233444987482841 ) ) ;
#24151=CARTESIAN_POINT ( 'NONE',  ( 0.1152809850208375703, 25.06245401136728290, 36.31554324828218938 ) ) ;
#24154=CARTESIAN_POINT ( 'NONE',  ( 0.1155031312995260795, 25.38218459480881961, -36.09274633117931330 ) ) ;
#24161=CARTESIAN_POINT ( 'NONE',  ( 4.975610109902397937, 0.9924324126411095959, -48.90260202733707473 ) ) ;
#24166=LINE ( 'NONE', #34826, #49628 ) ;
#24176=EDGE_CURVE ( 'NONE', #18514, #2406, #57397, .T. ) ;
#24177=CARTESIAN_POINT ( 'NONE',  ( 0.5987334308729317378, -45.74238939486933475, -17.86607732597938991 ) ) ;
#24180=DIRECTION ( 'NONE',  ( -1.000000000000000000, -0.000000000000000000, -0.000000000000000000 ) ) ;
#24182=CARTESIAN_POINT ( 'NONE',  ( -2.739355103387247858, -9.511660422587072006, 11.50547187021930640 ) ) ;
#24183=CARTESIAN_POINT ( 'NONE',  ( 4.226256110419179812, 18.16371129757565939, -40.01133391784768634 ) ) ;
#24185=EDGE_CURVE ( 'NONE', #55289, #30839, #47670, .T. ) ;
#24186=ORIENTED_EDGE ( 'NONE', *, *, #29414, .F. ) ;
#24188=B_SPLINE_CURVE_WITH_KNOTS ( 'NONE', 3,
 ( #53236, #6218, #57299, #931 ),
 .UNSPECIFIED., .F., .F.,
 ( 4, 4 ),
 ( 2.168573744943531741E-17, 0.004559932413162186803 ),
 .UNSPECIFIED. ) ;
#24194=CARTESIAN_POINT ( 'NONE',  ( 0.7242486021783879346, -31.25073749153447977, 37.87351143753605953 ) ) ;
#24197=CARTESIAN_POINT ( 'NONE',  ( 3.678748215320120529, 47.68472573843015994, -11.17048546618184446 ) ) ;
#24201=EDGE_CURVE ( 'NONE', #14207, #44808, #55358, .T. ) ;
#24204=CARTESIAN_POINT ( 'NONE',  ( -6.057079549204054558, -8.914624657271952302, -17.06929109013310608 ) ) ;
#24209=ORIENTED_EDGE ( 'NONE', *, *, #41898, .F. ) ;
#24211=CARTESIAN_POINT ( 'NONE',  ( -6.079354080745853928, -16.13757513887036410, -10.50579001719886030 ) ) ;
#24213=CARTESIAN_POINT ( 'NONE',  ( 4.060580049360325461, 34.91776364945923206, 26.68740294745280295 ) ) ;
#24214=CARTESIAN_POINT ( 'NONE',  ( 0.8753041380234465318, 36.80657072176691003, 32.50253343320412114 ) ) ;
#24219=VECTOR ( 'NONE', #43002, 1000.000000000000114 ) ;
#24220=FACE_OUTER_BOUND ( 'NONE', #40453, .T. ) ;
#24221=AXIS2_PLACEMENT_3D ( 'NONE', #59702, #35931, #30582 ) ;
#24227=CARTESIAN_POINT ( 'NONE',  ( 0.6028777368367059797, -13.88892840780163063, -47.10241498048729625 ) ) ;
#24231=ORIENTED_EDGE ( 'NONE', *, *, #24589, .F. ) ;
#24241=CARTESIAN_POINT ( 'NONE',  ( 0.5980271706414711508, 16.30306832862478217, 46.32773689609556556 ) ) ;
#24242=CARTESIAN_POINT ( 'NONE',  ( 4.335381028904216727, -48.26758661664255357, 8.366416787923856901 ) ) ;
#24246=CARTESIAN_POINT ( 'NONE',  ( 4.975610109902397937, -47.89734868211972696, -9.914302615979444511 ) ) ;
#24248=CARTESIAN_POINT ( 'NONE',  ( 0.7044674535452954967, 23.45856740197708845, -43.14508475200626947 ) ) ;
#24254=LINE ( 'NONE', #34911, #25862 ) ;
#24258=EDGE_CURVE ( 'NONE', #48887, #26359, #9606, .T. ) ;
#24260=CARTESIAN_POINT ( 'NONE',  ( -6.078075953587585900, 3.068021059656765193, -19.01006104736748625 ) ) ;
#24262=ORIENTED_EDGE ( 'NONE', *, *, #50786, .T. ) ;
#24271=CARTESIAN_POINT ( 'NONE',  ( 0.3676999524040323597, -43.63756228305270213, -6.458617600968101335 ) ) ;
#24279=CARTESIAN_POINT ( 'NONE',  ( 3.678834586032788234, 24.27644425923901039, -42.53547488575171798 ) ) ;
#24280=B_SPLINE_CURVE_WITH_KNOTS ( 'NONE', 3,
 ( #61668, #10313, #53207, #47917, #19715, #43536 ),
 .UNSPECIFIED., .F., .F.,
 ( 4, 2, 4 ),
 ( 2.224240575184740080E-17, 0.0002293755540694317251, 0.0004587511081388411698 ),
 .UNSPECIFIED. ) ;
#24281=CARTESIAN_POINT ( 'NONE',  ( -6.057079549204054558, -16.13440658954566587, -10.51247616420431541 ) ) ;
#24285=CARTESIAN_POINT ( 'NONE',  ( 0.6252788684277230669, 48.06490558434089877, -10.06027744856285722 ) ) ;
#24291=CARTESIAN_POINT ( 'NONE',  ( 1.296416391601052487, 44.03828134713403841, 1.713811561060474942 ) ) ;
#24292=VERTEX_POINT ( 'NONE', #27798 ) ;
#24293=CARTESIAN_POINT ( 'NONE',  ( 0.1157506346131639274, 41.84695283361572393, -13.99189759625102703 ) ) ;
#24311=DIRECTION ( 'NONE',  ( -1.000000000000000000, -0.000000000000000000, -0.000000000000000000 ) ) ;
#24314=EDGE_CURVE ( 'NONE', #55332, #56636, #17058, .T. ) ;
#24337=CARTESIAN_POINT ( 'NONE',  ( 0.1368894036331283204, 39.47291701970388544, -19.71674790321427295 ) ) ;
#24343=ORIENTED_EDGE ( 'NONE', *, *, #57768, .F. ) ;
#24350=CARTESIAN_POINT ( 'NONE',  ( 0.8744876279028306332, -35.88078294188929362, -33.50999053799506555 ) ) ;
#24353=EDGE_LOOP ( 'NONE', ( #52789, #16513, #9492, #3224 ) ) ;
#24356=CARTESIAN_POINT ( 'NONE',  ( -6.063463321072278589, 0.6016212027209763002, 19.24729862624639765 ) ) ;
#24357=ORIENTED_EDGE ( 'NONE', *, *, #40061, .F. ) ;
#24365=B_SPLINE_CURVE_WITH_KNOTS ( 'NONE', 3,
 ( #6566, #45766, #45162, #21630, #2812, #58902 ),
 .UNSPECIFIED., .F., .F.,
 ( 4, 2, 4 ),
 ( 1.870693080156664505E-17, 0.0002293755540694311559, 0.0004587511081388436092 ),
 .UNSPECIFIED. ) ;
#24366=CARTESIAN_POINT ( 'NONE',  ( 4.553261556744873317, -4.442710778081946366, -43.70128015019640344 ) ) ;
#24373=CARTESIAN_POINT ( 'NONE',  ( 0.7948878604505652534, 28.79738884442139124, 39.76693404125605724 ) ) ;
#24380=CARTESIAN_POINT ( 'NONE',  ( 0.2285344041767080614, 36.55576111592239386, -24.70177118206449762 ) ) ;
#24388=FACE_OUTER_BOUND ( 'NONE', #2862, .T. ) ;
#24393=CARTESIAN_POINT ( 'NONE',  ( -2.601141883200662974, -8.951945844433506494, 11.94395634066527734 ) ) ;
#24398=EDGE_CURVE ( 'NONE', #988, #1157, #41701, .T. ) ;
#24406=ORIENTED_EDGE ( 'NONE', *, *, #58180, .F. ) ;
#24408=CARTESIAN_POINT ( 'NONE',  ( 4.975610109902397937, -46.23629923292363486, -15.95788333023269878 ) ) ;
#24410=CARTESIAN_POINT ( 'NONE',  ( 0.6253024248130496510, -47.66998618349910544, 11.79053199319904977 ) ) ;
#24412=CARTESIAN_POINT ( 'NONE',  ( 0.8744876279028263033, -6.955970791787605911, -48.60004650947661275 ) ) ;
#24413=FACE_OUTER_BOUND ( 'NONE', #6523, .T. ) ;
#24416=ORIENTED_EDGE ( 'NONE', *, *, #24775, .T. ) ;
#24417=CARTESIAN_POINT ( 'NONE',  ( 3.240649175237394708, 23.64729060054057896, 37.09542511754295191 ) ) ;
#24423=CARTESIAN_POINT ( 'NONE',  ( 0.7948884756798489937, 32.36187196966092472, 36.92435357889731051 ) ) ;
#24434=CARTESIAN_POINT ( 'NONE',  ( 0.7948878604505683620, -31.28609773251230664, -37.84017357214558075 ) ) ;
#24435=ORIENTED_EDGE ( 'NONE', *, *, #35797, .F. ) ;
#24438=CARTESIAN_POINT ( 'NONE',  ( 0.1140933569871965259, 29.94445442560179771, -32.40801751475956394 ) ) ;
#24449=CARTESIAN_POINT ( 'NONE',  ( 2.009741617377216460, -36.09682931428869779, -25.22940726767382813 ) ) ;
#24454=EDGE_CURVE ( 'NONE', #19345, #11856, #52516, .T. ) ;
#24464=ORIENTED_EDGE ( 'NONE', *, *, #46010, .T. ) ;
#24467=CARTESIAN_POINT ( 'NONE',  ( 0.1368894036331274877, -0.7768805341913491702, 44.11641171445076282 ) ) ;
#24468=CARTESIAN_POINT ( 'NONE',  ( 5.901764892641307547, -37.31543133725939043, 31.71040919877821906 ) ) ;
#24469=ADVANCED_FACE ( 'NONE', ( #11167 ), #10910, .F. ) ;
#24472=CARTESIAN_POINT ( 'NONE',  ( 0.1157991065609915854, -40.92991374543836969, 16.48285552714316893 ) ) ;
#24473=EDGE_CURVE ( 'NONE', #50534, #54562, #604, .T. ) ;
#24480=DIRECTION ( 'NONE',  ( 0.000000000000000000, 0.000000000000000000, 1.000000000000000000 ) ) ;
#24483=DIRECTION ( 'NONE',  ( 0.1011922191286468153, 0.8906890386588646180, -0.4432078194264711390 ) ) ;
#24484=CARTESIAN_POINT ( 'NONE',  ( 0.2940133293162988104, 34.10816071058727772, -27.97988424777333449 ) ) ;
#24486=CARTESIAN_POINT ( 'NONE',  ( 0.1156495703730067853, 39.81346568422283383, 19.02185331250035460 ) ) ;
#24489=CARTESIAN_POINT ( 'NONE',  ( 0.5997462898726536595, -39.66574928371259290, 28.95133786038155321 ) ) ;
#24491=CARTESIAN_POINT ( 'NONE',  ( 4.553261556744875094, -3.993093339916522488, -43.74465420371214464 ) ) ;
#24512=CARTESIAN_POINT ( 'NONE',  ( 0.8744876279028306332, -13.11369837310865805, 47.31153099782990523 ) ) ;
#24517=( BOUNDED_SURFACE ( )  B_SPLINE_SURFACE ( 3, 1, ( 
 ( #12567, #56370 ),
 ( #46387, #2515 ),
 ( #17566, #56064 ),
 ( #26641, #40782 ) ),
 .UNSPECIFIED., .F., .F., .F. ) 
 B_SPLINE_SURFACE_WITH_KNOTS ( ( 4, 4 ),
 ( 2, 2 ),
 ( 0.000000000000000000, 1.000000000000000000 ),
 ( 0.000000000000000000, 1.000000000000000000 ),
 .UNSPECIFIED. ) 
 GEOMETRIC_REPRESENTATION_ITEM ( )  RATIONAL_B_SPLINE_SURFACE ( (
 ( 1.000000000000000000, 1.000000000000000000),
 ( 0.9953485035131437453, 0.8621029689291523912),
 ( 0.9953485035131437453, 0.8621029689291523912),
 ( 1.000000000000000000, 1.000000000000000000) ) ) 
 REPRESENTATION_ITEM ( '' )  SURFACE ( )  );
#24519=B_SPLINE_CURVE_WITH_KNOTS ( 'NONE', 3,
 ( #11854, #55029, #56881, #42823, #19312, #61877, #19015, #47507, #41901, #52493, #46909, #14007, #32802, #51560, #27462, #13382 ),
 .UNSPECIFIED., .F., .F.,
 ( 4, 3, 3, 3, 3, 4 ),
 ( 2.221635811791082109E-17, 0.0002612764279487786922, 0.0003919131003184823893, 0.0005225497727000684000, 0.0007837925190632490406, 0.001045051706266717385 ),
 .UNSPECIFIED. ) ;
#24529=CARTESIAN_POINT ( 'NONE',  ( 0.1152339509894530906, -1.637524258439203573, -44.09377739271456420 ) ) ;
#24536=CARTESIAN_POINT ( 'NONE',  ( 0.7044674535452954967, -29.95677278048739467, -38.91522179545113858 ) ) ;
#24537=CARTESIAN_POINT ( 'NONE',  ( 0.1158403557922069033, 37.00056559947007173, -24.03951855805625115 ) ) ;
#24540=CARTESIAN_POINT ( 'NONE',  ( 0.6021447746440204973, -35.45755941940524281, -33.97502934668098362 ) ) ;
#24543=ORIENTED_EDGE ( 'NONE', *, *, #34693, .F. ) ;
#24546=EDGE_CURVE ( 'NONE', #11211, #54760, #53521, .T. ) ;
#24554=CARTESIAN_POINT ( 'NONE',  ( 0.1158516988532803799, -31.66230134112594286, 30.73175609392555430 ) ) ;
#24556=CARTESIAN_POINT ( 'NONE',  ( -2.601141883200665639, 14.73012113219610342, -2.412251831840622973 ) ) ;
#24564=CARTESIAN_POINT ( 'NONE',  ( 0.1135584504625008206, -35.61847315347595355, 26.04374055988050074 ) ) ;
#24581=CARTESIAN_POINT ( 'NONE',  ( 2.009741617377216460, 43.84020297899651553, -4.188159546081140938 ) ) ;
#24582=CARTESIAN_POINT ( 'NONE',  ( 0.7948884756798493267, -34.66113248934519220, -34.77505627826086965 ) ) ;
#24583=ORIENTED_EDGE ( 'NONE', *, *, #12113, .T. ) ;
#24589=EDGE_CURVE ( 'NONE', #29266, #6519, #8709, .T. ) ;
#24595=CIRCLE ( 'NONE', #39639, 43.92652462719577500 ) ;
#24603=EDGE_LOOP ( 'NONE', ( #30864, #61517, #1367, #4523 ) ) ;
#24605=CARTESIAN_POINT ( 'NONE',  ( 0.5549461598389365813, 44.06152503503679441, 1.949283728355195811 ) ) ;
#24608=CARTESIAN_POINT ( 'NONE',  ( 4.335381028904216727, -46.16199858719131299, -16.39593651184625500 ) ) ;
#24614=CARTESIAN_POINT ( 'NONE',  ( 0.6253024248130462093, 28.65516068116093606, -39.87889158131772405 ) ) ;
#24617=ORIENTED_EDGE ( 'NONE', *, *, #53045, .T. ) ;
#24620=ORIENTED_EDGE ( 'NONE', *, *, #17706, .F. ) ;
#24623=( BOUNDED_SURFACE ( )  B_SPLINE_SURFACE ( 3, 1, ( 
 ( #7083, #40346 ),
 ( #59407, #15599 ),
 ( #49100, #1161 ),
 ( #11837, #59721 ) ),
 .UNSPECIFIED., .F., .F., .F. ) 
 B_SPLINE_SURFACE_WITH_KNOTS ( ( 4, 4 ),
 ( 2, 2 ),
 ( 0.000000000000000000, 1.000000000000000000 ),
 ( 0.000000000000000000, 1.000000000000000000 ),
 .UNSPECIFIED. ) 
 GEOMETRIC_REPRESENTATION_ITEM ( )  RATIONAL_B_SPLINE_SURFACE ( (
 ( 1.000000000000000000, 1.000000000000000000),
 ( 0.7211978278499968642, 0.9934217856018975334),
 ( 0.7211978278499968642, 0.9934217856018975334),
 ( 1.000000000000000000, 1.000000000000000000) ) ) 
 REPRESENTATION_ITEM ( '' )  SURFACE ( )  );
#24630=CARTESIAN_POINT ( 'NONE',  ( 0.1140933569871964842, 33.84285616430637589, -28.31273629881038190 ) ) ;
#24636=DIRECTION ( 'NONE',  ( -1.000000000000000000, -0.000000000000000000, -0.000000000000000000 ) ) ;
#24643=CARTESIAN_POINT ( 'NONE',  ( 0.5987334308729321819, 10.33658553128385016, -48.00747760634984473 ) ) ;
#24644=EDGE_CURVE ( 'NONE', #14065, #54546, #46132, .T. ) ;
#24654=ORIENTED_EDGE ( 'NONE', *, *, #35934, .F. ) ;
#24672=CARTESIAN_POINT ( 'NONE',  ( 0.8744876279028263033, -47.25615711918255357, -13.31186180466976587 ) ) ;
#24674=ORIENTED_EDGE ( 'NONE', *, *, #51052, .F. ) ;
#24676=CARTESIAN_POINT ( 'NONE',  ( 2.299652685299200972, -15.18162634922640564, 46.62402756359244904 ) ) ;
#24683=EDGE_LOOP ( 'NONE', ( #2424, #15067, #18337, #43324 ) ) ;
#24689=CARTESIAN_POINT ( 'NONE',  ( 5.901764892641288895, 30.49809846213706521, -38.31262791343699092 ) ) ;
#24695=CARTESIAN_POINT ( 'NONE',  ( 0.2279481005628801182, 10.55626456711305217, -42.83770261652724543 ) ) ;
#24697=DIRECTION ( 'NONE',  ( 0.000000000000000000, 0.000000000000000000, 1.000000000000000000 ) ) ;
#24698=EDGE_CURVE ( 'NONE', #21667, #8183, #59520, .T. ) ;
#24701=CARTESIAN_POINT ( 'NONE',  ( 0.8753041380234524160, -49.09527960836077654, 0.8898584437169385630 ) ) ;
#24705=ORIENTED_EDGE ( 'NONE', *, *, #51226, .F. ) ;
#24708=CARTESIAN_POINT ( 'NONE',  ( 0.6252788684277210685, -13.31242424175264460, 47.26757548236700757 ) ) ;
#24709=CARTESIAN_POINT ( 'NONE',  ( 0.7242486021783849370, -45.81454891244490568, 17.66461350619272963 ) ) ;
#24710=ORIENTED_EDGE ( 'NONE', *, *, #52298, .T. ) ;
#24712=CARTESIAN_POINT ( 'NONE',  ( -6.057079549204054558, 18.62933071312879818, -4.876399110062101805 ) ) ;
#24718=CARTESIAN_POINT ( 'NONE',  ( 0.6000166863083090663, -48.63754814943176541, -6.797969676319537413 ) ) ;
#24722=CIRCLE ( 'NONE', #59714, 48.91267123290010943 ) ;
#24723=CARTESIAN_POINT ( 'NONE',  ( 0.1157991065609915715, 29.60440130558512450, 32.71882927116385531 ) ) ;
#24724=CARTESIAN_POINT ( 'NONE',  ( 0.1119898979215349505, -1.975119484476948628, -44.08015666117655229 ) ) ;
#24734=CARTESIAN_POINT ( 'NONE',  ( 0.6029443449137434907, -47.49030531303264269, -12.49841747015503834 ) ) ;
#24745=EDGE_CURVE ( 'NONE', #11136, #462, #47764, .T. ) ;
#24749=EDGE_LOOP ( 'NONE', ( #51326, #61157, #59729, #39620 ) ) ;
#24752=CARTESIAN_POINT ( 'NONE',  ( 5.901764892641288895, 25.34839938110072666, -41.89809203598525045 ) ) ;
#24754=EDGE_LOOP ( 'NONE', ( #41065, #16009, #28994, #3591 ) ) ;
#24759=CARTESIAN_POINT ( 'NONE',  ( 0.6000166863083106206, -45.71468846346260761, 17.94410043432138480 ) ) ;
#24765=CARTESIAN_POINT ( 'NONE',  ( 3.727782113643637096, -36.46987195321302977, -24.55048300181119814 ) ) ;
#24768=CONICAL_SURFACE ( 'NONE', #37769, 43.92652462719577500, 1.486293639869522343 ) ;
#24774=LINE ( 'NONE', #58885, #36773 ) ;
#24775=EDGE_CURVE ( 'NONE', #36320, #9573, #12509, .T. ) ;
#24776=ORIENTED_EDGE ( 'NONE', *, *, #46503, .T. ) ;
#24785=CARTESIAN_POINT ( 'NONE',  ( 4.694002226626921015, 42.12595566887518572, 17.42666435179430096 ) ) ;
#24793=CARTESIAN_POINT ( 'NONE',  ( 3.894904216938898323, -9.202360858324848181, -42.98186695700143645 ) ) ;
#24794=VECTOR ( 'NONE', #14656, 1000.000000000000114 ) ;
#24806=CIRCLE ( 'NONE', #22802, 10.00000000000000000 ) ;
#24808=CARTESIAN_POINT ( 'NONE',  ( 2.359973842542475442, 19.01300918997274891, -39.70694367707632466 ) ) ;
#24813=CARTESIAN_POINT ( 'NONE',  ( 3.727782113643636652, 26.87588261961982994, 34.79173334748344359 ) ) ;
#24827=CARTESIAN_POINT ( 'NONE',  ( 0.5997462898726536595, -48.76843890605309184, 5.761162800240605897 ) ) ;
#24831=B_SPLINE_CURVE_WITH_KNOTS ( 'NONE', 3,
 ( #19596, #33086, #37476, #28058, #38716, #4526, #23363, #42486, #52158, #9248, #12507, #31599, #23667, #42794, #50687, #7779, #3077, #13667, #22205, #41333, #61244, #59012, #16122, #20818, #58690 ),
 .UNSPECIFIED., .F., .F.,
 ( 4, 3, 3, 3, 3, 3, 3, 3, 4 ),
 ( 4.906538933386797396E-18, 0.0005656085177311379053, 0.001131215744874498538, 0.001696821861372765699, 0.002262427090022497284, 0.002828031679238745492, 0.003393635864401604429, 0.003977030878808131623, 0.004561030005651156398 ),
 .UNSPECIFIED. ) ;
#24838=ORIENTED_EDGE ( 'NONE', *, *, #58733, .T. ) ;
#24839=ORIENTED_EDGE ( 'NONE', *, *, #23004, .T. ) ;
#24840=FACE_OUTER_BOUND ( 'NONE', #49980, .T. ) ;
#24846=CARTESIAN_POINT ( 'NONE',  ( 0.1149546198390367369, -1.140471116448518840, -44.10947620019723558 ) ) ;
#24856=VECTOR ( 'NONE', #29415, 1000.000000000000000 ) ;
#24862=DIRECTION ( 'NONE',  ( 0.1011922191286468015, -0.01903003979493037359, 0.9946848708878722745 ) ) ;
#24865=CARTESIAN_POINT ( 'NONE',  ( 0.1154773475650540393, -31.57118803706288190, 30.82537454718983128 ) ) ;
#24872=ORIENTED_EDGE ( 'NONE', *, *, #30122, .T. ) ;
#24878=CARTESIAN_POINT ( 'NONE',  ( 0.1129192098497455998, -42.80154921430131054, 10.72283417016679508 ) ) ;
#24879=FACE_OUTER_BOUND ( 'NONE', #54377, .T. ) ;
#24883=CARTESIAN_POINT ( 'NONE',  ( 0.6008123274975389894, -30.95730127580523217, 38.12086107208866537 ) ) ;
#24891=CARTESIAN_POINT ( 'NONE',  ( 0.2940135542859018680, -43.84964715722291118, -4.842416016667067780 ) ) ;
#24895=CARTESIAN_POINT ( 'NONE',  ( 0.7044674535453004927, -2.415488218027067369, -49.05066910328012142 ) ) ;
#24896=CARTESIAN_POINT ( 'NONE',  ( -6.077587904424778920, -4.290907484552348272, 18.77189746277512583 ) ) ;
#24898=B_SPLINE_CURVE_WITH_KNOTS ( 'NONE', 3,
 ( #25268, #19978, #35299, #40022 ),
 .UNSPECIFIED., .F., .F.,
 ( 4, 4 ),
 ( 0.000000000000000000, 0.004442905043737216571 ),
 .UNSPECIFIED. ) ;
#24906=AXIS2_PLACEMENT_3D ( 'NONE', #61450, #27347, #32676 ) ;
#24912=CARTESIAN_POINT ( 'NONE',  ( 0.7413678028165010536, -11.64920183752063387, 42.52978001728846635 ) ) ;
#24915=CARTESIAN_POINT ( 'NONE',  ( 0.2285344041767097267, 4.992133951191583208, 43.83582745778637246 ) ) ;
#24925=CARTESIAN_POINT ( 'NONE',  ( 3.678834586032787346, -21.50130846795401851, 44.00347831472237914 ) ) ;
#24927=ORIENTED_EDGE ( 'NONE', *, *, #49432, .T. ) ;
#24933=ORIENTED_EDGE ( 'NONE', *, *, #30200, .F. ) ;
#24938=VERTEX_POINT ( 'NONE', #55831 ) ;
#24941=CARTESIAN_POINT ( 'NONE',  ( 4.553261556744873317, 12.28162544311275006, -42.17465165592624032 ) ) ;
#24943=CARTESIAN_POINT ( 'NONE',  ( 0.1158516988532803521, 33.56623812058064971, -28.64000379303876187 ) ) ;
#24952=CARTESIAN_POINT ( 'NONE',  ( 1.479689385636123067, -16.75487965742231111, 40.75362380123991102 ) ) ;
#24953=ORIENTED_EDGE ( 'NONE', *, *, #54801, .F. ) ;
#24956=CARTESIAN_POINT ( 'NONE',  ( 0.7242003506639981270, 10.12622957855171357, -48.04655189135312554 ) ) ;
#24972=CARTESIAN_POINT ( 'NONE',  ( 0.1129192098497455998, -23.28677643606931014, 37.47903188453085477 ) ) ;
#24974=CARTESIAN_POINT ( 'NONE',  ( 0.1157506346131639274, 9.728079385241393595, -43.03841459995100394 ) ) ;
#24975=ADVANCED_FACE ( 'NONE', ( #41459 ), #38539, .F. ) ;
#24981=DIRECTION ( 'NONE',  ( -0.1011922191286467460, -0.5796805626819985235, 0.8085360721925158867 ) ) ;
#24982=VERTEX_POINT ( 'NONE', #3820 ) ;
#24983=ADVANCED_FACE ( 'NONE', ( #22956 ), #34508, .F. ) ;
#24984=DIRECTION ( 'NONE',  ( -0.9990097760809875105, 0.000000000000000000, 0.04449120468828677427 ) ) ;
#24988=CARTESIAN_POINT ( 'NONE',  ( 4.975610109902397937, -48.11736577406850301, -8.784561349451310619 ) ) ;
#24989=ORIENTED_EDGE ( 'NONE', *, *, #48374, .F. ) ;
#25001=FACE_OUTER_BOUND ( 'NONE', #32820, .T. ) ;
#25005=CARTESIAN_POINT ( 'NONE',  ( 5.901764892641307547, -48.05798712428978092, -9.403262253137295801 ) ) ;
#25007=CARTESIAN_POINT ( 'NONE',  ( 0.6008123274975393224, -48.64681338165629398, -6.711341070811670306 ) ) ;
#25014=VERTEX_POINT ( 'NONE', #3506 ) ;
#25017=CARTESIAN_POINT ( 'NONE',  ( 4.335381028904216727, 47.63237751920352991, -11.44174197980444774 ) ) ;
#25018=CARTESIAN_POINT ( 'NONE',  ( 0.1119899015040013296, 24.78191846902677398, 36.50777759857500371 ) ) ;
#25022=CARTESIAN_POINT ( 'NONE',  ( 0.7948884756798498818, -45.82899951237259728, 17.61821353869637008 ) ) ;
#25028=CARTESIAN_POINT ( 'NONE',  ( 0.8753041380234530822, 41.63161868429038037, 26.03740873433499203 ) ) ;
#25030=CARTESIAN_POINT ( 'NONE',  ( 0.8753041380234465318, -48.57841546934875510, -7.160717726619147072 ) ) ;
#25034=CARTESIAN_POINT ( 'NONE',  ( 0.8744876279028263033, -47.70753782033983725, 11.59055156152357213 ) ) ;
#25037=CARTESIAN_POINT ( 'NONE',  ( 1.657374760986086049, -18.95778414414311541, -39.76798797520839912 ) ) ;
#25041=CARTESIAN_POINT ( 'NONE',  ( 1.830465331921977912, 24.17895171870296878, 36.82056965424381190 ) ) ;
#25044=CARTESIAN_POINT ( 'NONE',  ( 3.390910168358337362, 40.43814545685926021, 17.28738061545269744 ) ) ;
#25045=CARTESIAN_POINT ( 'NONE',  ( 0.2940133293163010308, 5.036457840397877916, -43.82778390473260544 ) ) ;
#25046=ORIENTED_EDGE ( 'NONE', *, *, #20152, .T. ) ;
#25056=ORIENTED_EDGE ( 'NONE', *, *, #59059, .T. ) ;
#25059=CARTESIAN_POINT ( 'NONE',  ( 0.1158516988532803244, 29.62825737391777281, -32.69722501708185547 ) ) ;
#25064=ORIENTED_EDGE ( 'NONE', *, *, #26805, .F. ) ;
#25066=CARTESIAN_POINT ( 'NONE',  ( 0.1147471544378676767, -1.103879636312829815, 44.11047084561418785 ) ) ;
#25070=CARTESIAN_POINT ( 'NONE',  ( 3.894904216938898323, -36.51224477628893794, -24.47407432105578806 ) ) ;
#25071=LINE ( 'NONE', #54476, #14281 ) ;
#25075=ORIENTED_EDGE ( 'NONE', *, *, #37937, .T. ) ;
#25081=ORIENTED_EDGE ( 'NONE', *, *, #58983, .F. ) ;
#25088=EDGE_CURVE ( 'NONE', #22556, #17976, #7938, .T. ) ;
#25093=PRESENTATION_STYLE_ASSIGNMENT (( #31341 ) ) ;
#25096=CARTESIAN_POINT ( 'NONE',  ( 2.533389852662419894, -8.582510520014036359, -43.17164630758787069 ) ) ;
#25101=CARTESIAN_POINT ( 'NONE',  ( -6.078726893082806448, -12.94836301907731801, -14.25250631976393656 ) ) ;
#25103=CARTESIAN_POINT ( 'NONE',  ( 0.1139756605157205005, -43.81112104903924376, -5.247941703320747386 ) ) ;
#25106=ADVANCED_FACE ( 'NONE', ( #5960 ), #42934, .F. ) ;
#25108=CARTESIAN_POINT ( 'NONE',  ( 0.1129192098497455998, 36.71339784380029414, 24.47607416535571545 ) ) ;
#25109=ORIENTED_EDGE ( 'NONE', *, *, #35672, .T. ) ;
#25124=ORIENTED_EDGE ( 'NONE', *, *, #24314, .T. ) ;
#25125=VERTEX_POINT ( 'NONE', #35139 ) ;
#25130=CARTESIAN_POINT ( 'NONE',  ( 0.5997462898726536595, -43.04230894295718457, -23.64130434225950950 ) ) ;
#25134=ORIENTED_EDGE ( 'NONE', *, *, #7328, .T. ) ;
#25138=CARTESIAN_POINT ( 'NONE',  ( 0.8744876279028306332, -43.20725972823464645, -23.31271664041680580 ) ) ;
#25140=EDGE_LOOP ( 'NONE', ( #31075, #11404, #8532, #30833 ) ) ;
#25141=CARTESIAN_POINT ( 'NONE',  ( 0.1129192098497447394, -1.898585089631814826, -44.08341142019957459 ) ) ;
#25143=CARTESIAN_POINT ( 'NONE',  ( 0.6000166863083090663, 48.10206967781400778, 9.900220927796539172 ) ) ;
#25146=CARTESIAN_POINT ( 'NONE',  ( 1.479689385636123067, -42.90531205933121583, -10.03583790020046784 ) ) ;
#25147=CARTESIAN_POINT ( 'NONE',  ( -6.079354080745853928, 9.981161348512436859, -16.46722117975960842 ) ) ;
#25148=CARTESIAN_POINT ( 'NONE',  ( 2.359973842542475886, 8.319337843647435449, -43.23105958076618549 ) ) ;
#25164=CARTESIAN_POINT ( 'NONE',  ( 0.6039202388192952409, 44.16863261170576749, 21.46382086351711749 ) ) ;
#25168=EDGE_CURVE ( 'NONE', #5258, #60330, #34027, .T. ) ;
#25172=DIRECTION ( 'NONE',  ( 0.000000000000000000, 0.000000000000000000, 1.000000000000000000 ) ) ;
#25195=CARTESIAN_POINT ( 'NONE',  ( 4.335381028904216727, 48.44495715814551318, 7.269317272604989277 ) ) ;
#25200=CARTESIAN_POINT ( 'NONE',  ( 0.7242003506639976829, -0.7549803952411664465, 49.09624913095526466 ) ) ;
#25201=CARTESIAN_POINT ( 'NONE',  ( -6.078457390727109555, -19.21618051603926958, -1.238110420156709246 ) ) ;
#25202=CARTESIAN_POINT ( 'NONE',  ( 0.1129192098497455998, -1.898585089632445433, 44.08341142019953907 ) ) ;
#25204=B_SPLINE_CURVE_WITH_KNOTS ( 'NONE', 3,
 ( #20019, #58188, #53787, #15924 ),
 .UNSPECIFIED., .F., .F.,
 ( 4, 4 ),
 ( 0.000000000000000000, 0.004444103432399267029 ),
 .UNSPECIFIED. ) ;
#25218=CARTESIAN_POINT ( 'NONE',  ( 0.1140933569871964842, -40.75566919115180298, -16.90932816126367300 ) ) ;
#25221=CARTESIAN_POINT ( 'NONE',  ( 0.6008122571543325074, -34.97209109721812581, 34.47473560091786737 ) ) ;
#25229=CARTESIAN_POINT ( 'NONE',  ( 0.1152809850208375703, 9.602783458000070382, 43.06659764072982455 ) ) ;
#25231=EDGE_LOOP ( 'NONE', ( #48794, #60810, #35005, #11269 ) ) ;
#25239=DIRECTION ( 'NONE',  ( 0.000000000000000000, -1.000000000000000000, -0.000000000000000000 ) ) ;
#25241=DIRECTION ( 'NONE',  ( -1.000000000000000000, -0.000000000000000000, -0.000000000000000000 ) ) ;
#25244=EDGE_CURVE ( 'NONE', #5027, #35750, #43810, .T. ) ;
#25248=ORIENTED_EDGE ( 'NONE', *, *, #39326, .F. ) ;
#25249=EDGE_CURVE ( 'NONE', #59402, #41892, #23576, .T. ) ;
#25254=CARTESIAN_POINT ( 'NONE',  ( 0.6008122571543326185, -19.47898650447827507, 45.07908201398593206 ) ) ;
#25268=CARTESIAN_POINT ( 'NONE',  ( 0.8744876279028306332, -26.20733431478126008, -41.51536677536140729 ) ) ;
#25269=( BOUNDED_SURFACE ( )  B_SPLINE_SURFACE ( 3, 1, ( 
 ( #46355, #31006 ),
 ( #7169, #45435 ),
 ( #12847, #31939 ),
 ( #11601, #59186 ) ),
 .UNSPECIFIED., .F., .F., .F. ) 
 B_SPLINE_SURFACE_WITH_KNOTS ( ( 4, 4 ),
 ( 2, 2 ),
 ( 0.000000000000000000, 1.000000000000000000 ),
 ( 0.000000000000000000, 1.000000000000000000 ),
 .UNSPECIFIED. ) 
 GEOMETRIC_REPRESENTATION_ITEM ( )  RATIONAL_B_SPLINE_SURFACE ( (
 ( 1.000000000000000000, 1.000000000000000000),
 ( 0.7211978278499970862, 0.9934217856018976445),
 ( 0.7211978278499970862, 0.9934217856018976445),
 ( 1.000000000000000000, 1.000000000000000000) ) ) 
 REPRESENTATION_ITEM ( '' )  SURFACE ( )  );
#25270=CARTESIAN_POINT ( 'NONE',  ( 0.1158403557922069033, -22.90600150134859803, 37.71280157193356075 ) ) ;
#25272=CARTESIAN_POINT ( 'NONE',  ( 0.1156867017252034419, 9.940337221640810128, -42.98991164442244894 ) ) ;
#25274=ORIENTED_EDGE ( 'NONE', *, *, #42873, .T. ) ;
#25275=EDGE_LOOP ( 'NONE', ( #9639, #19468, #6586, #1589 ) ) ;
#25278=CARTESIAN_POINT ( 'NONE',  ( 0.6027444965799114707, 37.30784590784681853, 31.93216481236119719 ) ) ;
#25284=CARTESIAN_POINT ( 'NONE',  ( 4.694002226626920127, -20.78018001817206439, 40.57670378257081012 ) ) ;
#25285=ORIENTED_EDGE ( 'NONE', *, *, #25863, .F. ) ;
#25294=CARTESIAN_POINT ( 'NONE',  ( 4.335381028904201628, -27.18827219542433227, 40.74990432739517843 ) ) ;
#25299=CARTESIAN_POINT ( 'NONE',  ( 4.975610109902397937, 35.53430708602537891, 33.61193875773635398 ) ) ;
#25305=CARTESIAN_POINT ( 'NONE',  ( 0.1119898979215351864, 41.69625316766367717, -14.43550414879666732 ) ) ;
#25308=CARTESIAN_POINT ( 'NONE',  ( 4.834790513006555379, -39.34655703395279147, 26.16176199146916304 ) ) ;
#25314=CARTESIAN_POINT ( 'NONE',  ( 2.359973842542475886, 30.69728382343663498, 31.55649949686871381 ) ) ;
#25315=FACE_OUTER_BOUND ( 'NONE', #57878, .T. ) ;
#25316=CARTESIAN_POINT ( 'NONE',  ( 3.678748215320120085, -15.69769956952215395, -46.39175619142379503 ) ) ;
#25320=ADVANCED_FACE ( 'NONE', ( #27886 ), #12928, .F. ) ;
#25325=CARTESIAN_POINT ( 'NONE',  ( 0.3676999524040366896, -38.83470403830472151, -20.92406140260821346 ) ) ;
#25330=CARTESIAN_POINT ( 'NONE',  ( 0.5997462898726536595, -31.02483596213057737, 38.06587952047342327 ) ) ;
#25334=CARTESIAN_POINT ( 'NONE',  ( 0.6028777368367060907, 37.44903595938922791, -31.76648446119660107 ) ) ;
#25342=CARTESIAN_POINT ( 'NONE',  ( 3.727782113643637540, -19.72952865065639116, -39.28770132151922923 ) ) ;
#25344=CARTESIAN_POINT ( 'NONE',  ( 4.553261556744875094, -4.442710778082547662, 43.70128015019636791 ) ) ;
#25345=CARTESIAN_POINT ( 'NONE',  ( -2.739355103387247858, -14.83685109948653391, 1.647852057280082771 ) ) ;
#25351=CARTESIAN_POINT ( 'NONE',  ( 1.479689385636123067, 24.23631239248258495, -36.79925280330684956 ) ) ;
#25362=ORIENTED_EDGE ( 'NONE', *, *, #19031, .F. ) ;
#25368=ORIENTED_EDGE ( 'NONE', *, *, #54923, .F. ) ;
#25375=B_SPLINE_CURVE_WITH_KNOTS ( 'NONE', 3,
 ( #16386, #39915, #34893, #53957, #1036, #20174 ),
 .UNSPECIFIED., .F., .F.,
 ( 4, 2, 4 ),
 ( 2.005774019098183203E-18, 0.0002293801035737089383, 0.0004587602071474158709 ),
 .UNSPECIFIED. ) ;
#25376=CARTESIAN_POINT ( 'NONE',  ( 0.8753041380234530822, 43.84722337925244062, -22.10337824412636820 ) ) ;
#25377=CARTESIAN_POINT ( 'NONE',  ( 2.185380717157383135, -36.12942123712758047, -25.16912243478889977 ) ) ;
#25378=DIRECTION ( 'NONE',  ( 0.09722883295013595717, 0.6746907015591536716, -0.7316686485512220450 ) ) ;
#25381=CARTESIAN_POINT ( 'NONE',  ( -6.077587904424778920, -11.02178778841139284, 15.78975032548507151 ) ) ;
#25382=ORIENTED_EDGE ( 'NONE', *, *, #61384, .F. ) ;
#25387=ORIENTED_EDGE ( 'NONE', *, *, #27430, .F. ) ;
#25397=CARTESIAN_POINT ( 'NONE',  ( -2.739355103387247858, 9.839932234829875668, 11.22601000199861510 ) ) ;
#25399=SURFACE_STYLE_FILL_AREA ( #6255 ) ;
#25404=CARTESIAN_POINT ( 'NONE',  ( -2.601141883200662974, 13.24771294992769555, -6.877029087164502563 ) ) ;
#25406=ADVANCED_FACE ( 'NONE', ( #12414 ), #32129, .F. ) ;
#25409=DIRECTION ( 'NONE',  ( -1.000000000000000000, -0.000000000000000000, -0.000000000000000000 ) ) ;
#25410=CARTESIAN_POINT ( 'NONE',  ( 0.6026112563231247332, -45.58358175611240171, 18.26685712398343853 ) ) ;
#25413=CARTESIAN_POINT ( 'NONE',  ( 1.657374760986086271, 19.27187991371560827, -39.61672742470747011 ) ) ;
#25415=ORIENTED_EDGE ( 'NONE', *, *, #42260, .T. ) ;
#25420=B_SPLINE_CURVE_WITH_KNOTS ( 'NONE', 3,
 ( #41172, #32373, #41481, #33610, #990, #24813, #19509, #57675, #53299, #39245, #38940, #14200, #48311, #33921, #48611, #52996, #57993, #28576, #20126, #9471, #43327, #10412, #58294, #57368, #47699 ),
 .UNSPECIFIED., .F., .F.,
 ( 4, 3, 3, 3, 3, 3, 3, 3, 4 ),
 ( 6.254634441385501517E-18, 0.0005656085177311398569, 0.001131215744874498972, 0.001696821861372767000, 0.002262427090022497284, 0.002828031679238744624, 0.003393635864401603561, 0.003977030878808131623, 0.004561030005651157265 ),
 .UNSPECIFIED. ) ;
#25421=ORIENTED_EDGE ( 'NONE', *, *, #13045, .F. ) ;
#25424=CARTESIAN_POINT ( 'NONE',  ( 0.5987334308729317378, 37.78232974793878185, 31.36970617311787990 ) ) ;
#25429=DIRECTION ( 'NONE',  ( 0.000000000000000000, 0.000000000000000000, 1.000000000000000000 ) ) ;
#25431=CARTESIAN_POINT ( 'NONE',  ( 0.3676999524040323597, -11.75791688508830646, -42.51707861373114383 ) ) ;
#25439=DIRECTION ( 'NONE',  ( 1.000000000000000000, 0.000000000000000000, 0.000000000000000000 ) ) ;
#25448=CARTESIAN_POINT ( 'NONE',  ( 4.553261556744875094, 38.38432632180499837, -21.35844232721162683 ) ) ;
#25451=CARTESIAN_POINT ( 'NONE',  ( 0.6039202388192952409, -25.60584472520900334, 41.90351332236327409 ) ) ;
#25462=CARTESIAN_POINT ( 'NONE',  ( 0.5997462898726536595, -49.10477184366966696, 0.5225058138009974762 ) ) ;
#25474=EDGE_CURVE ( 'NONE', #10066, #52565, #51192, .T. ) ;
#25477=CARTESIAN_POINT ( 'NONE',  ( 0.6021448801613057400, 33.20790775271667172, -36.17700929200764648 ) ) ;
#25481=CARTESIAN_POINT ( 'NONE',  ( 0.6021447746440204973, -30.41329242676998135, 38.55609916540136339 ) ) ;
#25489=CARTESIAN_POINT ( 'NONE',  ( 3.390910168358336918, 43.71773359279901427, -4.780889670625141363 ) ) ;
#25495=LINE ( 'NONE', #25811, #10051 ) ;
#25497=AXIS2_PLACEMENT_3D ( 'NONE', #9241, #37791, #13657 ) ;
#25501=FACE_OUTER_BOUND ( 'NONE', #5683, .T. ) ;
#25502=CARTESIAN_POINT ( 'NONE',  ( 4.060580049360325461, -10.26916902627464623, 42.73186003287254664 ) ) ;
#25510=CARTESIAN_POINT ( 'NONE',  ( 0.1129192098497455998, 4.719118110135312349, -43.87119455916086963 ) ) ;
#25512=EDGE_CURVE ( 'NONE', #41953, #36415, #43674, .T. ) ;
#25519=CARTESIAN_POINT ( 'NONE',  ( 0.2940135542859015350, 37.40612138948920773, 23.38851494401085773 ) ) ;
#25520=CARTESIAN_POINT ( 'NONE',  ( 0.8753041380234530822, -38.81339214172321306, 30.07754840949971253 ) ) ;
#25521=DIRECTION ( 'NONE',  ( 0.09722883295013597105, 0.7627152102960371716, -0.6393841271303396523 ) ) ;
#25522=AXIS2_PLACEMENT_3D ( 'NONE', #60631, #32161, #51241 ) ;
#25523=VERTEX_POINT ( 'NONE', #25448 ) ;
#25530=ORIENTED_EDGE ( 'NONE', *, *, #419, .F. ) ;
#25531=CARTESIAN_POINT ( 'NONE',  ( 0.1365634738349396082, 42.07174034091315917, -13.29779246002983939 ) ) ;
#25539=ADVANCED_FACE ( 'NONE', ( #20159 ), #2087, .F. ) ;
#25544=CARTESIAN_POINT ( 'NONE',  ( 4.390527457369402420, 22.50004464754335487, 37.73504110885762231 ) ) ;
#25547=CARTESIAN_POINT ( 'NONE',  ( 0.6000166863083090663, 48.97316450298212942, -3.667784109282604899 ) ) ;
#25550=CARTESIAN_POINT ( 'NONE',  ( 0.5997462898726536595, 33.39998138387895921, -35.99990102348682797 ) ) ;
#25551=ORIENTED_EDGE ( 'NONE', *, *, #34879, .T. ) ;
#25554=CARTESIAN_POINT ( 'NONE',  ( 0.8744876279028306332, 48.92939099258504143, -4.032957658373305776 ) ) ;
#25555=CARTESIAN_POINT ( 'NONE',  ( 0.1158816050234198758, 44.03314403839271307, -2.832713787046244214 ) ) ;
#25561=DIRECTION ( 'NONE',  ( 0.000000000000000000, 1.000000000000000000, 0.000000000000000000 ) ) ;
#25562=EDGE_CURVE ( 'NONE', #45047, #30775, #18377, .T. ) ;
#25566=CARTESIAN_POINT ( 'NONE',  ( 0.5997462898726536595, 48.29911994996563607, 8.873930482212578852 ) ) ;
#25567=ORIENTED_EDGE ( 'NONE', *, *, #3108, .T. ) ;
#25573=CIRCLE ( 'NONE', #36597, 43.92652462719577500 ) ;
#25574=ORIENTED_EDGE ( 'NONE', *, *, #26383, .T. ) ;
#25575=CARTESIAN_POINT ( 'NONE',  ( 0.1149546198390367091, -23.10744346465573429, 37.58979411424008532 ) ) ;
#25584=EDGE_CURVE ( 'NONE', #46397, #14283, #16160, .T. ) ;
#25591=EDGE_CURVE ( 'NONE', #2327, #40973, #43019, .T. ) ;
#25604=VERTEX_POINT ( 'NONE', #26079 ) ;
#25606=EDGE_CURVE ( 'NONE', #14390, #4686, #35585, .T. ) ;
#25615=ORIENTED_EDGE ( 'NONE', *, *, #7612, .F. ) ;
#25618=CARTESIAN_POINT ( 'NONE',  ( 4.694002226626920127, 42.12595566887542020, -17.42666435179369344 ) ) ;
#25620=ORIENTED_EDGE ( 'NONE', *, *, #58020, .F. ) ;
#25623=CARTESIAN_POINT ( 'NONE',  ( 1.657374760986086271, 30.52321381783924892, 31.76828395558549545 ) ) ;
#25627=CARTESIAN_POINT ( 'NONE',  ( 0.1129192098497447394, -42.55567333040724520, 11.66046547873710537 ) ) ;
#25628=EDGE_LOOP ( 'NONE', ( #45809, #28388, #48215, #16410, #8090, #30763 ) ) ;
#25634=CARTESIAN_POINT ( 'NONE',  ( 0.1129192098497455998, -38.20615368646939203, -22.07354996984027196 ) ) ;
#25637=FACE_OUTER_BOUND ( 'NONE', #25275, .T. ) ;
#25639=EDGE_CURVE ( 'NONE', #31520, #57605, #9027, .T. ) ;
#25640=CARTESIAN_POINT ( 'NONE',  ( 0.6016118706126977189, 37.61760366456271498, -31.56686473693274309 ) ) ;
#25642=CARTESIAN_POINT ( 'NONE',  ( 0.1152339509894530906, 29.82972479065796634, 32.51353886258534942 ) ) ;
#25646=CARTESIAN_POINT ( 'NONE',  ( 0.1129192098497447394, -6.563350895509266536, 43.63340707310824484 ) ) ;
#25653=AXIS2_PLACEMENT_3D ( 'NONE', #32092, #45577, #21755 ) ;
#25656=CARTESIAN_POINT ( 'NONE',  ( 2.299746137290199943, -6.551208167574801955, 48.59385773152035881 ) ) ;
#25665=CARTESIAN_POINT ( 'NONE',  ( 2.533389852662419894, -43.98803057297956798, 1.582307822211680870 ) ) ;
#25684=ORIENTED_EDGE ( 'NONE', *, *, #47769, .F. ) ;
#25691=ORIENTED_EDGE ( 'NONE', *, *, #20960, .F. ) ;
#25692=CARTESIAN_POINT ( 'NONE',  ( 0.6000166863083090663, 46.77044519531211364, 14.97828220927751630 ) ) ;
#25694=CARTESIAN_POINT ( 'NONE',  ( -6.057079549204054558, 16.78313491342520436, -9.442330939842472404 ) ) ;
#25704=CARTESIAN_POINT ( 'NONE',  ( 0.8744876279028263033, 46.30617036199606673, 16.31222353896886545 ) ) ;
#25709=ORIENTED_EDGE ( 'NONE', *, *, #40714, .F. ) ;
#25718=CARTESIAN_POINT ( 'NONE',  ( -6.078457390727109555, 18.62514245781363798, 4.888617336594847096 ) ) ;
#25719=CARTESIAN_POINT ( 'NONE',  ( 0.5997462898726536595, 22.24958391914503153, 43.77793560195857481 ) ) ;
#25721=CARTESIAN_POINT ( 'NONE',  ( 0.1129192098497447394, -27.13044910148925837, 34.79785222304180081 ) ) ;
#25723=CARTESIAN_POINT ( 'NONE',  ( 0.1129192098497447394, -43.69739906996321110, 6.122834499276631703 ) ) ;
#25726=FACE_OUTER_BOUND ( 'NONE', #5243, .T. ) ;
#25727=CARTESIAN_POINT ( 'NONE',  ( 0.6029442701453591180, -45.48579272903533166, 18.50912977342572319 ) ) ;
#25729=CARTESIAN_POINT ( 'NONE',  ( 2.185380717157383135, -2.848313382796944015, -43.93981012636012196 ) ) ;
#25731=CARTESIAN_POINT ( 'NONE',  ( 2.879087469061463178, -42.08991748084939388, 12.82733500142047944 ) ) ;
#25741=ORIENTED_EDGE ( 'NONE', *, *, #32462, .T. ) ;
#25743=AXIS2_PLACEMENT_3D ( 'NONE', #19542, #29226, #52721 ) ;
#25746=EDGE_CURVE ( 'NONE', #40034, #41417, #1784, .T. ) ;
#25752=CARTESIAN_POINT ( 'NONE',  ( 0.5997462898726536595, 46.76781179977627545, -14.97743000668059210 ) ) ;
#25755=B_SPLINE_CURVE_WITH_KNOTS ( 'NONE', 3,
 ( #8245, #22991, #46491, #16743 ),
 .UNSPECIFIED., .F., .F.,
 ( 4, 4 ),
 ( 0.000000000000000000, 0.004442905043737216571 ),
 .UNSPECIFIED. ) ;
#25758=CARTESIAN_POINT ( 'NONE',  ( 0.3676999524040323597, 34.11874447325018167, -27.96179284115914854 ) ) ;
#25763=EDGE_LOOP ( 'NONE', ( #60145, #60234, #54932, #33828 ) ) ;
#25764=EDGE_CURVE ( 'NONE', #12356, #23235, #19027, .T. ) ;
#25765=ORIENTED_EDGE ( 'NONE', *, *, #13882, .T. ) ;
#25768=CARTESIAN_POINT ( 'NONE',  ( 0.7044674535452954967, 48.03641533699654076, 10.21300760708961164 ) ) ;
#25770=VERTEX_POINT ( 'NONE', #55725 ) ;
#25771=CARTESIAN_POINT ( 'NONE',  ( 3.390910168358337362, -42.99706393720556008, -9.238486310727259010 ) ) ;
#25773=CARTESIAN_POINT ( 'NONE',  ( 0.7242486021783859362, 46.33600717073790065, 16.24764296282079457 ) ) ;
#25783=CARTESIAN_POINT ( 'NONE',  ( 4.226256110419178924, -43.20794779182517686, 7.993778681330654834 ) ) ;
#25785=CARTESIAN_POINT ( 'NONE',  ( 0.5549461598389366923, -13.38796976693469531, -42.02356435366290555 ) ) ;
#25793=CARTESIAN_POINT ( 'NONE',  ( 1.479689385636123067, 41.43333151104896217, -14.99542880891405083 ) ) ;
#25794=CARTESIAN_POINT ( 'NONE',  ( 3.678834586032787790, 9.087502264074171165, 48.12514594501299570 ) ) ;
#25797=CARTESIAN_POINT ( 'NONE',  ( 0.7044674535452954967, 11.74740322167666307, -47.68439199946085694 ) ) ;
#25798=B_SPLINE_CURVE_WITH_KNOTS ( 'NONE', 3,
 ( #22255, #37287, #22559, #41377 ),
 .UNSPECIFIED., .F., .F.,
 ( 4, 4 ),
 ( 0.000000000000000000, 0.004444103432399265294 ),
 .UNSPECIFIED. ) ;
#25801=DIRECTION ( 'NONE',  ( 0.000000000000000000, 0.000000000000000000, 1.000000000000000000 ) ) ;
#25802=EDGE_LOOP ( 'NONE', ( #26462, #25620, #34322, #25421 ) ) ;
#25806=CARTESIAN_POINT ( 'NONE',  ( 4.553261556744875094, 43.59419396814060832, -5.393126930804686303 ) ) ;
#25809=ORIENTED_EDGE ( 'NONE', *, *, #45490, .T. ) ;
#25811=CARTESIAN_POINT ( 'NONE',  ( -2.601141883200662974, 4.732256851928817731, -14.15631211003633716 ) ) ;
#25815=CARTESIAN_POINT ( 'NONE',  ( -6.077587904424778920, -18.90214787454603851, -3.674891443665424973 ) ) ;
#25816=ADVANCED_FACE ( 'NONE', ( #9052 ), #39834, .F. ) ;
#25820=EDGE_LOOP ( 'NONE', ( #29585, #51095, #61820, #8666 ) ) ;
#25834=CARTESIAN_POINT ( 'NONE',  ( 0.1119898979215346868, 37.28332023458525413, 23.59905380597269797 ) ) ;
#25838=ORIENTED_EDGE ( 'NONE', *, *, #41286, .F. ) ;
#25843=CARTESIAN_POINT ( 'NONE',  ( 3.240649175237394708, -25.97541675339710565, -35.50412147744241764 ) ) ;
#25851=CARTESIAN_POINT ( 'NONE',  ( 0.1119899015040012463, -42.53546974785185597, -11.73435645964812046 ) ) ;
#25854=CARTESIAN_POINT ( 'NONE',  ( 2.879087469061463178, 21.87161467977467666, 38.18028480882303910 ) ) ;
#25858=CARTESIAN_POINT ( 'NONE',  ( 2.299652685299200972, -48.44937665196427190, -7.545835069377869075 ) ) ;
#25862=VECTOR ( 'NONE', #5125, 1000.000000000000000 ) ;
#25863=EDGE_CURVE ( 'NONE', #4535, #56737, #6990, .T. ) ;
#25868=B_SPLINE_CURVE_WITH_KNOTS ( 'NONE', 3,
 ( #36821, #55571, #7026, #16774, #45912, #13015 ),
 .UNSPECIFIED., .F., .F.,
 ( 4, 2, 4 ),
 ( 5.421010862427522170E-19, 0.0002293801035737086673, 0.0004587602071474167925 ),
 .UNSPECIFIED. ) ;
#25874=B_SPLINE_CURVE_WITH_KNOTS ( 'NONE', 3,
 ( #23581, #25424, #5671, #44568, #19825, #30426 ),
 .UNSPECIFIED., .F., .F.,
 ( 4, 2, 4 ),
 ( 0.000000000000000000, 0.0002447195606305710598, 0.0004894391212611486248 ),
 .UNSPECIFIED. ) ;
#25880=ORIENTED_EDGE ( 'NONE', *, *, #17789, .T. ) ;
#25886=ORIENTED_EDGE ( 'NONE', *, *, #21671, .T. ) ;
#25894=EDGE_CURVE ( 'NONE', #33022, #52994, #36221, .T. ) ;
#25901=LINE ( 'NONE', #16198, #58584 ) ;
#25907=CARTESIAN_POINT ( 'NONE',  ( 0.2285344041767113921, 29.09448245089918217, -33.16643274773119998 ) ) ;
#25911=CARTESIAN_POINT ( 'NONE',  ( 0.6000166863083106206, -39.66797998683873772, 28.95297645272788500 ) ) ;
#25917=EDGE_CURVE ( 'NONE', #22617, #28594, #5560, .T. ) ;
#25920=CARTESIAN_POINT ( 'NONE',  ( 0.1129192098497455998, 39.96249028893973332, -18.70698152272436587 ) ) ;
#25929=CARTESIAN_POINT ( 'NONE',  ( 0.1119899015040012741, 10.36499862923388804, -42.88972034891910567 ) ) ;
#25936=CARTESIAN_POINT ( 'NONE',  ( 0.1119899015040011631, 29.24697023967760146, 33.03900785423071085 ) ) ;
#25937=CARTESIAN_POINT ( 'NONE',  ( 1.834102595619085507, 30.56483960858423998, 31.71731900018039951 ) ) ;
#25941=CARTESIAN_POINT ( 'NONE',  ( 0.5980271706414734822, 40.77460832818560021, -27.37664257217675967 ) ) ;
#25944=CARTESIAN_POINT ( 'NONE',  ( 4.694002226626921015, 39.55162978021514419, 22.67053932254223625 ) ) ;
#25947=ADVANCED_FACE ( 'NONE', ( #24388 ), #3736, .F. ) ;
#25949=CARTESIAN_POINT ( 'NONE',  ( 4.975610109902397937, -41.30423662854430944, -26.19941685746064053 ) ) ;
#25953=EDGE_CURVE ( 'NONE', #40973, #48800, #43655, .T. ) ;
#25964=B_SPLINE_CURVE_WITH_KNOTS ( 'NONE', 3,
 ( #30357, #22433, #49469, #11582, #22743, #15975, #30664, #55618, #6520, #50614, #11267, #7701, #25665, #60944, #55936, #37171, #1846, #51231, #8313, #27433, #41876, #8628, #45960, #1528, #40117 ),
 .UNSPECIFIED., .F., .F.,
 ( 4, 3, 3, 3, 3, 3, 3, 3, 4 ),
 ( 5.057544569639794935E-18, 0.0005656085177311395316, 0.001131215744874499622, 0.001696821861372765916, 0.002262427090022498151, 0.002828031679238745925, 0.003393635864401605296, 0.003977030878808133357, 0.004561030005651159867 ),
 .UNSPECIFIED. ) ;
#25974=CARTESIAN_POINT ( 'NONE',  ( 0.6024113833632039894, -45.43637621081261813, -18.63001840928686903 ) ) ;
#25978=CARTESIAN_POINT ( 'NONE',  ( 0.6016117650947689910, 27.80883221307838582, -40.47492934137567033 ) ) ;
#25983=CARTESIAN_POINT ( 'NONE',  ( 4.834790513006555379, 33.61992680604640071, -33.20075093247837117 ) ) ;
#25986=ORIENTED_EDGE ( 'NONE', *, *, #11385, .F. ) ;
#25990=CARTESIAN_POINT ( 'NONE',  ( 4.975610109902397937, 0.9924324126411095959, -48.90260202733707473 ) ) ;
#25992=EDGE_CURVE ( 'NONE', #2416, #1120, #27990, .T. ) ;
#26001=CARTESIAN_POINT ( 'NONE',  ( 0.6029442701453591180, -25.53140348424445705, -41.94869081727089366 ) ) ;
#26002=CARTESIAN_POINT ( 'NONE',  ( 5.901764892641288895, -32.95403503760634578, -36.22185862403931367 ) ) ;
#26006=CARTESIAN_POINT ( 'NONE',  ( 0.8753041380234530822, 27.35839019124417604, -40.77568900725792389 ) ) ;
#26007=CARTESIAN_POINT ( 'NONE',  ( -6.077587904424778920, 15.43577113102525189, 11.51229738082446552 ) ) ;
#26011=ORIENTED_EDGE ( 'NONE', *, *, #55256, .F. ) ;
#26013=CARTESIAN_POINT ( 'NONE',  ( 0.6000166863083090663, -35.63988196839386546, 33.78790160674983412 ) ) ;
#26015=VERTEX_POINT ( 'NONE', #30616 ) ;
#26033=VECTOR ( 'NONE', #34589, 1000.000000000000114 ) ;
#26034=CARTESIAN_POINT ( 'NONE',  ( -6.077587904424778920, 16.77513308702627981, 9.454677747363296803 ) ) ;
#26045=LINE ( 'NONE', #2210, #30875 ) ;
#26046=CARTESIAN_POINT ( 'NONE',  ( 0.8744876279028263033, 49.04340454744552602, -2.257104511335871422 ) ) ;
#26047=CARTESIAN_POINT ( 'NONE',  ( 0.1119899015040012463, -18.37259944400937428, 40.11743882481150081 ) ) ;
#26053=CARTESIAN_POINT ( 'NONE',  ( 0.2279481005628788415, 3.480028581335672389, 43.98173357367804925 ) ) ;
#26055=VERTEX_POINT ( 'NONE', #2098 ) ;
#26059=CARTESIAN_POINT ( 'NONE',  ( 0.1157991065609915854, 44.02822103802267151, 2.908284333540335886 ) ) ;
#26060=EDGE_LOOP ( 'NONE', ( #57591, #36887, #58871, #25709 ) ) ;
#26061=CARTESIAN_POINT ( 'NONE',  ( -6.057079549204054558, -8.914624657272197439, 17.06929109013297463 ) ) ;
#26068=ORIENTED_EDGE ( 'NONE', *, *, #46334, .F. ) ;
#26069=CARTESIAN_POINT ( 'NONE',  ( 0.1156867017252034974, 43.33420080233410232, -8.312030323463241999 ) ) ;
#26074=B_SPLINE_CURVE_WITH_KNOTS ( 'NONE', 3,
 ( #17715, #56217, #3583, #61220, #9530, #51205, #23337, #27408, #32746, #27727, #47156, #36841, #8598, #46856, #32434, #37454, #51822, #55909, #18645, #51509, #33063, #3897, #13031, #42465, #8927 ),
 .UNSPECIFIED., .F., .F.,
 ( 4, 3, 3, 3, 3, 3, 3, 3, 4 ),
 ( 6.992893892674702526E-18, 0.0005656085177311379053, 0.001131215744874499839, 0.001696821861372766350, 0.002262427090022498151, 0.002828031679238744191, 0.003393635864401603995, 0.003977030878808131623, 0.004561030005651159000 ),
 .UNSPECIFIED. ) ;
#26078=FACE_OUTER_BOUND ( 'NONE', #45198, .T. ) ;
#26079=CARTESIAN_POINT ( 'NONE',  ( 0.3676999524040366896, -35.84016207189403502, -25.71834687500748373 ) ) ;
#26082=CARTESIAN_POINT ( 'NONE',  ( 0.5997462898726536595, 46.43852004798843325, 15.96920429754989890 ) ) ;
#26091=CARTESIAN_POINT ( 'NONE',  ( 0.5549461598389366923, -41.20260823449177678, -15.73412756214321817 ) ) ;
#26094=EDGE_CURVE ( 'NONE', #40325, #52094, #4061, .T. ) ;
#26103=CARTESIAN_POINT ( 'NONE',  ( 0.8744876279028306332, 46.86690837902563089, 14.62336997314605469 ) ) ;
#26108=CARTESIAN_POINT ( 'NONE',  ( 0.6016117650947691020, 48.26733837696657048, 9.045169995523039574 ) ) ;
#26113=CARTESIAN_POINT ( 'NONE',  ( 0.6021448801613057400, 17.20492824988890490, -45.99490822409718760 ) ) ;
#26119=CARTESIAN_POINT ( 'NONE',  ( 4.390527457369402420, -29.77348744142276971, 32.30672967361536507 ) ) ;
#26128=ORIENTED_EDGE ( 'NONE', *, *, #43030, .T. ) ;
#26129=B_SPLINE_CURVE_WITH_KNOTS ( 'NONE', 3,
 ( #57165, #9266, #47809, #52173 ),
 .UNSPECIFIED., .F., .F.,
 ( 4, 4 ),
 ( 2.178848519881467612E-17, 0.004559932413162186803 ),
 .UNSPECIFIED. ) ;
#26139=CARTESIAN_POINT ( 'NONE',  ( 0.6026777506516367566, -48.68174550883031770, 6.452444873898463662 ) ) ;
#26142=CARTESIAN_POINT ( 'NONE',  ( 3.390910168358336918, -43.82545004431705138, -3.664295968764966549 ) ) ;
#26146=CARTESIAN_POINT ( 'NONE',  ( 0.5997462898726536595, -34.91088276334750873, 34.53667463477217581 ) ) ;
#26147=VECTOR ( 'NONE', #60299, 1000.000000000000114 ) ;
#26161=CARTESIAN_POINT ( 'NONE',  ( 1.834102595619085063, 21.51996898927949431, 38.43291141142098155 ) ) ;
#26166=ADVANCED_FACE ( 'NONE', ( #36900 ), #33412, .F. ) ;
#26167=CARTESIAN_POINT ( 'NONE',  ( 0.8753041380234471980, 10.05717963662801218, 48.06237057854693973 ) ) ;
#26170=EDGE_CURVE ( 'NONE', #1120, #19414, #13809, .T. ) ;
#26190=CARTESIAN_POINT ( 'NONE',  ( 0.1129192098497455998, 43.99990943031669843, 3.310552508129313232 ) ) ;
#26192=ORIENTED_EDGE ( 'NONE', *, *, #29687, .T. ) ;
#26195=CARTESIAN_POINT ( 'NONE',  ( 0.6000166863083106206, 48.30184070261004337, -8.874438937089886181 ) ) ;
#26199=CARTESIAN_POINT ( 'NONE',  ( -6.078726893082806448, 9.979253153318998315, -16.46841060244408794 ) ) ;
#26201=ORIENTED_EDGE ( 'NONE', *, *, #57238, .F. ) ;
#26202=CARTESIAN_POINT ( 'NONE',  ( 0.1119898979215347840, 33.23178737380685988, -29.02773873717895015 ) ) ;
#26222=CARTESIAN_POINT ( 'NONE',  ( 0.6028777368367060907, -48.69304970598422955, -6.366061548683123128 ) ) ;
#26223=CARTESIAN_POINT ( 'NONE',  ( 0.1139756605157201813, -43.70943680385401819, 6.036584629152037529 ) ) ;
#26231=AXIS2_PLACEMENT_3D ( 'NONE', #1026, #20162, #58330 ) ;
#26238=ORIENTED_EDGE ( 'NONE', *, *, #10690, .T. ) ;
#26243=EDGE_CURVE ( 'NONE', #39259, #17964, #57805, .T. ) ;
#26247=CARTESIAN_POINT ( 'NONE',  ( 1.830465331921978134, -11.34470899496544405, -42.56375962832630222 ) ) ;
#26252=CARTESIAN_POINT ( 'NONE',  ( 0.1158816050234198758, -12.55998807466990819, -42.29880306662720102 ) ) ;
#26253=( BOUNDED_SURFACE ( )  B_SPLINE_SURFACE ( 3, 1, ( 
 ( #42170, #36223 ),
 ( #61227, #18349 ),
 ( #56530, #4203 ),
 ( #55287, #12411 ) ),
 .UNSPECIFIED., .F., .F., .F. ) 
 B_SPLINE_SURFACE_WITH_KNOTS ( ( 4, 4 ),
 ( 2, 2 ),
 ( 0.000000000000000000, 1.000000000000000000 ),
 ( 0.000000000000000000, 1.000000000000000000 ),
 .UNSPECIFIED. ) 
 GEOMETRIC_REPRESENTATION_ITEM ( )  RATIONAL_B_SPLINE_SURFACE ( (
 ( 1.000000000000000000, 1.000000000000000000),
 ( 0.9754377213608244057, 0.9999580625633939235),
 ( 0.9754377213608244057, 0.9999580625633939235),
 ( 1.000000000000000000, 1.000000000000000000) ) ) 
 REPRESENTATION_ITEM ( '' )  SURFACE ( )  );
#26262=CARTESIAN_POINT ( 'NONE',  ( 0.7948884756798486606, 40.66950405776249511, 27.50800036890706579 ) ) ;
#26267=B_SPLINE_CURVE_WITH_KNOTS ( 'NONE', 3,
 ( #48066, #13954, #38077, #52130 ),
 .UNSPECIFIED., .F., .F.,
 ( 4, 4 ),
 ( 0.000000000000000000, 0.004444103432399268763 ),
 .UNSPECIFIED. ) ;
#26270=CARTESIAN_POINT ( 'NONE',  ( 0.1158816050234198758, -38.44899847554016503, -21.64755315348761755 ) ) ;
#26271=CARTESIAN_POINT ( 'NONE',  ( 5.901764892641307547, 30.56558498816019309, -38.25880920482542535 ) ) ;
#26276=CARTESIAN_POINT ( 'NONE',  ( 0.6024113833632039894, -14.18099286842164020, 47.01533058872011850 ) ) ;
#26277=VECTOR ( 'NONE', #6948, 1000.000000000000227 ) ;
#26279=CARTESIAN_POINT ( 'NONE',  ( 4.694002226626921015, -40.92287315640955114, -20.08987864748195307 ) ) ;
#26280=ORIENTED_EDGE ( 'NONE', *, *, #47, .T. ) ;
#26284=ORIENTED_EDGE ( 'NONE', *, *, #45848, .T. ) ;
#26286=ORIENTED_EDGE ( 'NONE', *, *, #6897, .T. ) ;
#26288=CARTESIAN_POINT ( 'NONE',  ( 0.1155031312995260795, 20.25957159725990664, 39.19810443410890599 ) ) ;
#26289=EDGE_CURVE ( 'NONE', #44212, #14421, #18935, .T. ) ;
#26293=EDGE_CURVE ( 'NONE', #30775, #52200, #61906, .T. ) ;
#26296=CARTESIAN_POINT ( 'NONE',  ( 0.1135584504625008484, -1.845938478027137730, 44.08565031016998148 ) ) ;
#26310=CARTESIAN_POINT ( 'NONE',  ( 5.901764892641288895, -37.31543133725893568, -31.71040919877874487 ) ) ;
#26312=EDGE_LOOP ( 'NONE', ( #57064, #31218, #29729, #35804 ) ) ;
#26316=ORIENTED_EDGE ( 'NONE', *, *, #28935, .T. ) ;
#26322=CARTESIAN_POINT ( 'NONE',  ( 4.975610109902397937, -46.23629923292386934, 15.95788333023201488 ) ) ;
#26323=ORIENTED_EDGE ( 'NONE', *, *, #17712, .F. ) ;
#26327=B_SPLINE_CURVE_WITH_KNOTS ( 'NONE', 3,
 ( #2445, #55067, #26573, #17494, #36613, #12194, #17804, #8084, #55374, #3671, #50675, #46319, #21571, #12812, #46026, #2756, #31588, #55678, #3361, #51596, #22497, #13116, #7764, #3065, #32523 ),
 .UNSPECIFIED., .F., .F.,
 ( 4, 3, 3, 3, 3, 3, 3, 3, 4 ),
 ( 6.254634441385501517E-18, 0.0005656085177311384474, 0.001131215744874498321, 0.001696821861372765266, 0.002262427090022496850, 0.002828031679238745492, 0.003393635864401603128, 0.003977030878808130755, 0.004561030005651157265 ),
 .UNSPECIFIED. ) ;
#26346=CARTESIAN_POINT ( 'NONE',  ( 1.479689385636123067, -2.586709720683578073, -43.98741613335128875 ) ) ;
#26348=CARTESIAN_POINT ( 'NONE',  ( 0.7413678028165009426, -42.40789325331365944, 12.08539124669933607 ) ) ;
#26351=CARTESIAN_POINT ( 'NONE',  ( 0.7948884756798504370, 44.60603610063805036, -20.51828910968767872 ) ) ;
#26357=FACE_OUTER_BOUND ( 'NONE', #30198, .T. ) ;
#26358=EDGE_LOOP ( 'NONE', ( #36335, #15608, #7025, #7192 ) ) ;
#26359=VERTEX_POINT ( 'NONE', #44677 ) ;
#26362=EDGE_LOOP ( 'NONE', ( #36153, #10217, #36262, #21 ) ) ;
#26364=ORIENTED_EDGE ( 'NONE', *, *, #4727, .F. ) ;
#26366=CARTESIAN_POINT ( 'NONE',  ( 4.975610109902397937, 42.89797504594955058, -23.49921581872176191 ) ) ;
#26368=CARTESIAN_POINT ( 'NONE',  ( 0.7044674535453004927, 37.93506595837544637, 31.18867572604858651 ) ) ;
#26369=EDGE_CURVE ( 'NONE', #6519, #37845, #46717, .T. ) ;
#26372=FACE_OUTER_BOUND ( 'NONE', #58013, .T. ) ;
#26380=ORIENTED_EDGE ( 'NONE', *, *, #23004, .F. ) ;
#26383=EDGE_CURVE ( 'NONE', #4156, #40797, #32512, .T. ) ;
#26388=CARTESIAN_POINT ( 'NONE',  ( 3.221118495291109163, 7.937357278700688745, -43.26383916265416474 ) ) ;
#26394=CARTESIAN_POINT ( 'NONE',  ( 4.226256110419178924, 42.39738639032160705, 11.54508021873209422 ) ) ;
#26397=CARTESIAN_POINT ( 'NONE',  ( 4.390527457369401532, -14.87174614414513485, -41.34025282037742954 ) ) ;
#26407=CARTESIAN_POINT ( 'NONE',  ( 4.553261556744873317, 1.182159483579998449, -43.91061448874312845 ) ) ;
#26412=CARTESIAN_POINT ( 'NONE',  ( 0.8744876279028263033, 27.35388303025786882, 40.76904626731490566 ) ) ;
#26417=CARTESIAN_POINT ( 'NONE',  ( 0.5997462898726536595, 17.44942740672471260, -45.90282249842328355 ) ) ;
#26418=CARTESIAN_POINT ( 'NONE',  ( 0.5997462898726536595, 32.62638226927734308, -36.70246327105708417 ) ) ;
#26420=ORIENTED_EDGE ( 'NONE', *, *, #61917, .F. ) ;
#26421=CARTESIAN_POINT ( 'NONE',  ( 0.8744876279028306332, -47.70753782033967383, -11.59055156152427557 ) ) ;
#26423=CARTESIAN_POINT ( 'NONE',  ( 0.1129192098497447394, -38.20615368646970467, 22.07354996983974260 ) ) ;
#26424=ORIENTED_EDGE ( 'NONE', *, *, #11878, .T. ) ;
#26436=CARTESIAN_POINT ( 'NONE',  ( 0.1157506346131639274, 15.15184229040494124, -41.44107063058978468 ) ) ;
#26445=CARTESIAN_POINT ( 'NONE',  ( 0.2285344041767132794, 37.38477457461466003, 23.42818388822967535 ) ) ;
#26448=CARTESIAN_POINT ( 'NONE',  ( 2.359973842542475886, -43.83014173065230779, -4.129717968993866783 ) ) ;
#26452=DIRECTION ( 'NONE',  ( 0.000000000000000000, 0.000000000000000000, -1.000000000000000000 ) ) ;
#26454=B_SPLINE_CURVE_WITH_KNOTS ( 'NONE', 3,
 ( #16793, #16469, #29951, #49059 ),
 .UNSPECIFIED., .F., .F.,
 ( 4, 4 ),
 ( 0.000000000000000000, 0.005013413432710150247 ),
 .UNSPECIFIED. ) ;
#26455=VECTOR ( 'NONE', #33722, 1000.000000000000114 ) ;
#26461=EDGE_CURVE ( 'NONE', #24074, #39259, #6268, .T. ) ;
#26462=ORIENTED_EDGE ( 'NONE', *, *, #43822, .T. ) ;
#26463=CARTESIAN_POINT ( 'NONE',  ( 4.975610109902397937, 39.54077024310134902, 28.79195887257488451 ) ) ;
#26464=DIRECTION ( 'NONE',  ( 0.09722883295013595717, 0.8299705264940721028, 0.5492681305103249700 ) ) ;
#26467=CIRCLE ( 'NONE', #61457, 48.91267123290010943 ) ;
#26469=LINE ( 'NONE', #2649, #34387 ) ;
#26477=CARTESIAN_POINT ( 'NONE',  ( 0.7242003506639981270, 32.40045956039464414, -36.89474074175420526 ) ) ;
#26479=CARTESIAN_POINT ( 'NONE',  ( 0.1155031312995260795, 44.04397861420763860, -2.658868248527860079 ) ) ;
#26480=FACE_OUTER_BOUND ( 'NONE', #38258, .T. ) ;
#26488=CARTESIAN_POINT ( 'NONE',  ( 0.7413678028165011646, 36.43924871080639605, -24.83278569074033015 ) ) ;
#26489=DIRECTION ( 'NONE',  ( -1.000000000000000000, -0.000000000000000000, -0.000000000000000000 ) ) ;
#26490=CARTESIAN_POINT ( 'NONE',  ( 4.694002226626920127, 23.33724324709868370, -39.16194388780874647 ) ) ;
#26495=CARTESIAN_POINT ( 'NONE',  ( -2.601141883200665639, 7.298105880293888070, -13.02048685838622433 ) ) ;
#26506=CARTESIAN_POINT ( 'NONE',  ( 0.6021448801613057400, 37.22278796205431206, 32.03131584807110954 ) ) ;
#26512=EDGE_LOOP ( 'NONE', ( #38181, #23208, #54252, #38312, #29437, #6227, #46725, #44812, #36366, #59131, #31123, #25274, #44669, #17144, #11988, #19071, #23102, #13782, #40510, #31141, #56000, #38567, #31487, #60976, #54541, #42204, #15265, #32547, #7692, #37472, #18638, #39067, #60789, #46604, #3268, #36875, #12670, #59812, #18820, #46068, #17378, #35016, #6514, #5381, #21066, #16231, #41565, #39883, #41597, #13192, #6551, #32946, #33561, #61555, #18986, #26192, #61653, #17352, #10806, #15453, #34737, #39683, #26520, #13759, #53990, #3870, #3186, #53410, #30075, #39022, #23776, #54869, #52022, #56464, #49626, #7954, #58048, #19506, #32955, #61721, #5690, #1914, #39398, #60502, #26284, #57086, #42413, #52763, #15879, #43719, #34021, #7699, #45839, #43426, #23578, #26840, #17230, #48804, #46481, #52259, #361, #43652, #26316, #42172, #42662, #24464, #31597, #43346, #47135, #35011, #53634, #25886, #55027, #1925, #42369, #31938, #30880, #51254, #35564, #59862, #51457, #42422, #3598, #47432, #53404, #15004, #51703, #28580, #61037, #14076, #33736, #19379, #24262, #15746, #32757, #61482, #16805, #22901, #35412, #50957, #42630, #45203, #18080, #27808, #871, #32275, #43645, #38629, #52857, #2010 ) ) ;
#26515=ADVANCED_FACE ( 'NONE', ( #50887 ), #20961, .F. ) ;
#26520=ORIENTED_EDGE ( 'NONE', *, *, #54245, .T. ) ;
#26530=CARTESIAN_POINT ( 'NONE',  ( 0.1158816050234198619, 39.75203506927189778, -19.14987595668801745 ) ) ;
#26533=ORIENTED_EDGE ( 'NONE', *, *, #53181, .T. ) ;
#26538=( BOUNDED_SURFACE ( )  B_SPLINE_SURFACE ( 3, 1, ( 
 ( #33793, #49103 ),
 ( #52872, #15602 ),
 ( #10903, #34708 ),
 ( #53769, #29993 ) ),
 .UNSPECIFIED., .F., .F., .F. ) 
 B_SPLINE_SURFACE_WITH_KNOTS ( ( 4, 4 ),
 ( 2, 2 ),
 ( 0.000000000000000000, 1.000000000000000000 ),
 ( 0.000000000000000000, 1.000000000000000000 ),
 .UNSPECIFIED. ) 
 GEOMETRIC_REPRESENTATION_ITEM ( )  RATIONAL_B_SPLINE_SURFACE ( (
 ( 1.000000000000000000, 1.000000000000000000),
 ( 0.9754377213608244057, 0.9999580625633939235),
 ( 0.9754377213608244057, 0.9999580625633939235),
 ( 1.000000000000000000, 1.000000000000000000) ) ) 
 REPRESENTATION_ITEM ( '' )  SURFACE ( )  );
#26539=CARTESIAN_POINT ( 'NONE',  ( 0.1157991065609915993, -43.77224717097112006, 5.561721239068830869 ) ) ;
#26543=( BOUNDED_SURFACE ( )  B_SPLINE_SURFACE ( 3, 1, ( 
 ( #32317, #12605 ),
 ( #31078, #26368 ),
 ( #50481, #21994 ),
 ( #56407, #50183 ) ),
 .UNSPECIFIED., .F., .F., .F. ) 
 B_SPLINE_SURFACE_WITH_KNOTS ( ( 4, 4 ),
 ( 2, 2 ),
 ( 0.000000000000000000, 1.000000000000000000 ),
 ( 0.000000000000000000, 1.000000000000000000 ),
 .UNSPECIFIED. ) 
 GEOMETRIC_REPRESENTATION_ITEM ( )  RATIONAL_B_SPLINE_SURFACE ( (
 ( 1.000000000000000000, 1.000000000000000000),
 ( 0.9953485035131437453, 0.8621029689291515030),
 ( 0.9953485035131437453, 0.8621029689291515030),
 ( 1.000000000000000000, 1.000000000000000000) ) ) 
 REPRESENTATION_ITEM ( '' )  SURFACE ( )  );
#26555=VERTEX_POINT ( 'NONE', #60900 ) ;
#26558=VERTEX_POINT ( 'NONE', #37132 ) ;
#26566=CARTESIAN_POINT ( 'NONE',  ( 0.5997462898726536595, 4.195097405482933972, 48.92803682862026449 ) ) ;
#26567=CARTESIAN_POINT ( 'NONE',  ( 0.1129192098497455998, -12.08918212651712132, -42.43587472053631160 ) ) ;
#26573=CARTESIAN_POINT ( 'NONE',  ( 4.226256110419178924, 17.40803085720605381, 40.34585123233550519 ) ) ;
#26574=CARTESIAN_POINT ( 'NONE',  ( 3.678834586032787346, 29.51645078674245326, -39.08185643725441594 ) ) ;
#26575=CARTESIAN_POINT ( 'NONE',  ( 3.678748215320119197, -9.636375565730645576, -48.01825778030346470 ) ) ;
#26576=EDGE_CURVE ( 'NONE', #24938, #27055, #36171, .T. ) ;
#26578=B_SPLINE_CURVE_WITH_KNOTS ( 'NONE', 3,
 ( #5575, #20034, #19712, #39148, #24094, #53504 ),
 .UNSPECIFIED., .F., .F.,
 ( 4, 2, 4 ),
 ( 2.032984328646362425E-17, 0.0002293755540694319419, 0.0004587511081388435550 ),
 .UNSPECIFIED. ) ;
#26582=VERTEX_POINT ( 'NONE', #47746 ) ;
#26587=CARTESIAN_POINT ( 'NONE',  ( 4.553261556744875094, -39.47791437445886942, -19.26223877088359515 ) ) ;
#26589=VERTEX_POINT ( 'NONE', #29239 ) ;
#26594=CARTESIAN_POINT ( 'NONE',  ( -6.057079549204054558, -16.13440658954581508, 10.51247616420408093 ) ) ;
#26595=EDGE_CURVE ( 'NONE', #13208, #19087, #5104, .T. ) ;
#26600=VERTEX_POINT ( 'NONE', #56507 ) ;
#26601=CARTESIAN_POINT ( 'NONE',  ( 4.975610109902397937, 34.73360008816130318, 34.43873447229810836 ) ) ;
#26603=ORIENTED_EDGE ( 'NONE', *, *, #49077, .F. ) ;
#26604=CARTESIAN_POINT ( 'NONE',  ( 0.1155031312995260795, -1.582654180881167383, 44.09576893847694379 ) ) ;
#26611=CARTESIAN_POINT ( 'NONE',  ( 4.553261556744875094, 0.000000000000000000, 0.000000000000000000 ) ) ;
#26623=ORIENTED_EDGE ( 'NONE', *, *, #54245, .F. ) ;
#26624=CARTESIAN_POINT ( 'NONE',  ( 0.8753041380234465318, 40.66072100792138855, 27.52896828776844274 ) ) ;
#26639=AXIS2_PLACEMENT_3D ( 'NONE', #32324, #44664, #42056 ) ;
#26641=CARTESIAN_POINT ( 'NONE',  ( -6.077587904424778920, -1.855182226445892812, -19.16648951426968850 ) ) ;
#26644=CARTESIAN_POINT ( 'NONE',  ( 4.975610109902397937, 25.84633036597824329, 41.52609557555928177 ) ) ;
#26645=EDGE_CURVE ( 'NONE', #26948, #15373, #406, .T. ) ;
#26650=EDGE_CURVE ( 'NONE', #7783, #32624, #53331, .T. ) ;
#26652=CARTESIAN_POINT ( 'NONE',  ( 0.1129192098497447394, -44.12161472487018443, 0.4846667466135898827 ) ) ;
#26655=ORIENTED_EDGE ( 'NONE', *, *, #3643, .F. ) ;
#26658=CARTESIAN_POINT ( 'NONE',  ( 2.185380717157383135, -42.20433799401791219, 12.55442780671010539 ) ) ;
#26662=DIRECTION ( 'NONE',  ( -1.000000000000000000, -0.000000000000000000, -0.000000000000000000 ) ) ;
#26664=CARTESIAN_POINT ( 'NONE',  ( 0.5997462898726536595, -45.31995669577334240, -18.91172004968183984 ) ) ;
#26666=CARTESIAN_POINT ( 'NONE',  ( 3.727782113643637096, -10.44443373141009523, 42.70470208227845177 ) ) ;
#26675=FACE_OUTER_BOUND ( 'NONE', #57954, .T. ) ;
#26677=CARTESIAN_POINT ( 'NONE',  ( 0.6039202388192952409, -42.70269169458205738, -24.24961514924442341 ) ) ;
#26682=CARTESIAN_POINT ( 'NONE',  ( 0.1135584504625008345, 43.39109096822844691, -8.010323134691606839 ) ) ;
#26684=CARTESIAN_POINT ( 'NONE',  ( 2.299746137290198611, -43.34124262129089544, -22.93072231153081830 ) ) ;
#26688=CARTESIAN_POINT ( 'NONE',  ( 2.299652685299200972, 3.424355312338875024, 48.91375589292864134 ) ) ;
#26700=ORIENTED_EDGE ( 'NONE', *, *, #20997, .F. ) ;
#26709=CARTESIAN_POINT ( 'NONE',  ( 4.553261556744873317, 43.92594400279101308, -0.2258523573157051323 ) ) ;
#26714=CARTESIAN_POINT ( 'NONE',  ( 0.5980271706414711508, -20.51809962909660356, 44.62125984832933767 ) ) ;
#26716=CARTESIAN_POINT ( 'NONE',  ( 2.533389852662419894, 41.24849501674540164, -15.36268826042980429 ) ) ;
#26720=EDGE_CURVE ( 'NONE', #40797, #31069, #51909, .T. ) ;
#26724=CARTESIAN_POINT ( 'NONE',  ( 0.6016117650947691020, 17.28651784492412347, 45.96441400737769811 ) ) ;
#26728=ORIENTED_EDGE ( 'NONE', *, *, #58111, .T. ) ;
#26732=CARTESIAN_POINT ( 'NONE',  ( 0.5549461598389365813, 3.360523605541063219, -43.97640931867226755 ) ) ;
#26739=CARTESIAN_POINT ( 'NONE',  ( 0.3676999524040366896, 36.51379593394493384, -24.75264207750488055 ) ) ;
#26740=ORIENTED_EDGE ( 'NONE', *, *, #21734, .F. ) ;
#26747=B_SPLINE_CURVE_WITH_KNOTS ( 'NONE', 3,
 ( #54185, #27470, #30390, #1569, #53883, #55968 ),
 .UNSPECIFIED., .F., .F.,
 ( 4, 2, 4 ),
 ( 2.335442953235084577E-18, 0.0002447193893791696538, 0.0004894387787583370309 ),
 .UNSPECIFIED. ) ;
#26750=CARTESIAN_POINT ( 'NONE',  ( 4.553261556744873317, 43.92594400279101308, -0.2258523573157051323 ) ) ;
#26764=B_SPLINE_CURVE_WITH_KNOTS ( 'NONE', 3,
 ( #41361, #22545, #41662, #51031, #12235, #18157, #21928, #59819, #36048, #41981, #60729, #31318, #8123, #37275, #56343, #55722, #46669, #51335, #36975, #45746, #56037, #60416, #2796, #13156, #17849 ),
 .UNSPECIFIED., .F., .F.,
 ( 4, 3, 3, 3, 3, 3, 3, 3, 4 ),
 ( 5.057544569639794935E-18, 0.0005656085177311396400, 0.001131215744874499406, 0.001696821861372766133, 0.002262427090022497717, 0.002828031679238745492, 0.003393635864401605296, 0.003977030878808131623, 0.004561030005651158133 ),
 .UNSPECIFIED. ) ;
#26768=B_SPLINE_CURVE_WITH_KNOTS ( 'NONE', 3,
 ( #16263, #31594, #54446, #50385, #7141, #21269, #40717, #2454, #26270, #20965, #30348, #20657, #21896, #26900, #41031, #7450, #11574, #7774, #50683 ),
 .UNSPECIFIED., .F., .F.,
 ( 4, 3, 3, 3, 3, 3, 4 ),
 ( 0.000000000000000000, 0.0002612768053151701911, 0.0003919133833142908170, 0.0005225499612322570672, 0.0006531865391693378016, 0.0008112755173415183395, 0.0009693688056799708384 ),
 .UNSPECIFIED. ) ;
#26770=CARTESIAN_POINT ( 'NONE',  ( -6.077587904424778920, 3.067159685105589784, -19.01022232536993783 ) ) ;
#26784=CARTESIAN_POINT ( 'NONE',  ( 0.6016118706126977189, -42.95818191652615781, 23.79381560848482735 ) ) ;
#26788=CARTESIAN_POINT ( 'NONE',  ( 0.6028777368367060907, 41.20378776142268862, -26.71680563657839258 ) ) ;
#26792=DIRECTION ( 'NONE',  ( 1.000000000000000000, 0.000000000000000000, 0.000000000000000000 ) ) ;
#26794=CARTESIAN_POINT ( 'NONE',  ( 0.6016117650947689910, -39.56281703554725482, -29.09182982310174381 ) ) ;
#26796=AXIS2_PLACEMENT_3D ( 'NONE', #39677, #25241, #49656 ) ;
#26802=CARTESIAN_POINT ( 'NONE',  ( 4.060580049360325461, 35.51942230849218163, -25.88123515658008600 ) ) ;
#26804=AXIS2_PLACEMENT_3D ( 'NONE', #37291, #60751, #17871 ) ;
#26805=EDGE_CURVE ( 'NONE', #34863, #21853, #7906, .T. ) ;
#26806=CARTESIAN_POINT ( 'NONE',  ( -2.601141883200665639, 11.07005473184224975, 10.01245802505087390 ) ) ;
#26818=VERTEX_POINT ( 'NONE', #32039 ) ;
#26819=VERTEX_POINT ( 'NONE', #59906 ) ;
#26820=CARTESIAN_POINT ( 'NONE',  ( 4.975610109902397937, 20.32389311291169065, 44.49032227207074186 ) ) ;
#26821=B_SPLINE_CURVE_WITH_KNOTS ( 'NONE', 3,
 ( #14185, #56445, #46779, #32985 ),
 .UNSPECIFIED., .F., .F.,
 ( 4, 4 ),
 ( 0.000000000000000000, 0.005013413432710144176 ),
 .UNSPECIFIED. ) ;
#26826=VERTEX_POINT ( 'NONE', #55197 ) ;
#26827=CARTESIAN_POINT ( 'NONE',  ( 0.5987334308729321819, 43.97851305131931809, -21.85070471093932909 ) ) ;
#26828=CARTESIAN_POINT ( 'NONE',  ( 0.1149546198390366814, -42.61083234180030388, -11.45702981414493316 ) ) ;
#26836=CARTESIAN_POINT ( 'NONE',  ( 0.8753041380234465318, -43.21430456406349663, 23.31656511833038437 ) ) ;
#26839=ORIENTED_EDGE ( 'NONE', *, *, #9843, .T. ) ;
#26840=ORIENTED_EDGE ( 'NONE', *, *, #5571, .T. ) ;
#26844=CARTESIAN_POINT ( 'NONE',  ( 0.6039202388192953519, -30.75412344224312378, -38.28508331123577335 ) ) ;
#26845=ADVANCED_FACE ( 'NONE', ( #2887 ), #7775, .F. ) ;
#26850=CARTESIAN_POINT ( 'NONE',  ( 0.8744876279028263033, 10.05549467470504865, 48.05452192277508061 ) ) ;
#26854=CARTESIAN_POINT ( 'NONE',  ( 0.1157991065609915715, 43.29484680596880253, 8.514611299724311522 ) ) ;
#26862=CARTESIAN_POINT ( 'NONE',  ( 0.6029443449137436017, 32.98273704066490808, 36.38239402911363385 ) ) ;
#26864=CARTESIAN_POINT ( 'NONE',  ( 0.3676999524040323597, 33.04872056100222011, 29.21870381457103605 ) ) ;
#26869=VERTEX_POINT ( 'NONE', #55506 ) ;
#26871=CARTESIAN_POINT ( 'NONE',  ( -6.078457390727109555, 16.77598442640648457, 9.453087197443768019 ) ) ;
#26872=CARTESIAN_POINT ( 'NONE',  ( 4.335381028904216727, 43.17230378757408005, -23.14970914153703418 ) ) ;
#26875=B_SPLINE_CURVE_WITH_KNOTS ( 'NONE', 3,
 ( #34442, #29718, #56985, #43233 ),
 .UNSPECIFIED., .F., .F.,
 ( 4, 4 ),
 ( 0.000000000000000000, 0.005013413432710139839 ),
 .UNSPECIFIED. ) ;
#26879=CARTESIAN_POINT ( 'NONE',  ( 0.1152339509894530906, -12.76855756083752347, -42.23631882954315842 ) ) ;
#26881=CARTESIAN_POINT ( 'NONE',  ( -6.078726893082806448, -11.01388439747492498, -15.79520154185373038 ) ) ;
#26882=CARTESIAN_POINT ( 'NONE',  ( 4.975610109902397937, 0.000000000000000000, 0.000000000000000000 ) ) ;
#26889=EDGE_CURVE ( 'NONE', #48800, #49846, #9303, .T. ) ;
#26900=CARTESIAN_POINT ( 'NONE',  ( 0.1152809850208375841, -38.33721451012828396, -21.84498262975196425 ) ) ;
#26901=CARTESIAN_POINT ( 'NONE',  ( 0.8744876279028306332, -20.68330519280286239, -44.52584571550401193 ) ) ;
#26903=EDGE_CURVE ( 'NONE', #29313, #11906, #19480, .T. ) ;
#26904=CARTESIAN_POINT ( 'NONE',  ( 0.7242486021783826056, -7.027028552307343467, -48.59662881413720470 ) ) ;
#26910=AXIS2_PLACEMENT_3D ( 'NONE', #9085, #28189, #47310 ) ;
#26918=CARTESIAN_POINT ( 'NONE',  ( -2.739355103387247858, -10.53896796905780597, -10.57249833758277724 ) ) ;
#26924=CARTESIAN_POINT ( 'NONE',  ( 0.1149546198390367924, -1.687975947156362233, 44.09191878592994129 ) ) ;
#26926=AXIS2_PLACEMENT_3D ( 'NONE', #24007, #24311, #57182 ) ;
#26948=VERTEX_POINT ( 'NONE', #47985 ) ;
#26952=CARTESIAN_POINT ( 'NONE',  ( 0.8744876279028263033, 36.80052600666216023, 32.49725120702480297 ) ) ;
#26959=CARTESIAN_POINT ( 'NONE',  ( 0.3676999524040323597, 9.009680404095913531, 43.18305503711946614 ) ) ;
#26960=VECTOR ( 'NONE', #47874, 1000.000000000000000 ) ;
#26968=CARTESIAN_POINT ( 'NONE',  ( 0.7044674535452954967, 10.10543771684589309, 48.05915991111220364 ) ) ;
#26971=VECTOR ( 'NONE', #44533, 1000.000000000000000 ) ;
#26974=CARTESIAN_POINT ( 'NONE',  ( 3.678748215320120085, 15.16704763906588660, -46.56794477120276099 ) ) ;
#26986=B_SPLINE_CURVE_WITH_KNOTS ( 'NONE', 3,
 ( #40703, #50671, #8079, #46315, #36927, #11562 ),
 .UNSPECIFIED., .F., .F.,
 ( 4, 2, 4 ),
 ( 7.589415207398530075E-19, 0.0002293801035737103749, 0.0004587602071474199909 ),
 .UNSPECIFIED. ) ;
#26991=CARTESIAN_POINT ( 'NONE',  ( 0.8753041380234524160, 21.91949880997755074, -43.93943445007425908 ) ) ;
#26994=B_SPLINE_CURVE_WITH_KNOTS ( 'NONE', 3,
 ( #47934, #916, #57595, #20051 ),
 .UNSPECIFIED., .F., .F.,
 ( 4, 4 ),
 ( 2.194270917860438266E-17, 0.004559932413162188537 ),
 .UNSPECIFIED. ) ;
#26996=ORIENTED_EDGE ( 'NONE', *, *, #58391, .T. ) ;
#27007=ADVANCED_FACE ( 'NONE', ( #30324, #40379 ), #59758, .F. ) ;
#27012=CARTESIAN_POINT ( 'NONE',  ( 1.112077966505211624, 14.23398767724693315, -41.71838827103148617 ) ) ;
#27017=CARTESIAN_POINT ( 'NONE',  ( -6.078726893082806448, -18.90026279491055305, -3.684305572565921949 ) ) ;
#27020=VERTEX_POINT ( 'NONE', #17172 ) ;
#27023=CARTESIAN_POINT ( 'NONE',  ( -6.078457390727109555, -18.27642172158506995, 6.063573211587478085 ) ) ;
#27025=CARTESIAN_POINT ( 'NONE',  ( 4.553261556744873317, 17.98701270972406618, 40.07501640179154379 ) ) ;
#27029=EDGE_CURVE ( 'NONE', #31834, #33849, #59325, .T. ) ;
#27032=CARTESIAN_POINT ( 'NONE',  ( 0.6253024248130499840, 16.31346559490675929, 46.31754600258349797 ) ) ;
#27039=CARTESIAN_POINT ( 'NONE',  ( 0.6026777506516366456, -47.45694871474268695, 12.62475383219417679 ) ) ;
#27050=CARTESIAN_POINT ( 'NONE',  ( -6.078726893082806448, 12.00859800336359129, -15.05282748397562820 ) ) ;
#27051=CARTESIAN_POINT ( 'NONE',  ( 0.7242003506639982380, 5.529506971589458253, 48.78971435433054893 ) ) ;
#27055=VERTEX_POINT ( 'NONE', #34199 ) ;
#27061=CARTESIAN_POINT ( 'NONE',  ( 0.7044674535452954967, -13.16383595884541613, -47.31295959522628181 ) ) ;
#27068=CARTESIAN_POINT ( 'NONE',  ( 0.6029443449137436017, -48.70980349588596425, 6.236552042235133264 ) ) ;
#27079=B_SPLINE_CURVE_WITH_KNOTS ( 'NONE', 3,
 ( #13847, #43280, #57320, #5324, #32951, #52330, #18853, #47051, #10055, #47649, #19161, #33564, #14455, #17, #4086, #42652, #57029, #37974, #14764 ),
 .UNSPECIFIED., .F., .F.,
 ( 4, 3, 3, 3, 3, 3, 4 ),
 ( 3.469870442581001870E-18, 0.0002612768053151703538, 0.0003919133833142884860, 0.0005225499612322571756, 0.0006531865391693334648, 0.0008112755173415197489, 0.0009693688056799711636 ),
 .UNSPECIFIED. ) ;
#27083=DIRECTION ( 'NONE',  ( 1.000000000000000000, 0.000000000000000000, 0.000000000000000000 ) ) ;
#27089=FACE_OUTER_BOUND ( 'NONE', #24754, .T. ) ;
#27093=CARTESIAN_POINT ( 'NONE',  ( 0.1368894036331292086, 10.43885750709124771, 42.87063773575076198 ) ) ;
#27095=EDGE_CURVE ( 'NONE', #11906, #40747, #39848, .T. ) ;
#27102=VERTEX_POINT ( 'NONE', #31567 ) ;
#27103=FACE_OUTER_BOUND ( 'NONE', #28305, .T. ) ;
#27105=CARTESIAN_POINT ( 'NONE',  ( 4.335381028904201628, 35.88831783935764008, 33.34344748710889661 ) ) ;
#27106=CARTESIAN_POINT ( 'NONE',  ( 0.8744876279028306332, 10.05549467470575209, -48.05452192277493850 ) ) ;
#27108=CARTESIAN_POINT ( 'NONE',  ( 0.1129192098497455998, -43.69739906996312584, -6.122834499277253428 ) ) ;
#27114=CARTESIAN_POINT ( 'NONE',  ( 0.5997462898726536595, -2.096122762665173944, 49.06279547180476897 ) ) ;
#27129=B_SPLINE_CURVE_WITH_KNOTS ( 'NONE', 3,
 ( #9765, #10083, #29179, #48294 ),
 .UNSPECIFIED., .F., .F.,
 ( 4, 4 ),
 ( 2.153172013482225773E-17, 0.004559932413162188537 ),
 .UNSPECIFIED. ) ;
#27131=CARTESIAN_POINT ( 'NONE',  ( 3.559346040607745287, 37.93169158444295874, 22.23998774920272226 ) ) ;
#27138=CARTESIAN_POINT ( 'NONE',  ( -6.077587904424778920, -6.644566705895037728, 18.07334376048996916 ) ) ;
#27143=CARTESIAN_POINT ( 'NONE',  ( 0.5997462898726536595, -20.35457962188229430, 44.69052157405150183 ) ) ;
#27147=ORIENTED_EDGE ( 'NONE', *, *, #29983, .T. ) ;
#27148=ORIENTED_EDGE ( 'NONE', *, *, #28715, .F. ) ;
#27153=DIRECTION ( 'NONE',  ( -1.000000000000000000, -0.000000000000000000, -0.000000000000000000 ) ) ;
#27154=B_SPLINE_CURVE_WITH_KNOTS ( 'NONE', 3,
 ( #13354, #37477, #32452, #17424, #27431, #55615, #27131, #46255, #51534, #3300, #22121, #22429, #8625, #41558, #27749, #17736, #13054, #32148, #46881, #51229, #3919, #8310, #23058, #61245, #56549 ),
 .UNSPECIFIED., .F., .F.,
 ( 4, 3, 3, 3, 3, 3, 3, 3, 4 ),
 ( 5.553824967135426632E-18, 0.0005656085177311389895, 0.001131215744874499622, 0.001696821861372764615, 0.002262427090022497284, 0.002828031679238744191, 0.003393635864401603128, 0.003977030878808129888, 0.004561030005651157265 ),
 .UNSPECIFIED. ) ;
#27163=CARTESIAN_POINT ( 'NONE',  ( 0.1145239942831223490, 43.24690139962650903, 8.755055684326428889 ) ) ;
#27166=CARTESIAN_POINT ( 'NONE',  ( -6.072942160501519027, 0.6317110510324334127, -19.24591134337430631 ) ) ;
#27169=DIRECTION ( 'NONE',  ( 0.1011922191286468153, -0.9947837607124679904, 0.01286095682984215484 ) ) ;
#27179=FACE_OUTER_BOUND ( 'NONE', #18389, .T. ) ;
#27188=VECTOR ( 'NONE', #32602, 1000.000000000000000 ) ;
#27189=CARTESIAN_POINT ( 'NONE',  ( 0.6039202388192953519, 28.23800208753055330, 40.17684595576924522 ) ) ;
#27194=CARTESIAN_POINT ( 'NONE',  ( 0.5997462898726536595, -2.096122762664449635, -49.06279547180479739 ) ) ;
#27197=CARTESIAN_POINT ( 'NONE',  ( -2.601141883200662974, 8.168301201416390711, -12.49296934088642352 ) ) ;
#27199=DIRECTION ( 'NONE',  ( -1.000000000000000000, -0.000000000000000000, -0.000000000000000000 ) ) ;
#27210=VERTEX_POINT ( 'NONE', #46607 ) ;
#27212=VERTEX_POINT ( 'NONE', #3653 ) ;
#27217=CARTESIAN_POINT ( 'NONE',  ( -6.063463321072276813, -16.13029782234890419, 10.51826718817296502 ) ) ;
#27224=ORIENTED_EDGE ( 'NONE', *, *, #54161, .F. ) ;
#27229=ORIENTED_EDGE ( 'NONE', *, *, #18558, .F. ) ;
#27234=CARTESIAN_POINT ( 'NONE',  ( 0.6029443199889047422, -25.45693689080298583, -41.99383295189993248 ) ) ;
#27237=CARTESIAN_POINT ( 'NONE',  ( 2.299746137290199943, 41.78301696717512215, 25.66049163221338958 ) ) ;
#27238=VERTEX_POINT ( 'NONE', #10231 ) ;
#27244=B_SPLINE_CURVE_WITH_KNOTS ( 'NONE', 3,
 ( #61582, #38440, #41911, #18704, #28394, #9287 ),
 .UNSPECIFIED., .F., .F.,
 ( 4, 2, 4 ),
 ( 7.589415207398530075E-19, 0.0002293801035737091281, 0.0004587602071474174972 ),
 .UNSPECIFIED. ) ;
#27245=VERTEX_POINT ( 'NONE', #14949 ) ;
#27250=EDGE_LOOP ( 'NONE', ( #25415, #42656, #40647, #24543 ) ) ;
#27259=DIRECTION ( 'NONE',  ( 0.000000000000000000, 0.000000000000000000, 1.000000000000000000 ) ) ;
#27260=CARTESIAN_POINT ( 'NONE',  ( 1.657374760986086271, -43.51830422218594663, 6.859128580039654643 ) ) ;
#27263=CARTESIAN_POINT ( 'NONE',  ( -6.057079549204054558, -18.27326637954053723, 6.076098001356776912 ) ) ;
#27271=EDGE_CURVE ( 'NONE', #26589, #58614, #14419, .T. ) ;
#27276=CARTESIAN_POINT ( 'NONE',  ( 0.1119899015040015933, 44.06612416965094781, -2.266717639542120022 ) ) ;
#27280=( BOUNDED_SURFACE ( )  B_SPLINE_SURFACE ( 3, 1, ( 
 ( #55622, #8317 ),
 ( #51539, #51858 ),
 ( #46263, #13359 ),
 ( #27138, #18058 ) ),
 .UNSPECIFIED., .F., .F., .F. ) 
 B_SPLINE_SURFACE_WITH_KNOTS ( ( 4, 4 ),
 ( 2, 2 ),
 ( 0.000000000000000000, 1.000000000000000000 ),
 ( 0.000000000000000000, 1.000000000000000000 ),
 .UNSPECIFIED. ) 
 GEOMETRIC_REPRESENTATION_ITEM ( )  RATIONAL_B_SPLINE_SURFACE ( (
 ( 1.000000000000000000, 1.000000000000000000),
 ( 0.9953485035131437453, 0.8621029689291523912),
 ( 0.9953485035131437453, 0.8621029689291523912),
 ( 1.000000000000000000, 1.000000000000000000) ) ) 
 REPRESENTATION_ITEM ( '' )  SURFACE ( )  );
#27281=CARTESIAN_POINT ( 'NONE',  ( -6.078726893082806448, 5.482141236672210205, -18.45914864585846260 ) ) ;
#27284=CARTESIAN_POINT ( 'NONE',  ( 0.1154773475650540254, 4.057870454246698344, -43.93719742339823853 ) ) ;
#27286=FACE_OUTER_BOUND ( 'NONE', #31951, .T. ) ;
#27290=ORIENTED_EDGE ( 'NONE', *, *, #40629, .F. ) ;
#27292=EDGE_LOOP ( 'NONE', ( #52744, #6449, #25075, #29301 ) ) ;
#27293=CARTESIAN_POINT ( 'NONE',  ( 0.7044674535452954967, -49.10288787214294359, -0.8420958536080156431 ) ) ;
#27296=CARTESIAN_POINT ( 'NONE',  ( -6.078726893082806448, 16.77644806189609739, 9.452239506869414498 ) ) ;
#27305=EDGE_CURVE ( 'NONE', #13508, #19147, #60764, .T. ) ;
#27310=ORIENTED_EDGE ( 'NONE', *, *, #18619, .T. ) ;
#27312=CARTESIAN_POINT ( 'NONE',  ( 0.1135584504625007651, -12.96809409308794336, 42.17559232219589660 ) ) ;
#27320=VERTEX_POINT ( 'NONE', #35899 ) ;
#27329=CARTESIAN_POINT ( 'NONE',  ( -6.057079549204054558, -19.21795591696652394, 1.225316886878610623 ) ) ;
#27330=CARTESIAN_POINT ( 'NONE',  ( 3.727782113643637096, 11.85551640071832047, 42.33467263105117695 ) ) ;
#27334=CARTESIAN_POINT ( 'NONE',  ( -6.077587904424778920, 13.82827771187065302, 13.40055061993020935 ) ) ;
#27337=CARTESIAN_POINT ( 'NONE',  ( 0.5987334363312691865, 17.52678475750561660, -45.87346425261718252 ) ) ;
#27339=CARTESIAN_POINT ( 'NONE',  ( 4.060580049360325461, -20.77244662311260015, 38.72948690144431794 ) ) ;
#27343=DIRECTION ( 'NONE',  ( -1.000000000000000000, -0.000000000000000000, -0.000000000000000000 ) ) ;
#27344=CARTESIAN_POINT ( 'NONE',  ( 4.553261556744873317, -43.85016385001095074, -2.588956575693968976 ) ) ;
#27347=DIRECTION ( 'NONE',  ( 1.000000000000000000, 0.000000000000000000, 0.000000000000000000 ) ) ;
#27350=EDGE_LOOP ( 'NONE', ( #54818, #164, #10937, #40130 ) ) ;
#27352=CARTESIAN_POINT ( 'NONE',  ( 0.8744876279028263033, 49.04340454744552602, -2.257104511335871422 ) ) ;
#27370=EDGE_CURVE ( 'NONE', #4827, #14464, #17403, .T. ) ;
#27374=CARTESIAN_POINT ( 'NONE',  ( 0.6029442701453591180, -48.69309925925927729, 6.366106320679863373 ) ) ;
#27377=CARTESIAN_POINT ( 'NONE',  ( 0.9268187852002115479, -43.84180739359310763, -4.652983706366343064 ) ) ;
#27385=CARTESIAN_POINT ( 'NONE',  ( 0.1365634738349401078, 15.83466825643062670, -41.18404910680874309 ) ) ;
#27392=CARTESIAN_POINT ( 'NONE',  ( 3.678834586032788234, 47.03015561595837113, -13.66663207842711714 ) ) ;
#27395=CARTESIAN_POINT ( 'NONE',  ( 0.1140933569871964148, -17.51328393204253331, -40.49981278968541432 ) ) ;
#27406=CARTESIAN_POINT ( 'NONE',  ( 0.6024113833632039894, -39.22478373599367529, -29.54586620773526917 ) ) ;
#27408=CARTESIAN_POINT ( 'NONE',  ( 3.390910168358336918, -24.45985921503985239, -36.54876774549406804 ) ) ;
#27413=CARTESIAN_POINT ( 'NONE',  ( 0.6016118706126978299, -1.922093031779197103, 49.06991556097398188 ) ) ;
#27417=VERTEX_POINT ( 'NONE', #8281 ) ;
#27422=EDGE_LOOP ( 'NONE', ( #32141, #12289, #56402, #14472 ) ) ;
#27426=EDGE_CURVE ( 'NONE', #5016, #17395, #35394, .T. ) ;
#27427=VERTEX_POINT ( 'NONE', #51503 ) ;
#27428=ORIENTED_EDGE ( 'NONE', *, *, #48852, .F. ) ;
#27430=EDGE_CURVE ( 'NONE', #41260, #45047, #37615, .T. ) ;
#27431=CARTESIAN_POINT ( 'NONE',  ( 3.894904216938897878, 38.00528577904427863, 22.08444215572074398 ) ) ;
#27433=CARTESIAN_POINT ( 'NONE',  ( 1.296416391601052487, -44.05760425873812380, 1.111252022081158142 ) ) ;
#27434=B_SPLINE_CURVE_WITH_KNOTS ( 'NONE', 3,
 ( #53033, #42215, #37198, #53336, #33956, #396 ),
 .UNSPECIFIED., .F., .F.,
 ( 4, 2, 4 ),
 ( 0.000000000000000000, 0.0002447195606305712767, 0.0004894391212611425533 ),
 .UNSPECIFIED. ) ;
#27435=VECTOR ( 'NONE', #13337, 1000.000000000000000 ) ;
#27436=CARTESIAN_POINT ( 'NONE',  ( 0.1158403557922069033, -42.67143984150880698, -11.22891486459464794 ) ) ;
#27439=ORIENTED_EDGE ( 'NONE', *, *, #17420, .T. ) ;
#27441=CARTESIAN_POINT ( 'NONE',  ( 0.7242003506640002364, 21.98227798157471469, -43.90661828092436991 ) ) ;
#27442=CARTESIAN_POINT ( 'NONE',  ( 0.8753041380234471980, 17.79089796329372675, -45.76704357430848802 ) ) ;
#27443=B_SPLINE_CURVE_WITH_KNOTS ( 'NONE', 3,
 ( #47526, #61897, #9603, #187 ),
 .UNSPECIFIED., .F., .F.,
 ( 4, 4 ),
 ( 0.000000000000000000, 0.004442905043737214836 ),
 .UNSPECIFIED. ) ;
#27449=CARTESIAN_POINT ( 'NONE',  ( 0.1119899015040010937, -35.02332288806953642, -26.83892997253300194 ) ) ;
#27454=CARTESIAN_POINT ( 'NONE',  ( -6.078726893082806448, 18.62710865126528859, 4.881072071039118221 ) ) ;
#27455=ORIENTED_EDGE ( 'NONE', *, *, #10941, .T. ) ;
#27459=CARTESIAN_POINT ( 'NONE',  ( 4.975610109902397937, 8.374023221152469887, -48.19050883970174226 ) ) ;
#27460=ORIENTED_EDGE ( 'NONE', *, *, #47334, .T. ) ;
#27461=CARTESIAN_POINT ( 'NONE',  ( 0.5997462898726536595, 46.76781179977627545, -14.97743000668059210 ) ) ;
#27462=CARTESIAN_POINT ( 'NONE',  ( 0.6008122571543326185, -25.08364935383093552, 42.21806586710685849 ) ) ;
#27465=CARTESIAN_POINT ( 'NONE',  ( 0.1158516988532803660, -27.54943813816733211, -34.46694963445543891 ) ) ;
#27466=CARTESIAN_POINT ( 'NONE',  ( 0.1158403557922069033, -27.54054956984768054, 34.47402553480782217 ) ) ;
#27470=CARTESIAN_POINT ( 'NONE',  ( 0.7948884756798507700, 49.04591923990457047, -2.279572440812163148 ) ) ;
#27474=AXIS2_PLACEMENT_3D ( 'NONE', #41937, #36615, #55376 ) ;
#27480=ORIENTED_EDGE ( 'NONE', *, *, #28427, .F. ) ;
#27488=CARTESIAN_POINT ( 'NONE',  ( 4.834790513006553603, 13.88525928490777162, -45.16402235757200856 ) ) ;
#27490=CONICAL_SURFACE ( 'NONE', #11492, 43.92652462719577500, 1.486293639869522343 ) ;
#27491=CARTESIAN_POINT ( 'NONE',  ( 0.6024113833632039894, 48.24301168413373375, -9.173532184791364230 ) ) ;
#27506=EDGE_CURVE ( 'NONE', #51246, #5538, #2401, .T. ) ;
#27507=CARTESIAN_POINT ( 'NONE',  ( 2.359973842542475886, -32.65604482613386494, -29.52488155685024296 ) ) ;
#27508=CARTESIAN_POINT ( 'NONE',  ( 3.050102900204245682, 28.21179670450542432, -33.75677377774299259 ) ) ;
#27512=CARTESIAN_POINT ( 'NONE',  ( 0.5980271706414734822, -35.76345691233123603, -33.66042769368046095 ) ) ;
#27517=CARTESIAN_POINT ( 'NONE',  ( 3.559346040607745287, -25.77953508153773043, 35.62086260215708933 ) ) ;
#27523=CARTESIAN_POINT ( 'NONE',  ( -6.072942160501519915, -16.13052748855437102, 10.51714054436908441 ) ) ;
#27529=EDGE_LOOP ( 'NONE', ( #6242, #622, #60533, #47248 ) ) ;
#27530=FACE_OUTER_BOUND ( 'NONE', #2534, .T. ) ;
#27531=( BOUNDED_SURFACE ( )  B_SPLINE_SURFACE ( 3, 1, ( 
 ( #23078, #42208 ),
 ( #46279, #41578 ),
 ( #61569, #18382 ),
 ( #9271, #8646 ) ),
 .UNSPECIFIED., .F., .F., .F. ) 
 B_SPLINE_SURFACE_WITH_KNOTS ( ( 4, 4 ),
 ( 2, 2 ),
 ( 0.000000000000000000, 1.000000000000000000 ),
 ( 0.000000000000000000, 1.000000000000000000 ),
 .UNSPECIFIED. ) 
 GEOMETRIC_REPRESENTATION_ITEM ( )  RATIONAL_B_SPLINE_SURFACE ( (
 ( 1.000000000000000000, 1.000000000000000000),
 ( 0.9754377213608244057, 0.9999580625633939235),
 ( 0.9754377213608244057, 0.9999580625633939235),
 ( 1.000000000000000000, 1.000000000000000000) ) ) 
 REPRESENTATION_ITEM ( '' )  SURFACE ( )  );
#27532=ORIENTED_EDGE ( 'NONE', *, *, #3438, .F. ) ;
#27545=CARTESIAN_POINT ( 'NONE',  ( 2.533389852662419894, 0.1716090839524149758, 44.01614569741339267 ) ) ;
#27549=B_SPLINE_CURVE_WITH_KNOTS ( 'NONE', 3,
 ( #548, #19686, #35028, #13068 ),
 .UNSPECIFIED., .F., .F.,
 ( 4, 4 ),
 ( 0.000000000000000000, 0.005013413432710138971 ),
 .UNSPECIFIED. ) ;
#27552=CARTESIAN_POINT ( 'NONE',  ( 0.5980271706414711508, 44.54819170408511297, -20.67626317151492898 ) ) ;
#27553=CARTESIAN_POINT ( 'NONE',  ( 1.830465331921977024, 21.46140052792654274, -38.46796515619592327 ) ) ;
#27576=EDGE_CURVE ( 'NONE', #50764, #8016, #18637, .T. ) ;
#27578=ORIENTED_EDGE ( 'NONE', *, *, #47326, .T. ) ;
#27580=CARTESIAN_POINT ( 'NONE',  ( 0.5997462898726536595, 46.43852004798865352, -15.96920429754923632 ) ) ;
#27582=CARTESIAN_POINT ( 'NONE',  ( 0.6253024248130479856, -42.44617096408522627, -24.69345658074805172 ) ) ;
#27583=CARTESIAN_POINT ( 'NONE',  ( 4.553261556744875094, 0.000000000000000000, 0.000000000000000000 ) ) ;
#27592=CARTESIAN_POINT ( 'NONE',  ( 0.1152339509894530906, 4.014506894015464233, -43.94117004419824468 ) ) ;
#27593=B_SPLINE_CURVE_WITH_KNOTS ( 'NONE', 3,
 ( #6654, #30796, #39305, #5437, #39937, #29880 ),
 .UNSPECIFIED., .F., .F.,
 ( 4, 2, 4 ),
 ( 0.000000000000000000, 0.0002447195606305739330, 0.0004894391212611478659 ),
 .UNSPECIFIED. ) ;
#27598=EDGE_CURVE ( 'NONE', #14660, #38699, #47756, .T. ) ;
#27599=CARTESIAN_POINT ( 'NONE',  ( 2.299746137290199499, 12.16324681505486360, 47.50091330282182867 ) ) ;
#27600=ORIENTED_EDGE ( 'NONE', *, *, #9843, .F. ) ;
#27608=CARTESIAN_POINT ( 'NONE',  ( 1.834102595619085507, -0.1089527116822509439, 44.04754106830824867 ) ) ;
#27609=ORIENTED_EDGE ( 'NONE', *, *, #48813, .F. ) ;
#27610=CARTESIAN_POINT ( 'NONE',  ( 0.1139756605157202785, 15.61149954950636243, 41.27028351623944502 ) ) ;
#27620=CARTESIAN_POINT ( 'NONE',  ( 0.1152809850208375703, -12.76645052879538866, 42.23698643825781573 ) ) ;
#27626=DIRECTION ( 'NONE',  ( -1.000000000000000000, -0.000000000000000000, -0.000000000000000000 ) ) ;
#27634=CARTESIAN_POINT ( 'NONE',  ( 0.6000166863083090663, 46.44114019838995944, -15.97009639238106793 ) ) ;
#27642=CARTESIAN_POINT ( 'NONE',  ( 2.648799415243708655, -36.17482712903017728, -33.10437048902125667 ) ) ;
#27643=CARTESIAN_POINT ( 'NONE',  ( -6.078457390727109555, 7.790511441124262859, -17.60972579352727152 ) ) ;
#27648=B_SPLINE_CURVE_WITH_KNOTS ( 'NONE', 3,
 ( #44806, #20357, #2139, #10965, #39173, #40114, #16268, #15666, #16580, #39802, #30050, #50093, #39478, #25978, #6212, #54452 ),
 .UNSPECIFIED., .F., .F.,
 ( 4, 3, 3, 3, 3, 4 ),
 ( 2.221635811791082109E-17, 0.0002612764279487699644, 0.0003919131003184752335, 0.0005225497727000622200, 0.0007837925190632447038, 0.001045051706266714132 ),
 .UNSPECIFIED. ) ;
#27653=CARTESIAN_POINT ( 'NONE',  ( 0.6021448801613057400, -47.56697366610597300, 12.20344848290548079 ) ) ;
#27658=CARTESIAN_POINT ( 'NONE',  ( -6.057079549204054558, -17.34624894862996314, 8.362946760077596409 ) ) ;
#27663=CARTESIAN_POINT ( 'NONE',  ( 1.296416391601053153, -30.87567274504310078, 31.44837367205435186 ) ) ;
#27665=B_SPLINE_CURVE_WITH_KNOTS ( 'NONE', 3,
 ( #15055, #34161, #19144, #28208, #24434, #33859 ),
 .UNSPECIFIED., .F., .F.,
 ( 4, 2, 4 ),
 ( 0.000000000000000000, 0.0002447195606305751798, 0.0004894391212611503596 ),
 .UNSPECIFIED. ) ;
#27670=EDGE_CURVE ( 'NONE', #12205, #3830, #58834, .T. ) ;
#27674=ORIENTED_EDGE ( 'NONE', *, *, #23657, .F. ) ;
#27676=DIRECTION ( 'NONE',  ( 0.000000000000000000, 0.000000000000000000, -1.000000000000000000 ) ) ;
#27682=ORIENTED_EDGE ( 'NONE', *, *, #3991, .F. ) ;
#27684=ORIENTED_EDGE ( 'NONE', *, *, #47735, .T. ) ;
#27686=VERTEX_POINT ( 'NONE', #11388 ) ;
#27697=CONICAL_SURFACE ( 'NONE', #19701, 43.92652462719577500, 1.486293639869522343 ) ;
#27700=ADVANCED_FACE ( 'NONE', ( #6962 ), #12197, .F. ) ;
#27712=CARTESIAN_POINT ( 'NONE',  ( 4.553261556744873317, -39.47791437445913942, 19.26223877088302672 ) ) ;
#27724=CARTESIAN_POINT ( 'NONE',  ( 0.6252788684277219566, 32.50271218743920087, -36.81056956410968439 ) ) ;
#27726=CARTESIAN_POINT ( 'NONE',  ( 0.6008122571543326185, -39.61437304146983962, -29.02164707587397174 ) ) ;
#27727=CARTESIAN_POINT ( 'NONE',  ( 3.050102900204245682, -24.33449941209498846, -36.65047595244580947 ) ) ;
#27742=DIRECTION ( 'NONE',  ( 0.000000000000000000, 0.000000000000000000, 1.000000000000000000 ) ) ;
#27749=CARTESIAN_POINT ( 'NONE',  ( 2.185380717157383135, 37.66778067744588299, 22.80258980692837767 ) ) ;
#27750=CARTESIAN_POINT ( 'NONE',  ( -4.915099999999998914, 12.80000000000000071, 3.000000000000000000 ) ) ;
#27753=CARTESIAN_POINT ( 'NONE',  ( 0.1158816050234199313, -42.68251980219233133, -11.18680225268246708 ) ) ;
#27757=CARTESIAN_POINT ( 'NONE',  ( 0.6000166863083090663, -31.02657807334566087, 38.06803035050591433 ) ) ;
#27760=ORIENTED_EDGE ( 'NONE', *, *, #21348, .T. ) ;
#27764=CARTESIAN_POINT ( 'NONE',  ( 3.390910168358337362, 38.72858971300023967, -20.83730969620907203 ) ) ;
#27766=ORIENTED_EDGE ( 'NONE', *, *, #39779, .T. ) ;
#27767=VERTEX_POINT ( 'NONE', #36140 ) ;
#27768=CARTESIAN_POINT ( 'NONE',  ( 0.1147471544378677044, -44.12318868410672934, 0.3104976971916312833 ) ) ;
#27770=CARTESIAN_POINT ( 'NONE',  ( -2.739355103387248747, -0.7412303453947486354, -14.90966614401821388 ) ) ;
#27771=VERTEX_POINT ( 'NONE', #54896 ) ;
#27775=CARTESIAN_POINT ( 'NONE',  ( 4.975610109902397937, -11.44439439467527642, -47.55497076097196185 ) ) ;
#27776=CARTESIAN_POINT ( 'NONE',  ( 0.6021448801613057400, -13.72177509508782833, -47.15139474996232849 ) ) ;
#27779=EDGE_CURVE ( 'NONE', #41166, #24004, #33112, .T. ) ;
#27780=CARTESIAN_POINT ( 'NONE',  ( 0.1152809850208375841, -27.68358432278522230, 34.35934285653605968 ) ) ;
#27781=CARTESIAN_POINT ( 'NONE',  ( 4.975610109902397937, 45.11887670192763267, -18.88746601040027784 ) ) ;
#27795=CARTESIAN_POINT ( 'NONE',  ( 0.8753041380234530822, -43.21430456406316978, -23.31656511833100964 ) ) ;
#27796=CARTESIAN_POINT ( 'NONE',  ( -6.057079549204054558, -17.35362438320633771, 8.347631512370735862 ) ) ;
#27798=CARTESIAN_POINT ( 'NONE',  ( 0.3676999524040366896, -31.10876963919527682, 31.27610965031171020 ) ) ;
#27802=CARTESIAN_POINT ( 'NONE',  ( 0.08486401232817714080, 0.000000000000000000, -3.000000000000000000 ) ) ;
#27808=ORIENTED_EDGE ( 'NONE', *, *, #15802, .T. ) ;
#27809=AXIS2_PLACEMENT_3D ( 'NONE', #57850, #47869, #14665 ) ;
#27810=CARTESIAN_POINT ( 'NONE',  ( 0.1129192098497455998, 39.96249028893973332, -18.70698152272436587 ) ) ;
#27812=CARTESIAN_POINT ( 'NONE',  ( 0.3676999524040323597, -43.84864779214683495, 4.821480075982420566 ) ) ;
#27816=ADVANCED_FACE ( 'NONE', ( #22638 ), #16200, .F. ) ;
#27819=CARTESIAN_POINT ( 'NONE',  ( 4.335381028904201628, -15.96267600302313383, 46.31360299617006859 ) ) ;
#27829=CARTESIAN_POINT ( 'NONE',  ( 2.533389852662419894, -26.18899039574286292, 35.37777994427159456 ) ) ;
#27836=CARTESIAN_POINT ( 'NONE',  ( 4.335381028904216727, 38.64381571559575690, 30.10668288940879478 ) ) ;
#27837=ORIENTED_EDGE ( 'NONE', *, *, #680, .T. ) ;
#27839=FACE_OUTER_BOUND ( 'NONE', #1084, .T. ) ;
#27841=DIRECTION ( 'NONE',  ( 1.000000000000000000, 0.000000000000000000, 0.000000000000000000 ) ) ;
#27846=CARTESIAN_POINT ( 'NONE',  ( 0.1119899015040012186, 25.70258781475827803, -35.86555851812634899 ) ) ;
#27851=CARTESIAN_POINT ( 'NONE',  ( 3.559346040607745287, -28.99128698353359823, -33.05957592862291250 ) ) ;
#27863=CARTESIAN_POINT ( 'NONE',  ( -6.077587904424778920, -17.35179747939691808, -8.349320069797613542 ) ) ;
#27864=CARTESIAN_POINT ( 'NONE',  ( 2.009741617377216460, -34.45716542851557307, 27.42640749815687329 ) ) ;
#27870=EDGE_CURVE ( 'NONE', #36560, #31693, #45760, .T. ) ;
#27874=CARTESIAN_POINT ( 'NONE',  ( 2.533389852662419894, -41.36703057798246164, -15.04058884797672313 ) ) ;
#27884=AXIS2_PLACEMENT_3D ( 'NONE', #37689, #43008, #56140 ) ;
#27886=FACE_OUTER_BOUND ( 'NONE', #57796, .T. ) ;
#27895=CARTESIAN_POINT ( 'NONE',  ( 0.8744876279028263033, -42.33402326122615733, -24.86323641237110493 ) ) ;
#27898=CARTESIAN_POINT ( 'NONE',  ( 0.7044674535453004927, -13.16383595884607871, 47.31295959522610417 ) ) ;
#27901=B_SPLINE_CURVE_WITH_KNOTS ( 'NONE', 3,
 ( #51638, #27846, #33490, #61641, #17841, #28454 ),
 .UNSPECIFIED., .F., .F.,
 ( 4, 2, 4 ),
 ( 1.964714961417949990E-17, 0.0002293755540694315353, 0.0004587511081388433924 ),
 .UNSPECIFIED. ) ;
#27906=EDGE_CURVE ( 'NONE', #17426, #48474, #36114, .T. ) ;
#27913=EDGE_LOOP ( 'NONE', ( #21266, #42601, #12926, #26839 ) ) ;
#27915=CARTESIAN_POINT ( 'NONE',  ( 0.7044674535452954967, -14.77841640690501457, 46.83376059334789687 ) ) ;
#27916=ORIENTED_EDGE ( 'NONE', *, *, #56986, .T. ) ;
#27920=( BOUNDED_SURFACE ( )  B_SPLINE_SURFACE ( 3, 1, ( 
 ( #18923, #38046 ),
 ( #24211, #19532 ),
 ( #705, #32706 ),
 ( #51788, #8886 ) ),
 .UNSPECIFIED., .F., .F., .F. ) 
 B_SPLINE_SURFACE_WITH_KNOTS ( ( 4, 4 ),
 ( 2, 2 ),
 ( 0.000000000000000000, 1.000000000000000000 ),
 ( 0.000000000000000000, 1.000000000000000000 ),
 .UNSPECIFIED. ) 
 GEOMETRIC_REPRESENTATION_ITEM ( )  RATIONAL_B_SPLINE_SURFACE ( (
 ( 1.000000000000000000, 1.000000000000000000),
 ( 0.9754377213608244057, 0.9999580625633939235),
 ( 0.9754377213608244057, 0.9999580625633939235),
 ( 1.000000000000000000, 1.000000000000000000) ) ) 
 REPRESENTATION_ITEM ( '' )  SURFACE ( )  );
#27924=CARTESIAN_POINT ( 'NONE',  ( 4.975610109902397937, 8.374023221151757568, 48.19050883970187016 ) ) ;
#27925=B_SPLINE_CURVE_WITH_KNOTS ( 'NONE', 3,
 ( #55173, #2555, #40819, #22920, #37331, #12296 ),
 .UNSPECIFIED., .F., .F.,
 ( 4, 2, 4 ),
 ( 0.000000000000000000, 0.0002447195606305757761, 0.0004894391212611515522 ),
 .UNSPECIFIED. ) ;
#27926=CARTESIAN_POINT ( 'NONE',  ( 0.8753041380234465318, -38.81339214172277963, -30.07754840950027031 ) ) ;
#27928=ADVANCED_FACE ( 'NONE', ( #61743 ), #45910, .F. ) ;
#27937=ORIENTED_EDGE ( 'NONE', *, *, #57139, .T. ) ;
#27939=CARTESIAN_POINT ( 'NONE',  ( 0.6039202388192953519, -1.399875120786322480, 49.08771804122896043 ) ) ;
#27940=CARTESIAN_POINT ( 'NONE',  ( 0.5549461598389364703, 8.956512157940801799, -43.18562938561233011 ) ) ;
#27941=DIRECTION ( 'NONE',  ( -0.1011922191286467460, 0.3909116750757886116, 0.9148487290679595541 ) ) ;
#27943=EDGE_CURVE ( 'NONE', #47983, #46169, #42381, .T. ) ;
#27945=EDGE_LOOP ( 'NONE', ( #21131, #54950, #30136, #56684 ) ) ;
#27954=CARTESIAN_POINT ( 'NONE',  ( 0.2940133293163028072, -41.18723740816950141, 15.80670820446579050 ) ) ;
#27961=CARTESIAN_POINT ( 'NONE',  ( 2.009741617377216460, -21.64669824990051694, 38.35263397083436843 ) ) ;
#27969=ORIENTED_EDGE ( 'NONE', *, *, #3259, .T. ) ;
#27974=B_SPLINE_CURVE_WITH_KNOTS ( 'NONE', 3,
 ( #40970, #11511, #30595, #16836, #21519, #45049 ),
 .UNSPECIFIED., .F., .F.,
 ( 4, 2, 4 ),
 ( 2.611104600503255956E-18, 0.0002447193893791691660, 0.0004894387787583357298 ),
 .UNSPECIFIED. ) ;
#27984=CARTESIAN_POINT ( 'NONE',  ( -6.078726893082806448, -17.35055002122458490, 8.351793533709011896 ) ) ;
#27985=ORIENTED_EDGE ( 'NONE', *, *, #7063, .T. ) ;
#27990=B_SPLINE_CURVE_WITH_KNOTS ( 'NONE', 3,
 ( #49419, #25618, #30009, #35971 ),
 .UNSPECIFIED., .F., .F.,
 ( 4, 4 ),
 ( 0.000000000000000000, 0.005013413432710155451 ),
 .UNSPECIFIED. ) ;
#27996=VERTEX_POINT ( 'NONE', #57052 ) ;
#27997=CARTESIAN_POINT ( 'NONE',  ( 0.6021448801613057400, 46.52272187781679946, 15.72187926764014065 ) ) ;
#28000=CARTESIAN_POINT ( 'NONE',  ( 0.5987334308729320709, 16.39078228288969186, -46.29152365957120452 ) ) ;
#28001=CARTESIAN_POINT ( 'NONE',  ( 0.7948884756798505480, -2.440498779800571505, 49.03817503033675962 ) ) ;
#28003=VERTEX_POINT ( 'NONE', #10394 ) ;
#28009=CARTESIAN_POINT ( 'NONE',  ( 0.6252788684277214015, 41.52615316421481140, 26.21112234445213574 ) ) ;
#28010=ADVANCED_FACE ( 'NONE', ( #6570 ), #35425, .F. ) ;
#28011=CARTESIAN_POINT ( 'NONE',  ( 2.648799415243708655, -29.47778256948722131, 39.18644916390910993 ) ) ;
#28012=CARTESIAN_POINT ( 'NONE',  ( 3.559346040607745287, -4.982408603749695963, 43.68759418928067362 ) ) ;
#28015=FACE_OUTER_BOUND ( 'NONE', #5827, .T. ) ;
#28022=CARTESIAN_POINT ( 'NONE',  ( 3.240649175237397372, -39.19469574595558470, 19.97600417449955401 ) ) ;
#28026=( BOUNDED_SURFACE ( )  B_SPLINE_SURFACE ( 3, 1, ( 
 ( #21149, #50267 ),
 ( #1706, #49964 ),
 ( #35880, #54952 ),
 ( #6702, #12084 ) ),
 .UNSPECIFIED., .F., .F., .F. ) 
 B_SPLINE_SURFACE_WITH_KNOTS ( ( 4, 4 ),
 ( 2, 2 ),
 ( 0.000000000000000000, 1.000000000000000000 ),
 ( 0.000000000000000000, 1.000000000000000000 ),
 .UNSPECIFIED. ) 
 GEOMETRIC_REPRESENTATION_ITEM ( )  RATIONAL_B_SPLINE_SURFACE ( (
 ( 1.000000000000000000, 1.000000000000000000),
 ( 0.7211978278499970862, 0.9934217856018976445),
 ( 0.7211978278499970862, 0.9934217856018976445),
 ( 1.000000000000000000, 1.000000000000000000) ) ) 
 REPRESENTATION_ITEM ( '' )  SURFACE ( )  );
#28030=CARTESIAN_POINT ( 'NONE',  ( 0.2285344041767070900, 40.07377575118545110, 18.45517995954402579 ) ) ;
#28034=CARTESIAN_POINT ( 'NONE',  ( 0.6000166863083106206, -2.096232480231295714, -49.06556115135418850 ) ) ;
#28042=CARTESIAN_POINT ( 'NONE',  ( -2.601141883200662974, -1.938888835821362067, 14.79986951130705108 ) ) ;
#28045=ORIENTED_EDGE ( 'NONE', *, *, #13443, .T. ) ;
#28049=ORIENTED_EDGE ( 'NONE', *, *, #424, .F. ) ;
#28050=CARTESIAN_POINT ( 'NONE',  ( 0.6016117650947689910, 10.58756707388382168, -47.95262743271228345 ) ) ;
#28058=CARTESIAN_POINT ( 'NONE',  ( 4.060580049360325461, -39.81183563956297178, 18.61411930142365989 ) ) ;
#28069=ORIENTED_EDGE ( 'NONE', *, *, #2239, .F. ) ;
#28073=CARTESIAN_POINT ( 'NONE',  ( 0.5987334363312694085, 23.24905850218390313, -43.25556825697827890 ) ) ;
#28077=CARTESIAN_POINT ( 'NONE',  ( 0.8753041380234465318, 37.96023374381077531, -31.14737520222577771 ) ) ;
#28081=CARTESIAN_POINT ( 'NONE',  ( 4.975610109902397937, -23.13264022976521161, -43.09675583078175265 ) ) ;
#28083=ORIENTED_EDGE ( 'NONE', *, *, #51684, .F. ) ;
#28084=CARTESIAN_POINT ( 'NONE',  ( 0.7413678028165009426, 43.45184631738121084, 7.511534023149208039 ) ) ;
#28086=CARTESIAN_POINT ( 'NONE',  ( 0.1157991065609916131, 37.02429157203778942, -24.00300396047191143 ) ) ;
#28087=VERTEX_POINT ( 'NONE', #15719 ) ;
#28090=CARTESIAN_POINT ( 'NONE',  ( 0.6000166863083106206, 11.43688157230965885, -47.76003791465640091 ) ) ;
#28094=CARTESIAN_POINT ( 'NONE',  ( 0.1157506346131639274, 33.53794432182292695, -28.67310500223404546 ) ) ;
#28107=CARTESIAN_POINT ( 'NONE',  ( -6.072942160501519915, 5.492864488351274943, 18.45623477314995853 ) ) ;
#28117=CARTESIAN_POINT ( 'NONE',  ( 0.5997462898726536595, -48.76843890605300658, -5.761162800241320880 ) ) ;
#28121=VECTOR ( 'NONE', #22882, 1000.000000000000000 ) ;
#28133=CARTESIAN_POINT ( 'NONE',  ( 4.060580049360325461, -25.55452198193345481, 35.75519683394414017 ) ) ;
#28135=CARTESIAN_POINT ( 'NONE',  ( 3.678748215320120973, 36.06704015422782561, -33.13278480316439101 ) ) ;
#28136=LINE ( 'NONE', #37563, #55546 ) ;
#28139=CARTESIAN_POINT ( 'NONE',  ( -6.063463321072278589, -14.65282214633749192, -12.49460906260262050 ) ) ;
#28141=CARTESIAN_POINT ( 'NONE',  ( 0.7948884756798489937, -43.19977691860155034, 23.33405062956740750 ) ) ;
#28157=CARTESIAN_POINT ( 'NONE',  ( -6.078075953587585900, -18.89992925442663818, 3.686169885505006238 ) ) ;
#28164=CARTESIAN_POINT ( 'NONE',  ( -6.063463321072276813, -6.665223333113386772, -18.06641221712797218 ) ) ;
#28173=CARTESIAN_POINT ( 'NONE',  ( 0.3676999524040366896, -38.83470403830472151, -20.92406140260821346 ) ) ;
#28177=VERTEX_POINT ( 'NONE', #41091 ) ;
#28182=CARTESIAN_POINT ( 'NONE',  ( -6.078726893082806448, -8.909671472910916989, 17.07078778245215034 ) ) ;
#28183=CARTESIAN_POINT ( 'NONE',  ( -6.078457390727109555, 0.6215653986401029618, 19.24599094597940052 ) ) ;
#28189=DIRECTION ( 'NONE',  ( -1.000000000000000000, -0.000000000000000000, -0.000000000000000000 ) ) ;
#28190=CARTESIAN_POINT ( 'NONE',  ( 3.894904216938897878, 23.29122489240411653, -37.27791806804204811 ) ) ;
#28200=B_SPLINE_CURVE_WITH_KNOTS ( 'NONE', 3,
 ( #10110, #61470, #43034, #42120 ),
 .UNSPECIFIED., .F., .F.,
 ( 4, 4 ),
 ( 0.000000000000000000, 0.005013413432710135502 ),
 .UNSPECIFIED. ) ;
#28201=CIRCLE ( 'NONE', #24221, 48.91267123290010943 ) ;
#28203=CARTESIAN_POINT ( 'NONE',  ( 0.1139756605157203062, 3.841029851089543090, -43.95681641541004581 ) ) ;
#28204=LINE ( 'NONE', #56391, #33547 ) ;
#28208=CARTESIAN_POINT ( 'NONE',  ( 0.7242003506639982380, -31.25070601918658753, -37.87354020194578652 ) ) ;
#28216=CARTESIAN_POINT ( 'NONE',  ( 0.1119899015040012463, -43.83035649366780717, 5.085386694293604570 ) ) ;
#28228=CARTESIAN_POINT ( 'NONE',  ( 0.1158816050234198619, -31.70051762657859840, -30.69233167278335728 ) ) ;
#28230=CARTESIAN_POINT ( 'NONE',  ( 4.553261556744875094, -43.82122302957815663, -3.039733214544628748 ) ) ;
#28232=ORIENTED_EDGE ( 'NONE', *, *, #15088, .F. ) ;
#28234=CARTESIAN_POINT ( 'NONE',  ( 0.6021447746440204973, 46.52271636273428612, -15.72189560202788527 ) ) ;
#28237=CARTESIAN_POINT ( 'NONE',  ( 0.5980271706414734822, 33.53334604750687475, 35.88264128655829666 ) ) ;
#28241=DIRECTION ( 'NONE',  ( 0.09722883295013595717, 0.1030875952483898822, -0.9899088350697040628 ) ) ;
#28245=ADVANCED_FACE ( 'NONE', ( #18182 ), #52957, .F. ) ;
#28258=LINE ( 'NONE', #33292, #15674 ) ;
#28259=CARTESIAN_POINT ( 'NONE',  ( 0.2279481005628781476, -31.16006227558741770, -31.23385992884048079 ) ) ;
#28263=CARTESIAN_POINT ( 'NONE',  ( 0.5997462898726536595, -39.66574928371219499, -28.95133786038212875 ) ) ;
#28266=CARTESIAN_POINT ( 'NONE',  ( 0.6028777368367060907, -39.40737854605714574, 29.30184883994229850 ) ) ;
#28270=CARTESIAN_POINT ( 'NONE',  ( 3.221118495291109163, -30.25413894314359453, 31.92880355526516567 ) ) ;
#28291=ORIENTED_EDGE ( 'NONE', *, *, #17560, .T. ) ;
#28292=CARTESIAN_POINT ( 'NONE',  ( 0.1368894036331280151, -7.670678564336283145, -43.45137530948780835 ) ) ;
#28296=ORIENTED_EDGE ( 'NONE', *, *, #46186, .T. ) ;
#28298=ORIENTED_EDGE ( 'NONE', *, *, #2108, .T. ) ;
#28299=CARTESIAN_POINT ( 'NONE',  ( 3.221118495291108719, 34.68635812792123119, 27.04843765327941441 ) ) ;
#28300=CARTESIAN_POINT ( 'NONE',  ( 0.6000166863083090663, 37.05402083933936552, 32.23077754796270966 ) ) ;
#28305=EDGE_LOOP ( 'NONE', ( #9423, #59525, #54610, #28835 ) ) ;
#28315=EDGE_LOOP ( 'NONE', ( #18045, #11894, #14814, #17986 ) ) ;
#28317=FACE_OUTER_BOUND ( 'NONE', #26312, .T. ) ;
#28319=CARTESIAN_POINT ( 'NONE',  ( 4.975610109902397937, 38.85236532789244279, 29.71435874397685595 ) ) ;
#28320=CARTESIAN_POINT ( 'NONE',  ( -4.915099999999998914, 0.000000000000000000, 0.000000000000000000 ) ) ;
#28323=CARTESIAN_POINT ( 'NONE',  ( 0.1155031312995260795, -17.70651496066106034, -40.41560293351683697 ) ) ;
#28327=CARTESIAN_POINT ( 'NONE',  ( 4.975610109902397937, 2.142807115709095100, 48.86571174967821918 ) ) ;
#28332=DIRECTION ( 'NONE',  ( 0.1011922191286468153, -0.2707140367832097105, 0.9573265091265147353 ) ) ;
#28333=CARTESIAN_POINT ( 'NONE',  ( 0.6000166863083106206, -1.051715750663621884, -49.09905676984293876 ) ) ;
#28334=CARTESIAN_POINT ( 'NONE',  ( 0.1158403557922069033, -35.33903139989523368, -26.42145277801803971 ) ) ;
#28336=B_SPLINE_CURVE_WITH_KNOTS ( 'NONE', 3,
 ( #46797, #3836, #4742, #37388, #56461, #8863 ),
 .UNSPECIFIED., .F., .F.,
 ( 4, 2, 4 ),
 ( 8.131516293641283255E-19, 0.0002293801035737058755, 0.0004587602071474109378 ),
 .UNSPECIFIED. ) ;
#28342=CARTESIAN_POINT ( 'NONE',  ( -6.077587904424778920, 3.067159685105589784, -19.01022232536993783 ) ) ;
#28349=VERTEX_POINT ( 'NONE', #15030 ) ;
#28351=DIRECTION ( 'NONE',  ( 0.09722883295013597105, -0.03945211390408235458, 0.9944798061055105665 ) ) ;
#28353=EDGE_CURVE ( 'NONE', #45831, #57398, #61354, .T. ) ;
#28358=EDGE_CURVE ( 'NONE', #18917, #55928, #46414, .T. ) ;
#28366=B_SPLINE_CURVE_WITH_KNOTS ( 'NONE', 3,
 ( #46934, #56294, #51908, #47531, #33442, #9939 ),
 .UNSPECIFIED., .F., .F.,
 ( 4, 2, 4 ),
 ( 5.421010862427522170E-19, 0.0002293801035737090468, 0.0004587602071474175514 ),
 .UNSPECIFIED. ) ;
#28368=ADVANCED_FACE ( 'NONE', ( #54434 ), #54585, .F. ) ;
#28388=ORIENTED_EDGE ( 'NONE', *, *, #41588, .F. ) ;
#28390=CARTESIAN_POINT ( 'NONE',  ( 0.5980271706414734822, -49.10762822256506865, 0.7000665654016514639 ) ) ;
#28392=ORIENTED_EDGE ( 'NONE', *, *, #51209, .F. ) ;
#28393=CARTESIAN_POINT ( 'NONE',  ( 0.1119898979215349644, 24.78191822507562847, -36.50777776498444638 ) ) ;
#28394=CARTESIAN_POINT ( 'NONE',  ( 0.1119898979215348533, -43.68681028663498722, 6.198702705517695755 ) ) ;
#28395=FACE_OUTER_BOUND ( 'NONE', #35407, .T. ) ;
#28410=CARTESIAN_POINT ( 'NONE',  ( 0.8744876279028263033, -29.90976330662845939, -38.93271258621668096 ) ) ;
#28417=CARTESIAN_POINT ( 'NONE',  ( 4.553261556744875094, 0.000000000000000000, 0.000000000000000000 ) ) ;
#28421=VERTEX_POINT ( 'NONE', #59772 ) ;
#28422=EDGE_CURVE ( 'NONE', #52129, #1361, #13569, .T. ) ;
#28425=DIRECTION ( 'NONE',  ( -0.1011922191286467182, 0.8730847945189542658, -0.4769518595913168069 ) ) ;
#28427=EDGE_CURVE ( 'NONE', #60972, #14899, #55370, .T. ) ;
#28429=VECTOR ( 'NONE', #22233, 999.9999999999998863 ) ;
#28435=EDGE_LOOP ( 'NONE', ( #43602, #8933, #32166, #10766 ) ) ;
#28443=CARTESIAN_POINT ( 'NONE',  ( 4.975610109902397937, 38.85236532789286201, -29.71435874397630528 ) ) ;
#28446=ORIENTED_EDGE ( 'NONE', *, *, #12560, .F. ) ;
#28454=CARTESIAN_POINT ( 'NONE',  ( 0.3676999524040323597, 25.91024933382809436, -35.70167450949183774 ) ) ;
#28456=CARTESIAN_POINT ( 'NONE',  ( 4.834790513006553603, -31.42367164492852893, -35.28657253511732961 ) ) ;
#28461=CARTESIAN_POINT ( 'NONE',  ( 0.1152809850208375980, -38.55430589558707766, 21.45951489198335338 ) ) ;
#28462=VERTEX_POINT ( 'NONE', #22493 ) ;
#28466=CARTESIAN_POINT ( 'NONE',  ( 5.901764892641307547, 30.49809846213652520, 38.31262791343741014 ) ) ;
#28470=AXIS2_PLACEMENT_3D ( 'NONE', #34864, #25439, #15138 ) ;
#28474=CARTESIAN_POINT ( 'NONE',  ( 4.335381028904216727, -46.80143676542533626, 14.47005059964335771 ) ) ;
#28480=CARTESIAN_POINT ( 'NONE',  ( 0.1147471544378675379, 20.13337721096016608, -39.26320555627666664 ) ) ;
#28484=CARTESIAN_POINT ( 'NONE',  ( -6.078726893082806448, 0.6205993875982012131, 19.24600991553399254 ) ) ;
#28487=VECTOR ( 'NONE', #31831, 999.9999999999998863 ) ;
#28495=VERTEX_POINT ( 'NONE', #60081 ) ;
#28502=CARTESIAN_POINT ( 'NONE',  ( 0.1152809850208375286, 4.457062010796396301, -43.89851797864788097 ) ) ;
#28507=CARTESIAN_POINT ( 'NONE',  ( 0.1365634738349425503, 41.67041550752998091, 14.50651891575141406 ) ) ;
#28509=ORIENTED_EDGE ( 'NONE', *, *, #43024, .T. ) ;
#28510=CARTESIAN_POINT ( 'NONE',  ( 4.553261556744875094, 0.000000000000000000, 0.000000000000000000 ) ) ;
#28514=ORIENTED_EDGE ( 'NONE', *, *, #34450, .F. ) ;
#28516=EDGE_CURVE ( 'NONE', #57370, #47719, #26986, .T. ) ;
#28526=CARTESIAN_POINT ( 'NONE',  ( -6.078075953587585900, 15.43522972334799093, 11.51298647765255900 ) ) ;
#28530=ORIENTED_EDGE ( 'NONE', *, *, #21788, .F. ) ;
#28531=FACE_OUTER_BOUND ( 'NONE', #18860, .T. ) ;
#28537=CARTESIAN_POINT ( 'NONE',  ( 0.1152339509894530906, 25.06061834086574081, -36.31677434504207724 ) ) ;
#28538=CARTESIAN_POINT ( 'NONE',  ( 0.1129192098497447394, -0.9297496242502409913, 44.11448008785053077 ) ) ;
#28544=( BOUNDED_SURFACE ( )  B_SPLINE_SURFACE ( 3, 1, ( 
 ( #19099, #57259 ),
 ( #14395, #61350 ),
 ( #28164, #51343 ),
 ( #56043, #23167 ) ),
 .UNSPECIFIED., .F., .F., .F. ) 
 B_SPLINE_SURFACE_WITH_KNOTS ( ( 4, 4 ),
 ( 2, 2 ),
 ( 0.000000000000000000, 1.000000000000000000 ),
 ( 0.000000000000000000, 1.000000000000000000 ),
 .UNSPECIFIED. ) 
 GEOMETRIC_REPRESENTATION_ITEM ( )  RATIONAL_B_SPLINE_SURFACE ( (
 ( 1.000000000000000000, 1.000000000000000000),
 ( 0.7211978278499970862, 0.9934217856018976445),
 ( 0.7211978278499970862, 0.9934217856018976445),
 ( 1.000000000000000000, 1.000000000000000000) ) ) 
 REPRESENTATION_ITEM ( '' )  SURFACE ( )  );
#28547=B_SPLINE_CURVE_WITH_KNOTS ( 'NONE', 3,
 ( #6319, #59896, #25773, #30772, #35500, #26082 ),
 .UNSPECIFIED., .F., .F.,
 ( 4, 2, 4 ),
 ( 1.951563910473907981E-18, 0.0002447193893791694912, 0.0004894387787583370309 ),
 .UNSPECIFIED. ) ;
#28548=EDGE_CURVE ( 'NONE', #34766, #15927, #47962, .T. ) ;
#28563=CARTESIAN_POINT ( 'NONE',  ( 0.1147471544378676767, 39.88833925880920361, 18.86458532932503473 ) ) ;
#28568=CARTESIAN_POINT ( 'NONE',  ( 0.3676999524040366896, 21.13209774130265473, 38.72189339863005841 ) ) ;
#28569=VERTEX_POINT ( 'NONE', #13111 ) ;
#28573=EDGE_CURVE ( 'NONE', #16242, #60250, #59145, .T. ) ;
#28574=VERTEX_POINT ( 'NONE', #55991 ) ;
#28576=CARTESIAN_POINT ( 'NONE',  ( 1.657374760986086271, 26.21018067049697109, 35.41068873196552858 ) ) ;
#28577=EDGE_CURVE ( 'NONE', #60250, #3477, #17339, .T. ) ;
#28580=ORIENTED_EDGE ( 'NONE', *, *, #51052, .T. ) ;
#28586=ORIENTED_EDGE ( 'NONE', *, *, #53724, .F. ) ;
#28588=EDGE_LOOP ( 'NONE', ( #46292, #55082, #6915, #771 ) ) ;
#28590=CARTESIAN_POINT ( 'NONE',  ( 4.975610109902397937, 19.27143522741655701, 44.95621415792550124 ) ) ;
#28593=CARTESIAN_POINT ( 'NONE',  ( -6.078726893082806448, 17.85000270430350611, 7.222980321520863001 ) ) ;
#28594=VERTEX_POINT ( 'NONE', #52755 ) ;
#28595=CARTESIAN_POINT ( 'NONE',  ( -6.077587904424778920, -11.02178778841116547, -15.78975032548523139 ) ) ;
#28597=ORIENTED_EDGE ( 'NONE', *, *, #49160, .T. ) ;
#28598=ORIENTED_EDGE ( 'NONE', *, *, #50017, .F. ) ;
#28602=CARTESIAN_POINT ( 'NONE',  ( 0.6029443449137434907, 46.59195503072400157, 15.51545243936909557 ) ) ;
#28608=CARTESIAN_POINT ( 'NONE',  ( 2.648799415243696664, -31.64453936086654906, 37.45851828260384764 ) ) ;
#28612=CARTESIAN_POINT ( 'NONE',  ( -6.078726893082806448, 12.00859800336337280, 15.05282748397580406 ) ) ;
#28614=CARTESIAN_POINT ( 'NONE',  ( 2.706805983486680223, -5.384497782719996906, 43.67817872745656871 ) ) ;
#28621=CARTESIAN_POINT ( 'NONE',  ( -6.077587904424778920, 16.77513308702641837, -9.454677747363051665 ) ) ;
#28623=EDGE_CURVE ( 'NONE', #17224, #61039, #39782, .T. ) ;
#28628=CARTESIAN_POINT ( 'NONE',  ( 4.834790513006555379, 1.975078679465946951, 47.20898648704820744 ) ) ;
#28633=CARTESIAN_POINT ( 'NONE',  ( 0.3676999524040366896, 40.09552319080398775, 18.39292264373822405 ) ) ;
#28637=CARTESIAN_POINT ( 'NONE',  ( 0.6021448801613057400, 41.01326314309687859, 27.00839471316351137 ) ) ;
#28638=CARTESIAN_POINT ( 'NONE',  ( 0.1158516988532803521, -35.39112975881853629, -26.35166205815612273 ) ) ;
#28644=CARTESIAN_POINT ( 'NONE',  ( 0.6029443199889047422, 22.71403544353044524, -43.53860626759250607 ) ) ;
#28648=ADVANCED_FACE ( 'NONE', ( #16764 ), #13937, .F. ) ;
#28654=B_SPLINE_CURVE_WITH_KNOTS ( 'NONE', 3,
 ( #51942, #47259, #23445, #56947, #55706, #17831 ),
 .UNSPECIFIED., .F., .F.,
 ( 4, 2, 4 ),
 ( 0.000000000000000000, 0.0002447195606305753424, 0.0004894391212611506848 ),
 .UNSPECIFIED. ) ;
#28668=CARTESIAN_POINT ( 'NONE',  ( 5.901764892641307547, 42.64666365787686431, 24.06768676652583849 ) ) ;
#28671=B_SPLINE_CURVE_WITH_KNOTS ( 'NONE', 3,
 ( #19014, #23692, #38130, #31869 ),
 .UNSPECIFIED., .F., .F.,
 ( 4, 4 ),
 ( 0.000000000000000000, 0.005013413432710149380 ),
 .UNSPECIFIED. ) ;
#28672=CARTESIAN_POINT ( 'NONE',  ( 0.7948878604505659196, 48.02008979560216062, -10.23570336228642219 ) ) ;
#28673=B_SPLINE_CURVE_WITH_KNOTS ( 'NONE', 3,
 ( #3040, #50963, #46294, #17164 ),
 .UNSPECIFIED., .F., .F.,
 ( 4, 4 ),
 ( 0.000000000000000000, 0.005013413432710145043 ),
 .UNSPECIFIED. ) ;
#28679=CARTESIAN_POINT ( 'NONE',  ( 0.3676999524040366896, 44.06746933160592050, 2.002181318165502599 ) ) ;
#28683=CARTESIAN_POINT ( 'NONE',  ( 0.8744876279028263033, -20.68330519280349122, 44.52584571550372061 ) ) ;
#28684=CARTESIAN_POINT ( 'NONE',  ( 1.830465331921977912, -5.808636319045533902, -43.66504093655992591 ) ) ;
#28690=LINE ( 'NONE', #53408, #26455 ) ;
#28696=DIRECTION ( 'NONE',  ( 0.1011922191286468153, 0.08272061902647194487, -0.9914219253051130831 ) ) ;
#28700=CARTESIAN_POINT ( 'NONE',  ( 0.1129192098497447394, 44.06201484046244587, 2.343210614524684487 ) ) ;
#28702=CARTESIAN_POINT ( 'NONE',  ( 0.6039202388192953519, 10.75760111029238786, -47.91490093072120260 ) ) ;
#28705=ADVANCED_FACE ( 'NONE', ( #47055 ), #48574, .F. ) ;
#28714=CARTESIAN_POINT ( 'NONE',  ( -6.078726893082806448, 5.482141236672210205, -18.45914864585846260 ) ) ;
#28715=EDGE_CURVE ( 'NONE', #27427, #30264, #56151, .T. ) ;
#28716=CARTESIAN_POINT ( 'NONE',  ( 2.009741617377216460, -16.56455318118139175, 40.80587770812996240 ) ) ;
#28723=DIRECTION ( 'NONE',  ( -0.1011922191286467598, 0.9882612224441083004, -0.1144547552576855587 ) ) ;
#28725=CARTESIAN_POINT ( 'NONE',  ( 0.1119898979215351448, -40.68569781727580903, 17.07733297014341645 ) ) ;
#28731=B_SPLINE_CURVE_WITH_KNOTS ( 'NONE', 3,
 ( #61529, #52143, #3903, #13338, #51831, #13968 ),
 .UNSPECIFIED., .F., .F.,
 ( 4, 2, 4 ),
 ( 0.000000000000000000, 0.0002293801035737094262, 0.0004587602071474188524 ),
 .UNSPECIFIED. ) ;
#28735=ORIENTED_EDGE ( 'NONE', *, *, #8085, .F. ) ;
#28737=CARTESIAN_POINT ( 'NONE',  ( 0.3676999524040323597, 5.056646555325726489, -43.82215089355327109 ) ) ;
#28738=LINE ( 'NONE', #9011, #1471 ) ;
#28754=DIRECTION ( 'NONE',  ( 0.000000000000000000, 0.000000000000000000, -1.000000000000000000 ) ) ;
#28756=CARTESIAN_POINT ( 'NONE',  ( 4.975610109902397937, 35.53430708602585497, -33.61193875773584949 ) ) ;
#28758=ORIENTED_EDGE ( 'NONE', *, *, #19809, .F. ) ;
#28760=CARTESIAN_POINT ( 'NONE',  ( 3.240649175237396040, 2.400950397866095987, 43.92607829734675562 ) ) ;
#28764=CARTESIAN_POINT ( 'NONE',  ( 0.6008122571543326185, -8.267105668410495767, -48.40670939376742865 ) ) ;
#28766=LINE ( 'NONE', #18147, #17179 ) ;
#28768=ORIENTED_EDGE ( 'NONE', *, *, #6330, .F. ) ;
#28769=CARTESIAN_POINT ( 'NONE',  ( 4.553261556744875094, 0.000000000000000000, 0.000000000000000000 ) ) ;
#28777=ORIENTED_EDGE ( 'NONE', *, *, #42492, .F. ) ;
#28793=DIRECTION ( 'NONE',  ( 0.000000000000000000, 0.000000000000000000, 1.000000000000000000 ) ) ;
#28795=DIRECTION ( 'NONE',  ( 1.000000000000000000, 0.000000000000000000, 0.000000000000000000 ) ) ;
#28798=CARTESIAN_POINT ( 'NONE',  ( -6.077587904424778920, -11.02178778841116547, -15.78975032548523139 ) ) ;
#28799=CARTESIAN_POINT ( 'NONE',  ( 0.6000166863083106206, -8.353387137038740917, 48.39467331274394013 ) ) ;
#28805=CARTESIAN_POINT ( 'NONE',  ( 4.975610109902397937, 0.000000000000000000, 0.000000000000000000 ) ) ;
#28812=CARTESIAN_POINT ( 'NONE',  ( 2.648799415243708655, 33.97949776740066596, 35.35408314134042485 ) ) ;
#28813=CARTESIAN_POINT ( 'NONE',  ( 3.894904216938898323, 40.51735868841397092, 17.04312111646823880 ) ) ;
#28818=CARTESIAN_POINT ( 'NONE',  ( 5.901764892641307547, 19.78248028302040495, 44.79559064563818538 ) ) ;
#28826=ORIENTED_EDGE ( 'NONE', *, *, #51249, .T. ) ;
#28830=CARTESIAN_POINT ( 'NONE',  ( 4.975610109902397937, 47.45567470742089000, 11.84940273605495520 ) ) ;
#28835=ORIENTED_EDGE ( 'NONE', *, *, #8594, .F. ) ;
#28843=CARTESIAN_POINT ( 'NONE',  ( 0.7242003506639991262, 27.41645750814208427, -40.73511423612637827 ) ) ;
#28846=CARTESIAN_POINT ( 'NONE',  ( 0.1149546198390367924, -18.11085549359680158, 40.23609670822052209 ) ) ;
#28853=EDGE_LOOP ( 'NONE', ( #13886, #46651, #54681, #30274 ) ) ;
#28855=CARTESIAN_POINT ( 'NONE',  ( 0.1156495703730067576, 25.13225202099905786, -36.26724226604579826 ) ) ;
#28858=ADVANCED_FACE ( 'NONE', ( #30693 ), #31385, .F. ) ;
#28861=EDGE_CURVE ( 'NONE', #59386, #34059, #16001, .T. ) ;
#28862=CARTESIAN_POINT ( 'NONE',  ( 0.5987334363312690755, -25.97268459165310261, 41.67712276026960438 ) ) ;
#28865=B_SPLINE_CURVE_WITH_KNOTS ( 'NONE', 3,
 ( #58610, #14813, #6594, #33925 ),
 .UNSPECIFIED., .F., .F.,
 ( 4, 4 ),
 ( 6.938893903907228378E-18, 0.005013413432710140706 ),
 .UNSPECIFIED. ) ;
#28866=CARTESIAN_POINT ( 'NONE',  ( 2.185380717157383579, -8.443826973212180675, -43.21483066163343523 ) ) ;
#28868=DIRECTION ( 'NONE',  ( 1.000000000000000000, 0.000000000000000000, 0.000000000000000000 ) ) ;
#28869=VECTOR ( 'NONE', #87, 1000.000000000000114 ) ;
#28875=CARTESIAN_POINT ( 'NONE',  ( 4.553261556744875094, 0.000000000000000000, 0.000000000000000000 ) ) ;
#28876=CARTESIAN_POINT ( 'NONE',  ( 4.553261556744875094, 0.000000000000000000, 0.000000000000000000 ) ) ;
#28877=CARTESIAN_POINT ( 'NONE',  ( 0.7413678028165012757, -22.05608674998674701, 38.18396429192890196 ) ) ;
#28878=CARTESIAN_POINT ( 'NONE',  ( 0.7242003506639991262, -45.81453560520021995, -17.66465401319446116 ) ) ;
#28882=AXIS2_PLACEMENT_3D ( 'NONE', #54948, #7324, #26452 ) ;
#28886=ORIENTED_EDGE ( 'NONE', *, *, #40061, .T. ) ;
#28891=ORIENTED_EDGE ( 'NONE', *, *, #46428, .T. ) ;
#28894=EDGE_LOOP ( 'NONE', ( #12679, #50678, #43128, #53152 ) ) ;
#28897=ADVANCED_FACE ( 'NONE', ( #12237 ), #18220, .F. ) ;
#28899=CARTESIAN_POINT ( 'NONE',  ( 0.6000166863083106206, 44.47108027094632376, -20.83618250168447972 ) ) ;
#28902=CARTESIAN_POINT ( 'NONE',  ( 4.975610109902397937, 38.85236532789286201, -29.71435874397630528 ) ) ;
#28903=ADVANCED_FACE ( 'NONE', ( #54803 ), #44222, .F. ) ;
#28905=ORIENTED_EDGE ( 'NONE', *, *, #23967, .F. ) ;
#28906=CARTESIAN_POINT ( 'NONE',  ( 0.6000166863083090663, 27.66667954482571545, 40.57558779207488442 ) ) ;
#28909=ORIENTED_EDGE ( 'NONE', *, *, #20307, .F. ) ;
#28914=CIRCLE ( 'NONE', #22943, 43.92652462719577500 ) ;
#28925=ORIENTED_EDGE ( 'NONE', *, *, #45565, .F. ) ;
#28927=CARTESIAN_POINT ( 'NONE',  ( 4.335381028904216727, -32.17603896083203807, -36.93858909670704094 ) ) ;
#28935=EDGE_CURVE ( 'NONE', #37380, #16660, #53154, .T. ) ;
#28941=CARTESIAN_POINT ( 'NONE',  ( 0.1156867017252034557, -31.78337558606124347, 30.60653269533405663 ) ) ;
#28942=VECTOR ( 'NONE', #56667, 1000.000000000000114 ) ;
#28944=CARTESIAN_POINT ( 'NONE',  ( 0.8753041380234471980, 37.96023374381077531, -31.14737520222577416 ) ) ;
#28945=CARTESIAN_POINT ( 'NONE',  ( 4.553261556744873317, -39.47791437445913942, 19.26223877088302672 ) ) ;
#28946=CARTESIAN_POINT ( 'NONE',  ( 5.901764892641307547, -48.07448765165377580, 9.318535532510814789 ) ) ;
#28959=CIRCLE ( 'NONE', #1933, 48.91267123290010943 ) ;
#28960=CARTESIAN_POINT ( 'NONE',  ( 0.6026112563231247332, 48.23484943966749228, -9.216305899698413739 ) ) ;
#28965=ORIENTED_EDGE ( 'NONE', *, *, #29706, .F. ) ;
#28978=CARTESIAN_POINT ( 'NONE',  ( -2.601141883200662974, 10.36212650428623228, 10.74345204199085302 ) ) ;
#28986=B_SPLINE_CURVE_WITH_KNOTS ( 'NONE', 3,
 ( #38545, #57597, #14730, #33846, #52922, #10026, #29120, #5589, #24734, #48239, #43875, #917, #48845, #16898, #31287, #12504 ),
 .UNSPECIFIED., .F., .F.,
 ( 4, 3, 3, 3, 3, 4 ),
 ( 2.194378057379452319E-17, 0.0002612764279487753854, 0.0003919131003184781609, 0.0005225497727000660148, 0.0007837925190632443785, 0.001045051706266714783 ),
 .UNSPECIFIED. ) ;
#28988=ORIENTED_EDGE ( 'NONE', *, *, #11385, .T. ) ;
#28993=CARTESIAN_POINT ( 'NONE',  ( 1.657374760986086271, 44.02697161945633297, 1.586258891804838367 ) ) ;
#28994=ORIENTED_EDGE ( 'NONE', *, *, #26094, .F. ) ;
#29006=ORIENTED_EDGE ( 'NONE', *, *, #32836, .F. ) ;
#29007=CARTESIAN_POINT ( 'NONE',  ( 0.6026112563231248442, 4.888769112786662596, -48.86349282916715708 ) ) ;
#29010=CARTESIAN_POINT ( 'NONE',  ( 0.1157991065609915715, 9.739164777550831431, 43.03592725820383436 ) ) ;
#29013=ORIENTED_EDGE ( 'NONE', *, *, #4062, .F. ) ;
#29022=CARTESIAN_POINT ( 'NONE',  ( 2.648799415243696664, -36.17482712903065334, 33.10437048902073798 ) ) ;
#29031=DIRECTION ( 'NONE',  ( 0.000000000000000000, 0.000000000000000000, -1.000000000000000000 ) ) ;
#29035=B_SPLINE_CURVE_WITH_KNOTS ( 'NONE', 3,
 ( #20176, #40774, #31650, #55129 ),
 .UNSPECIFIED., .F., .F.,
 ( 4, 4 ),
 ( 0.000000000000000000, 0.004442905043737216571 ),
 .UNSPECIFIED. ) ;
#29036=CARTESIAN_POINT ( 'NONE',  ( 0.8753041380234471980, -13.11588273819783268, -47.31925557181583741 ) ) ;
#29037=CARTESIAN_POINT ( 'NONE',  ( 0.6026777506516368677, -19.71849354655656228, 44.97474183240662171 ) ) ;
#29040=CARTESIAN_POINT ( 'NONE',  ( 0.3676999524040366896, 39.37931578713023839, -19.88014264185028068 ) ) ;
#29042=CARTESIAN_POINT ( 'NONE',  ( 4.553261556744875094, 0.000000000000000000, 0.000000000000000000 ) ) ;
#29048=CARTESIAN_POINT ( 'NONE',  ( -2.739355103387248747, 8.323596231104431808, -12.39214722041991834 ) ) ;
#29051=ORIENTED_EDGE ( 'NONE', *, *, #21251, .T. ) ;
#29065=ADVANCED_FACE ( 'NONE', ( #22787 ), #61723, .F. ) ;
#29066=ADVANCED_FACE ( 'NONE', ( #13402 ), #40955, .F. ) ;
#29068=CARTESIAN_POINT ( 'NONE',  ( 2.648799415243696664, 3.327403256648802987, 48.92285611917237986 ) ) ;
#29069=EDGE_LOOP ( 'NONE', ( #1068, #35300, #48630, #57681 ) ) ;
#29074=CARTESIAN_POINT ( 'NONE',  ( -2.739355103387247858, 8.754959582419541420, -12.09124681996101103 ) ) ;
#29076=DIRECTION ( 'NONE',  ( 0.000000000000000000, 0.000000000000000000, -1.000000000000000000 ) ) ;
#29083=CARTESIAN_POINT ( 'NONE',  ( 0.3676999524040323597, 36.51379593394458567, 24.75264207750540635 ) ) ;
#29084=EDGE_LOOP ( 'NONE', ( #53739, #55584, #10533, #44529 ) ) ;
#29087=CARTESIAN_POINT ( 'NONE',  ( 2.648799415243708655, -49.01629645596155171, 1.385692978581188006 ) ) ;
#29099=CARTESIAN_POINT ( 'NONE',  ( 0.6008122571543325074, -20.27531257495885342, -44.72657208475775548 ) ) ;
#29101=B_SPLINE_CURVE_WITH_KNOTS ( 'NONE', 3,
 ( #20229, #29304, #52797, #39345 ),
 .UNSPECIFIED., .F., .F.,
 ( 4, 4 ),
 ( 0.000000000000000000, 0.004442905043737216571 ),
 .UNSPECIFIED. ) ;
#29102=CARTESIAN_POINT ( 'NONE',  ( 4.553261556744875094, 0.000000000000000000, 0.000000000000000000 ) ) ;
#29103=CARTESIAN_POINT ( 'NONE',  ( 0.9268187852002115479, 10.77474991967946849, 42.75112977544562654 ) ) ;
#29108=ORIENTED_EDGE ( 'NONE', *, *, #6830, .T. ) ;
#29109=CARTESIAN_POINT ( 'NONE',  ( -6.057079549204054558, -19.21795591696650618, -1.225316886878888401 ) ) ;
#29110=CARTESIAN_POINT ( 'NONE',  ( 4.335381028904201628, -23.55321997556108471, -42.95349434501429897 ) ) ;
#29112=CARTESIAN_POINT ( 'NONE',  ( 4.975610109902397937, -5.269241389990889424, -48.62802178077758697 ) ) ;
#29113=DIRECTION ( 'NONE',  ( -1.000000000000000000, -0.000000000000000000, -0.000000000000000000 ) ) ;
#29120=CARTESIAN_POINT ( 'NONE',  ( 0.6027444965799114707, -47.46805475837615518, -12.58261869974789171 ) ) ;
#29121=CARTESIAN_POINT ( 'NONE',  ( 4.226256110419179812, 40.57295234433516384, 16.87195270416243886 ) ) ;
#29123=ORIENTED_EDGE ( 'NONE', *, *, #27095, .T. ) ;
#29137=ORIENTED_EDGE ( 'NONE', *, *, #51930, .F. ) ;
#29147=AXIS2_PLACEMENT_3D ( 'NONE', #54974, #45008, #12406 ) ;
#29149=EDGE_LOOP ( 'NONE', ( #60058, #27609, #34565, #57149 ) ) ;
#29153=CARTESIAN_POINT ( 'NONE',  ( -6.078726893082806448, 15.43407385306362301, 11.51448676958282391 ) ) ;
#29158=ORIENTED_EDGE ( 'NONE', *, *, #48542, .F. ) ;
#29160=VERTEX_POINT ( 'NONE', #14329 ) ;
#29165=CARTESIAN_POINT ( 'NONE',  ( 0.1145239942831223490, 25.51135876117968593, -36.00161183701438006 ) ) ;
#29169=CARTESIAN_POINT ( 'NONE',  ( 4.834790513006553603, 43.62201989944812652, 18.15788315901754757 ) ) ;
#29171=CARTESIAN_POINT ( 'NONE',  ( 2.881901170002227897, 8.474399077991585715E-12, -49.00591519830774700 ) ) ;
#29176=CARTESIAN_POINT ( 'NONE',  ( 4.060580049360325461, -9.288457618609966104, -42.95570101193199264 ) ) ;
#29179=CARTESIAN_POINT ( 'NONE',  ( 3.240649175237395152, 13.46447809955735586, 41.88045781631560516 ) ) ;
#29194=CARTESIAN_POINT ( 'NONE',  ( 4.553261556744873317, -20.51767157960462384, -38.84024612145397981 ) ) ;
#29198=ORIENTED_EDGE ( 'NONE', *, *, #29412, .F. ) ;
#29201=ORIENTED_EDGE ( 'NONE', *, *, #1888, .T. ) ;
#29202=CARTESIAN_POINT ( 'NONE',  ( 4.553261556744873317, 42.43205150231990075, -11.36048287389704292 ) ) ;
#29212=CARTESIAN_POINT ( 'NONE',  ( -2.739355103387247858, 6.670587007382158262, 13.35480572408154920 ) ) ;
#29226=DIRECTION ( 'NONE',  ( 1.000000000000000000, 0.000000000000000000, 0.000000000000000000 ) ) ;
#29232=CARTESIAN_POINT ( 'NONE',  ( 0.6008122571543325074, -14.38934544891279188, -46.95211697056022615 ) ) ;
#29236=ORIENTED_EDGE ( 'NONE', *, *, #8594, .T. ) ;
#29239=CARTESIAN_POINT ( 'NONE',  ( 4.553261556744875094, -15.38244134641827898, 41.14510984366961566 ) ) ;
#29240=CARTESIAN_POINT ( 'NONE',  ( -6.072942160501519915, 16.77122109808136230, -9.462045506564152220 ) ) ;
#29241=LINE ( 'NONE', #48358, #23558 ) ;
#29248=CARTESIAN_POINT ( 'NONE',  ( 0.2940135542859017570, 40.08987455701127800, 18.41310692671174820 ) ) ;
#29252=CARTESIAN_POINT ( 'NONE',  ( -6.078075953587585900, -8.901949479773122675, 17.07484903906043172 ) ) ;
#29254=CARTESIAN_POINT ( 'NONE',  ( 0.6000166863083106206, -20.35571918921451484, 44.69304395538860319 ) ) ;
#29259=CARTESIAN_POINT ( 'NONE',  ( 0.6026777506516368677, 48.16831407909742069, -9.558237777678705527 ) ) ;
#29260=CARTESIAN_POINT ( 'NONE',  ( 0.5997462898726536595, -31.02483596213057737, 38.06587952047342327 ) ) ;
#29262=CARTESIAN_POINT ( 'NONE',  ( 0.6029442701453591180, -1.661030530721965937, -49.07938673959044706 ) ) ;
#29264=CARTESIAN_POINT ( 'NONE',  ( 0.5980271706414711508, -8.528665270202141713, 48.36642545765100465 ) ) ;
#29266=VERTEX_POINT ( 'NONE', #35283 ) ;
#29270=CARTESIAN_POINT ( 'NONE',  ( 0.1152809850208375564, 41.80610087945574094, 14.11365338055760787 ) ) ;
#29276=VECTOR ( 'NONE', #57877, 1000.000000000000227 ) ;
#29278=ORIENTED_EDGE ( 'NONE', *, *, #57942, .F. ) ;
#29283=CARTESIAN_POINT ( 'NONE',  ( 0.2940133293163010308, 14.47847103911990985, 41.67270600701866812 ) ) ;
#29287=B_SPLINE_CURVE_WITH_KNOTS ( 'NONE', 3,
 ( #49292, #39617, #15490, #30184, #20801, #39938, #6348, #58672, #15798, #58995, #16106, #35218, #54277, #6655, #44939, #1977 ),
 .UNSPECIFIED., .F., .F.,
 ( 4, 3, 3, 3, 3, 4 ),
 ( 2.081781105835003463E-17, 0.0002612764279487747349, 0.0003919131003184788114, 0.0005225497727000652558, 0.0007837925190632463301, 0.001045051706266715650 ),
 .UNSPECIFIED. ) ;
#29288=CARTESIAN_POINT ( 'NONE',  ( 2.299652685299200972, -42.07683617587559155, -25.17581343843097841 ) ) ;
#29291=ORIENTED_EDGE ( 'NONE', *, *, #35275, .F. ) ;
#29293=CARTESIAN_POINT ( 'NONE',  ( -6.077587904424778920, 7.800189710370847074, -17.60548385805273242 ) ) ;
#29301=ORIENTED_EDGE ( 'NONE', *, *, #7201, .F. ) ;
#29302=B_SPLINE_CURVE_WITH_KNOTS ( 'NONE', 3,
 ( #28590, #37402, #23291, #51779 ),
 .UNSPECIFIED., .F., .F.,
 ( 4, 4 ),
 ( 6.938893903907228378E-18, 0.005013413432710138104 ),
 .UNSPECIFIED. ) ;
#29304=CARTESIAN_POINT ( 'NONE',  ( 2.299746137290199943, 48.83328922304266939, -4.426194905876138286 ) ) ;
#29306=CARTESIAN_POINT ( 'NONE',  ( 0.7242486021783793859, 28.75996529048175887, -39.79793787200863164 ) ) ;
#29310=VERTEX_POINT ( 'NONE', #7348 ) ;
#29312=CARTESIAN_POINT ( 'NONE',  ( 0.1152339509894530906, 10.03623295132059567, 42.96762407443620191 ) ) ;
#29313=VERTEX_POINT ( 'NONE', #12401 ) ;
#29321=CARTESIAN_POINT ( 'NONE',  ( 0.3676999524040323597, 30.26295534861902681, -32.09523511193413725 ) ) ;
#29327=ADVANCED_FACE ( 'NONE', ( #27103 ), #43109, .F. ) ;
#29329=FACE_OUTER_BOUND ( 'NONE', #17838, .T. ) ;
#29342=DIRECTION ( 'NONE',  ( 0.09722883295013594329, -0.3959434903494651881, 0.9131129757554853343 ) ) ;
#29348=CARTESIAN_POINT ( 'NONE',  ( 0.1152809850208375564, -23.06252723633350143, 37.61735131509301766 ) ) ;
#29362=VERTEX_POINT ( 'NONE', #31178 ) ;
#29366=CARTESIAN_POINT ( 'NONE',  ( 0.8753041380234471980, 3.828530797420656384, 48.95386276695825956 ) ) ;
#29368=ORIENTED_EDGE ( 'NONE', *, *, #38292, .T. ) ;
#29370=CARTESIAN_POINT ( 'NONE',  ( -2.739355103387247858, 12.65256472621583406, -7.922131834294089181 ) ) ;
#29372=CARTESIAN_POINT ( 'NONE',  ( 0.8744876279028306332, 28.81338721758086052, 39.75095932715638014 ) ) ;
#29375=ORIENTED_EDGE ( 'NONE', *, *, #52542, .F. ) ;
#29378=ORIENTED_EDGE ( 'NONE', *, *, #25562, .F. ) ;
#29391=ORIENTED_EDGE ( 'NONE', *, *, #60624, .T. ) ;
#29394=CARTESIAN_POINT ( 'NONE',  ( 0.5980271706414734822, 48.06821839532983631, -10.07450361757529045 ) ) ;
#29398=EDGE_LOOP ( 'NONE', ( #33716, #51939, #55927, #57515 ) ) ;
#29403=CARTESIAN_POINT ( 'NONE',  ( 0.6021448801613057400, -19.63870604132753783, -45.00958079841749537 ) ) ;
#29406=DIRECTION ( 'NONE',  ( -1.000000000000000000, -0.000000000000000000, -0.000000000000000000 ) ) ;
#29409=B_SPLINE_CURVE_WITH_KNOTS ( 'NONE', 3,
 ( #12072, #25519, #26445, #40580, #25834, #44656 ),
 .UNSPECIFIED., .F., .F.,
 ( 4, 2, 4 ),
 ( 0.000000000000000000, 0.0002293801035737085318, 0.0004587602071474170635 ),
 .UNSPECIFIED. ) ;
#29412=EDGE_CURVE ( 'NONE', #41724, #14140, #26267, .T. ) ;
#29414=EDGE_CURVE ( 'NONE', #8183, #31776, #11299, .T. ) ;
#29415=DIRECTION ( 'NONE',  ( 0.000000000000000000, 0.000000000000000000, 1.000000000000000000 ) ) ;
#29421=EDGE_CURVE ( 'NONE', #2222, #41260, #18958, .T. ) ;
#29431=CARTESIAN_POINT ( 'NONE',  ( 2.648799415243708655, 18.22894499609817132, 45.52167645879077185 ) ) ;
#29432=ORIENTED_EDGE ( 'NONE', *, *, #37599, .T. ) ;
#29437=ORIENTED_EDGE ( 'NONE', *, *, #41588, .T. ) ;
#29441=FACE_OUTER_BOUND ( 'NONE', #47089, .T. ) ;
#29447=DIRECTION ( 'NONE',  ( -1.000000000000000000, -0.000000000000000000, -0.000000000000000000 ) ) ;
#29450=B_SPLINE_CURVE_WITH_KNOTS ( 'NONE', 3,
 ( #25325, #58506, #1498, #12177, #15943, #35057 ),
 .UNSPECIFIED., .F., .F.,
 ( 4, 2, 4 ),
 ( 0.000000000000000000, 0.0002293801035737090739, 0.0004587602071474181477 ),
 .UNSPECIFIED. ) ;
#29460=CARTESIAN_POINT ( 'NONE',  ( 0.1157506346131639274, -17.77584971692775184, 40.38514363777890281 ) ) ;
#29473=B_SPLINE_CURVE_WITH_KNOTS ( 'NONE', 3,
 ( #22746, #8955, #55938, #42194, #3612, #17433 ),
 .UNSPECIFIED., .F., .F.,
 ( 4, 2, 4 ),
 ( 0.000000000000000000, 0.0002447195606305751256, 0.0004894391212611502512 ),
 .UNSPECIFIED. ) ;
#29477=CARTESIAN_POINT ( 'NONE',  ( 0.8744876279028263033, 41.62483489565955352, -26.03311679934954626 ) ) ;
#29480=( BOUNDED_SURFACE ( )  B_SPLINE_SURFACE ( 3, 1, ( 
 ( #32621, #19443 ),
 ( #52010, #38262 ),
 ( #302, #27915 ),
 ( #8, #57306 ) ),
 .UNSPECIFIED., .F., .F., .F. ) 
 B_SPLINE_SURFACE_WITH_KNOTS ( ( 4, 4 ),
 ( 2, 2 ),
 ( 0.000000000000000000, 1.000000000000000000 ),
 ( 0.000000000000000000, 1.000000000000000000 ),
 .UNSPECIFIED. ) 
 GEOMETRIC_REPRESENTATION_ITEM ( )  RATIONAL_B_SPLINE_SURFACE ( (
 ( 1.000000000000000000, 1.000000000000000000),
 ( 0.9953485035131437453, 0.8621029689291523912),
 ( 0.9953485035131437453, 0.8621029689291523912),
 ( 1.000000000000000000, 1.000000000000000000) ) ) 
 REPRESENTATION_ITEM ( '' )  SURFACE ( )  );
#29483=CARTESIAN_POINT ( 'NONE',  ( 0.8753041380234530822, -47.71532843791157319, -11.59248721954040917 ) ) ;
#29489=CARTESIAN_POINT ( 'NONE',  ( 0.1158403557922069033, -43.75702967194915516, -5.680023016853070317 ) ) ;
#29495=CARTESIAN_POINT ( 'NONE',  ( 0.5997462898726536595, 23.17609050332929854, -43.29457771044543080 ) ) ;
#29498=LINE ( 'NONE', #24182, #50861 ) ;
#29502=EDGE_LOOP ( 'NONE', ( #34115, #60114, #44262, #27148 ) ) ;
#29503=CARTESIAN_POINT ( 'NONE',  ( 0.8744876279028263033, -14.81965677138014037, 46.80521149998127584 ) ) ;
#29508=DIRECTION ( 'NONE',  ( 0.09722883295013597105, 0.9421506058508642978, 0.3207784125186792790 ) ) ;
#29513=CARTESIAN_POINT ( 'NONE',  ( -6.078726893082806448, 7.791390017580090088, 17.60932374802262146 ) ) ;
#29519=CARTESIAN_POINT ( 'NONE',  ( -6.078075953587585900, -11.02105682227004024, -15.79023371478177218 ) ) ;
#29534=CARTESIAN_POINT ( 'NONE',  ( 4.975610109902397937, 7.237810502494091303, 48.37420290059321104 ) ) ;
#29536=EDGE_LOOP ( 'NONE', ( #24406, #4595, #61774, #22615 ) ) ;
#29538=CARTESIAN_POINT ( 'NONE',  ( 0.6026777506516367566, -14.13933751125005678, -47.02792282655249068 ) ) ;
#29539=CARTESIAN_POINT ( 'NONE',  ( 1.479689385636123067, -5.869565535353596708, 43.67072298112183404 ) ) ;
#29541=ORIENTED_EDGE ( 'NONE', *, *, #1619, .T. ) ;
#29542=B_SPLINE_CURVE_WITH_KNOTS ( 'NONE', 3,
 ( #39193, #48871, #25066, #1241, #15686, #34789, #8114, #41353, #6857, #60405, #54467, #2159, #26604, #12225, #26924, #21917, #12529, #26296, #46352 ),
 .UNSPECIFIED., .F., .F.,
 ( 4, 3, 3, 3, 3, 3, 4 ),
 ( 1.517943542627326963E-18, 0.0002612768053151708417, 0.0003919133833142907628, 0.0005225499612322602114, 0.0006531865391693355248, 0.0008112755173415186647, 0.0009693688056799723562 ),
 .UNSPECIFIED. ) ;
#29549=CARTESIAN_POINT ( 'NONE',  ( 0.1135584504625007929, -31.99564635880365771, 30.38471106029520996 ) ) ;
#29558=VERTEX_POINT ( 'NONE', #20185 ) ;
#29560=CARTESIAN_POINT ( 'NONE',  ( 0.1156495703730067576, -7.176750697220416697, -43.53661910002907831 ) ) ;
#29562=CARTESIAN_POINT ( 'NONE',  ( 5.901764892641307547, -44.10106349910979162, -21.28585600080873164 ) ) ;
#29565=CARTESIAN_POINT ( 'NONE',  ( 4.553261556744875094, 0.000000000000000000, 0.000000000000000000 ) ) ;
#29574=ORIENTED_EDGE ( 'NONE', *, *, #56988, .F. ) ;
#29578=CARTESIAN_POINT ( 'NONE',  ( 0.5549461598389364703, 43.94904939407230415, -3.701182625080478683 ) ) ;
#29585=ORIENTED_EDGE ( 'NONE', *, *, #35275, .T. ) ;
#29590=CARTESIAN_POINT ( 'NONE',  ( 1.479689385636123067, -11.40586458698099648, 42.56160356813574452 ) ) ;
#29592=CARTESIAN_POINT ( 'NONE',  ( 0.2940135542859015905, 5.036457902034579881, 43.82778388753477827 ) ) ;
#29595=CARTESIAN_POINT ( 'NONE',  ( 4.975610109902397937, -33.30777373088901072, 35.81957029655259817 ) ) ;
#29599=CARTESIAN_POINT ( 'NONE',  ( -6.078075953587585900, 7.799379819826517846, -17.60581860275797439 ) ) ;
#29600=CARTESIAN_POINT ( 'NONE',  ( 4.390527457369401532, 43.93270324789031633, 0.3208145280799595822 ) ) ;
#29605=CARTESIAN_POINT ( 'NONE',  ( 0.1158403557922069033, -40.88518614858649869, -16.59342824069968003 ) ) ;
#29606=ORIENTED_EDGE ( 'NONE', *, *, #27370, .F. ) ;
#29612=ORIENTED_EDGE ( 'NONE', *, *, #2465, .T. ) ;
#29615=CARTESIAN_POINT ( 'NONE',  ( 3.240649175237395152, 41.13842520339412800, 15.58508547241233444 ) ) ;
#29620=CARTESIAN_POINT ( 'NONE',  ( 0.3676999524040323597, -42.45338881270421894, -11.98584004733086061 ) ) ;
#29624=FACE_OUTER_BOUND ( 'NONE', #42265, .T. ) ;
#29630=CARTESIAN_POINT ( 'NONE',  ( 4.060580049360325461, -15.64928826502552006, 41.06783986475723225 ) ) ;
#29634=EDGE_CURVE ( 'NONE', #52990, #46812, #31484, .T. ) ;
#29637=FACE_OUTER_BOUND ( 'NONE', #52477, .T. ) ;
#29639=B_SPLINE_CURVE_WITH_KNOTS ( 'NONE', 3,
 ( #42746, #60898, #42147, #13940, #33351, #37129 ),
 .UNSPECIFIED., .F., .F.,
 ( 4, 2, 4 ),
 ( 1.870693080156664505E-17, 0.0002293755540694324298, 0.0004587511081388461571 ),
 .UNSPECIFIED. ) ;
#29640=CARTESIAN_POINT ( 'NONE',  ( 0.6028777368367060907, -19.95745447572438636, 44.86914129065165469 ) ) ;
#29642=ADVANCED_FACE ( 'NONE', ( #39927 ), #45859, .F. ) ;
#29657=CARTESIAN_POINT ( 'NONE',  ( 0.1129192098497447394, 41.72114954716796120, -14.36305915353690743 ) ) ;
#29658=CARTESIAN_POINT ( 'NONE',  ( 0.1158403557922069033, 9.855458665879178071, -43.00942038285294444 ) ) ;
#29660=ORIENTED_EDGE ( 'NONE', *, *, #39686, .T. ) ;
#29668=LINE ( 'NONE', #216, #26960 ) ;
#29672=CARTESIAN_POINT ( 'NONE',  ( -6.063463321072276813, -1.864608017455207767, -19.16621218239826518 ) ) ;
#29685=ORIENTED_EDGE ( 'NONE', *, *, #48374, .T. ) ;
#29686=CARTESIAN_POINT ( 'NONE',  ( -6.072942160501519027, 18.62280723096618118, 4.898490903053114742 ) ) ;
#29687=EDGE_CURVE ( 'NONE', #43286, #31957, #49334, .T. ) ;
#29689=CARTESIAN_POINT ( 'NONE',  ( 4.975610109902397937, 13.36434394399761949, -47.05150069959838532 ) ) ;
#29692=LINE ( 'NONE', #48807, #59264 ) ;
#29696=CARTESIAN_POINT ( 'NONE',  ( 0.1140933569871964703, -38.63098921247078010, 21.32127159786375614 ) ) ;
#29699=CARTESIAN_POINT ( 'NONE',  ( 4.553261556744875094, 22.57774691820428714, 37.68003330573307608 ) ) ;
#29706=EDGE_CURVE ( 'NONE', #46812, #28087, #32049, .T. ) ;
#29708=ORIENTED_EDGE ( 'NONE', *, *, #57658, .F. ) ;
#29712=CARTESIAN_POINT ( 'NONE',  ( 0.6000166863083090663, 41.44150143800037966, 26.35195325346236928 ) ) ;
#29717=LINE ( 'NONE', #15644, #37742 ) ;
#29718=CARTESIAN_POINT ( 'NONE',  ( 4.834790513006553603, 46.91907382339847032, -5.584787594785217912 ) ) ;
#29725=EDGE_CURVE ( 'NONE', #13345, #26826, #43377, .T. ) ;
#29726=CARTESIAN_POINT ( 'NONE',  ( 4.060580049360325461, -19.88058780675999415, -39.19476907467264226 ) ) ;
#29727=CARTESIAN_POINT ( 'NONE',  ( 0.5997462898726536595, 4.195097405482933972, 48.92803682862026449 ) ) ;
#29729=ORIENTED_EDGE ( 'NONE', *, *, #24112, .T. ) ;
#29733=CARTESIAN_POINT ( 'NONE',  ( 0.5549461598389366923, 24.50808299993816419, -36.66840006238268046 ) ) ;
#29743=CONICAL_SURFACE ( 'NONE', #2733, 43.92652462719577500, 1.486293639869522343 ) ;
#29745=CARTESIAN_POINT ( 'NONE',  ( 4.694002226626921015, 32.50760209236046450, -31.96154842386231820 ) ) ;
#29747=CARTESIAN_POINT ( 'NONE',  ( 3.678748215320119197, -38.11576136296564243, 30.75388674657139276 ) ) ;
#29750=CARTESIAN_POINT ( 'NONE',  ( 0.1129192098497447394, 20.83764143887560749, 38.89401608281161060 ) ) ;
#29753=CARTESIAN_POINT ( 'NONE',  ( 0.8744876279028263033, -35.88078294188978390, 33.50999053799454686 ) ) ;
#29758=CARTESIAN_POINT ( 'NONE',  ( 0.6039202388192952409, -45.58380534490273561, 18.26692100839678545 ) ) ;
#29762=CARTESIAN_POINT ( 'NONE',  ( 0.5980271706414734822, 43.94069670602981859, -21.93773953328744852 ) ) ;
#29763=CARTESIAN_POINT ( 'NONE',  ( 4.060580049360325461, -36.55588913668041329, -24.39538201762661629 ) ) ;
#29767=CARTESIAN_POINT ( 'NONE',  ( 0.1129192098497455998, -6.563350895508677674, -43.63340707310831590 ) ) ;
#29777=CARTESIAN_POINT ( 'NONE',  ( 2.299746137290197723, 38.15858813809509087, 30.79291296700212044 ) ) ;
#29779=CARTESIAN_POINT ( 'NONE',  ( 0.1154773475650540393, 25.39148992311906028, 36.08622825303670112 ) ) ;
#29785=EDGE_CURVE ( 'NONE', #51706, #9752, #23254, .T. ) ;
#29786=B_SPLINE_CURVE_WITH_KNOTS ( 'NONE', 3,
 ( #6886, #11953, #12558, #54821, #8435, #16629 ),
 .UNSPECIFIED., .F., .F.,
 ( 4, 2, 4 ),
 ( 0.000000000000000000, 0.0002447195606305759387, 0.0004894391212611518775 ),
 .UNSPECIFIED. ) ;
#29788=CARTESIAN_POINT ( 'NONE',  ( 4.553261556744875094, 40.63093864075490558, 16.69330377710913993 ) ) ;
#29793=CARTESIAN_POINT ( 'NONE',  ( 0.5997462898726536595, -35.63787911784795170, 33.78599121123970406 ) ) ;
#29799=CARTESIAN_POINT ( 'NONE',  ( 0.1156867017252034835, -43.74576137695434852, -5.766382646491231334 ) ) ;
#29808=DIRECTION ( 'NONE',  ( -0.000000000000000000, 1.000000000000000000, 0.000000000000000000 ) ) ;
#29812=CARTESIAN_POINT ( 'NONE',  ( 0.7242486021783840489, -14.75415305889595885, 46.83296306970812140 ) ) ;
#29820=ORIENTED_EDGE ( 'NONE', *, *, #47827, .F. ) ;
#29824=VERTEX_POINT ( 'NONE', #61434 ) ;
#29829=DIRECTION ( 'NONE',  ( 0.000000000000000000, 0.000000000000000000, 1.000000000000000000 ) ) ;
#29842=CARTESIAN_POINT ( 'NONE',  ( 0.6000166863083106206, -19.40010892967622169, -45.11606427011503939 ) ) ;
#29844=CARTESIAN_POINT ( 'NONE',  ( 0.5980271706414711508, 48.06821839532968710, 10.07450361757597967 ) ) ;
#29846=CARTESIAN_POINT ( 'NONE',  ( 0.6039202388192952409, -25.30794220682896878, -42.08410357967478177 ) ) ;
#29851=CARTESIAN_POINT ( 'NONE',  ( 2.185380717157383579, -5.603685766289446590, 43.67400266634471251 ) ) ;
#29853=ORIENTED_EDGE ( 'NONE', *, *, #46312, .F. ) ;
#29858=CARTESIAN_POINT ( 'NONE',  ( -6.079354080745853928, -12.94667982361282554, -14.25399722158730498 ) ) ;
#29860=CARTESIAN_POINT ( 'NONE',  ( 4.975610109902397937, 13.36434394399692316, 47.05150069959858428 ) ) ;
#29863=CARTESIAN_POINT ( 'NONE',  ( -6.079354080745853928, -17.34853647870671622, -8.355910321152581588 ) ) ;
#29864=CARTESIAN_POINT ( 'NONE',  ( -6.057079549204054558, 19.09996424292742745, -2.454098005099244251 ) ) ;
#29868=CARTESIAN_POINT ( 'NONE',  ( 0.1156867017252034280, -6.918830238422117418, -43.57835007669613248 ) ) ;
#29870=CARTESIAN_POINT ( 'NONE',  ( 0.1156867017252034557, -35.43631104193246273, 26.29088562628884418 ) ) ;
#29878=EDGE_CURVE ( 'NONE', #28421, #28462, #60528, .T. ) ;
#29879=CARTESIAN_POINT ( 'NONE',  ( 0.6024113833632039894, -30.78790221898711010, 38.25763905489927907 ) ) ;
#29880=CARTESIAN_POINT ( 'NONE',  ( 0.8744876279028306332, 23.49358985382604459, 43.10917867646859492 ) ) ;
#29881=CARTESIAN_POINT ( 'NONE',  ( 0.6029442701453591180, 48.21847811021937957, 9.301805947909977945 ) ) ;
#29888=ORIENTED_EDGE ( 'NONE', *, *, #56300, .T. ) ;
#29900=CARTESIAN_POINT ( 'NONE',  ( 0.6000166863083090663, 49.04012132094733545, 2.624877622903674990 ) ) ;
#29905=CARTESIAN_POINT ( 'NONE',  ( 0.1140933569871964287, 15.59435692983238653, -41.27670023183653569 ) ) ;
#29910=CARTESIAN_POINT ( 'NONE',  ( 0.1119898979215347840, 33.95944467168810377, 28.17299107021446503 ) ) ;
#29918=CARTESIAN_POINT ( 'NONE',  ( 0.1155031312995260795, -40.83589324745333471, -16.71440861096808206 ) ) ;
#29928=CARTESIAN_POINT ( 'NONE',  ( 0.2940133293162999761, 42.11535308342802608, -13.13535626605661122 ) ) ;
#29929=DIRECTION ( 'NONE',  ( -1.000000000000000000, -0.000000000000000000, -0.000000000000000000 ) ) ;
#29939=CARTESIAN_POINT ( 'NONE',  ( 4.553261556744875094, -29.69864478935419072, 32.36556910513705532 ) ) ;
#29941=CARTESIAN_POINT ( 'NONE',  ( 0.1119898979215351031, -31.30369549611587132, 31.09726606212005962 ) ) ;
#29951=CARTESIAN_POINT ( 'NONE',  ( 4.834790513006555379, 7.995814508775468177, 46.56883390493727859 ) ) ;
#29952=CARTESIAN_POINT ( 'NONE',  ( 0.6029443449137434907, 22.67547108931568189, 43.55872528967004342 ) ) ;
#29971=CARTESIAN_POINT ( 'NONE',  ( 0.1129192098497447394, 9.345467776859020859, -43.12324222292247811 ) ) ;
#29973=VERTEX_POINT ( 'NONE', #6572 ) ;
#29979=DIRECTION ( 'NONE',  ( -1.000000000000000000, -0.000000000000000000, -0.000000000000000000 ) ) ;
#29981=VERTEX_POINT ( 'NONE', #25719 ) ;
#29982=CARTESIAN_POINT ( 'NONE',  ( -6.078726893082806448, -8.903615017412294108, -17.07394743140643456 ) ) ;
#29983=EDGE_CURVE ( 'NONE', #50438, #33616, #46372, .T. ) ;
#29990=CARTESIAN_POINT ( 'NONE',  ( 0.6039202388192952409, 46.55074123944880427, 15.63944381705665165 ) ) ;
#29993=CARTESIAN_POINT ( 'NONE',  ( 0.6000166863083106206, 4.195342255946718169, 48.93079383234981350 ) ) ;
#29995=CARTESIAN_POINT ( 'NONE',  ( 2.648799415243696664, -26.59464913125750485, 41.19759824158324335 ) ) ;
#30009=CARTESIAN_POINT ( 'NONE',  ( 4.834790513006555379, 43.62201989944838232, -18.15788315901691874 ) ) ;
#30013=CARTESIAN_POINT ( 'NONE',  ( 4.226256110419179812, 31.27626226520831310, 30.86458599600995356 ) ) ;
#30025=CARTESIAN_POINT ( 'NONE',  ( 2.009741617377216460, 11.13136660361437791, 42.60981993811969915 ) ) ;
#30028=( BOUNDED_SURFACE ( )  B_SPLINE_SURFACE ( 3, 1, ( 
 ( #39041, #14607 ),
 ( #10201, #24608 ),
 ( #34324, #10508 ),
 ( #13995, #33402 ) ),
 .UNSPECIFIED., .F., .F., .F. ) 
 B_SPLINE_SURFACE_WITH_KNOTS ( ( 4, 4 ),
 ( 2, 2 ),
 ( 0.000000000000000000, 1.000000000000000000 ),
 ( 0.000000000000000000, 1.000000000000000000 ),
 .UNSPECIFIED. ) 
 GEOMETRIC_REPRESENTATION_ITEM ( )  RATIONAL_B_SPLINE_SURFACE ( (
 ( 1.000000000000000000, 1.000000000000000000),
 ( 0.7211978278499968642, 0.9934217856018975334),
 ( 0.7211978278499968642, 0.9934217856018975334),
 ( 1.000000000000000000, 1.000000000000000000) ) ) 
 REPRESENTATION_ITEM ( '' )  SURFACE ( )  );
#30030=CARTESIAN_POINT ( 'NONE',  ( 0.6026112563231247332, 37.50532343773836885, -31.70002695164217243 ) ) ;
#30033=CARTESIAN_POINT ( 'NONE',  ( 0.1129192098497455998, -44.12161472487017733, -0.4846667466135657909 ) ) ;
#30036=CARTESIAN_POINT ( 'NONE',  ( 0.8744876279028263033, 27.35388303025786882, 40.76904626731490566 ) ) ;
#30039=ADVANCED_FACE ( 'NONE', ( #9380 ), #23878, .F. ) ;
#30048=VERTEX_POINT ( 'NONE', #46388 ) ;
#30050=CARTESIAN_POINT ( 'NONE',  ( 0.6029442701453591180, 28.02372554534090199, -40.32636893792552257 ) ) ;
#30051=CARTESIAN_POINT ( 'NONE',  ( 0.6021448801613057400, -14.22267499166645166, 47.00273028993500191 ) ) ;
#30058=ORIENTED_EDGE ( 'NONE', *, *, #41056, .T. ) ;
#30059=CARTESIAN_POINT ( 'NONE',  ( -6.057079549204054558, 9.975405573751219279, 16.47187040802930724 ) ) ;
#30075=ORIENTED_EDGE ( 'NONE', *, *, #34419, .T. ) ;
#30076=CARTESIAN_POINT ( 'NONE',  ( 0.6000166863083090663, 27.66667954482629099, -40.57558779207448652 ) ) ;
#30078=CARTESIAN_POINT ( 'NONE',  ( -6.057079549204054558, 15.43788712751036840, 11.51098919024721035 ) ) ;
#30083=CARTESIAN_POINT ( 'NONE',  ( 0.1157506346131639274, 25.32019492611800615, 36.13624757367900742 ) ) ;
#30087=CARTESIAN_POINT ( 'NONE',  ( 4.553261556744875094, 0.000000000000000000, 0.000000000000000000 ) ) ;
#30089=ORIENTED_EDGE ( 'NONE', *, *, #7977, .T. ) ;
#30096=CARTESIAN_POINT ( 'NONE',  ( 0.7413678028165011646, -7.957411786230919937, -43.37240700531383197 ) ) ;
#30099=CARTESIAN_POINT ( 'NONE',  ( 3.678748215320120085, 18.63777698665937876, 45.29068428821796743 ) ) ;
#30103=CARTESIAN_POINT ( 'NONE',  ( 2.648799415243708655, 6.085982952328954809, 48.65673925360762553 ) ) ;
#30110=CARTESIAN_POINT ( 'NONE',  ( -2.739355103387247858, -3.994689410813018426, -14.38367211327327588 ) ) ;
#30111=CARTESIAN_POINT ( 'NONE',  ( 0.5997462898726536595, -45.71211507932792273, 17.94308126043545215 ) ) ;
#30118=CARTESIAN_POINT ( 'NONE',  ( 0.1156495703730067576, 4.372604530253175525, 43.90698444271800582 ) ) ;
#30122=EDGE_CURVE ( 'NONE', #40320, #2416, #44247, .T. ) ;
#30124=CARTESIAN_POINT ( 'NONE',  ( 0.6008123274975392114, 10.50252768641605705, 47.97136086619308770 ) ) ;
#30129=CARTESIAN_POINT ( 'NONE',  ( 0.1119899015040010243, -12.01552140189033757, -42.45690230849656643 ) ) ;
#30131=ORIENTED_EDGE ( 'NONE', *, *, #32508, .T. ) ;
#30136=ORIENTED_EDGE ( 'NONE', *, *, #30779, .F. ) ;
#30143=CARTESIAN_POINT ( 'NONE',  ( 0.8753041380234465318, -45.84117188851855218, 17.59901382919725421 ) ) ;
#30145=EDGE_CURVE ( 'NONE', #28177, #29973, #38536, .T. ) ;
#30150=CARTESIAN_POINT ( 'NONE',  ( 1.834102595619085507, -42.91893299130839523, -9.907721016725536956 ) ) ;
#30153=CARTESIAN_POINT ( 'NONE',  ( 1.657374760986086271, -5.806532005084459769, 43.67121057774989623 ) ) ;
#30161=AXIS2_PLACEMENT_3D ( 'NONE', #16522, #40978, #55328 ) ;
#30163=CARTESIAN_POINT ( 'NONE',  ( 0.1129192098497447394, -31.35755906439637641, 31.04279751098549056 ) ) ;
#30166=CARTESIAN_POINT ( 'NONE',  ( 3.894904216938897878, -14.62320875324691549, -41.45221463607420276 ) ) ;
#30169=CARTESIAN_POINT ( 'NONE',  ( 0.1155031312995260795, -6.875818018218064154, -43.58514378904990849 ) ) ;
#30179=EDGE_CURVE ( 'NONE', #45900, #53021, #1508, .T. ) ;
#30181=CARTESIAN_POINT ( 'NONE',  ( 0.6029442701453591180, -30.54986712454941866, 38.44802782758372217 ) ) ;
#30184=CARTESIAN_POINT ( 'NONE',  ( 0.6021448801613057400, 49.02259304973922127, -2.885569147777831578 ) ) ;
#30188=ORIENTED_EDGE ( 'NONE', *, *, #26595, .T. ) ;
#30190=CARTESIAN_POINT ( 'NONE',  ( 3.050102900204245682, 43.74992430961583523, -4.622701816140248887 ) ) ;
#30191=EDGE_CURVE ( 'NONE', #28349, #60557, #19399, .T. ) ;
#30192=CARTESIAN_POINT ( 'NONE',  ( 0.1157991065609915576, 41.85057238631154064, 13.98112858376594758 ) ) ;
#30198=EDGE_LOOP ( 'NONE', ( #7549, #16518, #39631, #10464 ) ) ;
#30200=EDGE_CURVE ( 'NONE', #10972, #9573, #48231, .T. ) ;
#30204=B_SPLINE_CURVE_WITH_KNOTS ( 'NONE', 3,
 ( #19757, #14749, #10351, #43896, #57933, #1540, #33864, #25059, #52939, #10041, #44506, #53544, #1235, #20678, #5308, #39812, #24438, #20368, #58867 ),
 .UNSPECIFIED., .F., .F.,
 ( 4, 3, 3, 3, 3, 3, 4 ),
 ( 1.355252715606880543E-20, 0.0002612768053151701369, 0.0003919133833142879981, 0.0005225499612322599945, 0.0006531865391693327059, 0.0008112755173415169300, 0.0009693688056799694289 ),
 .UNSPECIFIED. ) ;
#30206=MANIFOLD_SOLID_BREP ( 'Move Face1', #16058 ) ;
#30210=LINE ( 'NONE', #44963, #15965 ) ;
#30214=DIRECTION ( 'NONE',  ( -1.000000000000000000, -0.000000000000000000, -0.000000000000000000 ) ) ;
#30218=CARTESIAN_POINT ( 'NONE',  ( 0.1154773475650540809, -40.96660263512894318, -16.39149470248417728 ) ) ;
#30231=CARTESIAN_POINT ( 'NONE',  ( 0.3676999524040323597, 41.59822836379060362, 14.68121181363330408 ) ) ;
#30233=CARTESIAN_POINT ( 'NONE',  ( 4.553261556744875094, 7.233533384971297941, -43.32684572631779218 ) ) ;
#30238=CARTESIAN_POINT ( 'NONE',  ( 0.2285344041767087830, -41.17386732079742728, -15.84972618516879450 ) ) ;
#30247=CARTESIAN_POINT ( 'NONE',  ( 0.6039202388192952409, 37.50551550546116175, -31.70015803617710404 ) ) ;
#30249=CARTESIAN_POINT ( 'NONE',  ( -6.078075953587585900, -1.843738688193441666, -19.16757162232072531 ) ) ;
#30264=VERTEX_POINT ( 'NONE', #50375 ) ;
#30268=CARTESIAN_POINT ( 'NONE',  ( 0.1368894036331258779, -42.83744898368259868, -10.57422765471428860 ) ) ;
#30273=ORIENTED_EDGE ( 'NONE', *, *, #18335, .T. ) ;
#30274=ORIENTED_EDGE ( 'NONE', *, *, #6733, .F. ) ;
#30277=CARTESIAN_POINT ( 'NONE',  ( -6.078726893082806448, -18.90026279491059924, 3.684305572565647946 ) ) ;
#30282=CARTESIAN_POINT ( 'NONE',  ( 4.975610109902397937, 0.000000000000000000, 0.000000000000000000 ) ) ;
#30284=( BOUNDED_SURFACE ( )  B_SPLINE_SURFACE ( 3, 1, ( 
 ( #40215, #21070 ),
 ( #54246, #21381 ),
 ( #20158, #30766 ),
 ( #54552, #45216 ) ),
 .UNSPECIFIED., .F., .F., .F. ) 
 B_SPLINE_SURFACE_WITH_KNOTS ( ( 4, 4 ),
 ( 2, 2 ),
 ( 0.000000000000000000, 1.000000000000000000 ),
 ( 0.000000000000000000, 1.000000000000000000 ),
 .UNSPECIFIED. ) 
 GEOMETRIC_REPRESENTATION_ITEM ( )  RATIONAL_B_SPLINE_SURFACE ( (
 ( 1.000000000000000000, 1.000000000000000000),
 ( 0.9754377213608244057, 0.9999580625633939235),
 ( 0.9754377213608244057, 0.9999580625633939235),
 ( 1.000000000000000000, 1.000000000000000000) ) ) 
 REPRESENTATION_ITEM ( '' )  SURFACE ( )  );
#30285=CARTESIAN_POINT ( 'NONE',  ( 4.553261556744873317, -20.11719049292697648, 39.04917684785332455 ) ) ;
#30297=CARTESIAN_POINT ( 'NONE',  ( 0.1157991065609916131, 39.78975866839436293, -19.07137831014408746 ) ) ;
#30308=VERTEX_POINT ( 'NONE', #41935 ) ;
#30309=CARTESIAN_POINT ( 'NONE',  ( 0.1129192098497447394, 43.40062318508790895, 7.958498283669150020 ) ) ;
#30315=ORIENTED_EDGE ( 'NONE', *, *, #19937, .T. ) ;
#30317=CARTESIAN_POINT ( 'NONE',  ( -6.057079549204054558, -18.90348671888462917, 3.672794708214838000 ) ) ;
#30323=CARTESIAN_POINT ( 'NONE',  ( 4.553261556744873317, -29.69864478935373242, -32.36556910513746743 ) ) ;
#30324=FACE_OUTER_BOUND ( 'NONE', #23888, .T. ) ;
#30325=EDGE_LOOP ( 'NONE', ( #14807, #24989, #55784, #38582 ) ) ;
#30329=CARTESIAN_POINT ( 'NONE',  ( 1.479689385636123067, 10.94758276098252558, 42.68177921501317229 ) ) ;
#30336=CARTESIAN_POINT ( 'NONE',  ( 0.2285344041767098933, -2.173305968327541304, -44.06560916932259175 ) ) ;
#30338=EDGE_CURVE ( 'NONE', #32393, #48631, #50770, .T. ) ;
#30339=CARTESIAN_POINT ( 'NONE',  ( 0.1119898979215348950, -17.34614202713813569, 40.57182107111018610 ) ) ;
#30343=CARTESIAN_POINT ( 'NONE',  ( 0.3676999524040323597, 40.09552319080426486, -18.39292264373764851 ) ) ;
#30344=ORIENTED_EDGE ( 'NONE', *, *, #14205, .F. ) ;
#30348=CARTESIAN_POINT ( 'NONE',  ( 0.1157991065609915993, -38.40619918333140959, -21.72340281419956654 ) ) ;
#30349=CARTESIAN_POINT ( 'NONE',  ( 4.975610109902397937, -22.11219452748553138, -43.62912170003438916 ) ) ;
#30355=CARTESIAN_POINT ( 'NONE',  ( 4.834790513006553603, 24.88720127704591789, -40.16486715427035392 ) ) ;
#30357=CARTESIAN_POINT ( 'NONE',  ( 4.553261556744875094, -43.85016385001095784, 2.588956575693979190 ) ) ;
#30372=EDGE_LOOP ( 'NONE', ( #42960, #23216, #4440, #49002 ) ) ;
#30376=ORIENTED_EDGE ( 'NONE', *, *, #49706, .F. ) ;
#30379=ORIENTED_EDGE ( 'NONE', *, *, #56080, .F. ) ;
#30382=VERTEX_POINT ( 'NONE', #50987 ) ;
#30386=EDGE_LOOP ( 'NONE', ( #22516, #248, #60174, #43483 ) ) ;
#30388=LINE ( 'NONE', #11300, #55757 ) ;
#30390=CARTESIAN_POINT ( 'NONE',  ( 0.7242486021783806072, 49.04682582606951513, -2.328162099418285003 ) ) ;
#30394=EDGE_LOOP ( 'NONE', ( #47585, #27532, #28586, #49232 ) ) ;
#30400=CARTESIAN_POINT ( 'NONE',  ( 4.335381028904201628, 0.5556724879614545198, -48.98416147848676871 ) ) ;
#30401=EDGE_CURVE ( 'NONE', #15298, #6759, #54417, .T. ) ;
#30411=DIRECTION ( 'NONE',  ( 0.000000000000000000, 0.000000000000000000, 1.000000000000000000 ) ) ;
#30412=CARTESIAN_POINT ( 'NONE',  ( 0.1154773475650541087, 37.07776829763225379, 23.92034130427944660 ) ) ;
#30416=CARTESIAN_POINT ( 'NONE',  ( 4.975610109902397937, 14.46773809681615575, -46.72401910687593585 ) ) ;
#30421=AXIS2_PLACEMENT_3D ( 'NONE', #35914, #26489, #16480 ) ;
#30426=CARTESIAN_POINT ( 'NONE',  ( 0.8744876279028306332, 37.95405449045402690, 31.14225101233274273 ) ) ;
#30437=ORIENTED_EDGE ( 'NONE', *, *, #7129, .F. ) ;
#30438=DIRECTION ( 'NONE',  ( -1.000000000000000000, -0.000000000000000000, -0.000000000000000000 ) ) ;
#30449=( BOUNDED_SURFACE ( )  B_SPLINE_SURFACE ( 3, 1, ( 
 ( #261, #25028 ),
 ( #39769, #58824 ),
 ( #53506, #15945 ),
 ( #52588, #29712 ) ),
 .UNSPECIFIED., .F., .F., .F. ) 
 B_SPLINE_SURFACE_WITH_KNOTS ( ( 4, 4 ),
 ( 2, 2 ),
 ( 0.000000000000000000, 1.000000000000000000 ),
 ( 0.000000000000000000, 1.000000000000000000 ),
 .UNSPECIFIED. ) 
 GEOMETRIC_REPRESENTATION_ITEM ( )  RATIONAL_B_SPLINE_SURFACE ( (
 ( 1.000000000000000000, 1.000000000000000000),
 ( 0.9953485035131437453, 0.8621029689291515030),
 ( 0.9953485035131437453, 0.8621029689291515030),
 ( 1.000000000000000000, 1.000000000000000000) ) ) 
 REPRESENTATION_ITEM ( '' )  SURFACE ( )  );
#30453=CARTESIAN_POINT ( 'NONE',  ( 3.727782113643637096, -43.01752167612853839, -9.070314479100884952 ) ) ;
#30454=CARTESIAN_POINT ( 'NONE',  ( 0.7242486021783813843, 48.03329165852890981, 10.18893295790429931 ) ) ;
#30456=CARTESIAN_POINT ( 'NONE',  ( 1.657374760986086049, 8.592625930871594875, -43.20945760900450949 ) ) ;
#30466=CARTESIAN_POINT ( 'NONE',  ( 2.879087469061463178, -14.16979277963087647, -41.65715604029755070 ) ) ;
#30468=EDGE_CURVE ( 'NONE', #44808, #59478, #27593, .T. ) ;
#30470=CARTESIAN_POINT ( 'NONE',  ( 4.335381028904201628, 34.47659336712107603, -34.80116890942784380 ) ) ;
#30475=VECTOR ( 'NONE', #19149, 1000.000000000000000 ) ;
#30481=CARTESIAN_POINT ( 'NONE',  ( -6.077587904424778920, -4.278847002849283321, 18.77465018902185179 ) ) ;
#30483=CARTESIAN_POINT ( 'NONE',  ( 0.5997462898726536595, 48.09935696025624452, 9.899671214447447909 ) ) ;
#30486=VERTEX_POINT ( 'NONE', #5736 ) ;
#30487=CARTESIAN_POINT ( 'NONE',  ( 0.6028777368367060907, 17.04167399223566548, -46.05563132618456734 ) ) ;
#30488=CARTESIAN_POINT ( 'NONE',  ( 0.6252788684277217346, 49.04477175441831349, 2.460628929903515782 ) ) ;
#30490=ORIENTED_EDGE ( 'NONE', *, *, #7328, .F. ) ;
#30497=CIRCLE ( 'NONE', #25497, 48.91267123290010943 ) ;
#30501=CARTESIAN_POINT ( 'NONE',  ( -6.078726893082806448, -18.27395335922926378, 6.070969436048390122 ) ) ;
#30516=CARTESIAN_POINT ( 'NONE',  ( 0.8744876279028263033, 46.86690837902584406, -14.62336997314537790 ) ) ;
#30531=CARTESIAN_POINT ( 'NONE',  ( 0.7242003506640004584, -48.58741756788937494, 7.090453314815819752 ) ) ;
#30538=DIRECTION ( 'NONE',  ( 0.000000000000000000, 0.000000000000000000, 1.000000000000000000 ) ) ;
#30541=CARTESIAN_POINT ( 'NONE',  ( 2.009741617377216460, 21.57548988114320920, 38.39273777697718515 ) ) ;
#30545=CARTESIAN_POINT ( 'NONE',  ( 0.5549461598389365813, -32.28688909427809506, -30.04620588494645261 ) ) ;
#30546=CARTESIAN_POINT ( 'NONE',  ( 0.8753041380234524160, -14.82204010568715624, -46.81287702094778780 ) ) ;
#30553=( BOUNDED_SURFACE ( )  B_SPLINE_SURFACE ( 3, 1, ( 
 ( #59593, #49578 ),
 ( #44302, #58339 ),
 ( #29858, #54568 ),
 ( #15464, #6633 ) ),
 .UNSPECIFIED., .F., .F., .F. ) 
 B_SPLINE_SURFACE_WITH_KNOTS ( ( 4, 4 ),
 ( 2, 2 ),
 ( 0.000000000000000000, 1.000000000000000000 ),
 ( 0.000000000000000000, 1.000000000000000000 ),
 .UNSPECIFIED. ) 
 GEOMETRIC_REPRESENTATION_ITEM ( )  RATIONAL_B_SPLINE_SURFACE ( (
 ( 1.000000000000000000, 1.000000000000000000),
 ( 0.9754377213608244057, 0.9999580625633939235),
 ( 0.9754377213608244057, 0.9999580625633939235),
 ( 1.000000000000000000, 1.000000000000000000) ) ) 
 REPRESENTATION_ITEM ( '' )  SURFACE ( )  );
#30556=CARTESIAN_POINT ( 'NONE',  ( 2.648799415243696664, 36.42501529472001920, 32.82888551366023933 ) ) ;
#30557=CARTESIAN_POINT ( 'NONE',  ( 0.1129192098497447394, 43.99990943031675528, -3.310552508128703497 ) ) ;
#30558=CARTESIAN_POINT ( 'NONE',  ( -6.078726893082806448, 18.62537590944114640, 4.887679766589625885 ) ) ;
#30559=CARTESIAN_POINT ( 'NONE',  ( 4.975610109902397937, -36.86873347511098586, -32.14258700041121131 ) ) ;
#30564=CARTESIAN_POINT ( 'NONE',  ( 0.7242003506639987931, 48.34642798422387244, 8.581059100850049859 ) ) ;
#30567=CARTESIAN_POINT ( 'NONE',  ( -6.077587904424778920, 0.6110050725292486273, -19.24636833782607681 ) ) ;
#30573=CARTESIAN_POINT ( 'NONE',  ( 0.1155031312995260795, -23.01756397718155611, 37.64483206348730704 ) ) ;
#30582=DIRECTION ( 'NONE',  ( 0.000000000000000000, 0.000000000000000000, 1.000000000000000000 ) ) ;
#30583=CARTESIAN_POINT ( 'NONE',  ( 0.6026777506516368677, 37.50538381255011444, 31.70004062632291664 ) ) ;
#30588=CARTESIAN_POINT ( 'NONE',  ( -6.078726893082806448, -11.01388439747492498, -15.79520154185373038 ) ) ;
#30593=ORIENTED_EDGE ( 'NONE', *, *, #18369, .F. ) ;
#30594=FACE_OUTER_BOUND ( 'NONE', #2466, .T. ) ;
#30595=CARTESIAN_POINT ( 'NONE',  ( 0.7242486021783826056, 11.72324082283336644, -47.68204155637450015 ) ) ;
#30599=VERTEX_POINT ( 'NONE', #6973 ) ;
#30603=ORIENTED_EDGE ( 'NONE', *, *, #34879, .F. ) ;
#30607=ORIENTED_EDGE ( 'NONE', *, *, #17420, .F. ) ;
#30612=ORIENTED_EDGE ( 'NONE', *, *, #20152, .F. ) ;
#30616=CARTESIAN_POINT ( 'NONE',  ( 4.975610109902397937, 0.9924324126411095959, -48.90260202733707473 ) ) ;
#30625=VERTEX_POINT ( 'NONE', #17035 ) ;
#30631=CARTESIAN_POINT ( 'NONE',  ( 0.5997462898726536595, 44.01516392039482639, 21.77652348757905898 ) ) ;
#30632=CARTESIAN_POINT ( 'NONE',  ( 0.3676999524040323597, -38.02468164711575582, -22.36233818182566324 ) ) ;
#30633=B_SPLINE_CURVE_WITH_KNOTS ( 'NONE', 3,
 ( #47992, #38602, #48592, #14788, #57349, #29793 ),
 .UNSPECIFIED., .F., .F.,
 ( 4, 2, 4 ),
 ( 4.445228907190568179E-18, 0.0002447193893791691660, 0.0004894387787583338867 ),
 .UNSPECIFIED. ) ;
#30634=FACE_OUTER_BOUND ( 'NONE', #21067, .T. ) ;
#30639=CARTESIAN_POINT ( 'NONE',  ( 0.5997462898726536595, 37.05192695178169515, -32.22896739432000146 ) ) ;
#30640=CARTESIAN_POINT ( 'NONE',  ( 0.8744876279028263033, 3.827863332834932297, 48.94586308039354350 ) ) ;
#30643=CARTESIAN_POINT ( 'NONE',  ( 1.112077966505212068, -21.94633083862179035, 38.22811645700467409 ) ) ;
#30647=B_SPLINE_CURVE_WITH_KNOTS ( 'NONE', 3,
 ( #54150, #29745, #25983, #2145 ),
 .UNSPECIFIED., .F., .F.,
 ( 4, 4 ),
 ( 0.000000000000000000, 0.005013413432710150247 ),
 .UNSPECIFIED. ) ;
#30649=EDGE_CURVE ( 'NONE', #53648, #30599, #7374, .T. ) ;
#30650=ORIENTED_EDGE ( 'NONE', *, *, #55935, .F. ) ;
#30660=CARTESIAN_POINT ( 'NONE',  ( 0.3676999524040366896, -32.25712563511761743, -30.09033780274121739 ) ) ;
#30662=CARTESIAN_POINT ( 'NONE',  ( 0.6016117650947689910, -13.63814917008489580, 47.17575586526422882 ) ) ;
#30664=CARTESIAN_POINT ( 'NONE',  ( 3.559346040607745287, -43.92278903503267884, 2.053992435721407439 ) ) ;
#30665=CARTESIAN_POINT ( 'NONE',  ( 0.2279481005628809787, -0.6549591441850819429, -44.11433458177015865 ) ) ;
#30667=VECTOR ( 'NONE', #10472, 1000.000000000000000 ) ;
#30677=CIRCLE ( 'NONE', #43732, 49.35315702047511621 ) ;
#30678=ORIENTED_EDGE ( 'NONE', *, *, #32454, .F. ) ;
#30693=FACE_OUTER_BOUND ( 'NONE', #60627, .T. ) ;
#30698=FACE_OUTER_BOUND ( 'NONE', #628, .T. ) ;
#30701=CARTESIAN_POINT ( 'NONE',  ( -4.915099999999998914, 0.000000000000000000, 49.35315702047512332 ) ) ;
#30702=CARTESIAN_POINT ( 'NONE',  ( 4.975610109902397937, -36.86873347511144772, 32.14258700041067840 ) ) ;
#30705=VECTOR ( 'NONE', #5606, 1000.000000000000000 ) ;
#30707=COLOUR_RGB ( '', 0.72549020, 0.75294118, 0.79215686) ;
#30715=CARTESIAN_POINT ( 'NONE',  ( 0.5980271706414711508, 46.38528005876693072, 16.13861941776375986 ) ) ;
#30721=CARTESIAN_POINT ( 'NONE',  ( 0.8753041380234465318, 32.34805756193355819, 36.94240787824763572 ) ) ;
#30730=CARTESIAN_POINT ( 'NONE',  ( 3.221118495291109163, -3.296306199338291165, -43.86223643525207905 ) ) ;
#30734=CARTESIAN_POINT ( 'NONE',  ( 4.553261556744873317, 35.06776520399894537, -26.45357082552063233 ) ) ;
#30735=CARTESIAN_POINT ( 'NONE',  ( 3.678834586032785570, 26.48313750915808740, 41.19776446968182171 ) ) ;
#30742=CARTESIAN_POINT ( 'NONE',  ( 0.6016118706126978299, 10.58757829817042229, 47.95262496010037978 ) ) ;
#30747=CARTESIAN_POINT ( 'NONE',  ( 0.1155031312995260795, 44.02238668353053441, 2.995179997516315140 ) ) ;
#30750=CARTESIAN_POINT ( 'NONE',  ( 0.7242486021783861583, 41.59294671404158805, -26.09670948638677501 ) ) ;
#30756=ORIENTED_EDGE ( 'NONE', *, *, #56207, .T. ) ;
#30757=CARTESIAN_POINT ( 'NONE',  ( 1.830465331921977246, 30.51707817982678606, -31.76608246612618558 ) ) ;
#30762=ADVANCED_FACE ( 'NONE', ( #25726 ), #11441, .F. ) ;
#30763=ORIENTED_EDGE ( 'NONE', *, *, #25764, .F. ) ;
#30766=CARTESIAN_POINT ( 'NONE',  ( 0.6039202388192952409, 17.12343321804727481, -46.02555537607413783 ) ) ;
#30768=CARTESIAN_POINT ( 'NONE',  ( 4.060580049360325461, 12.98590958963613318, -41.98611492492495501 ) ) ;
#30770=CARTESIAN_POINT ( 'NONE',  ( 0.7413678028165009426, -42.88130420167055235, -10.28007012301159584 ) ) ;
#30771=FACE_OUTER_BOUND ( 'NONE', #11186, .T. ) ;
#30772=CARTESIAN_POINT ( 'NONE',  ( 0.6253024248130495399, 46.38379508687873454, 16.12413658947630779 ) ) ;
#30774=ORIENTED_EDGE ( 'NONE', *, *, #11978, .F. ) ;
#30775=VERTEX_POINT ( 'NONE', #1282 ) ;
#30779=EDGE_CURVE ( 'NONE', #3481, #18802, #5966, .T. ) ;
#30782=CARTESIAN_POINT ( 'NONE',  ( 3.390910168358336918, -43.32159816751995862, 7.572071628396552789 ) ) ;
#30788=CARTESIAN_POINT ( 'NONE',  ( 0.8744876279028306332, -42.33402326122651971, 24.86323641237049387 ) ) ;
#30792=CARTESIAN_POINT ( 'NONE',  ( 1.830465331921977468, -23.88195676858206440, 37.01389194318758058 ) ) ;
#30794=DIRECTION ( 'NONE',  ( 0.09722883295013597105, 0.9783250423059166589, -0.1828296082156304347 ) ) ;
#30795=CARTESIAN_POINT ( 'NONE',  ( -6.078726893082806448, -4.281536037414130469, 18.77398440472997265 ) ) ;
#30796=CARTESIAN_POINT ( 'NONE',  ( 0.5987334308729317378, 23.24905889540555037, 43.25556804675779432 ) ) ;
#30797=CARTESIAN_POINT ( 'NONE',  ( 0.6024113833632039894, 48.15977990201467662, 9.600909794929371799 ) ) ;
#30800=ORIENTED_EDGE ( 'NONE', *, *, #49749, .F. ) ;
#30803=CARTESIAN_POINT ( 'NONE',  ( 4.060580049360325461, 1.911233126685682349, -43.90688877949186519 ) ) ;
#30811=CIRCLE ( 'NONE', #41851, 43.92652462719577500 ) ;
#30820=CARTESIAN_POINT ( 'NONE',  ( 0.7948878604505666967, -0.7064023212773177240, 49.09378415908586391 ) ) ;
#30823=CARTESIAN_POINT ( 'NONE',  ( 0.6039202388192952409, 41.25132197622592400, -26.64380130654654621 ) ) ;
#30828=VECTOR ( 'NONE', #42348, 1000.000000000000114 ) ;
#30829=ORIENTED_EDGE ( 'NONE', *, *, #50010, .T. ) ;
#30831=CARTESIAN_POINT ( 'NONE',  ( 0.2279481005628812007, -40.60382094950545451, -17.25784492262615544 ) ) ;
#30833=ORIENTED_EDGE ( 'NONE', *, *, #38727, .T. ) ;
#30837=CARTESIAN_POINT ( 'NONE',  ( 4.060580049360325461, -43.82307209454128127, -3.317536217714249336 ) ) ;
#30839=VERTEX_POINT ( 'NONE', #15412 ) ;
#30841=CARTESIAN_POINT ( 'NONE',  ( 0.6016117650947689910, -35.03314589365777465, 34.41263929195476834 ) ) ;
#30844=EDGE_LOOP ( 'NONE', ( #8015, #4375, #13401, #19956 ) ) ;
#30857=CARTESIAN_POINT ( 'NONE',  ( 4.553261556744873317, -36.69060082144796553, 24.15241969627054530 ) ) ;
#30864=ORIENTED_EDGE ( 'NONE', *, *, #59252, .F. ) ;
#30868=FACE_OUTER_BOUND ( 'NONE', #60112, .T. ) ;
#30875=VECTOR ( 'NONE', #1590, 999.9999999999998863 ) ;
#30877=EDGE_CURVE ( 'NONE', #8147, #15568, #44251, .T. ) ;
#30878=CARTESIAN_POINT ( 'NONE',  ( 0.6252788684277199582, -45.25543936479831331, 19.06277889167080275 ) ) ;
#30880=ORIENTED_EDGE ( 'NONE', *, *, #56895, .T. ) ;
#30885=EDGE_CURVE ( 'NONE', #31776, #31779, #13281, .T. ) ;
#30891=B_SPLINE_CURVE_WITH_KNOTS ( 'NONE', 3,
 ( #40997, #25936, #31877, #45074, #11862, #7106 ),
 .UNSPECIFIED., .F., .F.,
 ( 4, 2, 4 ),
 ( 1.252987389397349539E-17, 0.0002293755540694274696, 0.0004587511081388424166 ),
 .UNSPECIFIED. ) ;
#30894=CARTESIAN_POINT ( 'NONE',  ( 0.8744876279028306332, 46.86690837902563089, 14.62336997314605469 ) ) ;
#30895=EDGE_CURVE ( 'NONE', #23672, #25014, #3144, .T. ) ;
#30900=ORIENTED_EDGE ( 'NONE', *, *, #19339, .T. ) ;
#30901=VERTEX_POINT ( 'NONE', #26652 ) ;
#30904=ORIENTED_EDGE ( 'NONE', *, *, #29634, .T. ) ;
#30906=CARTESIAN_POINT ( 'NONE',  ( 4.975610109902397937, -28.45381238669816426, 39.78479568629648355 ) ) ;
#30911=CARTESIAN_POINT ( 'NONE',  ( 0.8744876279028306332, -20.68330519280286239, -44.52584571550401193 ) ) ;
#30912=CARTESIAN_POINT ( 'NONE',  ( -6.078726893082806448, 15.42998809551244577, -11.51996131248123234 ) ) ;
#30918=CARTESIAN_POINT ( 'NONE',  ( 0.8744876279028306332, 48.35212675551500183, 8.510105087371359289 ) ) ;
#30919=CARTESIAN_POINT ( 'NONE',  ( 4.975610109902397937, -41.30423662854469313, 26.19941685746003301 ) ) ;
#30922=DIRECTION ( 'NONE',  ( 0.000000000000000000, 0.000000000000000000, 1.000000000000000000 ) ) ;
#30954=ORIENTED_EDGE ( 'NONE', *, *, #15858, .F. ) ;
#30958=CARTESIAN_POINT ( 'NONE',  ( 0.3676999524040323597, -11.75791688508830646, -42.51707861373114383 ) ) ;
#30962=CARTESIAN_POINT ( 'NONE',  ( 0.1156867017252034419, -12.43470245650705586, -42.33581205189435792 ) ) ;
#30965=CARTESIAN_POINT ( 'NONE',  ( 4.335381028904201628, 45.77817886910082734, 17.43889867775355285 ) ) ;
#30968=ADVANCED_FACE ( 'NONE', ( #54513 ), #53277, .F. ) ;
#30976=ADVANCED_FACE ( 'NONE', ( #2528 ), #39458, .F. ) ;
#30995=CARTESIAN_POINT ( 'NONE',  ( 5.901764892641307547, -27.98073834948241156, -40.18793038783513794 ) ) ;
#30996=ORIENTED_EDGE ( 'NONE', *, *, #17610, .F. ) ;
#30998=CARTESIAN_POINT ( 'NONE',  ( 0.1140933569871963454, 20.07213292652290448, 39.29452162660719239 ) ) ;
#30999=ORIENTED_EDGE ( 'NONE', *, *, #12198, .F. ) ;
#31005=ORIENTED_EDGE ( 'NONE', *, *, #53036, .T. ) ;
#31006=CARTESIAN_POINT ( 'NONE',  ( 0.8753041380234471980, 11.79227530596935658, -47.66634631457717575 ) ) ;
#31007=CARTESIAN_POINT ( 'NONE',  ( 0.6000166863083090663, 41.44150143800075625, -26.35195325346177242 ) ) ;
#31012=CARTESIAN_POINT ( 'NONE',  ( 0.1129192098497455998, -0.9297496242496093855, -44.11448008785053787 ) ) ;
#31014=CARTESIAN_POINT ( 'NONE',  ( -6.077587904424778920, 19.09718056542704900, 2.468545289316316893 ) ) ;
#31017=EDGE_LOOP ( 'NONE', ( #2412, #58073, #5315, #61086 ) ) ;
#31023=CARTESIAN_POINT ( 'NONE',  ( 0.5980271706414711508, 40.77460832818520231, 27.37664257217734587 ) ) ;
#31024=CARTESIAN_POINT ( 'NONE',  ( -6.078726893082806448, -14.66462719274117887, 12.47969352855413838 ) ) ;
#31030=CARTESIAN_POINT ( 'NONE',  ( -6.078457390727109555, 18.62736532255359734, -4.880140589945706431 ) ) ;
#31034=CIRCLE ( 'NONE', #6987, 43.92652462719577500 ) ;
#31035=ORIENTED_EDGE ( 'NONE', *, *, #40714, .T. ) ;
#31045=CARTESIAN_POINT ( 'NONE',  ( 4.834790513006555379, -31.42367164492902631, 35.28657253511686775 ) ) ;
#31048=ADVANCED_FACE ( 'NONE', ( #3748 ), #34685, .F. ) ;
#31057=ORIENTED_EDGE ( 'NONE', *, *, #17266, .T. ) ;
#31065=VERTEX_POINT ( 'NONE', #4352 ) ;
#31069=VERTEX_POINT ( 'NONE', #42321 ) ;
#31074=CARTESIAN_POINT ( 'NONE',  ( 5.901764892641307547, 19.86141101510697027, -44.76065035194043418 ) ) ;
#31075=ORIENTED_EDGE ( 'NONE', *, *, #36113, .F. ) ;
#31078=CARTESIAN_POINT ( 'NONE',  ( -6.078075953587585900, -14.65899360350491243, -12.48635578459696482 ) ) ;
#31080=CARTESIAN_POINT ( 'NONE',  ( 0.1140933569871964287, 43.38147022400296748, -8.062133172296839234 ) ) ;
#31091=ORIENTED_EDGE ( 'NONE', *, *, #9922, .F. ) ;
#31099=CARTESIAN_POINT ( 'NONE',  ( 3.221118495291109163, 42.30175278488824375, 12.05500439601543050 ) ) ;
#31101=CARTESIAN_POINT ( 'NONE',  ( 0.1368894036331270159, -18.44144849573008216, -40.08458934930814621 ) ) ;
#31103=CARTESIAN_POINT ( 'NONE',  ( 0.1129192098497447394, 25.64022107388777272, 35.91003830501040994 ) ) ;
#31113=AXIS2_PLACEMENT_3D ( 'NONE', #17262, #22574, #32595 ) ;
#31118=ORIENTED_EDGE ( 'NONE', *, *, #5361, .T. ) ;
#31123=ORIENTED_EDGE ( 'NONE', *, *, #47380, .T. ) ;
#31125=CARTESIAN_POINT ( 'NONE',  ( 3.727782113643637540, -30.05637732902805936, 32.08413872556130997 ) ) ;
#31129=ORIENTED_EDGE ( 'NONE', *, *, #57839, .F. ) ;
#31138=CARTESIAN_POINT ( 'NONE',  ( -6.078726893082806448, 16.77980020642716141, -9.446287434813061878 ) ) ;
#31139=CARTESIAN_POINT ( 'NONE',  ( 0.1154773475650540393, 15.07002877585266809, -41.47092792235417136 ) ) ;
#31141=ORIENTED_EDGE ( 'NONE', *, *, #2613, .T. ) ;
#31144=ORIENTED_EDGE ( 'NONE', *, *, #1194, .F. ) ;
#31147=FACE_OUTER_BOUND ( 'NONE', #17827, .T. ) ;
#31148=CARTESIAN_POINT ( 'NONE',  ( 3.559346040607745287, -43.82484226701208030, -3.579592408850357010 ) ) ;
#31150=CARTESIAN_POINT ( 'NONE',  ( 4.335381028904201628, -48.81116855472419758, 4.150502618556926038 ) ) ;
#31155=LINE ( 'NONE', #54017, #19452 ) ;
#31156=EDGE_CURVE ( 'NONE', #58292, #23810, #2247, .T. ) ;
#31160=CARTESIAN_POINT ( 'NONE',  ( 0.5997462898726536595, -43.04230894295751852, 23.64130434225888777 ) ) ;
#31166=B_SPLINE_CURVE_WITH_KNOTS ( 'NONE', 3,
 ( #60621, #26827, #12747, #44497, #56241, #41256 ),
 .UNSPECIFIED., .F., .F.,
 ( 4, 2, 4 ),
 ( 0.000000000000000000, 0.0002447195606305743124, 0.0004894391212611486248 ),
 .UNSPECIFIED. ) ;
#31171=CARTESIAN_POINT ( 'NONE',  ( 4.694002226626921015, -26.36364849202877991, 37.19197238161595465 ) ) ;
#31176=B_SPLINE_CURVE_WITH_KNOTS ( 'NONE', 3,
 ( #32492, #52192, #42221, #9286, #28393, #47514 ),
 .UNSPECIFIED., .F., .F.,
 ( 4, 2, 4 ),
 ( 0.000000000000000000, 0.0002293801035737127873, 0.0004587602071474255745 ),
 .UNSPECIFIED. ) ;
#31178=CARTESIAN_POINT ( 'NONE',  ( 4.553261556744873317, 7.233533384970671776, 43.32684572631789166 ) ) ;
#31181=CARTESIAN_POINT ( 'NONE',  ( -6.078726893082806448, -1.845620846545350080, -19.16736092839902383 ) ) ;
#31190=CARTESIAN_POINT ( 'NONE',  ( 0.8744876279028306332, -45.16590161815026505, 19.24555484778404590 ) ) ;
#31191=ORIENTED_EDGE ( 'NONE', *, *, #17564, .F. ) ;
#31193=CARTESIAN_POINT ( 'NONE',  ( -6.072942160501519915, 0.6026766405724340858, -19.24684242040570581 ) ) ;
#31196=EDGE_CURVE ( 'NONE', #1986, #38401, #40935, .T. ) ;
#31198=DIRECTION ( 'NONE',  ( 0.1011922191286468015, 0.5796805626819869772, 0.8085360721925242133 ) ) ;
#31202=VECTOR ( 'NONE', #590, 1000.000000000000000 ) ;
#31204=EDGE_CURVE ( 'NONE', #48474, #49527, #56647, .T. ) ;
#31205=( BOUNDED_SURFACE ( )  B_SPLINE_SURFACE ( 3, 1, ( 
 ( #30795, #45860 ),
 ( #21102, #16403 ),
 ( #35837, #25797 ),
 ( #30481, #1657 ) ),
 .UNSPECIFIED., .F., .F., .F. ) 
 B_SPLINE_SURFACE_WITH_KNOTS ( ( 4, 4 ),
 ( 2, 2 ),
 ( 0.000000000000000000, 1.000000000000000000 ),
 ( 0.000000000000000000, 1.000000000000000000 ),
 .UNSPECIFIED. ) 
 GEOMETRIC_REPRESENTATION_ITEM ( )  RATIONAL_B_SPLINE_SURFACE ( (
 ( 1.000000000000000000, 1.000000000000000000),
 ( 0.9953485035131437453, 0.8621029689291523912),
 ( 0.9953485035131437453, 0.8621029689291523912),
 ( 1.000000000000000000, 1.000000000000000000) ) ) 
 REPRESENTATION_ITEM ( '' )  SURFACE ( )  );
#31208=EDGE_LOOP ( 'NONE', ( #42127, #23165, #47504, #19234 ) ) ;
#31210=CARTESIAN_POINT ( 'NONE',  ( -6.078726893082806448, -18.90156862012333860, 3.677600436084480062 ) ) ;
#31218=ORIENTED_EDGE ( 'NONE', *, *, #60368, .T. ) ;
#31229=EDGE_LOOP ( 'NONE', ( #27460, #33200, #59509, #40493 ) ) ;
#31232=VERTEX_POINT ( 'NONE', #43246 ) ;
#31241=CARTESIAN_POINT ( 'NONE',  ( 0.8744876279028306332, -8.712669995481570950, -48.31603700562917680 ) ) ;
#31248=VECTOR ( 'NONE', #57585, 1000.000000000000000 ) ;
#31270=CARTESIAN_POINT ( 'NONE',  ( 0.1140933569871964287, -12.19049900475206449, -42.40685892752544106 ) ) ;
#31276=LINE ( 'NONE', #41022, #10505 ) ;
#31280=DIRECTION ( 'NONE',  ( 0.09722883295013591554, -0.8634569929835322899, 0.4949632060173673187 ) ) ;
#31286=FACE_OUTER_BOUND ( 'NONE', #31468, .T. ) ;
#31287=CARTESIAN_POINT ( 'NONE',  ( 0.6008122571543326185, -47.61009277872437906, -12.03468387896310787 ) ) ;
#31290=CARTESIAN_POINT ( 'NONE',  ( 0.3676999524040323597, -40.57213187173838520, -17.31625533148287843 ) ) ;
#31296=CARTESIAN_POINT ( 'NONE',  ( 0.3676999524040323597, -0.5887207181719652516, -44.10900124961835900 ) ) ;
#31301=CARTESIAN_POINT ( 'NONE',  ( 0.6000166863083106206, -34.91285637184702040, 34.53861522509602366 ) ) ;
#31302=VERTEX_POINT ( 'NONE', #40713 ) ;
#31305=( BOUNDED_SURFACE ( )  B_SPLINE_SURFACE ( 3, 1, ( 
 ( #17681, #23008 ),
 ( #36809, #28608 ),
 ( #56800, #52102 ),
 ( #47732, #13929 ) ),
 .UNSPECIFIED., .F., .F., .F. ) 
 B_SPLINE_SURFACE_WITH_KNOTS ( ( 4, 4 ),
 ( 2, 2 ),
 ( 0.000000000000000000, 1.000000000000000000 ),
 ( 0.000000000000000000, 1.000000000000000000 ),
 .UNSPECIFIED. ) 
 GEOMETRIC_REPRESENTATION_ITEM ( )  RATIONAL_B_SPLINE_SURFACE ( (
 ( 1.000000000000000000, 1.000000000000000000),
 ( 0.7211978278499970862, 0.9934217856018976445),
 ( 0.7211978278499970862, 0.9934217856018976445),
 ( 1.000000000000000000, 1.000000000000000000) ) ) 
 REPRESENTATION_ITEM ( '' )  SURFACE ( )  );
#31310=VERTEX_POINT ( 'NONE', #17501 ) ;
#31313=CARTESIAN_POINT ( 'NONE',  ( 0.1129192098497455998, -40.71518461128082578, -17.00663193740825463 ) ) ;
#31315=DIRECTION ( 'NONE',  ( -1.000000000000000000, -0.000000000000000000, -0.000000000000000000 ) ) ;
#31318=CARTESIAN_POINT ( 'NONE',  ( 2.706805983486679779, 5.870773205767990888, 43.61548045460686041 ) ) ;
#31324=B_SPLINE_CURVE_WITH_KNOTS ( 'NONE', 3,
 ( #10503, #58701, #786, #59329, #53395, #16432 ),
 .UNSPECIFIED., .F., .F.,
 ( 4, 2, 4 ),
 ( 1.737169676453554432E-17, 0.0002293755540694307222, 0.0004587511081388440429 ),
 .UNSPECIFIED. ) ;
#31326=CARTESIAN_POINT ( 'NONE',  ( 0.8753041380234465318, 44.61941359694289133, -20.49990873486825294 ) ) ;
#31340=CONICAL_SURFACE ( 'NONE', #12353, 43.92652462719577500, 1.486293639869522343 ) ;
#31341=SURFACE_STYLE_USAGE ( .BOTH. , #16630 ) ;
#31346=CARTESIAN_POINT ( 'NONE',  ( -6.057079549204054558, 0.6257114429644480280, 19.24681054850080031 ) ) ;
#31354=CARTESIAN_POINT ( 'NONE',  ( 0.1119898979215350060, 43.19989880356775558, -8.984990351321133772 ) ) ;
#31358=CARTESIAN_POINT ( 'NONE',  ( -6.078726893082806448, -4.288195875146425529, -18.77246434022707788 ) ) ;
#31359=CARTESIAN_POINT ( 'NONE',  ( -6.078726893082806448, -11.01388439747515235, 15.79520154185357050 ) ) ;
#31360=ORIENTED_EDGE ( 'NONE', *, *, #53238, .T. ) ;
#31362=DIRECTION ( 'NONE',  ( -1.000000000000000000, -0.000000000000000000, -0.000000000000000000 ) ) ;
#31367=EDGE_CURVE ( 'NONE', #57370, #12019, #8383, .T. ) ;
#31374=DIRECTION ( 'NONE',  ( 0.000000000000000000, 0.000000000000000000, 1.000000000000000000 ) ) ;
#31383=ORIENTED_EDGE ( 'NONE', *, *, #29706, .T. ) ;
#31385=( BOUNDED_SURFACE ( )  B_SPLINE_SURFACE ( 3, 1, ( 
 ( #25694, #49494 ),
 ( #21930, #16936 ),
 ( #2174, #20999 ),
 ( #49810, #58883 ) ),
 .UNSPECIFIED., .F., .F., .F. ) 
 B_SPLINE_SURFACE_WITH_KNOTS ( ( 4, 4 ),
 ( 2, 2 ),
 ( 0.000000000000000000, 1.000000000000000000 ),
 ( 0.000000000000000000, 1.000000000000000000 ),
 .UNSPECIFIED. ) 
 GEOMETRIC_REPRESENTATION_ITEM ( )  RATIONAL_B_SPLINE_SURFACE ( (
 ( 1.000000000000000000, 1.000000000000000000),
 ( 0.7211978278499968642, 0.9934217856018975334),
 ( 0.7211978278499968642, 0.9934217856018975334),
 ( 1.000000000000000000, 1.000000000000000000) ) ) 
 REPRESENTATION_ITEM ( '' )  SURFACE ( )  );
#31391=CARTESIAN_POINT ( 'NONE',  ( -2.601141883200662974, 14.73012113219607144, 2.412251831840835692 ) ) ;
#31394=VECTOR ( 'NONE', #25521, 1000.000000000000000 ) ;
#31397=EDGE_CURVE ( 'NONE', #54532, #9438, #33487, .T. ) ;
#31402=CARTESIAN_POINT ( 'NONE',  ( -6.079354080745853928, 0.6160181061932726854, -19.24612888195971649 ) ) ;
#31404=FACE_OUTER_BOUND ( 'NONE', #14132, .T. ) ;
#31408=ORIENTED_EDGE ( 'NONE', *, *, #39071, .F. ) ;
#31415=CARTESIAN_POINT ( 'NONE',  ( 0.3676999524040366896, 25.91024933382758277, 35.70167450949220722 ) ) ;
#31418=CARTESIAN_POINT ( 'NONE',  ( 0.5997462898726536595, -42.52950339524503676, 24.55184251941493301 ) ) ;
#31419=CARTESIAN_POINT ( 'NONE',  ( 5.901764892641307547, -37.25947723020409086, -31.77613607680425289 ) ) ;
#31420=CARTESIAN_POINT ( 'NONE',  ( 0.7044674535452954967, -20.64605418817902205, 44.55943412196435816 ) ) ;
#31427=CARTESIAN_POINT ( 'NONE',  ( 0.6021447746440204973, 17.20494439911720974, 45.99490218830531063 ) ) ;
#31428=CARTESIAN_POINT ( 'NONE',  ( 0.5997462898726536595, -47.63132954987539591, 11.95023328037892441 ) ) ;
#31439=CARTESIAN_POINT ( 'NONE',  ( 5.901764892641307547, 48.56171591663477471, 6.304856435458333408 ) ) ;
#31447=ORIENTED_EDGE ( 'NONE', *, *, #29412, .T. ) ;
#31458=CARTESIAN_POINT ( 'NONE',  ( -6.078457390727109555, 9.985927120572020144, 16.46437883979022487 ) ) ;
#31459=DIRECTION ( 'NONE',  ( 1.000000000000000000, 0.000000000000000000, 0.000000000000000000 ) ) ;
#31468=EDGE_LOOP ( 'NONE', ( #17939, #20432, #24357, #16289 ) ) ;
#31475=CARTESIAN_POINT ( 'NONE',  ( -6.057079549204054558, 15.42772006041544053, -11.52461213391554473 ) ) ;
#31479=B_SPLINE_CURVE_WITH_KNOTS ( 'NONE', 3,
 ( #19742, #24423, #57294, #38866, #58224, #923 ),
 .UNSPECIFIED., .F., .F.,
 ( 4, 2, 4 ),
 ( 4.445228907190568179E-18, 0.0002447193893791738822, 0.0004894387787583433192 ),
 .UNSPECIFIED. ) ;
#31481=CARTESIAN_POINT ( 'NONE',  ( 0.5997462898726536595, -43.04230894295751852, 23.64130434225888777 ) ) ;
#31483=CARTESIAN_POINT ( 'NONE',  ( 0.8753041380234530822, 48.93739466471257060, -4.033575498629232037 ) ) ;
#31484=B_SPLINE_CURVE_WITH_KNOTS ( 'NONE', 3,
 ( #43696, #44314, #15174, #53650, #34279, #29560, #11089, #48670, #5725, #39296, #10781, #29868, #30169, #48983, #6032, #1341, #20478, #6334, #1650 ),
 .UNSPECIFIED., .F., .F.,
 ( 4, 3, 3, 3, 3, 3, 4 ),
 ( 1.734776414728241573E-18, 0.0002612768053151722511, 0.0003919133833142921723, 0.0005225499612322614040, 0.0006531865391693354164, 0.0008112755173415183395, 0.0009693688056799726815 ),
 .UNSPECIFIED. ) ;
#31485=CARTESIAN_POINT ( 'NONE',  ( 0.6021448801613057400, 41.29830282053138291, -26.57049722475356290 ) ) ;
#31486=EDGE_CURVE ( 'NONE', #1744, #3087, #7254, .T. ) ;
#31487=ORIENTED_EDGE ( 'NONE', *, *, #29878, .T. ) ;
#31496=CARTESIAN_POINT ( 'NONE',  ( 1.830465331921977468, -13.71215074184886795, 41.86111534480661334 ) ) ;
#31497=CIRCLE ( 'NONE', #37518, 48.91267123290010943 ) ;
#31499=CARTESIAN_POINT ( 'NONE',  ( 0.5549461598389364703, 36.47739348819886374, -24.79147958016848818 ) ) ;
#31500=FACE_OUTER_BOUND ( 'NONE', #35422, .T. ) ;
#31501=CARTESIAN_POINT ( 'NONE',  ( 4.553261556744875094, 0.000000000000000000, 0.000000000000000000 ) ) ;
#31504=CARTESIAN_POINT ( 'NONE',  ( 2.648799415243696664, -2.956030660112017650, 48.94669903094667518 ) ) ;
#31505=CARTESIAN_POINT ( 'NONE',  ( -2.601141883200665639, -11.02917173973140308, 10.05747474294113175 ) ) ;
#31507=CARTESIAN_POINT ( 'NONE',  ( 0.8744876279028263033, 37.95405449045444612, -31.14225101233220627 ) ) ;
#31510=CARTESIAN_POINT ( 'NONE',  ( 0.8753041380234530822, -8.714053517583518982, -48.32394436680091587 ) ) ;
#31512=ORIENTED_EDGE ( 'NONE', *, *, #47864, .T. ) ;
#31513=VERTEX_POINT ( 'NONE', #10259 ) ;
#31520=VERTEX_POINT ( 'NONE', #43174 ) ;
#31522=B_SPLINE_CURVE_WITH_KNOTS ( 'NONE', 3,
 ( #38039, #37104, #61175, #28902 ),
 .UNSPECIFIED., .F., .F.,
 ( 4, 4 ),
 ( 0.000000000000000000, 0.005013413432710153717 ),
 .UNSPECIFIED. ) ;
#31523=CARTESIAN_POINT ( 'NONE',  ( 0.1157506346131639274, -42.70450186874222709, -11.10253033976606929 ) ) ;
#31526=CARTESIAN_POINT ( 'NONE',  ( 4.553261556744875094, 0.000000000000000000, 0.000000000000000000 ) ) ;
#31527=CARTESIAN_POINT ( 'NONE',  ( 0.1158516988532803382, 33.63005810211861046, 28.56503721126445328 ) ) ;
#31529=CARTESIAN_POINT ( 'NONE',  ( 0.8753041380234465318, -31.30612550145435335, 37.82941757363136048 ) ) ;
#31531=ORIENTED_EDGE ( 'NONE', *, *, #32909, .T. ) ;
#31532=FACE_OUTER_BOUND ( 'NONE', #52620, .T. ) ;
#31533=CARTESIAN_POINT ( 'NONE',  ( 0.5980271706414734822, 44.54819170408481455, 20.67626317151556847 ) ) ;
#31536=ORIENTED_EDGE ( 'NONE', *, *, #269, .T. ) ;
#31539=CARTESIAN_POINT ( 'NONE',  ( 0.1145239942831223490, 39.89514688507366458, -18.85000625260029139 ) ) ;
#31540=EDGE_LOOP ( 'NONE', ( #45660, #49571, #34390, #41516 ) ) ;
#31546=CARTESIAN_POINT ( 'NONE',  ( 0.6253024248130477636, 10.25657594887568358, 48.02339926767562872 ) ) ;
#31555=ADVANCED_FACE ( 'NONE', ( #34381 ), #51306, .F. ) ;
#31559=CARTESIAN_POINT ( 'NONE',  ( 0.5997462898726536595, -2.096122762665173944, 49.06279547180476897 ) ) ;
#31560=CARTESIAN_POINT ( 'NONE',  ( 0.6016118706126977189, 32.75634973515021642, 36.58650853542129511 ) ) ;
#31567=CARTESIAN_POINT ( 'NONE',  ( 4.553261556744873317, -43.82122302957819215, 3.039733214543990591 ) ) ;
#31568=ORIENTED_EDGE ( 'NONE', *, *, #42189, .T. ) ;
#31575=CARTESIAN_POINT ( 'NONE',  ( 0.2279481005628793411, -38.06357991528984996, -22.30845963093949891 ) ) ;
#31582=CARTESIAN_POINT ( 'NONE',  ( 4.975610109902397937, -46.59897809419034331, -14.86555238512655919 ) ) ;
#31583=CARTESIAN_POINT ( 'NONE',  ( 0.6021448801613057400, 22.94537434242217699, -43.41717327179489416 ) ) ;
#31588=CARTESIAN_POINT ( 'NONE',  ( 1.834102595619085951, 16.42859871478874112, 40.86929029388846857 ) ) ;
#31593=CARTESIAN_POINT ( 'NONE',  ( 3.727782113643637096, -33.03100872435383195, -29.01258758810796934 ) ) ;
#31594=CARTESIAN_POINT ( 'NONE',  ( 0.1139756605157202368, -38.63988289368274565, -21.30527328286372679 ) ) ;
#31595=B_SPLINE_CURVE_WITH_KNOTS ( 'NONE', 3,
 ( #59141, #1506, #25640, #16250, #35374, #30030, #11560, #25334, #44174, #20039, #39774, #10316, #58828, #586, #49140, #30639 ),
 .UNSPECIFIED., .F., .F.,
 ( 4, 3, 3, 3, 3, 4 ),
 ( 1.962735358247463844E-17, 0.0002612764279487714823, 0.0003919131003184828229, 0.0005225497727000612443, 0.0007837925190632434027, 0.001045051706266712831 ),
 .UNSPECIFIED. ) ;
#31597=ORIENTED_EDGE ( 'NONE', *, *, #48672, .T. ) ;
#31599=CARTESIAN_POINT ( 'NONE',  ( 2.706805983486679779, -40.14236207468513840, 18.03792893834089028 ) ) ;
#31600=CARTESIAN_POINT ( 'NONE',  ( -6.078457390727109555, 13.82950465835784648, 13.39922803529989004 ) ) ;
#31601=ADVANCED_FACE ( 'NONE', ( #2999 ), #31340, .F. ) ;
#31605=CARTESIAN_POINT ( 'NONE',  ( 0.2940133293163009198, -0.6094640175106790236, -44.11200633829074746 ) ) ;
#31610=ORIENTED_EDGE ( 'NONE', *, *, #25639, .T. ) ;
#31616=VERTEX_POINT ( 'NONE', #35626 ) ;
#31630=FACE_OUTER_BOUND ( 'NONE', #19086, .T. ) ;
#31634=VERTEX_POINT ( 'NONE', #59082 ) ;
#31639=CARTESIAN_POINT ( 'NONE',  ( -6.072942160501519027, -8.893884846139481937, -17.07931423191899967 ) ) ;
#31649=EDGE_CURVE ( 'NONE', #7712, #31065, #38587, .T. ) ;
#31650=CARTESIAN_POINT ( 'NONE',  ( 3.678748215320119641, -18.11950377857164796, 45.50050985558087291 ) ) ;
#31651=CARTESIAN_POINT ( 'NONE',  ( 3.678834586032788234, 36.06700467432391832, 33.13281671471128220 ) ) ;
#31657=DIRECTION ( 'NONE',  ( 0.1011922191286468015, 0.9481578383257814879, 0.3012587731655313461 ) ) ;
#31664=CARTESIAN_POINT ( 'NONE',  ( 0.1129192098497447394, -40.71518461128108157, 17.00663193740767909 ) ) ;
#31665=CARTESIAN_POINT ( 'NONE',  ( -6.078457390727109555, -4.289140445936316048, -18.77226105914099108 ) ) ;
#31671=CARTESIAN_POINT ( 'NONE',  ( 0.1365634738349414956, -18.44080531820494429, 40.08490138243215029 ) ) ;
#31677=B_SPLINE_CURVE_WITH_KNOTS ( 'NONE', 3,
 ( #56650, #36968, #32249, #61949, #56031, #38198, #4014, #51329, #52566, #52255, #47271, #41974, #4317, #9351, #37899, #18454 ),
 .UNSPECIFIED., .F., .F.,
 ( 4, 3, 3, 3, 3, 4 ),
 ( 1.868480190406682863E-17, 0.0002612764279487713196, 0.0003919131003184810340, 0.0005225497727000705684, 0.0007837925190632463301, 0.001045051706266716951 ),
 .UNSPECIFIED. ) ;
#31679=DIRECTION ( 'NONE',  ( 0.000000000000000000, 0.000000000000000000, -1.000000000000000000 ) ) ;
#31685=CARTESIAN_POINT ( 'NONE',  ( 1.112077966505211624, -11.53183610920814672, 42.54464808972942791 ) ) ;
#31691=CARTESIAN_POINT ( 'NONE',  ( 0.1139756605157204866, 44.05734318149369244, 2.430171081038008385 ) ) ;
#31693=VERTEX_POINT ( 'NONE', #30894 ) ;
#31694=CARTESIAN_POINT ( 'NONE',  ( 4.298430060108861639, 0.6201974722425471764, 48.94032081561889669 ) ) ;
#31703=CARTESIAN_POINT ( 'NONE',  ( 3.221118495291108719, -37.36356056591105101, 23.21046663682675870 ) ) ;
#31704=AXIS2_PLACEMENT_3D ( 'NONE', #30282, #29979, #59709 ) ;
#31706=ORIENTED_EDGE ( 'NONE', *, *, #47859, .T. ) ;
#31708=EDGE_LOOP ( 'NONE', ( #36117, #56824, #56346, #5703 ) ) ;
#31713=ORIENTED_EDGE ( 'NONE', *, *, #25953, .F. ) ;
#31719=ORIENTED_EDGE ( 'NONE', *, *, #22325, .F. ) ;
#31724=CARTESIAN_POINT ( 'NONE',  ( -6.078075953587585900, -18.27673012847649048, 6.062698248962721692 ) ) ;
#31734=CARTESIAN_POINT ( 'NONE',  ( 0.8744876279028306332, 37.95405449045402690, 31.14225101233274273 ) ) ;
#31735=CARTESIAN_POINT ( 'NONE',  ( 4.335381028904216727, -11.88755795484514444, 47.52307664213822136 ) ) ;
#31736=CARTESIAN_POINT ( 'NONE',  ( 0.5987334363312689645, 16.39078270287454941, 46.29152350980928077 ) ) ;
#31737=CARTESIAN_POINT ( 'NONE',  ( 4.975610109902397937, 8.374023221151757568, 48.19050883970187016 ) ) ;
#31740=CARTESIAN_POINT ( 'NONE',  ( 0.5997462898726536595, -39.04071682475809268, 29.78882441375220580 ) ) ;
#31749=CARTESIAN_POINT ( 'NONE',  ( 3.894904216938897878, 2.001151192542965696, -43.91036012583801806 ) ) ;
#31752=EDGE_LOOP ( 'NONE', ( #20166, #50608, #35816, #45142 ) ) ;
#31767=CARTESIAN_POINT ( 'NONE',  ( 0.7242486021783850481, 48.94187082523895782, 3.962920955507279075 ) ) ;
#31776=VERTEX_POINT ( 'NONE', #51228 ) ;
#31779=VERTEX_POINT ( 'NONE', #34307 ) ;
#31792=CARTESIAN_POINT ( 'NONE',  ( -2.601141883200665639, -1.938888835821155343, -14.79986951130707418 ) ) ;
#31808=CARTESIAN_POINT ( 'NONE',  ( 4.975610109902397937, 45.55079628452135410, -17.82061629079668919 ) ) ;
#31814=CARTESIAN_POINT ( 'NONE',  ( 5.901764892641288895, 35.20706988846465890, 34.03606465660275404 ) ) ;
#31826=ORIENTED_EDGE ( 'NONE', *, *, #34196, .T. ) ;
#31827=CARTESIAN_POINT ( 'NONE',  ( 2.359973842542475886, -19.18972130672883480, -39.62184360681084883 ) ) ;
#31829=CARTESIAN_POINT ( 'NONE',  ( 0.8744876279028263033, -8.712669995482247742, 48.31603700562906312 ) ) ;
#31830=ORIENTED_EDGE ( 'NONE', *, *, #58968, .T. ) ;
#31831=DIRECTION ( 'NONE',  ( 0.09722883295013591554, 0.9927043560032293712, -0.07130649069592721878 ) ) ;
#31834=VERTEX_POINT ( 'NONE', #43727 ) ;
#31838=VECTOR ( 'NONE', #45572, 1000.000000000000114 ) ;
#31844=EDGE_CURVE ( 'NONE', #47787, #59402, #19287, .T. ) ;
#31847=CARTESIAN_POINT ( 'NONE',  ( -2.601141883200662974, -12.77988133643097868, 7.711683376288982927 ) ) ;
#31849=VERTEX_POINT ( 'NONE', #57770 ) ;
#31850=CARTESIAN_POINT ( 'NONE',  ( -6.078075953587585900, 12.00179475453301237, -15.05828997320744733 ) ) ;
#31854=CARTESIAN_POINT ( 'NONE',  ( 4.694002226626920127, -44.81211596887070669, -8.376098963038668188 ) ) ;
#31855=CARTESIAN_POINT ( 'NONE',  ( -6.078075953587585900, 16.77554405305491514, -9.453903742430952661 ) ) ;
#31856=CARTESIAN_POINT ( 'NONE',  ( 4.553261556744875094, 38.38432632180499837, -21.35844232721162683 ) ) ;
#31867=CIRCLE ( 'NONE', #4818, 48.91267123290010943 ) ;
#31869=CARTESIAN_POINT ( 'NONE',  ( 4.975610109902397937, -16.35148546628954236, 46.09857188876348744 ) ) ;
#31870=CARTESIAN_POINT ( 'NONE',  ( 0.6029443199889047422, -48.70424120927577150, -6.279691878037166219 ) ) ;
#31872=ORIENTED_EDGE ( 'NONE', *, *, #58101, .T. ) ;
#31873=CARTESIAN_POINT ( 'NONE',  ( 0.1152809850208375564, -27.33770535629795262, -34.63517212808380208 ) ) ;
#31877=CARTESIAN_POINT ( 'NONE',  ( 0.1365634738349354727, 29.18960898986780350, 33.08820555185599943 ) ) ;
#31878=CARTESIAN_POINT ( 'NONE',  ( 4.975610109902397937, -17.43163075979710541, 45.70106843599904778 ) ) ;
#31881=CARTESIAN_POINT ( 'NONE',  ( 0.2279481005628775092, 33.09720086222342417, 29.17325456918634430 ) ) ;
#31884=CONICAL_SURFACE ( 'NONE', #24906, 43.92652462719577500, 1.486293639869522343 ) ;
#31892=CARTESIAN_POINT ( 'NONE',  ( 0.6028777368367060907, 44.20642035250607904, 21.38532742158998801 ) ) ;
#31904=CARTESIAN_POINT ( 'NONE',  ( 0.6021447746440204973, -1.835079692253900996, -49.07314562580602058 ) ) ;
#31906=CARTESIAN_POINT ( 'NONE',  ( -2.739355103387248747, -12.87605224490611633, 7.553465796405332000 ) ) ;
#31917=CARTESIAN_POINT ( 'NONE',  ( 0.8744876279028306332, 33.66006955981207227, 35.74003032466684004 ) ) ;
#31919=CARTESIAN_POINT ( 'NONE',  ( -6.078726893082806448, -6.647148524917478873, -18.07233957617019371 ) ) ;
#31920=ORIENTED_EDGE ( 'NONE', *, *, #34519, .F. ) ;
#31924=ORIENTED_EDGE ( 'NONE', *, *, #4919, .T. ) ;
#31925=CARTESIAN_POINT ( 'NONE',  ( 2.648799415243708655, 3.327403256649515750, -48.92285611917233012 ) ) ;
#31933=( BOUNDED_SURFACE ( )  B_SPLINE_SURFACE ( 3, 1, ( 
 ( #30317, #59748 ),
 ( #40372, #25017 ),
 ( #49424, #11863 ),
 ( #40074, #20929 ) ),
 .UNSPECIFIED., .F., .F., .F. ) 
 B_SPLINE_SURFACE_WITH_KNOTS ( ( 4, 4 ),
 ( 2, 2 ),
 ( 0.000000000000000000, 1.000000000000000000 ),
 ( 0.000000000000000000, 1.000000000000000000 ),
 .UNSPECIFIED. ) 
 GEOMETRIC_REPRESENTATION_ITEM ( )  RATIONAL_B_SPLINE_SURFACE ( (
 ( 1.000000000000000000, 1.000000000000000000),
 ( 0.7211978278499968642, 0.9934217856018975334),
 ( 0.7211978278499968642, 0.9934217856018975334),
 ( 1.000000000000000000, 1.000000000000000000) ) ) 
 REPRESENTATION_ITEM ( '' )  SURFACE ( )  );
#31936=VECTOR ( 'NONE', #23392, 1000.000000000000114 ) ;
#31938=ORIENTED_EDGE ( 'NONE', *, *, #27305, .T. ) ;
#31939=CARTESIAN_POINT ( 'NONE',  ( 4.335381028904201628, 12.96255624111893923, -47.24117889469074782 ) ) ;
#31943=DIRECTION ( 'NONE',  ( 0.000000000000000000, 0.000000000000000000, 1.000000000000000000 ) ) ;
#31951=EDGE_LOOP ( 'NONE', ( #44326, #6595, #28083, #27674 ) ) ;
#31952=( BOUNDED_SURFACE ( )  B_SPLINE_SURFACE ( 3, 1, ( 
 ( #28798, #52596 ),
 ( #58211, #38231 ),
 ( #9687, #15337 ),
 ( #44175, #5278 ) ),
 .UNSPECIFIED., .F., .F., .F. ) 
 B_SPLINE_SURFACE_WITH_KNOTS ( ( 4, 4 ),
 ( 2, 2 ),
 ( 0.000000000000000000, 1.000000000000000000 ),
 ( 0.000000000000000000, 1.000000000000000000 ),
 .UNSPECIFIED. ) 
 GEOMETRIC_REPRESENTATION_ITEM ( )  RATIONAL_B_SPLINE_SURFACE ( (
 ( 1.000000000000000000, 1.000000000000000000),
 ( 0.7211978278499970862, 0.9934217856018976445),
 ( 0.7211978278499970862, 0.9934217856018976445),
 ( 1.000000000000000000, 1.000000000000000000) ) ) 
 REPRESENTATION_ITEM ( '' )  SURFACE ( )  );
#31956=ADVANCED_FACE ( 'NONE', ( #56435 ), #47484, .F. ) ;
#31957=VERTEX_POINT ( 'NONE', #51421 ) ;
#31958=CARTESIAN_POINT ( 'NONE',  ( 4.834790513006555379, 18.70372717509382454, -43.39078163255459941 ) ) ;
#31961=DIRECTION ( 'NONE',  ( 0.09722883295013594329, 0.7529176304110362095, -0.6508929219613506234 ) ) ;
#31964=B_SPLINE_CURVE_WITH_KNOTS ( 'NONE', 3,
 ( #48098, #61852, #52160, #5150, #33088, #3921 ),
 .UNSPECIFIED., .F., .F.,
 ( 4, 2, 4 ),
 ( 0.000000000000000000, 0.0002447195606305749629, 0.0004894391212611499259 ),
 .UNSPECIFIED. ) ;
#31966=CARTESIAN_POINT ( 'NONE',  ( 2.185380717157383579, -43.46326555698310301, 7.054385174511375034 ) ) ;
#31971=CARTESIAN_POINT ( 'NONE',  ( 0.2940133293163019190, 21.11549836636102739, -38.73469088966953677 ) ) ;
#31978=CARTESIAN_POINT ( 'NONE',  ( 0.8744876279028306332, 33.66006955981207227, 35.74003032466684004 ) ) ;
#31987=CARTESIAN_POINT ( 'NONE',  ( 0.5987334308729320709, 46.41165616633498558, -16.04746330320246273 ) ) ;
#31990=VERTEX_POINT ( 'NONE', #13549 ) ;
#31995=B_SPLINE_CURVE_WITH_KNOTS ( 'NONE', 3,
 ( #58165, #52549, #5841, #33788 ),
 .UNSPECIFIED., .F., .F.,
 ( 4, 4 ),
 ( 0.000000000000000000, 0.004442905043737213969 ),
 .UNSPECIFIED. ) ;
#31996=ADVANCED_FACE ( 'NONE', ( #45298 ), #58729, .T. ) ;
#31998=B_SPLINE_CURVE_WITH_KNOTS ( 'NONE', 3,
 ( #47020, #27276, #17892, #32920, #3751, #51686 ),
 .UNSPECIFIED., .F., .F.,
 ( 4, 2, 4 ),
 ( 1.867239236438689166E-17, 0.0002293755540694309119, 0.0004587511081388431214 ),
 .UNSPECIFIED. ) ;
#31999=CARTESIAN_POINT ( 'NONE',  ( -6.079354080745853928, 19.25598488485689330, -0.001167186744193668890 ) ) ;
#32001=CARTESIAN_POINT ( 'NONE',  ( -6.077587904424778920, -19.21610359950805247, 1.239912838430311970 ) ) ;
#32003=ORIENTED_EDGE ( 'NONE', *, *, #12676, .T. ) ;
#32004=EDGE_LOOP ( 'NONE', ( #16831, #61338, #24872, #10002 ) ) ;
#32005=CARTESIAN_POINT ( 'NONE',  ( 0.1158516988532803799, 44.03663622717940740, 2.777918038363759390 ) ) ;
#32007=CARTESIAN_POINT ( 'NONE',  ( -6.078075953587585900, 19.25604180663921738, -0.005309246513132053445 ) ) ;
#32008=EDGE_CURVE ( 'NONE', #59505, #40325, #23708, .T. ) ;
#32013=ORIENTED_EDGE ( 'NONE', *, *, #32537, .T. ) ;
#32017=CARTESIAN_POINT ( 'NONE',  ( 2.533389852662419894, -37.55112757475649943, 22.96439308142020153 ) ) ;
#32021=ORIENTED_EDGE ( 'NONE', *, *, #20307, .T. ) ;
#32028=CARTESIAN_POINT ( 'NONE',  ( 4.335381028904216727, -17.86707742387240216, 45.61276566920378883 ) ) ;
#32029=CARTESIAN_POINT ( 'NONE',  ( 1.296416391601052265, 8.720348633736866972, -43.20026497351888395 ) ) ;
#32032=EDGE_CURVE ( 'NONE', #24292, #4853, #14725, .T. ) ;
#32036=CARTESIAN_POINT ( 'NONE',  ( -4.915099999999999802, 0.000000000000000000, 0.000000000000000000 ) ) ;
#32039=CARTESIAN_POINT ( 'NONE',  ( 0.8744876279028306332, -49.08725279547490317, 0.8897546699139438076 ) ) ;
#32042=EDGE_CURVE ( 'NONE', #9806, #31849, #45358, .T. ) ;
#32043=CARTESIAN_POINT ( 'NONE',  ( 0.8753041380234530822, -26.21158409634513120, -41.52217705074249210 ) ) ;
#32049=LINE ( 'NONE', #51125, #39234 ) ;
#32053=CARTESIAN_POINT ( 'NONE',  ( 4.553261556744875094, 0.000000000000000000, 0.000000000000000000 ) ) ;
#32055=CARTESIAN_POINT ( 'NONE',  ( 4.553261556744873317, -15.38244134641770167, -41.14510984366982171 ) ) ;
#32060=CARTESIAN_POINT ( 'NONE',  ( 0.6024113833632039894, -47.55614101750226297, 12.24562455019367668 ) ) ;
#32070=CARTESIAN_POINT ( 'NONE',  ( 1.834102595619085285, -30.72137182784087273, 31.56572599946387570 ) ) ;
#32080=ORIENTED_EDGE ( 'NONE', *, *, #47739, .T. ) ;
#32092=CARTESIAN_POINT ( 'NONE',  ( 4.553261556744875094, 0.000000000000000000, 0.000000000000000000 ) ) ;
#32095=ORIENTED_EDGE ( 'NONE', *, *, #44068, .T. ) ;
#32098=B_SPLINE_CURVE_WITH_KNOTS ( 'NONE', 3,
 ( #7277, #40854, #54901, #41154, #45855, #40538, #16712, #12333, #60216, #59919, #54269, #12035, #26716, #40241, #1653, #17030, #6645, #17328, #25793, #44931, #36144, #55209, #6966, #1970, #49912 ),
 .UNSPECIFIED., .F., .F.,
 ( 4, 3, 3, 3, 3, 3, 3, 3, 4 ),
 ( 7.757919228897728493E-18, 0.0005656085177311412663, 0.001131215744874502441, 0.001696821861372768735, 0.002262427090022499018, 0.002828031679238746793, 0.003393635864401606164, 0.003977030878808133357, 0.004561030005651160735 ),
 .UNSPECIFIED. ) ;
#32101=CARTESIAN_POINT ( 'NONE',  ( 0.1129192098497455998, 15.69290830752535726, -41.23935519181593889 ) ) ;
#32106=CARTESIAN_POINT ( 'NONE',  ( -6.077587904424778920, 15.42837212129427193, -11.52221137980032495 ) ) ;
#32109=EDGE_CURVE ( 'NONE', #49082, #53370, #10167, .T. ) ;
#32117=CARTESIAN_POINT ( 'NONE',  ( 4.335381028904201628, 8.818319717467213437, 48.18707383754355078 ) ) ;
#32123=CARTESIAN_POINT ( 'NONE',  ( 4.553261556744873317, 12.71466023209499419, 42.04612920360230532 ) ) ;
#32124=CARTESIAN_POINT ( 'NONE',  ( 0.1129192098497455998, -35.06977877439224045, -26.77802092202373174 ) ) ;
#32129=( BOUNDED_SURFACE ( )  B_SPLINE_SURFACE ( 3, 1, ( 
 ( #30567, #7364 ),
 ( #31193, #31504 ),
 ( #2367, #40018 ),
 ( #16184, #54359 ) ),
 .UNSPECIFIED., .F., .F., .F. ) 
 B_SPLINE_SURFACE_WITH_KNOTS ( ( 4, 4 ),
 ( 2, 2 ),
 ( 0.000000000000000000, 1.000000000000000000 ),
 ( 0.000000000000000000, 1.000000000000000000 ),
 .UNSPECIFIED. ) 
 GEOMETRIC_REPRESENTATION_ITEM ( )  RATIONAL_B_SPLINE_SURFACE ( (
 ( 1.000000000000000000, 1.000000000000000000),
 ( 0.7211978278499970862, 0.9934217856018976445),
 ( 0.7211978278499970862, 0.9934217856018976445),
 ( 1.000000000000000000, 1.000000000000000000) ) ) 
 REPRESENTATION_ITEM ( '' )  SURFACE ( )  );
#32130=EDGE_CURVE ( 'NONE', #20167, #23759, #26469, .T. ) ;
#32132=CARTESIAN_POINT ( 'NONE',  ( 0.6029442701453591180, -1.486909339572786815, 49.08497046728426483 ) ) ;
#32140=B_SPLINE_CURVE_WITH_KNOTS ( 'NONE', 3,
 ( #52481, #28684, #51243, #8328 ),
 .UNSPECIFIED., .F., .F.,
 ( 4, 4 ),
 ( 2.204559228842524708E-17, 0.004559932413162186803 ),
 .UNSPECIFIED. ) ;
#32141=ORIENTED_EDGE ( 'NONE', *, *, #58835, .T. ) ;
#32146=ORIENTED_EDGE ( 'NONE', *, *, #5684, .F. ) ;
#32148=CARTESIAN_POINT ( 'NONE',  ( 1.657374760986086493, 37.58311877771095055, 22.98694477725811325 ) ) ;
#32151=EDGE_CURVE ( 'NONE', #40264, #13345, #42253, .T. ) ;
#32153=CARTESIAN_POINT ( 'NONE',  ( 0.1139756605157204034, -42.78034046113214117, -10.80729798444754408 ) ) ;
#32154=CIRCLE ( 'NONE', #44173, 43.92652462719577500 ) ;
#32158=CARTESIAN_POINT ( 'NONE',  ( -6.078726893082806448, 12.00325722817150620, -15.05708661006732108 ) ) ;
#32159=CARTESIAN_POINT ( 'NONE',  ( -6.077587904424778920, -6.644566705895037728, 18.07334376048996916 ) ) ;
#32161=DIRECTION ( 'NONE',  ( -1.000000000000000000, -0.000000000000000000, -0.000000000000000000 ) ) ;
#32163=CARTESIAN_POINT ( 'NONE',  ( 3.221118495291108719, 38.77389282677542326, -20.76888669908632323 ) ) ;
#32164=CARTESIAN_POINT ( 'NONE',  ( 1.830465331921976135, 37.57662538868725477, -22.98637162052015626 ) ) ;
#32166=ORIENTED_EDGE ( 'NONE', *, *, #32356, .F. ) ;
#32177=CARTESIAN_POINT ( 'NONE',  ( 0.1156867017252034419, -27.41316746739866872, -34.57544007933292818 ) ) ;
#32178=CARTESIAN_POINT ( 'NONE',  ( 0.1154773475650540254, -27.37012761473843270, 34.60953256545158041 ) ) ;
#32184=CARTESIAN_POINT ( 'NONE',  ( 0.5997462898726536595, -39.04071682475767346, -29.78882441375276358 ) ) ;
#32192=CARTESIAN_POINT ( 'NONE',  ( 0.7242003506640003474, -48.79688540705116395, -5.465862118380373502 ) ) ;
#32195=CARTESIAN_POINT ( 'NONE',  ( -6.078075953587585900, 16.77554405305477658, 9.453903742431199575 ) ) ;
#32201=CARTESIAN_POINT ( 'NONE',  ( 0.1129192098497447394, -40.71518461128108157, 17.00663193740767909 ) ) ;
#32218=CARTESIAN_POINT ( 'NONE',  ( 4.975610109902397937, 30.04451009524531102, -38.59762713269398660 ) ) ;
#32221=ORIENTED_EDGE ( 'NONE', *, *, #35236, .T. ) ;
#32224=CARTESIAN_POINT ( 'NONE',  ( 3.221118495291109163, 28.14629310243162763, -33.80159174142189471 ) ) ;
#32230=ADVANCED_FACE ( 'NONE', ( #16628 ), #6635, .F. ) ;
#32242=ORIENTED_EDGE ( 'NONE', *, *, #49831, .F. ) ;
#32247=ORIENTED_EDGE ( 'NONE', *, *, #46654, .F. ) ;
#32249=CARTESIAN_POINT ( 'NONE',  ( 0.6016118706126978299, -42.61631147553848820, -24.40084119459445589 ) ) ;
#32258=CARTESIAN_POINT ( 'NONE',  ( 0.5997462898726536595, 46.43852004798865352, -15.96920429754923632 ) ) ;
#32259=ORIENTED_EDGE ( 'NONE', *, *, #14524, .F. ) ;
#32272=LINE ( 'NONE', #4035, #28942 ) ;
#32275=ORIENTED_EDGE ( 'NONE', *, *, #58020, .T. ) ;
#32277=CARTESIAN_POINT ( 'NONE',  ( 2.648799415243696664, 46.95584109391764827, -14.13033794544045030 ) ) ;
#32279=B_SPLINE_CURVE_WITH_KNOTS ( 'NONE', 3,
 ( #48504, #5568, #24708, #43847, #890, #37133 ),
 .UNSPECIFIED., .F., .F.,
 ( 4, 2, 4 ),
 ( 0.000000000000000000, 0.0002447195606305758845, 0.0004894391212611517690 ),
 .UNSPECIFIED. ) ;
#32282=CARTESIAN_POINT ( 'NONE',  ( -6.078075953587585900, 0.6224930363967494662, 19.24597819459363279 ) ) ;
#32284=EDGE_CURVE ( 'NONE', #8036, #54532, #24365, .T. ) ;
#32285=LINE ( 'NONE', #3139, #28121 ) ;
#32290=CARTESIAN_POINT ( 'NONE',  ( 2.185380717157383579, 23.99818600003833780, -36.91756860594645673 ) ) ;
#32294=CARTESIAN_POINT ( 'NONE',  ( -6.078075953587585900, 5.483964907265516331, -18.45863762965772636 ) ) ;
#32296=B_SPLINE_CURVE_WITH_KNOTS ( 'NONE', 3,
 ( #2282, #21411, #40248, #39306 ),
 .UNSPECIFIED., .F., .F.,
 ( 4, 4 ),
 ( 2.380113941701692686E-17, 0.004559932413162186803 ),
 .UNSPECIFIED. ) ;
#32297=( BOUNDED_SURFACE ( )  B_SPLINE_SURFACE ( 3, 1, ( 
 ( #16971, #21650 ),
 ( #36083, #7525 ),
 ( #55145, #12272 ),
 ( #31359, #58811 ) ),
 .UNSPECIFIED., .F., .F., .F. ) 
 B_SPLINE_SURFACE_WITH_KNOTS ( ( 4, 4 ),
 ( 2, 2 ),
 ( 0.000000000000000000, 1.000000000000000000 ),
 ( 0.000000000000000000, 1.000000000000000000 ),
 .UNSPECIFIED. ) 
 GEOMETRIC_REPRESENTATION_ITEM ( )  RATIONAL_B_SPLINE_SURFACE ( (
 ( 1.000000000000000000, 1.000000000000000000),
 ( 0.9754377213608244057, 0.9999580625633939235),
 ( 0.9754377213608244057, 0.9999580625633939235),
 ( 1.000000000000000000, 1.000000000000000000) ) ) 
 REPRESENTATION_ITEM ( '' )  SURFACE ( )  );
#32302=VECTOR ( 'NONE', #39801, 1000.000000000000227 ) ;
#32308=ORIENTED_EDGE ( 'NONE', *, *, #21884, .F. ) ;
#32309=CARTESIAN_POINT ( 'NONE',  ( -4.915099999999998914, 0.000000000000000000, 0.000000000000000000 ) ) ;
#32312=B_SPLINE_CURVE_WITH_KNOTS ( 'NONE', 3,
 ( #17664, #21434, #50244, #22359, #54928, #17359 ),
 .UNSPECIFIED., .F., .F.,
 ( 4, 2, 4 ),
 ( 2.196881373128401347E-17, 0.0002293755540694319690, 0.0004587511081388419287 ),
 .UNSPECIFIED. ) ;
#32316=CARTESIAN_POINT ( 'NONE',  ( -6.079354080745853928, -1.847856142170532623, 19.16711723045499483 ) ) ;
#32317=CARTESIAN_POINT ( 'NONE',  ( -6.077587904424778920, -14.65844225831500225, -12.48703695652317158 ) ) ;
#32319=CARTESIAN_POINT ( 'NONE',  ( 0.1129192098497447394, 15.69290830752478882, 41.23935519181615206 ) ) ;
#32321=CARTESIAN_POINT ( 'NONE',  ( 2.879087469061463178, -37.45964864250908022, 23.08411575874515975 ) ) ;
#32323=EDGE_LOOP ( 'NONE', ( #32755, #39742, #15809, #5832 ) ) ;
#32324=CARTESIAN_POINT ( 'NONE',  ( 4.975610109902397937, 0.000000000000000000, 0.000000000000000000 ) ) ;
#32327=ORIENTED_EDGE ( 'NONE', *, *, #21888, .T. ) ;
#32331=CARTESIAN_POINT ( 'NONE',  ( 0.1157991065609915715, -12.63256843914561145, 42.27718746756933399 ) ) ;
#32335=CARTESIAN_POINT ( 'NONE',  ( 5.901764892641307547, -16.95277890151849221, 45.94120976809283263 ) ) ;
#32340=CARTESIAN_POINT ( 'NONE',  ( 4.553261556744875094, -43.82122302957815663, -3.039733214544628748 ) ) ;
#32341=EDGE_CURVE ( 'NONE', #9094, #39332, #318, .T. ) ;
#32348=CARTESIAN_POINT ( 'NONE',  ( -6.078457390727109555, 9.978433202401264523, 16.46892169702449138 ) ) ;
#32349=DIRECTION ( 'NONE',  ( 1.000000000000000000, 0.000000000000000000, 0.000000000000000000 ) ) ;
#32350=CARTESIAN_POINT ( 'NONE',  ( 0.8744876279028263033, 37.95405449045444612, -31.14225101233220627 ) ) ;
#32355=CARTESIAN_POINT ( 'NONE',  ( -6.077587904424778920, 5.484810954822468609, -18.45840919970596516 ) ) ;
#32356=EDGE_CURVE ( 'NONE', #55001, #14065, #17248, .T. ) ;
#32360=CARTESIAN_POINT ( 'NONE',  ( 0.1129192098497455998, -31.35755906439593943, -31.04279751098591689 ) ) ;
#32365=ORIENTED_EDGE ( 'NONE', *, *, #33078, .F. ) ;
#32371=ORIENTED_EDGE ( 'NONE', *, *, #27305, .F. ) ;
#32372=CARTESIAN_POINT ( 'NONE',  ( 1.112077966505210957, -30.92531005629962948, 31.41107325530738947 ) ) ;
#32373=CARTESIAN_POINT ( 'NONE',  ( 4.390527457369401532, 27.14076954505956252, 34.54799509567215665 ) ) ;
#32377=EDGE_LOOP ( 'NONE', ( #61455, #54943, #16593, #8904 ) ) ;
#32389=FACE_OUTER_BOUND ( 'NONE', #30844, .T. ) ;
#32393=VERTEX_POINT ( 'NONE', #55740 ) ;
#32394=ADVANCED_FACE ( 'NONE', ( #17554 ), #35064, .F. ) ;
#32396=B_SPLINE_CURVE_WITH_KNOTS ( 'NONE', 3,
 ( #34036, #47505, #5174, #28081 ),
 .UNSPECIFIED., .F., .F.,
 ( 4, 4 ),
 ( 0.000000000000000000, 0.005013413432710147645 ),
 .UNSPECIFIED. ) ;
#32401=DIRECTION ( 'NONE',  ( 0.000000000000000000, 0.000000000000000000, -1.000000000000000000 ) ) ;
#32403=CARTESIAN_POINT ( 'NONE',  ( 4.553261556744873317, -43.07273893850290136, 8.618510669437750238 ) ) ;
#32410=CARTESIAN_POINT ( 'NONE',  ( 0.2285344041767103096, 30.21943416597249765, 32.14478136469291059 ) ) ;
#32415=CARTESIAN_POINT ( 'NONE',  ( 4.553261556744875094, 7.233533384971297941, -43.32684572631779218 ) ) ;
#32418=AXIS2_PLACEMENT_3D ( 'NONE', #18556, #9450, #57352 ) ;
#32424=CARTESIAN_POINT ( 'NONE',  ( 0.6000166863083106206, 22.25084548767499015, 43.78039923061538019 ) ) ;
#32431=CARTESIAN_POINT ( 'NONE',  ( 0.1152809850208375564, -35.22899213320485501, -26.56808980277553900 ) ) ;
#32433=EDGE_CURVE ( 'NONE', #27055, #18471, #22349, .T. ) ;
#32434=CARTESIAN_POINT ( 'NONE',  ( 2.185380717157382691, -24.04382478636127018, -36.88786104818167644 ) ) ;
#32442=CARTESIAN_POINT ( 'NONE',  ( 0.1149546198390367507, -7.312467115531964268, 43.51407116907684269 ) ) ;
#32447=CARTESIAN_POINT ( 'NONE',  ( -6.077587904424778920, -6.656176160390709917, 18.06907137391894125 ) ) ;
#32450=EDGE_LOOP ( 'NONE', ( #29378, #25387, #2985, #40668 ) ) ;
#32452=CARTESIAN_POINT ( 'NONE',  ( 4.226256110419178924, 38.08231154255455664, 21.92178819264073653 ) ) ;
#32454=EDGE_CURVE ( 'NONE', #36974, #21596, #25798, .T. ) ;
#32457=CARTESIAN_POINT ( 'NONE',  ( 0.1156495703730067437, -42.71546320847479450, -11.06038679778003875 ) ) ;
#32462=EDGE_CURVE ( 'NONE', #8721, #7194, #51979, .T. ) ;
#32468=CARTESIAN_POINT ( 'NONE',  ( -6.078726893082806448, 16.77644806189623239, -9.452239506869167585 ) ) ;
#32470=CARTESIAN_POINT ( 'NONE',  ( 0.2279481005628813950, -34.89833595118959408, -26.99277004886345210 ) ) ;
#32475=CARTESIAN_POINT ( 'NONE',  ( 0.08486401232817714080, 0.000000000000000000, 0.000000000000000000 ) ) ;
#32476=LINE ( 'NONE', #32795, #39190 ) ;
#32481=CARTESIAN_POINT ( 'NONE',  ( 0.5549461598389365813, 43.45051165307260277, 7.567742896862155177 ) ) ;
#32488=CARTESIAN_POINT ( 'NONE',  ( -6.079354080745853928, -4.283721817891463779, 18.77345686428268934 ) ) ;
#32491=ORIENTED_EDGE ( 'NONE', *, *, #7190, .F. ) ;
#32492=CARTESIAN_POINT ( 'NONE',  ( 0.3676999524040366896, 24.55639947021014180, -36.64606156713571750 ) ) ;
#32494=CARTESIAN_POINT ( 'NONE',  ( 50.15577769773999961, 0.000000000000000000, 10.00000000000000000 ) ) ;
#32501=CARTESIAN_POINT ( 'NONE',  ( -6.079354080745853928, 5.479977851902325447, -18.45976159084461088 ) ) ;
#32508=EDGE_CURVE ( 'NONE', #2406, #29558, #26578, .T. ) ;
#32512=B_SPLINE_CURVE_WITH_KNOTS ( 'NONE', 3,
 ( #1406, #25851, #54644, #40298, #16455, #29620 ),
 .UNSPECIFIED., .F., .F.,
 ( 4, 2, 4 ),
 ( 2.197015137584159369E-17, 0.0002293755540694313998, 0.0004587511081388407903 ),
 .UNSPECIFIED. ) ;
#32520=AXIS2_PLACEMENT_3D ( 'NONE', #17272, #31362, #45478 ) ;
#32522=CARTESIAN_POINT ( 'NONE',  ( 0.6028777368367060907, -1.486945628974875477, -49.08491440358785241 ) ) ;
#32523=CARTESIAN_POINT ( 'NONE',  ( 0.3676999524040366896, 16.00695768809390884, 41.10629986868691077 ) ) ;
#32527=CARTESIAN_POINT ( 'NONE',  ( 2.185380717157383579, 32.57763254378428996, -29.62292458400025197 ) ) ;
#32531=CARTESIAN_POINT ( 'NONE',  ( 1.112077966505211624, 28.84925631676179236, -33.32792725475640339 ) ) ;
#32534=ADVANCED_FACE ( 'NONE', ( #58204 ), #36705, .F. ) ;
#32536=B_SPLINE_CURVE_WITH_KNOTS ( 'NONE', 3,
 ( #39715, #58766, #54069, #11190 ),
 .UNSPECIFIED., .F., .F.,
 ( 4, 4 ),
 ( 2.308109569601360422E-17, 0.004559932413162187670 ),
 .UNSPECIFIED. ) ;
#32537=EDGE_CURVE ( 'NONE', #19087, #52200, #4143, .T. ) ;
#32541=CARTESIAN_POINT ( 'NONE',  ( -6.078457390727109555, -6.646245994447022909, -18.07268450504254176 ) ) ;
#32545=CARTESIAN_POINT ( 'NONE',  ( 4.335381028904201628, -28.85261930641560468, -39.58892783119288339 ) ) ;
#32547=ORIENTED_EDGE ( 'NONE', *, *, #30468, .T. ) ;
#32548=FACE_OUTER_BOUND ( 'NONE', #43895, .T. ) ;
#32553=CARTESIAN_POINT ( 'NONE',  ( 0.5987334363312690755, -43.08218153649183790, 23.56880439328305243 ) ) ;
#32560=ORIENTED_EDGE ( 'NONE', *, *, #45215, .T. ) ;
#32578=CARTESIAN_POINT ( 'NONE',  ( 2.533389852662419894, -34.30621192938689745, 27.57778734397685483 ) ) ;
#32581=LINE ( 'NONE', #8752, #34931 ) ;
#32583=CARTESIAN_POINT ( 'NONE',  ( 3.050102900204245682, 42.79960004823801967, -10.17936564275614053 ) ) ;
#32584=CARTESIAN_POINT ( 'NONE',  ( 2.706805983486679779, -39.13097409860326081, -20.13809771091093381 ) ) ;
#32585=CARTESIAN_POINT ( 'NONE',  ( 1.834102595619085285, -41.29959790234792649, -15.31473009759111825 ) ) ;
#32595=DIRECTION ( 'NONE',  ( 0.000000000000000000, 0.000000000000000000, -1.000000000000000000 ) ) ;
#32602=DIRECTION ( 'NONE',  ( -0.1011922191286467321, -0.6783146913069645345, 0.7277700971769569538 ) ) ;
#32604=ORIENTED_EDGE ( 'NONE', *, *, #55780, .F. ) ;
#32611=CARTESIAN_POINT ( 'NONE',  ( 4.553261556744873317, 31.71129487083125653, 30.39627186743183174 ) ) ;
#32612=EDGE_CURVE ( 'NONE', #60714, #47165, #22811, .T. ) ;
#32621=CARTESIAN_POINT ( 'NONE',  ( -6.078726893082806448, 5.475592473157615991, -18.46109228449443052 ) ) ;
#32624=VERTEX_POINT ( 'NONE', #16243 ) ;
#32634=EDGE_LOOP ( 'NONE', ( #1262, #12938, #9926, #33010 ) ) ;
#32638=VERTEX_POINT ( 'NONE', #16873 ) ;
#32646=CARTESIAN_POINT ( 'NONE',  ( 0.6026777506516367566, 28.23790448320244550, 40.17669898130948525 ) ) ;
#32650=DIRECTION ( 'NONE',  ( -1.000000000000000000, 0.000000000000000000, -0.000000000000000000 ) ) ;
#32658=FACE_OUTER_BOUND ( 'NONE', #12822, .T. ) ;
#32662=CARTESIAN_POINT ( 'NONE',  ( 0.2279481005628849200, -41.17370996425396612, 15.85020803814284385 ) ) ;
#32676=DIRECTION ( 'NONE',  ( 0.000000000000000000, 0.000000000000000000, -1.000000000000000000 ) ) ;
#32682=CARTESIAN_POINT ( 'NONE',  ( 0.3676999524040366896, 14.45783756353458216, -41.67639039443420756 ) ) ;
#32689=CARTESIAN_POINT ( 'NONE',  ( 4.975610109902397937, 14.46773809681547718, 46.72401910687614190 ) ) ;
#32694=EDGE_CURVE ( 'NONE', #8818, #14042, #29450, .T. ) ;
#32699=CARTESIAN_POINT ( 'NONE',  ( 4.975610109902397937, -32.45573888811600227, -36.59336579715246529 ) ) ;
#32705=VERTEX_POINT ( 'NONE', #45084 ) ;
#32706=CARTESIAN_POINT ( 'NONE',  ( 0.6039202388192952409, 41.06127625758627886, 26.93576256479796882 ) ) ;
#32716=CARTESIAN_POINT ( 'NONE',  ( 5.901764892641288895, -48.05798712428990882, 9.403262253136601245 ) ) ;
#32719=CARTESIAN_POINT ( 'NONE',  ( 0.8753041380234465318, -29.91468680897799359, -38.93905290314259560 ) ) ;
#32720=CARTESIAN_POINT ( 'NONE',  ( 0.1368894036331277653, 30.13294619814276132, 32.23145791525983839 ) ) ;
#32722=CARTESIAN_POINT ( 'NONE',  ( 0.6000166863083090663, -34.91285637184651591, -34.53861522509652815 ) ) ;
#32729=CARTESIAN_POINT ( 'NONE',  ( 0.6027444965799114707, 32.91815440601231302, 36.44082362391626617 ) ) ;
#32730=CARTESIAN_POINT ( 'NONE',  ( 4.553261556744875094, 0.000000000000000000, 0.000000000000000000 ) ) ;
#32732=CARTESIAN_POINT ( 'NONE',  ( 0.6029443199889047422, -42.78819218835079852, 24.09788893465896464 ) ) ;
#32737=CARTESIAN_POINT ( 'NONE',  ( 0.3676999524040366896, -22.15802448780013378, 38.14410221935873579 ) ) ;
#32744=CARTESIAN_POINT ( 'NONE',  ( 0.1154773475650540393, -35.46900651670787141, -26.24677516884419504 ) ) ;
#32746=CARTESIAN_POINT ( 'NONE',  ( 3.221118495291109163, -24.39610253492621084, -36.60043170192283668 ) ) ;
#32755=ORIENTED_EDGE ( 'NONE', *, *, #18052, .T. ) ;
#32757=ORIENTED_EDGE ( 'NONE', *, *, #3438, .T. ) ;
#32759=CARTESIAN_POINT ( 'NONE',  ( -6.078726893082806448, 3.076629396955338436, -19.00863995194055178 ) ) ;
#32762=CARTESIAN_POINT ( 'NONE',  ( 0.6026777506516368677, 10.75755792781037812, -47.91472986532454570 ) ) ;
#32769=ADVANCED_FACE ( 'NONE', ( #27179 ), #49482, .F. ) ;
#32778=CARTESIAN_POINT ( 'NONE',  ( 0.1139756605157203340, 33.85464405449629055, 28.29873311013023951 ) ) ;
#32787=CARTESIAN_POINT ( 'NONE',  ( -6.078726893082806448, -17.34758611459996303, -8.357948149232475643 ) ) ;
#32788=CARTESIAN_POINT ( 'NONE',  ( 0.5997462898726536595, -49.10477184366966696, -0.5225058138009923692 ) ) ;
#32795=CARTESIAN_POINT ( 'NONE',  ( -2.739355103387247858, 1.171460933655153136, 14.88204442379933390 ) ) ;
#32801=CARTESIAN_POINT ( 'NONE',  ( 2.359973842542475886, 43.47549606496694707, 6.929439842984741915 ) ) ;
#32802=CARTESIAN_POINT ( 'NONE',  ( 0.6021447746440204973, -25.23315518945873137, 42.12871963724009561 ) ) ;
#32803=B_SPLINE_CURVE_WITH_KNOTS ( 'NONE', 3,
 ( #24161, #14783, #52973, #29171 ),
 .UNSPECIFIED., .F., .F.,
 ( 4, 4 ),
 ( 0.000000000000000000, 0.002320612883253031153 ),
 .UNSPECIFIED. ) ;
#32804=CARTESIAN_POINT ( 'NONE',  ( 0.1156867017252034696, 37.04796616592829395, -23.96645593831968313 ) ) ;
#32805=ORIENTED_EDGE ( 'NONE', *, *, #23975, .F. ) ;
#32807=CARTESIAN_POINT ( 'NONE',  ( 0.6000166863083106206, 10.41802958826996495, -47.99258423138293495 ) ) ;
#32812=CARTESIAN_POINT ( 'NONE',  ( 0.1152339509894530906, 33.45292367112824650, -28.77228854833953164 ) ) ;
#32815=CARTESIAN_POINT ( 'NONE',  ( 0.1365634738349432442, -38.75391421075912746, 21.09494614755793407 ) ) ;
#32816=ORIENTED_EDGE ( 'NONE', *, *, #57839, .T. ) ;
#32820=EDGE_LOOP ( 'NONE', ( #46806, #31713, #22165, #12894 ) ) ;
#32826=B_SPLINE_CURVE_WITH_KNOTS ( 'NONE', 3,
 ( #33430, #5797, #10226, #38754, #48431, #23707 ),
 .UNSPECIFIED., .F., .F.,
 ( 4, 2, 4 ),
 ( 1.910689091754275557E-17, 0.0002293755540694318064, 0.0004587511081388444766 ),
 .UNSPECIFIED. ) ;
#32830=ADVANCED_FACE ( 'NONE', ( #8673 ), #17855, .F. ) ;
#32832=FACE_OUTER_BOUND ( 'NONE', #29536, .T. ) ;
#32833=CARTESIAN_POINT ( 'NONE',  ( -6.078726893082806448, 12.00859800336359129, -15.05282748397562820 ) ) ;
#32834=CARTESIAN_POINT ( 'NONE',  ( 4.553261556744875094, 0.000000000000000000, 0.000000000000000000 ) ) ;
#32836=EDGE_CURVE ( 'NONE', #9438, #31616, #251, .T. ) ;
#32838=CARTESIAN_POINT ( 'NONE',  ( 4.975610109902397937, 45.55079628452135410, -17.82061629079668919 ) ) ;
#32840=VECTOR ( 'NONE', #24981, 1000.000000000000114 ) ;
#32842=LINE ( 'NONE', #24037, #24794 ) ;
#32848=ADVANCED_FACE ( 'NONE', ( #29329 ), #9325, .F. ) ;
#32849=CARTESIAN_POINT ( 'NONE',  ( 4.553261556744873317, 42.54662847375970358, 10.92355122382355148 ) ) ;
#32872=LINE ( 'NONE', #51948, #2155 ) ;
#32879=VECTOR ( 'NONE', #56560, 1000.000000000000114 ) ;
#32882=CARTESIAN_POINT ( 'NONE',  ( 0.5549461598389366923, -28.17959065316841816, -33.92828268696586491 ) ) ;
#32886=CARTESIAN_POINT ( 'NONE',  ( 3.559346040607745287, 0.6451424477637347499, 43.96605591549100467 ) ) ;
#32888=B_SPLINE_CURVE_WITH_KNOTS ( 'NONE', 3,
 ( #44564, #1290, #6589, #39872, #20423, #30118, #39552, #58928, #58606, #15736, #53911, #11034, #12587, #47024, #7860, #51376, #12279, #12896, #7535 ),
 .UNSPECIFIED., .F., .F.,
 ( 4, 3, 3, 3, 3, 3, 4 ),
 ( 8.674676106452504675E-19, 0.0002612768053151718175, 0.0003919133833142909255, 0.0005225499612322609703, 0.0006531865391693360669, 0.0008112755173415194237, 0.0009693688056799724647 ),
 .UNSPECIFIED. ) ;
#32901=SHAPE_REPRESENTATION_RELATIONSHIP ( 'NONE' , 'NONE' ,  #2385, #48247 ) ;
#32907=CARTESIAN_POINT ( 'NONE',  ( 4.553261556744875094, -4.442710778082547662, 43.70128015019636791 ) ) ;
#32909=EDGE_CURVE ( 'NONE', #23299, #60472, #39918, .T. ) ;
#32913=CARTESIAN_POINT ( 'NONE',  ( 3.678748215320120085, -48.77537477639203445, -4.424435525802461910 ) ) ;
#32915=CARTESIAN_POINT ( 'NONE',  ( 4.335381028904201628, 31.32980982056168884, 37.65899446708290554 ) ) ;
#32919=CARTESIAN_POINT ( 'NONE',  ( 0.8753041380234471980, -49.09527960836077654, -0.8898584437169385630 ) ) ;
#32920=CARTESIAN_POINT ( 'NONE',  ( 0.2279481005628799517, 44.07067687752851981, -2.068556653656985045 ) ) ;
#32921=CARTESIAN_POINT ( 'NONE',  ( -2.739355103387248747, -12.11899594566302518, -8.716507570123491533 ) ) ;
#32927=CARTESIAN_POINT ( 'NONE',  ( 0.1158403557922069033, 4.274622882211749797, -43.91660171733112605 ) ) ;
#32937=ORIENTED_EDGE ( 'NONE', *, *, #28577, .F. ) ;
#32942=ADVANCED_FACE ( 'NONE', ( #30868 ), #37440, .F. ) ;
#32946=ORIENTED_EDGE ( 'NONE', *, *, #55214, .T. ) ;
#32949=CARTESIAN_POINT ( 'NONE',  ( 0.6000166863083106206, 37.05402083933937973, 32.23077754796269545 ) ) ;
#32951=CARTESIAN_POINT ( 'NONE',  ( 0.1154773475650540671, -23.02726780139724383, -37.63892357186712445 ) ) ;
#32952=ORIENTED_EDGE ( 'NONE', *, *, #28353, .T. ) ;
#32955=ORIENTED_EDGE ( 'NONE', *, *, #58254, .T. ) ;
#32960=CARTESIAN_POINT ( 'NONE',  ( 0.6029443199889047422, 46.60566125691656225, -15.47417140463258356 ) ) ;
#32980=EDGE_CURVE ( 'NONE', #29362, #8504, #26454, .T. ) ;
#32985=CARTESIAN_POINT ( 'NONE',  ( 4.553261556744875094, 31.71129487083167220, -30.39627186743139831 ) ) ;
#33006=CONICAL_SURFACE ( 'NONE', #47982, 43.92652462719577500, 1.486293639869522343 ) ;
#33008=CARTESIAN_POINT ( 'NONE',  ( -2.739355103387248747, 8.754959582419377995, 12.09124681996112649 ) ) ;
#33010=ORIENTED_EDGE ( 'NONE', *, *, #9858, .F. ) ;
#33011=FACE_OUTER_BOUND ( 'NONE', #35936, .T. ) ;
#33022=VERTEX_POINT ( 'NONE', #5805 ) ;
#33035=VERTEX_POINT ( 'NONE', #49362 ) ;
#33038=CARTESIAN_POINT ( 'NONE',  ( 0.5997462898726536595, -25.00873172704203640, -42.26245340191634625 ) ) ;
#33040=B_SPLINE_CURVE_WITH_KNOTS ( 'NONE', 3,
 ( #9819, #5700, #14537, #34254 ),
 .UNSPECIFIED., .F., .F.,
 ( 4, 4 ),
 ( 0.000000000000000000, 0.004444103432399266161 ),
 .UNSPECIFIED. ) ;
#33042=CARTESIAN_POINT ( 'NONE',  ( 0.8744876279028306332, -47.25615711918273121, 13.31186180466906954 ) ) ;
#33045=CARTESIAN_POINT ( 'NONE',  ( 4.335381028904201628, -43.68634339260519539, 22.16439145674265276 ) ) ;
#33047=CARTESIAN_POINT ( 'NONE',  ( 1.830465331921977246, -38.97216206803106076, 20.53160099995884380 ) ) ;
#33049=CARTESIAN_POINT ( 'NONE',  ( -6.063463321072276813, -14.65282214633766422, 12.49460906260241444 ) ) ;
#33050=CARTESIAN_POINT ( 'NONE',  ( 0.6039202388192952409, 22.55960655125555903, 43.61912269981525014 ) ) ;
#33054=( BOUNDED_SURFACE ( )  B_SPLINE_SURFACE ( 3, 1, ( 
 ( #40048, #59098 ),
 ( #6768, #45650 ),
 ( #37181, #42199 ),
 ( #3617, #7713 ) ),
 .UNSPECIFIED., .F., .F., .F. ) 
 B_SPLINE_SURFACE_WITH_KNOTS ( ( 4, 4 ),
 ( 2, 2 ),
 ( 0.000000000000000000, 1.000000000000000000 ),
 ( 0.000000000000000000, 1.000000000000000000 ),
 .UNSPECIFIED. ) 
 GEOMETRIC_REPRESENTATION_ITEM ( )  RATIONAL_B_SPLINE_SURFACE ( (
 ( 1.000000000000000000, 1.000000000000000000),
 ( 0.9754377213608244057, 0.9999580625633939235),
 ( 0.9754377213608244057, 0.9999580625633939235),
 ( 1.000000000000000000, 1.000000000000000000) ) ) 
 REPRESENTATION_ITEM ( '' )  SURFACE ( )  );
#33060=CARTESIAN_POINT ( 'NONE',  ( -6.078726893082806448, 0.6137717894417996645, 19.24622886331775717 ) ) ;
#33061=CARTESIAN_POINT ( 'NONE',  ( 0.1135584504625008345, -35.10173505342547884, -26.73612253813879036 ) ) ;
#33062=CARTESIAN_POINT ( 'NONE',  ( 0.6029442701453591180, -39.40744528971698202, -29.30185115135630269 ) ) ;
#33063=CARTESIAN_POINT ( 'NONE',  ( 1.112077966505211624, -23.74200319157113981, -37.13956932410471978 ) ) ;
#33065=B_SPLINE_CURVE_WITH_KNOTS ( 'NONE', 3,
 ( #4985, #10964, #19136, #47625 ),
 .UNSPECIFIED., .F., .F.,
 ( 4, 4 ),
 ( 2.170598744017606518E-17, 0.001844835322069226938 ),
 .UNSPECIFIED. ) ;
#33076=CARTESIAN_POINT ( 'NONE',  ( 0.5980271706414734822, -7.146479349118088464, 48.58988655835998571 ) ) ;
#33078=EDGE_CURVE ( 'NONE', #12519, #2779, #16045, .T. ) ;
#33081=CARTESIAN_POINT ( 'NONE',  ( -2.739355103387247858, -0.7412303453949566912, 14.90966614401820323 ) ) ;
#33086=CARTESIAN_POINT ( 'NONE',  ( 4.390527457369402420, -39.72119411615135931, 18.77264165256562833 ) ) ;
#33088=CARTESIAN_POINT ( 'NONE',  ( 0.7948878604505666967, -47.70571118704327063, -11.61308604277228262 ) ) ;
#33089=CARTESIAN_POINT ( 'NONE',  ( 0.7242003506640013466, 48.03330260386865547, -10.18889174990159319 ) ) ;
#33090=ADVANCED_FACE ( 'NONE', ( #23034 ), #3363, .F. ) ;
#33092=ORIENTED_EDGE ( 'NONE', *, *, #47739, .F. ) ;
#33095=CARTESIAN_POINT ( 'NONE',  ( 4.553261556744875094, 43.92594400279101308, 0.2258523573163287723 ) ) ;
#33096=ORIENTED_EDGE ( 'NONE', *, *, #52825, .F. ) ;
#33103=CARTESIAN_POINT ( 'NONE',  ( 0.1135584504625008068, -44.12216505757947260, -0.4319754240288274927 ) ) ;
#33104=CARTESIAN_POINT ( 'NONE',  ( -6.077587904424778920, 18.62786028128793347, 4.878405757493543327 ) ) ;
#33110=CARTESIAN_POINT ( 'NONE',  ( 0.3676999524040366896, 43.44964275340416293, 7.620966337964807380 ) ) ;
#33112=B_SPLINE_CURVE_WITH_KNOTS ( 'NONE', 3,
 ( #50514, #60830, #12030, #61133 ),
 .UNSPECIFIED., .F., .F.,
 ( 4, 4 ),
 ( 0.000000000000000000, 0.004444103432399266161 ),
 .UNSPECIFIED. ) ;
#33113=ORIENTED_EDGE ( 'NONE', *, *, #24112, .F. ) ;
#33119=B_SPLINE_CURVE_WITH_KNOTS ( 'NONE', 3,
 ( #16723, #46170, #54911, #26113, #3216, #40866, #21726, #30487, #40251, #7604, #35533, #12046, #50531, #45868, #2913, #7930 ),
 .UNSPECIFIED., .F., .F.,
 ( 4, 3, 3, 3, 3, 4 ),
 ( 2.194378057379452319E-17, 0.0002612764279487740844, 0.0003919131003184766972, 0.0005225497727000625453, 0.0007837925190632439448, 0.001045051706266715433 ),
 .UNSPECIFIED. ) ;
#33140=CARTESIAN_POINT ( 'NONE',  ( 3.240649175237395152, -3.235903588307554646, 43.87247252395092545 ) ) ;
#33142=VERTEX_POINT ( 'NONE', #32123 ) ;
#33146=CARTESIAN_POINT ( 'NONE',  ( -6.063463321072278589, 3.088760411028451003, -19.00736729804350134 ) ) ;
#33147=CARTESIAN_POINT ( 'NONE',  ( 0.5997462898726536595, -35.63787911784747564, -33.78599121124021565 ) ) ;
#33148=CARTESIAN_POINT ( 'NONE',  ( 4.390527457369401532, 31.78221389532359709, -30.33275814265031656 ) ) ;
#33152=CARTESIAN_POINT ( 'NONE',  ( -6.072942160501519027, 0.6026766405721472042, 19.24684242040572002 ) ) ;
#33153=ORIENTED_EDGE ( 'NONE', *, *, #43822, .F. ) ;
#33160=CARTESIAN_POINT ( 'NONE',  ( 3.221118495291109163, -25.92278810600130612, 35.53548193669403332 ) ) ;
#33161=ORIENTED_EDGE ( 'NONE', *, *, #18089, .F. ) ;
#33162=CARTESIAN_POINT ( 'NONE',  ( 0.2285344041767058687, 42.10476663782116447, 13.17914248614367168 ) ) ;
#33164=B_SPLINE_CURVE_WITH_KNOTS ( 'NONE', 3,
 ( #19342, #38458, #14649, #47232 ),
 .UNSPECIFIED., .F., .F.,
 ( 4, 4 ),
 ( 0.000000000000000000, 0.005013413432710139839 ),
 .UNSPECIFIED. ) ;
#33166=CARTESIAN_POINT ( 'NONE',  ( 4.975610109902397937, 0.000000000000000000, 0.000000000000000000 ) ) ;
#33169=CARTESIAN_POINT ( 'NONE',  ( 0.5997462898726536595, -43.04230894295751852, 23.64130434225888777 ) ) ;
#33184=CARTESIAN_POINT ( 'NONE',  ( 1.479689385636123067, -28.38236120443074029, -33.70497615677716396 ) ) ;
#33186=CARTESIAN_POINT ( 'NONE',  ( -6.078726893082806448, -1.852420388636693227, 19.16670498475111373 ) ) ;
#33188=CARTESIAN_POINT ( 'NONE',  ( 0.1139756605157203756, -38.24967839416645177, 21.99812088424507195 ) ) ;
#33190=AXIS2_PLACEMENT_3D ( 'NONE', #60962, #27153, #13376 ) ;
#33200=ORIENTED_EDGE ( 'NONE', *, *, #21284, .F. ) ;
#33204=B_SPLINE_CURVE_WITH_KNOTS ( 'NONE', 3,
 ( #33702, #13985, #58084, #15203, #34311, #52777 ),
 .UNSPECIFIED., .F., .F.,
 ( 4, 2, 4 ),
 ( 6.345130535746553974E-19, 0.0002293801035737092365, 0.0004587602071474178767 ),
 .UNSPECIFIED. ) ;
#33205=LINE ( 'NONE', #51663, #4980 ) ;
#33206=CARTESIAN_POINT ( 'NONE',  ( 0.8744876279028263033, -2.462621419133342204, 49.03351451941333750 ) ) ;
#33211=CARTESIAN_POINT ( 'NONE',  ( 2.648799415243696664, 48.82680556394801386, 4.523330820315231371 ) ) ;
#33221=ORIENTED_EDGE ( 'NONE', *, *, #14948, .T. ) ;
#33224=CARTESIAN_POINT ( 'NONE',  ( 4.390527457369401532, 23.04872909145247561, -37.40242537453222127 ) ) ;
#33225=CARTESIAN_POINT ( 'NONE',  ( 4.834790513006555379, -44.98626621068886067, -14.45078521553118733 ) ) ;
#33231=DIRECTION ( 'NONE',  ( -1.000000000000000000, -0.000000000000000000, -0.000000000000000000 ) ) ;
#33237=CARTESIAN_POINT ( 'NONE',  ( -6.078075953587585900, 17.84675544569229899, 7.231078364171431794 ) ) ;
#33239=FACE_OUTER_BOUND ( 'NONE', #7866, .T. ) ;
#33248=ORIENTED_EDGE ( 'NONE', *, *, #51418, .T. ) ;
#33254=EDGE_CURVE ( 'NONE', #17733, #59505, #52635, .T. ) ;
#33261=EDGE_LOOP ( 'NONE', ( #55174, #28758, #46579, #40654 ) ) ;
#33262=ADVANCED_FACE ( 'NONE', ( #33980 ), #17483, .F. ) ;
#33263=CARTESIAN_POINT ( 'NONE',  ( 0.1157991065609915993, -17.93514196423987528, 40.31467534608533754 ) ) ;
#33264=ORIENTED_EDGE ( 'NONE', *, *, #7861, .F. ) ;
#33268=EDGE_CURVE ( 'NONE', #31990, #17395, #13955, .T. ) ;
#33272=CARTESIAN_POINT ( 'NONE',  ( -6.077587904424778920, -12.94128980615176872, -14.25899854643104803 ) ) ;
#33273=CARTESIAN_POINT ( 'NONE',  ( 0.2285344041767088386, -0.6544525949336760240, 44.11431584073858403 ) ) ;
#33275=EDGE_CURVE ( 'NONE', #10036, #41130, #57713, .T. ) ;
#33277=CARTESIAN_POINT ( 'NONE',  ( 4.694002226626921015, -45.47116547585233803, -3.264641130934661017 ) ) ;
#33282=CARTESIAN_POINT ( 'NONE',  ( -6.077587904424778920, 9.976910903712887801, 16.46988980574263906 ) ) ;
#33283=CARTESIAN_POINT ( 'NONE',  ( 0.6000166863083106206, -39.04292238714129581, -29.79049669240368203 ) ) ;
#33289=EDGE_CURVE ( 'NONE', #44428, #26819, #38353, .T. ) ;
#33292=CARTESIAN_POINT ( 'NONE',  ( -2.601141883200662974, 14.91765895884288362, 0.5088011959923715022 ) ) ;
#33296=B_SPLINE_CURVE_WITH_KNOTS ( 'NONE', 3,
 ( #13039, #49679, #30878, #59689, #54981, #31190 ),
 .UNSPECIFIED., .F., .F.,
 ( 4, 2, 4 ),
 ( 0.000000000000000000, 0.0002447195606305758303, 0.0004894391212611516606 ),
 .UNSPECIFIED. ) ;
#33298=CARTESIAN_POINT ( 'NONE',  ( 0.1152339509894530906, 37.10134772748614296, 23.88373269108917896 ) ) ;
#33300=CARTESIAN_POINT ( 'NONE',  ( 0.6029442701453591180, -39.30324803684850110, 29.44146597763503337 ) ) ;
#33305=CARTESIAN_POINT ( 'NONE',  ( -6.077587904424778920, 15.42837212129427193, -11.52221137980032495 ) ) ;
#33310=ORIENTED_EDGE ( 'NONE', *, *, #10654, .F. ) ;
#33316=EDGE_CURVE ( 'NONE', #20594, #40325, #42446, .T. ) ;
#33318=LINE ( 'NONE', #4449, #22578 ) ;
#33319=CARTESIAN_POINT ( 'NONE',  ( 2.648799415243696664, 21.44335952302192183, 44.09875049994073493 ) ) ;
#33320=B_SPLINE_CURVE_WITH_KNOTS ( 'NONE', 3,
 ( #4031, #18171, #13169, #51042 ),
 .UNSPECIFIED., .F., .F.,
 ( 4, 4 ),
 ( 0.000000000000000000, 0.005013413432710144176 ),
 .UNSPECIFIED. ) ;
#33322=CARTESIAN_POINT ( 'NONE',  ( -6.079354080745853928, 17.84913307564918128, 7.225053888790617052 ) ) ;
#33326=LINE ( 'NONE', #44898, #22982 ) ;
#33330=( BOUNDED_SURFACE ( )  B_SPLINE_SURFACE ( 3, 1, ( 
 ( #28182, #14114 ),
 ( #42613, #23482 ),
 ( #47610, #42929 ),
 ( #49960, #9692 ) ),
 .UNSPECIFIED., .F., .F., .F. ) 
 B_SPLINE_SURFACE_WITH_KNOTS ( ( 4, 4 ),
 ( 2, 2 ),
 ( 0.000000000000000000, 1.000000000000000000 ),
 ( 0.000000000000000000, 1.000000000000000000 ),
 .UNSPECIFIED. ) 
 GEOMETRIC_REPRESENTATION_ITEM ( )  RATIONAL_B_SPLINE_SURFACE ( (
 ( 1.000000000000000000, 1.000000000000000000),
 ( 0.9754377213608244057, 0.9999580625633939235),
 ( 0.9754377213608244057, 0.9999580625633939235),
 ( 1.000000000000000000, 1.000000000000000000) ) ) 
 REPRESENTATION_ITEM ( '' )  SURFACE ( )  );
#33333=CARTESIAN_POINT ( 'NONE',  ( 0.5549461598389366923, 34.14561923851002234, 27.91584464574730973 ) ) ;
#33335=CARTESIAN_POINT ( 'NONE',  ( 0.1129192098497455998, -31.35755906439593943, -31.04279751098591689 ) ) ;
#33338=( BOUNDED_SURFACE ( )  B_SPLINE_SURFACE ( 3, 1, ( 
 ( #17375, #3249 ),
 ( #60885, #7966 ),
 ( #37121, #7640 ),
 ( #41819, #32716 ) ),
 .UNSPECIFIED., .F., .F., .F. ) 
 B_SPLINE_SURFACE_WITH_KNOTS ( ( 4, 4 ),
 ( 2, 2 ),
 ( 0.000000000000000000, 1.000000000000000000 ),
 ( 0.000000000000000000, 1.000000000000000000 ),
 .UNSPECIFIED. ) 
 GEOMETRIC_REPRESENTATION_ITEM ( )  RATIONAL_B_SPLINE_SURFACE ( (
 ( 1.000000000000000000, 1.000000000000000000),
 ( 0.7211978278499970862, 0.9934217856018976445),
 ( 0.7211978278499970862, 0.9934217856018976445),
 ( 1.000000000000000000, 1.000000000000000000) ) ) 
 REPRESENTATION_ITEM ( '' )  SURFACE ( )  );
#33349=VERTEX_POINT ( 'NONE', #11391 ) ;
#33350=ORIENTED_EDGE ( 'NONE', *, *, #11463, .F. ) ;
#33351=CARTESIAN_POINT ( 'NONE',  ( 0.2940133293163002537, 19.68859035591863105, 39.47910788473912902 ) ) ;
#33359=CARTESIAN_POINT ( 'NONE',  ( 4.553261556744875094, 42.43205150231973732, 11.36048287389764688 ) ) ;
#33367=CARTESIAN_POINT ( 'NONE',  ( -2.601141883200662974, -10.40580972892359490, 10.70114719807309811 ) ) ;
#33374=DIRECTION ( 'NONE',  ( -1.000000000000000000, -0.000000000000000000, -0.000000000000000000 ) ) ;
#33379=CARTESIAN_POINT ( 'NONE',  ( 4.553261556744875094, -24.94552653848424129, -36.15605442441715667 ) ) ;
#33383=CARTESIAN_POINT ( 'NONE',  ( 4.553261556744875094, 0.000000000000000000, 0.000000000000000000 ) ) ;
#33384=CIRCLE ( 'NONE', #6310, 43.92652462719577500 ) ;
#33387=ORIENTED_EDGE ( 'NONE', *, *, #10654, .T. ) ;
#33395=DIRECTION ( 'NONE',  ( -1.000000000000000000, -0.000000000000000000, -0.000000000000000000 ) ) ;
#33399=CARTESIAN_POINT ( 'NONE',  ( 3.221118495291109163, 43.97607529046792507, 0.9307103248849385446 ) ) ;
#33402=CARTESIAN_POINT ( 'NONE',  ( 0.8753041380234524160, -45.84117188851829638, -17.59901382919792212 ) ) ;
#33407=ORIENTED_EDGE ( 'NONE', *, *, #58285, .T. ) ;
#33412=( BOUNDED_SURFACE ( )  B_SPLINE_SURFACE ( 3, 1, ( 
 ( #40993, #50960 ),
 ( #12462, #17160 ),
 ( #27166, #46291 ),
 ( #55340, #8347 ) ),
 .UNSPECIFIED., .F., .F., .F. ) 
 B_SPLINE_SURFACE_WITH_KNOTS ( ( 4, 4 ),
 ( 2, 2 ),
 ( 0.000000000000000000, 1.000000000000000000 ),
 ( 0.000000000000000000, 1.000000000000000000 ),
 .UNSPECIFIED. ) 
 GEOMETRIC_REPRESENTATION_ITEM ( )  RATIONAL_B_SPLINE_SURFACE ( (
 ( 1.000000000000000000, 1.000000000000000000),
 ( 0.7211978278499968642, 0.9934217856018975334),
 ( 0.7211978278499968642, 0.9934217856018975334),
 ( 1.000000000000000000, 1.000000000000000000) ) ) 
 REPRESENTATION_ITEM ( '' )  SURFACE ( )  );
#33415=ORIENTED_EDGE ( 'NONE', *, *, #43378, .F. ) ;
#33417=CARTESIAN_POINT ( 'NONE',  ( -2.601141883200662974, 0.9866742854875989455, -14.89368662634427132 ) ) ;
#33421=CARTESIAN_POINT ( 'NONE',  ( 0.1156495703730067715, -27.40426530387594894, 34.58249841156435878 ) ) ;
#33430=CARTESIAN_POINT ( 'NONE',  ( 0.1129192098497455998, -7.520259262076605999, 43.47870154933683295 ) ) ;
#33435=ORIENTED_EDGE ( 'NONE', *, *, #56207, .F. ) ;
#33441=CARTESIAN_POINT ( 'NONE',  ( 0.2285344041767091994, -40.60359876977020122, 17.25830053159842947 ) ) ;
#33442=CARTESIAN_POINT ( 'NONE',  ( 0.1119898979215349089, 3.677941539627681333, -43.97083185798182114 ) ) ;
#33454=LINE ( 'NONE', #29048, #33802 ) ;
#33459=CARTESIAN_POINT ( 'NONE',  ( 0.1135584504625007790, 10.23925027504970764, -42.91980668572665536 ) ) ;
#33460=ORIENTED_EDGE ( 'NONE', *, *, #17266, .F. ) ;
#33475=VERTEX_POINT ( 'NONE', #31734 ) ;
#33478=EDGE_CURVE ( 'NONE', #20821, #23099, #54376, .T. ) ;
#33481=ORIENTED_EDGE ( 'NONE', *, *, #55143, .T. ) ;
#33482=CARTESIAN_POINT ( 'NONE',  ( 0.6029442701453591180, -7.923526166500598045, -48.46403778315481503 ) ) ;
#33483=ADVANCED_FACE ( 'NONE', ( #8519 ), #49854, .F. ) ;
#33485=CARTESIAN_POINT ( 'NONE',  ( -6.077587904424778920, 17.84644683124317055, -7.231898567702747194 ) ) ;
#33487=B_SPLINE_CURVE_WITH_KNOTS ( 'NONE', 3,
 ( #41625, #56308, #56620, #3678 ),
 .UNSPECIFIED., .F., .F.,
 ( 4, 4 ),
 ( 2.120273707634171297E-17, 0.004559932413162188537 ),
 .UNSPECIFIED. ) ;
#33490=CARTESIAN_POINT ( 'NONE',  ( 0.1365634738349438548, 25.76331610226886326, -35.82058295223323796 ) ) ;
#33494=CARTESIAN_POINT ( 'NONE',  ( 0.8744876279028263033, 48.01195819035220325, 10.25679877483054625 ) ) ;
#33495=ORIENTED_EDGE ( 'NONE', *, *, #46010, .F. ) ;
#33510=CARTESIAN_POINT ( 'NONE',  ( -6.077587904424778920, 18.62786028128800098, -4.878405757493267103 ) ) ;
#33513=CARTESIAN_POINT ( 'NONE',  ( 4.975610109902397937, 0.000000000000000000, 0.000000000000000000 ) ) ;
#33514=CARTESIAN_POINT ( 'NONE',  ( 0.8744876279028263033, 44.61213666265857825, -20.49651952824592982 ) ) ;
#33515=CARTESIAN_POINT ( 'NONE',  ( 0.7948884756798504370, 37.94263149402783597, -31.16176118111038917 ) ) ;
#33517=ORIENTED_EDGE ( 'NONE', *, *, #54918, .F. ) ;
#33518=CARTESIAN_POINT ( 'NONE',  ( 0.1152339509894530906, 20.21078498592564898, -39.22329487317357888 ) ) ;
#33522=CARTESIAN_POINT ( 'NONE',  ( 4.975610109902397937, 2.142807115709817189, -48.86571174967818365 ) ) ;
#33524=CARTESIAN_POINT ( 'NONE',  ( 4.335381028904201628, -17.86707742387175912, -45.61276566920401621 ) ) ;
#33541=LINE ( 'NONE', #20062, #13072 ) ;
#33542=VECTOR ( 'NONE', #27169, 1000.000000000000114 ) ;
#33547=VECTOR ( 'NONE', #4065, 1000.000000000000000 ) ;
#33549=CARTESIAN_POINT ( 'NONE',  ( 4.975610109902397937, 45.55079628452109830, 17.82061629079735354 ) ) ;
#33553=FACE_OUTER_BOUND ( 'NONE', #59576, .T. ) ;
#33558=CARTESIAN_POINT ( 'NONE',  ( 4.975610109902397937, -37.61482235126130291, -31.26618855282533360 ) ) ;
#33561=ORIENTED_EDGE ( 'NONE', *, *, #61613, .T. ) ;
#33564=CARTESIAN_POINT ( 'NONE',  ( 0.1156867017252034557, -22.76669660009247309, -37.79709424273940499 ) ) ;
#33565=ORIENTED_EDGE ( 'NONE', *, *, #44629, .F. ) ;
#33568=CARTESIAN_POINT ( 'NONE',  ( -6.078726893082806448, -1.845620846545631188, 19.16736092839899186 ) ) ;
#33576=CARTESIAN_POINT ( 'NONE',  ( 0.1147471544378677183, 24.98894974753881115, -36.36625604854348381 ) ) ;
#33580=CARTESIAN_POINT ( 'NONE',  ( 0.1158516988532803521, -40.88093175327997386, 16.60396271425774728 ) ) ;
#33591=EDGE_CURVE ( 'NONE', #1548, #42575, #4378, .T. ) ;
#33595=CARTESIAN_POINT ( 'NONE',  ( 4.975610109902397937, -41.30423662854469313, 26.19941685746003301 ) ) ;
#33597=CARTESIAN_POINT ( 'NONE',  ( 0.9268187852002115479, -22.00118040109542505, 38.20605179637225746 ) ) ;
#33603=B_SPLINE_CURVE_WITH_KNOTS ( 'NONE', 3,
 ( #31737, #25794, #55210, #45540 ),
 .UNSPECIFIED., .F., .F.,
 ( 4, 4 ),
 ( 0.000000000000000000, 0.004444103432399266161 ),
 .UNSPECIFIED. ) ;
#33606=CARTESIAN_POINT ( 'NONE',  ( 0.8744876279028263033, 5.599149760998344050, -48.77498920895221346 ) ) ;
#33610=CARTESIAN_POINT ( 'NONE',  ( 4.060580049360325461, 27.00639131667134052, 34.67163858847787594 ) ) ;
#33611=ORIENTED_EDGE ( 'NONE', *, *, #5955, .T. ) ;
#33616=VERTEX_POINT ( 'NONE', #19189 ) ;
#33620=CARTESIAN_POINT ( 'NONE',  ( -6.079354080745853928, -17.34853647870684057, 8.355910321152332898 ) ) ;
#33628=CARTESIAN_POINT ( 'NONE',  ( 3.678834586032788234, 48.39168880843644160, -7.540346404231043742 ) ) ;
#33629=VERTEX_POINT ( 'NONE', #33905 ) ;
#33631=CARTESIAN_POINT ( 'NONE',  ( 4.975610109902397937, -47.89734868211972696, -9.914302615979444511 ) ) ;
#33634=CARTESIAN_POINT ( 'NONE',  ( 2.533389852662419894, 34.52020495688822166, 27.30944857495383005 ) ) ;
#33638=EDGE_CURVE ( 'NONE', #11233, #33142, #27129, .T. ) ;
#33641=CARTESIAN_POINT ( 'NONE',  ( 0.1147471544378676767, -1.724555973322355662, -44.09056696355949612 ) ) ;
#33643=EDGE_CURVE ( 'NONE', #22365, #34842, #56749, .T. ) ;
#33645=EDGE_LOOP ( 'NONE', ( #41932, #43639, #40752, #9186 ) ) ;
#33647=CARTESIAN_POINT ( 'NONE',  ( 3.678834586032788234, -29.06827489512433615, -39.41633879814102670 ) ) ;
#33648=AXIS2_PLACEMENT_3D ( 'NONE', #11016, #48904, #24480 ) ;
#33656=CARTESIAN_POINT ( 'NONE',  ( 0.1145239942831223490, -17.56161902965139276, -40.47882184256428673 ) ) ;
#33660=FACE_OUTER_BOUND ( 'NONE', #29149, .T. ) ;
#33663=ORIENTED_EDGE ( 'NONE', *, *, #7690, .T. ) ;
#33665=CARTESIAN_POINT ( 'NONE',  ( 0.6029443449137436017, 41.13259312748885321, 26.82628040917691337 ) ) ;
#33674=CARTESIAN_POINT ( 'NONE',  ( 0.6016118706126977189, 48.26733626538113242, -9.045181293293902414 ) ) ;
#33675=CARTESIAN_POINT ( 'NONE',  ( 0.6029443199889047422, -30.61794975149917519, 38.39373379692413124 ) ) ;
#33682=CARTESIAN_POINT ( 'NONE',  ( 2.299652685299201416, -18.66303054524520633, -45.34283863770990308 ) ) ;
#33685=CONICAL_SURFACE ( 'NONE', #42708, 43.92652462719577500, 1.486293639869522343 ) ;
#33688=AXIS2_PLACEMENT_3D ( 'NONE', #53413, #48726, #34640 ) ;
#33698=EDGE_CURVE ( 'NONE', #52962, #37659, #49520, .T. ) ;
#33702=CARTESIAN_POINT ( 'NONE',  ( 0.3676999524040366896, -44.10520818713899871, 0.8253448321555690859 ) ) ;
#33703=( BOUNDED_SURFACE ( )  B_SPLINE_SURFACE ( 3, 1, ( 
 ( #61194, #56801 ),
 ( #3556, #22377 ),
 ( #51797, #46204 ),
 ( #22689, #50875 ) ),
 .UNSPECIFIED., .F., .F., .F. ) 
 B_SPLINE_SURFACE_WITH_KNOTS ( ( 4, 4 ),
 ( 2, 2 ),
 ( 0.000000000000000000, 1.000000000000000000 ),
 ( 0.000000000000000000, 1.000000000000000000 ),
 .UNSPECIFIED. ) 
 GEOMETRIC_REPRESENTATION_ITEM ( )  RATIONAL_B_SPLINE_SURFACE ( (
 ( 1.000000000000000000, 1.000000000000000000),
 ( 0.7211978278499970862, 0.9934217856018976445),
 ( 0.7211978278499970862, 0.9934217856018976445),
 ( 1.000000000000000000, 1.000000000000000000) ) ) 
 REPRESENTATION_ITEM ( '' )  SURFACE ( )  );
#33710=CARTESIAN_POINT ( 'NONE',  ( -6.077587904424778920, 19.09876248768967955, 2.456276212633274003 ) ) ;
#33712=CARTESIAN_POINT ( 'NONE',  ( 0.1158816050234199174, 41.87450319480698369, -13.90927832395560593 ) ) ;
#33714=CARTESIAN_POINT ( 'NONE',  ( 0.5997462898726536595, -39.66574928371259290, 28.95133786038155321 ) ) ;
#33715=CARTESIAN_POINT ( 'NONE',  ( 0.1145239942831223490, -40.77578764147322943, -16.86062344405307201 ) ) ;
#33716=ORIENTED_EDGE ( 'NONE', *, *, #5786, .F. ) ;
#33721=EDGE_CURVE ( 'NONE', #31232, #19850, #39229, .T. ) ;
#33722=DIRECTION ( 'NONE',  ( 0.09722883295013595717, -0.3959434903494524760, -0.9131129757554907744 ) ) ;
#33726=AXIS2_PLACEMENT_3D ( 'NONE', #5413, #43684, #39285 ) ;
#33734=CARTESIAN_POINT ( 'NONE',  ( 0.1129192098497455998, -27.88830454350494392, 34.19348267541455044 ) ) ;
#33736=ORIENTED_EDGE ( 'NONE', *, *, #23694, .T. ) ;
#33740=CARTESIAN_POINT ( 'NONE',  ( 0.8753041380234471980, -35.88662119133365991, 33.51550010581227212 ) ) ;
#33749=CARTESIAN_POINT ( 'NONE',  ( 0.8753041380234471980, 36.80657072176690292, 32.50253343320412824 ) ) ;
#33752=CARTESIAN_POINT ( 'NONE',  ( 0.5997462898726536595, -20.35457962188229430, 44.69052157405150183 ) ) ;
#33767=CARTESIAN_POINT ( 'NONE',  ( -6.072942160501519027, 3.087637228658090205, -19.00712126107541167 ) ) ;
#33768=CARTESIAN_POINT ( 'NONE',  ( 0.7242003506640004584, -35.83729897872414227, -33.56634737405257596 ) ) ;
#33769=CARTESIAN_POINT ( 'NONE',  ( 0.1145239942831223490, 10.13668889349744973, -42.94406849590660613 ) ) ;
#33771=AXIS2_PLACEMENT_3D ( 'NONE', #32309, #51386, #56703 ) ;
#33772=CARTESIAN_POINT ( 'NONE',  ( 0.1365634738349378596, -22.32623199351180432, -38.05787677465910690 ) ) ;
#33776=VECTOR ( 'NONE', #36642, 1000.000000000000114 ) ;
#33777=CARTESIAN_POINT ( 'NONE',  ( 0.8753041380234524160, -2.462982411634174085, -49.04153388213872944 ) ) ;
#33788=CARTESIAN_POINT ( 'NONE',  ( 4.975610109902397937, 42.89797504594955058, -23.49921581872176191 ) ) ;
#33789=ORIENTED_EDGE ( 'NONE', *, *, #53281, .T. ) ;
#33793=CARTESIAN_POINT ( 'NONE',  ( -6.078726893082806448, -1.845620846545350080, -19.16736092839902383 ) ) ;
#33802=VECTOR ( 'NONE', #48160, 1000.000000000000114 ) ;
#33810=CARTESIAN_POINT ( 'NONE',  ( -6.072942160501519027, 19.25627044167812230, 0.01452466776899024453 ) ) ;
#33811=ORIENTED_EDGE ( 'NONE', *, *, #12198, .T. ) ;
#33813=CARTESIAN_POINT ( 'NONE',  ( 0.6253024248130479856, -49.10165524324679609, -0.6867894808279696450 ) ) ;
#33817=CARTESIAN_POINT ( 'NONE',  ( 4.553261556744873317, -36.93702150832076825, -23.77385134801438937 ) ) ;
#33819=VERTEX_POINT ( 'NONE', #53894 ) ;
#33821=CARTESIAN_POINT ( 'NONE',  ( 4.553261556744873317, -9.554252317234828595, 42.87488575474283437 ) ) ;
#33828=ORIENTED_EDGE ( 'NONE', *, *, #49160, .F. ) ;
#33829=CARTESIAN_POINT ( 'NONE',  ( -2.739355103387248747, 14.70078895384969186, 2.595066682262317848 ) ) ;
#33831=EDGE_CURVE ( 'NONE', #7571, #23099, #21918, .T. ) ;
#33846=CARTESIAN_POINT ( 'NONE',  ( 0.6021448801613057400, -47.43444021936057453, -12.70885595570491589 ) ) ;
#33848=CARTESIAN_POINT ( 'NONE',  ( 0.1119899015040010382, 4.795286430103810282, -43.86304294329986675 ) ) ;
#33849=VERTEX_POINT ( 'NONE', #15723 ) ;
#33853=CARTESIAN_POINT ( 'NONE',  ( -6.063463321072278589, -6.635954031850681112, -18.07718359055509794 ) ) ;
#33854=ORIENTED_EDGE ( 'NONE', *, *, #19292, .T. ) ;
#33858=AXIS2_PLACEMENT_3D ( 'NONE', #42552, #27199, #9317 ) ;
#33859=CARTESIAN_POINT ( 'NONE',  ( 0.8744876279028306332, -31.30103973185180521, -37.82320666052162039 ) ) ;
#33860=VECTOR ( 'NONE', #22800, 1000.000000000000000 ) ;
#33864=CARTESIAN_POINT ( 'NONE',  ( 0.1157506346131639274, 29.59596297817652299, -32.72643633512880257 ) ) ;
#33871=EDGE_CURVE ( 'NONE', #38401, #2370, #42791, .T. ) ;
#33878=CARTESIAN_POINT ( 'NONE',  ( 0.7044674535452954967, 5.553212498071502523, -48.79512838144981401 ) ) ;
#33879=ORIENTED_EDGE ( 'NONE', *, *, #53896, .F. ) ;
#33887=CARTESIAN_POINT ( 'NONE',  ( 0.1158403557922069033, 25.27520615740563414, -36.16772402134896680 ) ) ;
#33891=B_SPLINE_CURVE_WITH_KNOTS ( 'NONE', 3,
 ( #30918, #40349, #55017, #50028 ),
 .UNSPECIFIED., .F., .F.,
 ( 4, 4 ),
 ( 0.000000000000000000, 0.004442905043737215703 ),
 .UNSPECIFIED. ) ;
#33893=CARTESIAN_POINT ( 'NONE',  ( 0.1129192098497455998, -41.07894348801367812, 16.10814047907867064 ) ) ;
#33897=LINE ( 'NONE', #57049, #38859 ) ;
#33898=CARTESIAN_POINT ( 'NONE',  ( 4.226256110419179812, -9.374554497711095280, -42.92953503075280253 ) ) ;
#33905=CARTESIAN_POINT ( 'NONE',  ( 0.5997462898726536595, 44.01516392039513903, -21.77652348757843015 ) ) ;
#33906=CARTESIAN_POINT ( 'NONE',  ( 0.2279481005628771206, 34.08161525712255013, -28.01690540617190095 ) ) ;
#33907=CARTESIAN_POINT ( 'NONE',  ( 0.1129192098497447394, -43.82135468580274562, -5.161459220630158384 ) ) ;
#33908=DIRECTION ( 'NONE',  ( 0.000000000000000000, 0.000000000000000000, 1.000000000000000000 ) ) ;
#33910=CARTESIAN_POINT ( 'NONE',  ( 0.1368894036331284314, -17.27553727570517594, 40.60070366088567795 ) ) ;
#33916=CARTESIAN_POINT ( 'NONE',  ( 2.185380717157383579, 19.08024733508938198, -39.68329578927402679 ) ) ;
#33920=CARTESIAN_POINT ( 'NONE',  ( 3.240649175237395596, -21.22199265827904213, -38.53429569889141248 ) ) ;
#33921=CARTESIAN_POINT ( 'NONE',  ( 2.359973842542475886, 26.40990395922420220, 35.22290259897746267 ) ) ;
#33925=CARTESIAN_POINT ( 'NONE',  ( 4.553261556744875094, -41.61700166486733110, -14.05577241741153216 ) ) ;
#33932=CARTESIAN_POINT ( 'NONE',  ( 0.5980271706414711508, 33.53334604750737924, -35.88264128655782059 ) ) ;
#33940=VECTOR ( 'NONE', #55621, 1000.000000000000114 ) ;
#33942=ORIENTED_EDGE ( 'NONE', *, *, #51350, .T. ) ;
#33949=FACE_OUTER_BOUND ( 'NONE', #9344, .T. ) ;
#33956=CARTESIAN_POINT ( 'NONE',  ( 0.7948878604505683620, 33.64624533417287466, 35.75791971313581286 ) ) ;
#33957=B_SPLINE_CURVE_WITH_KNOTS ( 'NONE', 3,
 ( #61349, #23777, #61655, #33813, #51652, #52578 ),
 .UNSPECIFIED., .F., .F.,
 ( 4, 2, 4 ),
 ( 2.521789927402474235E-18, 0.0002447193893791697623, 0.0004894387787583369225 ),
 .UNSPECIFIED. ) ;
#33961=B_SPLINE_CURVE_WITH_KNOTS ( 'NONE', 3,
 ( #14619, #54019, #25843, #15842 ),
 .UNSPECIFIED., .F., .F.,
 ( 4, 4 ),
 ( 2.189128766608093472E-17, 0.004559932413162186803 ),
 .UNSPECIFIED. ) ;
#33968=CARTESIAN_POINT ( 'NONE',  ( 1.830465331921978578, 43.45643058836503769, -7.205185382556205553 ) ) ;
#33973=CARTESIAN_POINT ( 'NONE',  ( 0.6000166863083106206, 44.47108027094602534, 20.83618250168510144 ) ) ;
#33974=CARTESIAN_POINT ( 'NONE',  ( -6.063463321072278589, 19.10058954492600236, -2.447025033736572652 ) ) ;
#33980=FACE_OUTER_BOUND ( 'NONE', #26358, .T. ) ;
#33981=CARTESIAN_POINT ( 'NONE',  ( -6.072942160501519027, 16.77122109808123085, 9.462045506564395581 ) ) ;
#33988=B_SPLINE_CURVE_WITH_KNOTS ( 'NONE', 3,
 ( #14991, #57543, #28760, #43501 ),
 .UNSPECIFIED., .F., .F.,
 ( 4, 4 ),
 ( 2.175771182130668512E-17, 0.004559932413162186803 ),
 .UNSPECIFIED. ) ;
#33990=CARTESIAN_POINT ( 'NONE',  ( 0.6008122571543326185, 22.32719153875445528, -43.73843925492870710 ) ) ;
#33998=CARTESIAN_POINT ( 'NONE',  ( 3.894904216938897878, 43.66689113967132840, -5.032588863824957848 ) ) ;
#33999=CARTESIAN_POINT ( 'NONE',  ( 0.1158403557922069033, 41.86432774633747300, 13.93981239224752500 ) ) ;
#34011=FACE_OUTER_BOUND ( 'NONE', #41717, .T. ) ;
#34021=ORIENTED_EDGE ( 'NONE', *, *, #26461, .T. ) ;
#34023=LINE ( 'NONE', #57163, #39684 ) ;
#34024=CARTESIAN_POINT ( 'NONE',  ( 0.8744876279028263033, -19.05609938968970241, -45.24616145519706834 ) ) ;
#34025=CARTESIAN_POINT ( 'NONE',  ( 0.1158816050234198480, -40.90156038422842499, -16.55307824667295336 ) ) ;
#34027=B_SPLINE_CURVE_WITH_KNOTS ( 'NONE', 3,
 ( #20719, #39859, #58914, #16027, #6574, #25721 ),
 .UNSPECIFIED., .F., .F.,
 ( 4, 2, 4 ),
 ( 0.000000000000000000, 0.0002293801035737086402, 0.0004587602071474172804 ),
 .UNSPECIFIED. ) ;
#34029=ORIENTED_EDGE ( 'NONE', *, *, #11739, .F. ) ;
#34036=CARTESIAN_POINT ( 'NONE',  ( 4.553261556744873317, -20.51767157960462384, -38.84024612145397981 ) ) ;
#34040=CARTESIAN_POINT ( 'NONE',  ( 0.1129192098497455998, 9.345467776858411568, 43.12324222292260600 ) ) ;
#34042=VERTEX_POINT ( 'NONE', #16180 ) ;
#34044=EDGE_CURVE ( 'NONE', #7116, #16048, #407, .T. ) ;
#34048=CARTESIAN_POINT ( 'NONE',  ( -2.601141883200662974, 11.65089574274766981, 9.330169122851570407 ) ) ;
#34059=VERTEX_POINT ( 'NONE', #20566 ) ;
#34066=CARTESIAN_POINT ( 'NONE',  ( 3.678748215320120085, -23.78921895854951885, 42.80988058429586118 ) ) ;
#34075=CARTESIAN_POINT ( 'NONE',  ( -6.078726893082806448, 18.62537590944121391, -4.887679766589349661 ) ) ;
#34081=CARTESIAN_POINT ( 'NONE',  ( 0.1140933569871964842, 10.18798020565364126, -42.93198119599321672 ) ) ;
#34084=ORIENTED_EDGE ( 'NONE', *, *, #42492, .T. ) ;
#34085=B_SPLINE_CURVE_WITH_KNOTS ( 'NONE', 3,
 ( #13486, #19724, #38234, #32907 ),
 .UNSPECIFIED., .F., .F.,
 ( 4, 4 ),
 ( 7.046480070129584215E-18, 0.005013413432710147645 ),
 .UNSPECIFIED. ) ;
#34086=CARTESIAN_POINT ( 'NONE',  ( 0.1129192098497455998, -22.45785791439690371, -37.98152716363461678 ) ) ;
#34092=ORIENTED_EDGE ( 'NONE', *, *, #40584, .T. ) ;
#34096=CARTESIAN_POINT ( 'NONE',  ( 2.299746137290197723, 36.48830940075291096, -32.75491741343678598 ) ) ;
#34098=ORIENTED_EDGE ( 'NONE', *, *, #57238, .T. ) ;
#34100=LINE ( 'NONE', #29370, #57596 ) ;
#34103=ORIENTED_EDGE ( 'NONE', *, *, #3730, .F. ) ;
#34106=VERTEX_POINT ( 'NONE', #45015 ) ;
#34112=CARTESIAN_POINT ( 'NONE',  ( 0.6028777368367060907, -30.54986267508339637, -38.44796119230016274 ) ) ;
#34113=EDGE_CURVE ( 'NONE', #16660, #9776, #20873, .T. ) ;
#34114=LINE ( 'NONE', #558, #29276 ) ;
#34115=ORIENTED_EDGE ( 'NONE', *, *, #49786, .T. ) ;
#34119=CARTESIAN_POINT ( 'NONE',  ( 0.1157506346131639274, -38.40058778857950017, 21.73328132828619630 ) ) ;
#34121=EDGE_LOOP ( 'NONE', ( #1922, #34818, #11046, #42299 ) ) ;
#34123=CARTESIAN_POINT ( 'NONE',  ( 0.1365634738349374988, 24.71873689235127358, 36.54923618996653545 ) ) ;
#34124=CARTESIAN_POINT ( 'NONE',  ( 4.975610109902397937, -4.123593823331679786, -48.73854102369041641 ) ) ;
#34130=ORIENTED_EDGE ( 'NONE', *, *, #4919, .F. ) ;
#34133=CARTESIAN_POINT ( 'NONE',  ( 0.1156495703730068131, -42.64630798246201238, 11.32410564663129904 ) ) ;
#34136=CARTESIAN_POINT ( 'NONE',  ( 0.3676999524040366896, -23.56959980820299094, -37.28839696479317212 ) ) ;
#34139=CARTESIAN_POINT ( 'NONE',  ( 2.299746137290199055, -45.91772730306088590, -17.20010630803993479 ) ) ;
#34140=CARTESIAN_POINT ( 'NONE',  ( 0.1147471544378676628, 29.89391364686623831, 32.45467786540100263 ) ) ;
#34151=CARTESIAN_POINT ( 'NONE',  ( 0.5549461598389366923, 40.10986404279688600, 18.34166028295022954 ) ) ;
#34157=ORIENTED_EDGE ( 'NONE', *, *, #55926, .F. ) ;
#34161=CARTESIAN_POINT ( 'NONE',  ( 0.5987334308729317378, -31.08900172172731402, -38.01364069010184465 ) ) ;
#34165=CARTESIAN_POINT ( 'NONE',  ( 3.678834586032787790, 48.72167542788264427, 4.981035347034825200 ) ) ;
#34171=DIRECTION ( 'NONE',  ( 0.000000000000000000, 0.000000000000000000, -1.000000000000000000 ) ) ;
#34183=CARTESIAN_POINT ( 'NONE',  ( 0.7044674535453004927, 27.40191655692358452, -40.75460332058581514 ) ) ;
#34190=DIRECTION ( 'NONE',  ( -1.000000000000000000, -0.000000000000000000, -0.000000000000000000 ) ) ;
#34193=CARTESIAN_POINT ( 'NONE',  ( -6.078726893082806448, -19.21623043802547315, 1.237145513439503297 ) ) ;
#34196=EDGE_CURVE ( 'NONE', #35035, #8488, #22577, .T. ) ;
#34197=ORIENTED_EDGE ( 'NONE', *, *, #7507, .T. ) ;
#34198=CARTESIAN_POINT ( 'NONE',  ( 0.1158816050234198897, -40.89729701497818581, 16.56360885114767001 ) ) ;
#34199=CARTESIAN_POINT ( 'NONE',  ( 4.553261556744875094, 35.06776520399859010, 26.45357082552112260 ) ) ;
#34200=EDGE_CURVE ( 'NONE', #52454, #27212, #56224, .T. ) ;
#34208=CARTESIAN_POINT ( 'NONE',  ( -2.739355103387248747, -6.282164585816906843, -13.54186010368313120 ) ) ;
#34219=ORIENTED_EDGE ( 'NONE', *, *, #30885, .T. ) ;
#34234=ORIENTED_EDGE ( 'NONE', *, *, #16007, .F. ) ;
#34236=CARTESIAN_POINT ( 'NONE',  ( 0.8753041380234530822, -20.68664920503281834, -44.53314352862253855 ) ) ;
#34242=CARTESIAN_POINT ( 'NONE',  ( 2.299652685299201860, 48.35891399284305692, -8.105378602567647306 ) ) ;
#34250=ADVANCED_FACE ( 'NONE', ( #46863 ), #26253, .F. ) ;
#34251=ORIENTED_EDGE ( 'NONE', *, *, #11664, .T. ) ;
#34252=FACE_OUTER_BOUND ( 'NONE', #15362, .T. ) ;
#34254=CARTESIAN_POINT ( 'NONE',  ( 0.8744876279028263033, 33.66006955981258386, -35.74003032466635688 ) ) ;
#34259=CARTESIAN_POINT ( 'NONE',  ( 2.185380717157383579, -42.93410716945229666, -9.771501656817383363 ) ) ;
#34260=CARTESIAN_POINT ( 'NONE',  ( 0.5997462898726536595, -13.47075269803089803, -47.22383351542737984 ) ) ;
#34263=B_SPLINE_CURVE_WITH_KNOTS ( 'NONE', 3,
 ( #52147, #9238, #30488, #49297, #35223, #6353 ),
 .UNSPECIFIED., .F., .F.,
 ( 4, 2, 4 ),
 ( 0.000000000000000000, 0.0002447195606305754508, 0.0004894391212611509017 ),
 .UNSPECIFIED. ) ;
#34269=ADVANCED_FACE ( 'NONE', ( #31500 ), #19870, .F. ) ;
#34272=CARTESIAN_POINT ( 'NONE',  ( 0.1145239942831223490, -31.92292654912315442, 30.46099540796330274 ) ) ;
#34279=CARTESIAN_POINT ( 'NONE',  ( 0.1154773475650540948, -7.219714285311297886, -43.52952280561541443 ) ) ;
#34280=CARTESIAN_POINT ( 'NONE',  ( 0.6016117650947689910, 41.34545092125629395, 26.49725914811730121 ) ) ;
#34284=CARTESIAN_POINT ( 'NONE',  ( 0.6026777506516366456, 32.88586037763411696, -36.47007784280113185 ) ) ;
#34285=CARTESIAN_POINT ( 'NONE',  ( -2.601141883200662974, 12.74835759521958778, 7.763685084661515745 ) ) ;
#34286=CARTESIAN_POINT ( 'NONE',  ( 4.553261556744875094, -9.554252317234240621, -42.87488575474295516 ) ) ;
#34295=CARTESIAN_POINT ( 'NONE',  ( 4.553261556744875094, 1.182159483579356074, 43.91061448874314976 ) ) ;
#34301=B_SPLINE_CURVE_WITH_KNOTS ( 'NONE', 3,
 ( #35780, #21354, #44880, #26053, #1920, #55464 ),
 .UNSPECIFIED., .F., .F.,
 ( 4, 2, 4 ),
 ( 1.867170871510376464E-17, 0.0002293755540694311830, 0.0004587511081388436635 ),
 .UNSPECIFIED. ) ;
#34304=EDGE_LOOP ( 'NONE', ( #38725, #912, #21902, #55728 ) ) ;
#34305=ORIENTED_EDGE ( 'NONE', *, *, #38146, .T. ) ;
#34306=CARTESIAN_POINT ( 'NONE',  ( -6.072942160501519915, -18.90394509709858539, -3.666745430883196377 ) ) ;
#34307=CARTESIAN_POINT ( 'NONE',  ( 4.553261556744873317, -43.15908619232978083, -8.175135770535248980 ) ) ;
#34311=CARTESIAN_POINT ( 'NONE',  ( 0.1119898979215349505, -44.12081468618291069, 0.5612661394878653009 ) ) ;
#34313=CARTESIAN_POINT ( 'NONE',  ( 0.6000166863083106206, 40.87138819217380359, -27.22780029589406681 ) ) ;
#34319=ORIENTED_EDGE ( 'NONE', *, *, #4210, .T. ) ;
#34322=ORIENTED_EDGE ( 'NONE', *, *, #11907, .T. ) ;
#34323=DIRECTION ( 'NONE',  ( 0.000000000000000000, 0.000000000000000000, 1.000000000000000000 ) ) ;
#34324=CARTESIAN_POINT ( 'NONE',  ( -6.072942160501519027, 17.84350912780779197, 7.239706091745748751 ) ) ;
#34328=ORIENTED_EDGE ( 'NONE', *, *, #13780, .F. ) ;
#34336=ORIENTED_EDGE ( 'NONE', *, *, #17358, .T. ) ;
#34339=CARTESIAN_POINT ( 'NONE',  ( 0.1140933569871965120, 9.448435536941939716, 43.10077744064668792 ) ) ;
#34346=CARTESIAN_POINT ( 'NONE',  ( 4.335381028904216727, 48.97680438974856543, 1.014632658971305945 ) ) ;
#34348=CARTESIAN_POINT ( 'NONE',  ( 0.7413678028165009426, 21.21902926989227822, 38.65538628203963611 ) ) ;
#34351=VERTEX_POINT ( 'NONE', #14575 ) ;
#34354=CARTESIAN_POINT ( 'NONE',  ( 2.359973842542475886, -16.42991230730133267, 40.84352918403218524 ) ) ;
#34380=ORIENTED_EDGE ( 'NONE', *, *, #37118, .T. ) ;
#34381=FACE_OUTER_BOUND ( 'NONE', #710, .T. ) ;
#34384=CARTESIAN_POINT ( 'NONE',  ( 0.8744876279028263033, 48.35212675551510841, -8.510105087370661181 ) ) ;
#34387=VECTOR ( 'NONE', #55269, 1000.000000000000114 ) ;
#34390=ORIENTED_EDGE ( 'NONE', *, *, #17195, .F. ) ;
#34391=EDGE_CURVE ( 'NONE', #23436, #41057, #32296, .T. ) ;
#34401=CARTESIAN_POINT ( 'NONE',  ( 0.7242003506639993482, 28.75993203985512636, 39.79796456087851197 ) ) ;
#34411=ORIENTED_EDGE ( 'NONE', *, *, #26170, .F. ) ;
#34418=CARTESIAN_POINT ( 'NONE',  ( 0.1119899015040009826, -27.94769331548668845, 34.14509842621640701 ) ) ;
#34419=EDGE_CURVE ( 'NONE', #18115, #3927, #43522, .T. ) ;
#34420=VERTEX_POINT ( 'NONE', #53977 ) ;
#34438=CARTESIAN_POINT ( 'NONE',  ( -6.077587904424778920, -4.278847002849007097, -18.77465018902190863 ) ) ;
#34442=CARTESIAN_POINT ( 'NONE',  ( 4.975610109902397937, 48.58133226360784818, -5.683622315980244366 ) ) ;
#34444=CARTESIAN_POINT ( 'NONE',  ( 0.3676999524040366896, -2.238562284875889041, -44.05609404179596567 ) ) ;
#34450=EDGE_CURVE ( 'NONE', #4022, #27996, #29287, .T. ) ;
#34456=CARTESIAN_POINT ( 'NONE',  ( 0.7413678028165009426, 24.45722514617033383, -36.69237291208864349 ) ) ;
#34470=CARTESIAN_POINT ( 'NONE',  ( 0.1129192098497455998, 41.72114954716776936, 14.36305915353748297 ) ) ;
#34471=ORIENTED_EDGE ( 'NONE', *, *, #51958, .F. ) ;
#34474=CARTESIAN_POINT ( 'NONE',  ( 0.1119898979215347701, -13.09165672777951883, -42.13751098930518424 ) ) ;
#34479=DIRECTION ( 'NONE',  ( 1.000000000000000000, 0.000000000000000000, 0.000000000000000000 ) ) ;
#34483=DIRECTION ( 'NONE',  ( 0.000000000000000000, 0.000000000000000000, -1.000000000000000000 ) ) ;
#34484=B_SPLINE_CURVE_WITH_KNOTS ( 'NONE', 3,
 ( #7135, #26262, #45400, #3364, #2447, #21573 ),
 .UNSPECIFIED., .F., .F.,
 ( 4, 2, 4 ),
 ( 1.734723475976807094E-18, 0.0002447193893791696538, 0.0004894387787583375730 ),
 .UNSPECIFIED. ) ;
#34485=CARTESIAN_POINT ( 'NONE',  ( 0.2940135542859031448, -32.24540453331401579, -30.10771388156783601 ) ) ;
#34487=VERTEX_POINT ( 'NONE', #26412 ) ;
#34495=CARTESIAN_POINT ( 'NONE',  ( -2.739355103387247858, 14.87824819718636782, 1.218727834234354157 ) ) ;
#34496=EDGE_CURVE ( 'NONE', #55928, #28003, #3864, .T. ) ;
#34501=DIRECTION ( 'NONE',  ( 0.000000000000000000, 0.000000000000000000, 1.000000000000000000 ) ) ;
#34508=( BOUNDED_SURFACE ( )  B_SPLINE_SURFACE ( 3, 1, ( 
 ( #36143, #23257 ),
 ( #42085, #31735 ),
 ( #8216, #42384 ),
 ( #32355, #61437 ) ),
 .UNSPECIFIED., .F., .F., .F. ) 
 B_SPLINE_SURFACE_WITH_KNOTS ( ( 4, 4 ),
 ( 2, 2 ),
 ( 0.000000000000000000, 1.000000000000000000 ),
 ( 0.000000000000000000, 1.000000000000000000 ),
 .UNSPECIFIED. ) 
 GEOMETRIC_REPRESENTATION_ITEM ( )  RATIONAL_B_SPLINE_SURFACE ( (
 ( 1.000000000000000000, 1.000000000000000000),
 ( 0.7211978278499968642, 0.9934217856018975334),
 ( 0.7211978278499968642, 0.9934217856018975334),
 ( 1.000000000000000000, 1.000000000000000000) ) ) 
 REPRESENTATION_ITEM ( '' )  SURFACE ( )  );
#34511=CARTESIAN_POINT ( 'NONE',  ( 0.5980271706414734822, -47.67913160907356485, -11.77920421107915949 ) ) ;
#34516=CARTESIAN_POINT ( 'NONE',  ( 0.1157506346131639274, -43.77365856608008698, -5.550448229024145697 ) ) ;
#34519=EDGE_CURVE ( 'NONE', #47731, #36259, #57414, .T. ) ;
#34524=EDGE_LOOP ( 'NONE', ( #56643, #17237, #52175, #10348 ) ) ;
#34527=CARTESIAN_POINT ( 'NONE',  ( 1.296416391601052265, 19.39309367396150918, -39.57543798657334833 ) ) ;
#34533=CARTESIAN_POINT ( 'NONE',  ( 4.975610109902397937, 25.84633036597824329, 41.52609557555928177 ) ) ;
#34535=VERTEX_POINT ( 'NONE', #59927 ) ;
#34536=CARTESIAN_POINT ( 'NONE',  ( -6.078075953587585900, -8.911363828324937231, 17.06993757945112478 ) ) ;
#34538=ADVANCED_FACE ( 'NONE', ( #17036 ), #42376, .F. ) ;
#34540=ORIENTED_EDGE ( 'NONE', *, *, #50619, .T. ) ;
#34545=CARTESIAN_POINT ( 'NONE',  ( 0.1129192098497455998, -12.08918212651712132, -42.43587472053631160 ) ) ;
#34546=CARTESIAN_POINT ( 'NONE',  ( 0.7948884756798507700, 41.61600058688303960, -26.05392753027271624 ) ) ;
#34547=VERTEX_POINT ( 'NONE', #24489 ) ;
#34552=CARTESIAN_POINT ( 'NONE',  ( 0.2285344041767079226, 43.44439842031292898, 7.686703857477898083 ) ) ;
#34559=B_SPLINE_CURVE_WITH_KNOTS ( 'NONE', 3,
 ( #12561, #31651, #7832, #26952 ),
 .UNSPECIFIED., .F., .F.,
 ( 4, 4 ),
 ( 0.000000000000000000, 0.004444103432399266161 ),
 .UNSPECIFIED. ) ;
#34560=CARTESIAN_POINT ( 'NONE',  ( -6.078457390727109555, -18.90176508385429344, -3.676654423833525254 ) ) ;
#34562=EDGE_CURVE ( 'NONE', #34535, #32393, #59177, .T. ) ;
#34565=ORIENTED_EDGE ( 'NONE', *, *, #41261, .F. ) ;
#34566=CARTESIAN_POINT ( 'NONE',  ( 4.060580049360325461, -43.03904816311536763, -8.894269366971370161 ) ) ;
#34567=CARTESIAN_POINT ( 'NONE',  ( 0.1158516988532803244, 36.95306216529235144, -24.11251449850959361 ) ) ;
#34574=CARTESIAN_POINT ( 'NONE',  ( 4.975610109902397937, -4.123593823331679786, -48.73854102369041641 ) ) ;
#34575=CARTESIAN_POINT ( 'NONE',  ( 0.3676999524040323597, -42.45338881270421894, -11.98584004733086061 ) ) ;
#34588=CARTESIAN_POINT ( 'NONE',  ( 0.1157506346131639274, -35.30612916330391471, 26.46540956242572307 ) ) ;
#34589=DIRECTION ( 'NONE',  ( 0.09722883295013595717, -0.7201826484181221844, 0.6869377751737153481 ) ) ;
#34595=EDGE_CURVE ( 'NONE', #31849, #14207, #56906, .T. ) ;
#34603=CARTESIAN_POINT ( 'NONE',  ( 0.5997462898726536595, -34.91088276334701135, -34.53667463477266608 ) ) ;
#34605=ORIENTED_EDGE ( 'NONE', *, *, #25584, .F. ) ;
#34612=CARTESIAN_POINT ( 'NONE',  ( -6.063463321072276813, -18.90456390296425582, -3.665776332267282722 ) ) ;
#34616=CARTESIAN_POINT ( 'NONE',  ( 4.226256110419179812, -10.18024542482925909, 42.74564133426272150 ) ) ;
#34620=CARTESIAN_POINT ( 'NONE',  ( 3.678834586032788678, 43.29171918419824294, 22.90064234262600351 ) ) ;
#34621=CARTESIAN_POINT ( 'NONE',  ( 0.1145239942831223490, 15.54503240824534060, -41.29524728260233957 ) ) ;
#34625=CARTESIAN_POINT ( 'NONE',  ( 0.7044674535453004927, -19.10600803152214411, 45.24116687167030904 ) ) ;
#34628=CARTESIAN_POINT ( 'NONE',  ( 4.975610109902397937, 0.000000000000000000, 0.000000000000000000 ) ) ;
#34634=CARTESIAN_POINT ( 'NONE',  ( 0.1129192098497447394, 43.21532672376840623, -8.909956450123800664 ) ) ;
#34638=CARTESIAN_POINT ( 'NONE',  ( 3.050102900204245682, -28.82147234748848774, -33.23774933567278822 ) ) ;
#34640=DIRECTION ( 'NONE',  ( 0.000000000000000000, 0.000000000000000000, 1.000000000000000000 ) ) ;
#34642=EDGE_LOOP ( 'NONE', ( #30612, #17977, #50865, #8873 ) ) ;
#34647=CARTESIAN_POINT ( 'NONE',  ( 0.1157991065609915993, 33.65088663166012850, -28.54050094936765092 ) ) ;
#34649=CARTESIAN_POINT ( 'NONE',  ( 0.1119898979215348395, -41.10694714348719714, -16.03683899009958580 ) ) ;
#34659=B_SPLINE_CURVE_WITH_KNOTS ( 'NONE', 3,
 ( #10585, #48791, #43823, #9973, #44436, #545 ),
 .UNSPECIFIED., .F., .F.,
 ( 4, 2, 4 ),
 ( 1.951563910473907981E-18, 0.0002447193893791689491, 0.0004894387787583359467 ),
 .UNSPECIFIED. ) ;
#34660=VECTOR ( 'NONE', #40594, 1000.000000000000114 ) ;
#34663=CARTESIAN_POINT ( 'NONE',  ( 0.6029443199889047422, 22.71407876865105280, 43.53858366490483434 ) ) ;
#34666=CARTESIAN_POINT ( 'NONE',  ( 0.6021447746440204973, -19.63869024154479348, 45.00958769734666731 ) ) ;
#34672=CIRCLE ( 'NONE', #18667, 43.92652462719577500 ) ;
#34677=CARTESIAN_POINT ( 'NONE',  ( 0.6000166863083090663, -47.63401213562571002, 11.95091500980225518 ) ) ;
#34681=CARTESIAN_POINT ( 'NONE',  ( 0.1158816050234199035, -22.86878204857423214, 37.73540577388786232 ) ) ;
#34684=EDGE_CURVE ( 'NONE', #54546, #14082, #9883, .T. ) ;
#34685=( BOUNDED_SURFACE ( )  B_SPLINE_SURFACE ( 3, 1, ( 
 ( #23489, #56683 ),
 ( #19129, #57287 ),
 ( #13186, #32915 ),
 ( #23809, #14420 ) ),
 .UNSPECIFIED., .F., .F., .F. ) 
 B_SPLINE_SURFACE_WITH_KNOTS ( ( 4, 4 ),
 ( 2, 2 ),
 ( 0.000000000000000000, 1.000000000000000000 ),
 ( 0.000000000000000000, 1.000000000000000000 ),
 .UNSPECIFIED. ) 
 GEOMETRIC_REPRESENTATION_ITEM ( )  RATIONAL_B_SPLINE_SURFACE ( (
 ( 1.000000000000000000, 1.000000000000000000),
 ( 0.7211978278499970862, 0.9934217856018976445),
 ( 0.7211978278499970862, 0.9934217856018976445),
 ( 1.000000000000000000, 1.000000000000000000) ) ) 
 REPRESENTATION_ITEM ( '' )  SURFACE ( )  );
#34690=FACE_OUTER_BOUND ( 'NONE', #12077, .T. ) ;
#34693=EDGE_CURVE ( 'NONE', #21937, #5016, #3091, .T. ) ;
#34704=CONICAL_SURFACE ( 'NONE', #12714, 44.12552607296456131, 0.04450589592585061510 ) ;
#34708=CARTESIAN_POINT ( 'NONE',  ( 0.6039202388192952409, 4.542059820466225695, 48.89717175293780116 ) ) ;
#34711=CARTESIAN_POINT ( 'NONE',  ( 4.975610109902397937, -46.23629923292386934, 15.95788333023201488 ) ) ;
#34714=B_SPLINE_CURVE_WITH_KNOTS ( 'NONE', 3,
 ( #26901, #49462, #2134, #30349 ),
 .UNSPECIFIED., .F., .F.,
 ( 4, 4 ),
 ( 0.000000000000000000, 0.004442905043737215703 ),
 .UNSPECIFIED. ) ;
#34717=ORIENTED_EDGE ( 'NONE', *, *, #47899, .F. ) ;
#34719=CARTESIAN_POINT ( 'NONE',  ( 0.6024113833632038784, -30.44748741247445523, -38.52911080427468704 ) ) ;
#34722=B_SPLINE_CURVE_WITH_KNOTS ( 'NONE', 3,
 ( #44922, #6958, #6637, #47003, #13174, #8759, #4036, #23176, #13479, #56361, #56054, #1961, #27874, #60748, #42303, #54570, #32585, #35511, #49901, #49581, #61361, #16388, #21088, #26091, #40232 ),
 .UNSPECIFIED., .F., .F.,
 ( 4, 3, 3, 3, 3, 3, 3, 3, 4 ),
 ( 6.992893892674702526E-18, 0.0005656085177311402905, 0.001131215744874500924, 0.001696821861372767000, 0.002262427090022498585, 0.002828031679238746793, 0.003393635864401606164, 0.003977030878808133357, 0.004561030005651159867 ),
 .UNSPECIFIED. ) ;
#34729=ORIENTED_EDGE ( 'NONE', *, *, #15010, .F. ) ;
#34732=ORIENTED_EDGE ( 'NONE', *, *, #44629, .T. ) ;
#34734=CARTESIAN_POINT ( 'NONE',  ( 3.559346040607745287, 31.04985557733589019, 31.13417334969039629 ) ) ;
#34736=CARTESIAN_POINT ( 'NONE',  ( 0.6000166863083090663, 32.62822748873757916, -36.70452632376071733 ) ) ;
#34737=ORIENTED_EDGE ( 'NONE', *, *, #52740, .T. ) ;
#34742=DIRECTION ( 'NONE',  ( -1.000000000000000000, -0.000000000000000000, -0.000000000000000000 ) ) ;
#34750=CARTESIAN_POINT ( 'NONE',  ( 0.1129192098497455998, 29.30421273086464140, 32.98810246148426728 ) ) ;
#34752=STYLED_ITEM ( 'NONE', ( #25093 ), #48247 ) ;
#34754=EDGE_CURVE ( 'NONE', #14421, #25770, #11321, .T. ) ;
#34759=EDGE_CURVE ( 'NONE', #10554, #38699, #21085, .T. ) ;
#34764=CARTESIAN_POINT ( 'NONE',  ( 1.112077966505211402, 40.15882174338756982, 18.17413990568401161 ) ) ;
#34766=VERTEX_POINT ( 'NONE', #29495 ) ;
#34770=EDGE_CURVE ( 'NONE', #13767, #52623, #48603, .T. ) ;
#34773=CARTESIAN_POINT ( 'NONE',  ( 4.694002226626920127, -30.90320716794954237, -33.51531826166844752 ) ) ;
#34789=CARTESIAN_POINT ( 'NONE',  ( 0.1156495703730067159, -1.277995041157171219, 44.10566496387792768 ) ) ;
#34791=CARTESIAN_POINT ( 'NONE',  ( 0.1129192098497447394, 25.64022107388777272, 35.91003830501040994 ) ) ;
#34795=VECTOR ( 'NONE', #55416, 1000.000000000000000 ) ;
#34802=ORIENTED_EDGE ( 'NONE', *, *, #54222, .T. ) ;
#34804=ADVANCED_FACE ( 'NONE', ( #50159 ), #57509, .F. ) ;
#34807=( BOUNDED_SURFACE ( )  B_SPLINE_SURFACE ( 3, 1, ( 
 ( #1600, #35158 ),
 ( #34536, #996 ),
 ( #39877, #38945 ),
 ( #53915, #6288 ) ),
 .UNSPECIFIED., .F., .F., .F. ) 
 B_SPLINE_SURFACE_WITH_KNOTS ( ( 4, 4 ),
 ( 2, 2 ),
 ( 0.000000000000000000, 1.000000000000000000 ),
 ( 0.000000000000000000, 1.000000000000000000 ),
 .UNSPECIFIED. ) 
 GEOMETRIC_REPRESENTATION_ITEM ( )  RATIONAL_B_SPLINE_SURFACE ( (
 ( 1.000000000000000000, 1.000000000000000000),
 ( 0.9953485035131437453, 0.8621029689291515030),
 ( 0.9953485035131437453, 0.8621029689291515030),
 ( 1.000000000000000000, 1.000000000000000000) ) ) 
 REPRESENTATION_ITEM ( '' )  SURFACE ( )  );
#34809=CARTESIAN_POINT ( 'NONE',  ( 0.1158403557922069033, 25.21309394138425830, 36.21105081445097795 ) ) ;
#34811=LINE ( 'NONE', #1566, #9561 ) ;
#34818=ORIENTED_EDGE ( 'NONE', *, *, #22301, .T. ) ;
#34825=ADVANCED_FACE ( 'NONE', ( #51064 ), #32297, .F. ) ;
#34826=CARTESIAN_POINT ( 'NONE',  ( -2.739355103387247858, -14.76959508014213540, -2.169476462112044146 ) ) ;
#34829=CARTESIAN_POINT ( 'NONE',  ( 0.3676999524040323597, -2.238562284876542741, 44.05609404179593724 ) ) ;
#34832=CARTESIAN_POINT ( 'NONE',  ( 0.1157991065609915993, 39.71911272509257174, 19.21807612299130952 ) ) ;
#34840=CARTESIAN_POINT ( 'NONE',  ( 2.009741617377216460, 19.14496109139358637, -39.66074308976157425 ) ) ;
#34842=VERTEX_POINT ( 'NONE', #53794 ) ;
#34845=ORIENTED_EDGE ( 'NONE', *, *, #9195, .F. ) ;
#34847=ADVANCED_FACE ( 'NONE', ( #10929 ), #31933, .F. ) ;
#34850=B_SPLINE_CURVE_WITH_KNOTS ( 'NONE', 3,
 ( #30163, #48359, #48058, #34894, #24865, #5418, #44305, #24554, #19869, #53958, #58342, #28941, #5108, #38984, #58040, #34272, #10458, #29549, #10773 ),
 .UNSPECIFIED., .F., .F.,
 ( 4, 3, 3, 3, 3, 3, 4 ),
 ( 7.758025766973964006E-18, 0.0002612768053151714922, 0.0003919133833142863718, 0.0005225499612322580430, 0.0006531865391693282607, 0.0008112755173415173637, 0.0009693688056799695373 ),
 .UNSPECIFIED. ) ;
#34851=CARTESIAN_POINT ( 'NONE',  ( -6.078726893082806448, -4.281536037413855134, -18.77398440473003305 ) ) ;
#34854=CARTESIAN_POINT ( 'NONE',  ( -6.078726893082806448, 19.09748444646205456, 2.465791776663210033 ) ) ;
#34863=VERTEX_POINT ( 'NONE', #54413 ) ;
#34864=CARTESIAN_POINT ( 'NONE',  ( 4.553261556744875094, 0.000000000000000000, 0.000000000000000000 ) ) ;
#34870=CARTESIAN_POINT ( 'NONE',  ( 0.6000166863083106206, -20.35571918921390377, -44.69304395538888031 ) ) ;
#34878=CARTESIAN_POINT ( 'NONE',  ( 0.6039202388192953519, -25.30794220682954787, 42.08410357967443360 ) ) ;
#34879=EDGE_CURVE ( 'NONE', #30382, #47787, #52469, .T. ) ;
#34887=CARTESIAN_POINT ( 'NONE',  ( -2.601141883200662974, -2.823446916239099380, -14.65686102071546948 ) ) ;
#34889=CARTESIAN_POINT ( 'NONE',  ( 2.299746137290199943, -2.858736841029653419, -48.95006599954567861 ) ) ;
#34893=CARTESIAN_POINT ( 'NONE',  ( 0.2285344041767086165, 15.94802410072414212, 41.13589305677194830 ) ) ;
#34894=CARTESIAN_POINT ( 'NONE',  ( 0.1152339509894530906, -31.54074419499066551, 30.85650897430565465 ) ) ;
#34896=FACE_OUTER_BOUND ( 'NONE', #3650, .T. ) ;
#34897=CARTESIAN_POINT ( 'NONE',  ( 4.553261556744875094, -14.95853073564453339, -41.30111286702108941 ) ) ;
#34909=CARTESIAN_POINT ( 'NONE',  ( 0.1129192098497447394, 20.83764143887560749, 38.89401608281161060 ) ) ;
#34911=CARTESIAN_POINT ( 'NONE',  ( -2.601141883200665639, -14.31801740503244069, -4.217796232462731609 ) ) ;
#34922=ORIENTED_EDGE ( 'NONE', *, *, #53365, .F. ) ;
#34924=CARTESIAN_POINT ( 'NONE',  ( -6.077587904424778920, 0.6110050725289616347, 19.24636833782608392 ) ) ;
#34927=ORIENTED_EDGE ( 'NONE', *, *, #33316, .T. ) ;
#34931=VECTOR ( 'NONE', #31961, 999.9999999999998863 ) ;
#34932=CARTESIAN_POINT ( 'NONE',  ( -6.078457390727109555, -17.35098001992619743, -8.350928294844221611 ) ) ;
#34933=CARTESIAN_POINT ( 'NONE',  ( 0.6000166863083106206, 33.40185771989302310, -36.00193581695957334 ) ) ;
#34934=CARTESIAN_POINT ( 'NONE',  ( 1.657374760986086271, -11.34341091359688569, 42.57014771054400626 ) ) ;
#34938=CARTESIAN_POINT ( 'NONE',  ( 0.1158403557922069033, 15.27446809072172051, -41.39602555474792922 ) ) ;
#34948=CARTESIAN_POINT ( 'NONE',  ( 0.1139756605157203340, -41.04710786557956226, -16.18919873145358679 ) ) ;
#34951=CARTESIAN_POINT ( 'NONE',  ( 0.6029443199889047422, -35.27625851169997873, 34.16318526235686193 ) ) ;
#34959=LINE ( 'NONE', #35578, #34660 ) ;
#34961=( BOUNDED_SURFACE ( )  B_SPLINE_SURFACE ( 3, 1, ( 
 ( #29293, #48404 ),
 ( #29599, #34625 ),
 ( #54005, #6073 ),
 ( #44353, #58090 ) ),
 .UNSPECIFIED., .F., .F., .F. ) 
 B_SPLINE_SURFACE_WITH_KNOTS ( ( 4, 4 ),
 ( 2, 2 ),
 ( 0.000000000000000000, 1.000000000000000000 ),
 ( 0.000000000000000000, 1.000000000000000000 ),
 .UNSPECIFIED. ) 
 GEOMETRIC_REPRESENTATION_ITEM ( )  RATIONAL_B_SPLINE_SURFACE ( (
 ( 1.000000000000000000, 1.000000000000000000),
 ( 0.9953485035131437453, 0.8621029689291515030),
 ( 0.9953485035131437453, 0.8621029689291515030),
 ( 1.000000000000000000, 1.000000000000000000) ) ) 
 REPRESENTATION_ITEM ( '' )  SURFACE ( )  );
#34962=VERTEX_POINT ( 'NONE', #31878 ) ;
#34963=DIRECTION ( 'NONE',  ( 0.09722883295013592941, 0.6746907015591432355, 0.7316686485512315929 ) ) ;
#34969=CARTESIAN_POINT ( 'NONE',  ( 0.1149546198390367230, 33.77510505806843355, -28.39346479983835181 ) ) ;
#34970=CARTESIAN_POINT ( 'NONE',  ( 50.15577769773999961, 12.80000000000000071, 3.000000000000000000 ) ) ;
#34976=CARTESIAN_POINT ( 'NONE',  ( -2.601141883200662974, -7.351091256667716678, 12.99064605035223252 ) ) ;
#34981=ORIENTED_EDGE ( 'NONE', *, *, #51450, .T. ) ;
#34982=( BOUNDED_SURFACE ( )  B_SPLINE_SURFACE ( 3, 1, ( 
 ( #7497, #60131 ),
 ( #36361, #12547 ),
 ( #31639, #50726 ),
 ( #46071, #3116 ) ),
 .UNSPECIFIED., .F., .F., .F. ) 
 B_SPLINE_SURFACE_WITH_KNOTS ( ( 4, 4 ),
 ( 2, 2 ),
 ( 0.000000000000000000, 1.000000000000000000 ),
 ( 0.000000000000000000, 1.000000000000000000 ),
 .UNSPECIFIED. ) 
 GEOMETRIC_REPRESENTATION_ITEM ( )  RATIONAL_B_SPLINE_SURFACE ( (
 ( 1.000000000000000000, 1.000000000000000000),
 ( 0.7211978278499968642, 0.9934217856018975334),
 ( 0.7211978278499968642, 0.9934217856018975334),
 ( 1.000000000000000000, 1.000000000000000000) ) ) 
 REPRESENTATION_ITEM ( '' )  SURFACE ( )  );
#34985=CARTESIAN_POINT ( 'NONE',  ( 0.5997462898726536595, 48.97040376101519144, -3.667585803694250135 ) ) ;
#34988=CARTESIAN_POINT ( 'NONE',  ( 0.6029443449137436017, -19.91765779110959755, 44.88681817749597514 ) ) ;
#34989=CARTESIAN_POINT ( 'NONE',  ( 0.8744876279028306332, -24.68559978112762110, 42.43785119236699188 ) ) ;
#35000=LINE ( 'NONE', #5520, #45836 ) ;
#35005=ORIENTED_EDGE ( 'NONE', *, *, #41056, .F. ) ;
#35011=ORIENTED_EDGE ( 'NONE', *, *, #1734, .T. ) ;
#35016=ORIENTED_EDGE ( 'NONE', *, *, #4988, .T. ) ;
#35018=CIRCLE ( 'NONE', #61011, 43.92652462719577500 ) ;
#35021=ORIENTED_EDGE ( 'NONE', *, *, #56283, .T. ) ;
#35025=DIRECTION ( 'NONE',  ( 0.09722883295013597105, 0.5755877901554996567, -0.8119391909909651206 ) ) ;
#35026=B_SPLINE_CURVE_WITH_KNOTS ( 'NONE', 3,
 ( #44449, #20311, #1478, #53784, #34719, #39433, #53186, #34112, #20612, #10290, #58485, #35343, #39126, #20915, #59112, #11524 ),
 .UNSPECIFIED., .F., .F.,
 ( 4, 3, 3, 3, 3, 4 ),
 ( 2.221635811791082109E-17, 0.0002612764279487725665, 0.0003919131003184764804, 0.0005225497727000608106, 0.0007837925190632426438, 0.001045051706266715216 ),
 .UNSPECIFIED. ) ;
#35028=CARTESIAN_POINT ( 'NONE',  ( 4.694002226626921015, 45.58690636503205695, 0.3445860007825484739 ) ) ;
#35035=VERTEX_POINT ( 'NONE', #31559 ) ;
#35039=VERTEX_POINT ( 'NONE', #22778 ) ;
#35045=B_SPLINE_CURVE_WITH_KNOTS ( 'NONE', 3,
 ( #59355, #6104, #30238, #44681, #34649, #11779 ),
 .UNSPECIFIED., .F., .F.,
 ( 4, 2, 4 ),
 ( 1.029992063861229212E-18, 0.0002293801035737119199, 0.0004587602071474228098 ),
 .UNSPECIFIED. ) ;
#35049=CARTESIAN_POINT ( 'NONE',  ( 4.553261556744875094, 31.39705178283641018, 30.72075365562384519 ) ) ;
#35057=CARTESIAN_POINT ( 'NONE',  ( 0.1129192098497447394, -38.68182264534125636, -21.22895156665819627 ) ) ;
#35062=CARTESIAN_POINT ( 'NONE',  ( 3.221118495291109163, 11.62016450294477998, 42.42326244628355880 ) ) ;
#35064=( BOUNDED_SURFACE ( )  B_SPLINE_SURFACE ( 3, 1, ( 
 ( #36990, #8141 ),
 ( #60746, #36671 ),
 ( #12869, #9064 ),
 ( #18473, #61060 ) ),
 .UNSPECIFIED., .F., .F., .F. ) 
 B_SPLINE_SURFACE_WITH_KNOTS ( ( 4, 4 ),
 ( 2, 2 ),
 ( 0.000000000000000000, 1.000000000000000000 ),
 ( 0.000000000000000000, 1.000000000000000000 ),
 .UNSPECIFIED. ) 
 GEOMETRIC_REPRESENTATION_ITEM ( )  RATIONAL_B_SPLINE_SURFACE ( (
 ( 1.000000000000000000, 1.000000000000000000),
 ( 0.7211978278499970862, 0.9934217856018976445),
 ( 0.7211978278499970862, 0.9934217856018976445),
 ( 1.000000000000000000, 1.000000000000000000) ) ) 
 REPRESENTATION_ITEM ( '' )  SURFACE ( )  );
#35065=CARTESIAN_POINT ( 'NONE',  ( 0.1145239942831223490, 20.69812692061546144, -38.96835925058644534 ) ) ;
#35066=CARTESIAN_POINT ( 'NONE',  ( 0.1129192098497455998, 30.02178898772931603, -32.33641869102712718 ) ) ;
#35070=CARTESIAN_POINT ( 'NONE',  ( 0.5549461598389363592, -22.10837605659374461, 38.16329917089240098 ) ) ;
#35080=CARTESIAN_POINT ( 'NONE',  ( -6.077587904424778920, -12.95044751835546393, 14.25068175450744157 ) ) ;
#35085=CARTESIAN_POINT ( 'NONE',  ( 0.5997462898726536595, 16.46871699354542429, -46.26373299606095202 ) ) ;
#35087=CARTESIAN_POINT ( 'NONE',  ( 0.2940133293163011974, 43.96669231856046878, 3.629120574337435734 ) ) ;
#35102=B_SPLINE_CURVE_WITH_KNOTS ( 'NONE', 3,
 ( #33907, #25103, #38928, #57980, #4728, #52983, #34516, #15102, #10398, #29489, #48598, #29799, #5961, #23874, #44245, #43005, #44553, #2201, #21030 ),
 .UNSPECIFIED., .F., .F.,
 ( 4, 3, 3, 3, 3, 3, 4 ),
 ( 8.674676106452504675E-19, 0.0002612768053151721427, 0.0003919133833142923349, 0.0005225499612322608619, 0.0006531865391693370427, 0.0008112755173415195321, 0.0009693688056799730068 ),
 .UNSPECIFIED. ) ;
#35108=CARTESIAN_POINT ( 'NONE',  ( 2.706805983486679779, -36.23450656517427149, -24.97672210875754928 ) ) ;
#35109=CARTESIAN_POINT ( 'NONE',  ( 2.648799415243696664, -34.24682227764476750, -35.09519379021880070 ) ) ;
#35110=CARTESIAN_POINT ( 'NONE',  ( -6.078457390727109555, 17.85037638348246958, -7.222089310270190410 ) ) ;
#35113=CARTESIAN_POINT ( 'NONE',  ( -6.078075953587585900, -18.27338415406079619, -6.072775790794155526 ) ) ;
#35114=CARTESIAN_POINT ( 'NONE',  ( -2.601141883200665639, -14.73982649082953600, -2.352220756992938089 ) ) ;
#35117=B_SPLINE_CURVE_WITH_KNOTS ( 'NONE', 3,
 ( #21602, #46053, #46656, #11922 ),
 .UNSPECIFIED., .F., .F.,
 ( 4, 4 ),
 ( 2.147596245779529078E-17, 0.004559932413162189405 ),
 .UNSPECIFIED. ) ;
#35127=CARTESIAN_POINT ( 'NONE',  ( 3.678834586032788234, 45.86476391165511046, 17.17660621183629033 ) ) ;
#35136=B_SPLINE_CURVE_WITH_KNOTS ( 'NONE', 3,
 ( #9213, #4485, #43370, #57413 ),
 .UNSPECIFIED., .F., .F.,
 ( 4, 4 ),
 ( 2.189128766608093472E-17, 0.004559932413162189405 ),
 .UNSPECIFIED. ) ;
#35139=CARTESIAN_POINT ( 'NONE',  ( 0.8744876279028306332, 40.65405044375329879, -27.52450240960324024 ) ) ;
#35142=CARTESIAN_POINT ( 'NONE',  ( 0.6000166863083090663, -45.32251430608251042, -18.91277818522175735 ) ) ;
#35143=CARTESIAN_POINT ( 'NONE',  ( 0.1152809850208375564, 36.85883374870061857, 24.25637353718406786 ) ) ;
#35144=ORIENTED_EDGE ( 'NONE', *, *, #19903, .F. ) ;
#35149=ADVANCED_FACE ( 'NONE', ( #28395 ), #48755, .F. ) ;
#35155=AXIS2_PLACEMENT_3D ( 'NONE', #29565, #23952, #58056 ) ;
#35158=CARTESIAN_POINT ( 'NONE',  ( 0.8753041380234530822, 21.91949880997755429, -43.93943445007425908 ) ) ;
#35161=ADVANCED_FACE ( 'NONE', ( #56588 ), #14739, .F. ) ;
#35162=CARTESIAN_POINT ( 'NONE',  ( 0.6026777506516368677, 11.09719736516042943, 47.83720938010385026 ) ) ;
#35178=CARTESIAN_POINT ( 'NONE',  ( 0.2940135542859015905, 43.44929869485245177, 7.641923293053564770 ) ) ;
#35184=VERTEX_POINT ( 'NONE', #24071 ) ;
#35187=CARTESIAN_POINT ( 'NONE',  ( 3.678748215320119197, 29.51641561576747463, 39.08188868896642987 ) ) ;
#35193=ORIENTED_EDGE ( 'NONE', *, *, #42260, .F. ) ;
#35198=FACE_OUTER_BOUND ( 'NONE', #20737, .T. ) ;
#35205=CARTESIAN_POINT ( 'NONE',  ( 4.553261556744873317, 31.71129487083125653, 30.39627186743183174 ) ) ;
#35206=CARTESIAN_POINT ( 'NONE',  ( 4.834790513006555379, 19.54670848745931266, 43.01761881172255642 ) ) ;
#35208=CARTESIAN_POINT ( 'NONE',  ( 5.901764892641288895, 35.14701960959055071, -34.09807149975986107 ) ) ;
#35216=CARTESIAN_POINT ( 'NONE',  ( -2.739355103387247858, 14.70078895384972384, -2.595066682262118896 ) ) ;
#35218=CARTESIAN_POINT ( 'NONE',  ( 0.6026777506516367566, 48.99513320406567374, -3.320137490087010423 ) ) ;
#35223=CARTESIAN_POINT ( 'NONE',  ( 0.7948878604505663636, 49.04591925934078489, 2.279572614469686620 ) ) ;
#35230=B_SPLINE_CURVE_WITH_KNOTS ( 'NONE', 3,
 ( #19526, #13916, #75, #28292, #47410, #42721 ),
 .UNSPECIFIED., .F., .F.,
 ( 4, 2, 4 ),
 ( 5.421010862427522170E-19, 0.0002293801035737092907, 0.0004587602071474180393 ),
 .UNSPECIFIED. ) ;
#35236=EDGE_CURVE ( 'NONE', #43286, #54532, #28766, .T. ) ;
#35248=VERTEX_POINT ( 'NONE', #56646 ) ;
#35250=CARTESIAN_POINT ( 'NONE',  ( 0.2940135542859002027, 34.10816074289976285, 27.97988419253970349 ) ) ;
#35252=B_SPLINE_CURVE_WITH_KNOTS ( 'NONE', 3,
 ( #56493, #45902, #39271, #61795 ),
 .UNSPECIFIED., .F., .F.,
 ( 4, 4 ),
 ( 0.000000000000000000, 0.004444103432399267029 ),
 .UNSPECIFIED. ) ;
#35262=ORIENTED_EDGE ( 'NONE', *, *, #47533, .T. ) ;
#35272=CARTESIAN_POINT ( 'NONE',  ( 4.694002226626921015, -30.90320716795002198, 33.51531826166802119 ) ) ;
#35273=CARTESIAN_POINT ( 'NONE',  ( 3.559346040607745287, 22.13704001167854329, 37.99186414304161019 ) ) ;
#35275=EDGE_CURVE ( 'NONE', #31849, #59478, #32872, .T. ) ;
#35279=CARTESIAN_POINT ( 'NONE',  ( -6.072942160501519027, 5.465015824218939500, 18.46450011048381867 ) ) ;
#35281=CARTESIAN_POINT ( 'NONE',  ( 0.5987334363312690755, 33.46066802764950410, -35.94365871214991870 ) ) ;
#35283=CARTESIAN_POINT ( 'NONE',  ( 0.3676999524040323597, 10.61898383218351860, -42.81574203134477585 ) ) ;
#35286=CARTESIAN_POINT ( 'NONE',  ( -6.077587904424778920, -1.842868750311569270, -19.16767738050324610 ) ) ;
#35288=CARTESIAN_POINT ( 'NONE',  ( 0.8744876279028306332, -35.88078294188929362, -33.50999053799506555 ) ) ;
#35290=CARTESIAN_POINT ( 'NONE',  ( 0.1129192098497455998, -32.03190746135001632, 30.34647742609778831 ) ) ;
#35296=EDGE_LOOP ( 'NONE', ( #24776, #6904, #57547, #40841 ) ) ;
#35299=CARTESIAN_POINT ( 'NONE',  ( 3.678748215320120085, -26.95178576869570364, -40.89271399867971013 ) ) ;
#35300=ORIENTED_EDGE ( 'NONE', *, *, #25562, .T. ) ;
#35301=CARTESIAN_POINT ( 'NONE',  ( 0.1156495703730067715, -22.75696492371722712, 37.80295624275665034 ) ) ;
#35321=VERTEX_POINT ( 'NONE', #14688 ) ;
#35336=CARTESIAN_POINT ( 'NONE',  ( 0.1152809850208375564, 39.85000777899687563, -18.94524115717834434 ) ) ;
#35341=VERTEX_POINT ( 'NONE', #44141 ) ;
#35342=DIRECTION ( 'NONE',  ( 0.09722883295013598492, 0.8933953294778579357, 0.4386243715416464628 ) ) ;
#35343=CARTESIAN_POINT ( 'NONE',  ( 0.6026777506516367566, -30.75401662176760453, -38.28494289228157044 ) ) ;
#35344=( BOUNDED_SURFACE ( )  B_SPLINE_SURFACE ( 3, 1, ( 
 ( #45700, #3062 ),
 ( #8373, #50984 ),
 ( #36610, #30965 ),
 ( #55063, #22191 ) ),
 .UNSPECIFIED., .F., .F., .F. ) 
 B_SPLINE_SURFACE_WITH_KNOTS ( ( 4, 4 ),
 ( 2, 2 ),
 ( 0.000000000000000000, 1.000000000000000000 ),
 ( 0.000000000000000000, 1.000000000000000000 ),
 .UNSPECIFIED. ) 
 GEOMETRIC_REPRESENTATION_ITEM ( )  RATIONAL_B_SPLINE_SURFACE ( (
 ( 1.000000000000000000, 1.000000000000000000),
 ( 0.7211978278499970862, 0.9934217856018976445),
 ( 0.7211978278499970862, 0.9934217856018976445),
 ( 1.000000000000000000, 1.000000000000000000) ) ) 
 REPRESENTATION_ITEM ( '' )  SURFACE ( )  );
#35345=CARTESIAN_POINT ( 'NONE',  ( -6.077587904424778920, 16.78120357693980935, 9.443898977818069085 ) ) ;
#35353=B_SPLINE_CURVE_WITH_KNOTS ( 'NONE', 3,
 ( #13860, #47979, #33273, #24467, #43292, #28538 ),
 .UNSPECIFIED., .F., .F.,
 ( 4, 2, 4 ),
 ( 6.345130535746553974E-19, 0.0002293801035737091281, 0.0004587602071474176598 ),
 .UNSPECIFIED. ) ;
#35355=VERTEX_POINT ( 'NONE', #57550 ) ;
#35357=CARTESIAN_POINT ( 'NONE',  ( 3.727782113643637096, 31.10430010538506806, 31.06928211047236132 ) ) ;
#35374=CARTESIAN_POINT ( 'NONE',  ( 0.6024113833632039894, 37.53342516667872530, -31.66676277042214949 ) ) ;
#35376=CARTESIAN_POINT ( 'NONE',  ( 0.1155031312995260795, 29.53975840367626660, 32.77719185629308640 ) ) ;
#35379=CARTESIAN_POINT ( 'NONE',  ( 1.657374760986086271, -21.77053621054746202, 38.30057702381891005 ) ) ;
#35394=B_SPLINE_CURVE_WITH_KNOTS ( 'NONE', 3,
 ( #37141, #37447, #46848, #50582, #21789, #50895 ),
 .UNSPECIFIED., .F., .F.,
 ( 4, 2, 4 ),
 ( 2.224043620450102089E-17, 0.0002293755540694315353, 0.0004587511081388407903 ),
 .UNSPECIFIED. ) ;
#35396=ORIENTED_EDGE ( 'NONE', *, *, #44180, .F. ) ;
#35397=CARTESIAN_POINT ( 'NONE',  ( 4.975610109902397937, 25.84633036597884725, -41.52609557555889808 ) ) ;
#35398=CARTESIAN_POINT ( 'NONE',  ( 4.834790513006553603, -42.36901421273557133, -20.91544825160086418 ) ) ;
#35401=CARTESIAN_POINT ( 'NONE',  ( 4.553261556744875094, 35.33793455049291765, -26.09156851415253087 ) ) ;
#35406=CARTESIAN_POINT ( 'NONE',  ( 0.1156495703730067437, 20.52988295744289360, 39.05722543889626763 ) ) ;
#35407=EDGE_LOOP ( 'NONE', ( #3318, #48622, #12018, #6182 ) ) ;
#35409=ORIENTED_EDGE ( 'NONE', *, *, #17821, .F. ) ;
#35412=ORIENTED_EDGE ( 'NONE', *, *, #39784, .T. ) ;
#35421=CARTESIAN_POINT ( 'NONE',  ( -6.072942160501519915, 15.44092479507863835, 11.50573786255126763 ) ) ;
#35422=EDGE_LOOP ( 'NONE', ( #9406, #1136, #30188, #47098 ) ) ;
#35424=CARTESIAN_POINT ( 'NONE',  ( 0.3676999524040323597, -38.83470403830501994, 20.92406140260764857 ) ) ;
#35425=( BOUNDED_SURFACE ( )  B_SPLINE_SURFACE ( 3, 1, ( 
 ( #11315, #29483 ),
 ( #48593, #39854 ),
 ( #25718, #34511 ),
 ( #49211, #44856 ) ),
 .UNSPECIFIED., .F., .F., .F. ) 
 B_SPLINE_SURFACE_WITH_KNOTS ( ( 4, 4 ),
 ( 2, 2 ),
 ( 0.000000000000000000, 1.000000000000000000 ),
 ( 0.000000000000000000, 1.000000000000000000 ),
 .UNSPECIFIED. ) 
 GEOMETRIC_REPRESENTATION_ITEM ( )  RATIONAL_B_SPLINE_SURFACE ( (
 ( 1.000000000000000000, 1.000000000000000000),
 ( 0.9953485035131437453, 0.8621029689291515030),
 ( 0.9953485035131437453, 0.8621029689291515030),
 ( 1.000000000000000000, 1.000000000000000000) ) ) 
 REPRESENTATION_ITEM ( '' )  SURFACE ( )  );
#35428=CARTESIAN_POINT ( 'NONE',  ( 3.678748215320120085, 38.46437741425435064, 30.31673604518275411 ) ) ;
#35433=CARTESIAN_POINT ( 'NONE',  ( -6.078457390727109555, -14.66526260008077287, 12.47896565858644990 ) ) ;
#35437=CARTESIAN_POINT ( 'NONE',  ( 4.834790513006555379, -44.69577334950041347, 15.32570342967882127 ) ) ;
#35441=CARTESIAN_POINT ( 'NONE',  ( 4.553261556744875094, -43.15908619232990873, 8.175135770534621926 ) ) ;
#35455=CARTESIAN_POINT ( 'NONE',  ( 2.299652685299201416, 15.71955970131786984, 46.44542138526527708 ) ) ;
#35458=CARTESIAN_POINT ( 'NONE',  ( 2.299652685299202748, 48.99838078751366766, -1.854832892733276672 ) ) ;
#35459=CARTESIAN_POINT ( 'NONE',  ( 0.3676999524040366896, -42.45338881270437525, 11.98584004733023534 ) ) ;
#35460=ORIENTED_EDGE ( 'NONE', *, *, #56995, .F. ) ;
#35461=EDGE_CURVE ( 'NONE', #12356, #2992, #10190, .T. ) ;
#35464=VECTOR ( 'NONE', #40621, 1000.000000000000114 ) ;
#35473=CARTESIAN_POINT ( 'NONE',  ( 0.6016117650947688800, 11.26679697061805641, 47.79759764117200405 ) ) ;
#35476=CARTESIAN_POINT ( 'NONE',  ( 0.8753041380234524160, -20.68664920503281834, -44.53314352862253145 ) ) ;
#35479=ADVANCED_FACE ( 'NONE', ( #59730 ), #2264, .F. ) ;
#35486=CARTESIAN_POINT ( 'NONE',  ( 0.1139756605157204172, 43.23286577299607814, -8.824655049866100498 ) ) ;
#35496=CARTESIAN_POINT ( 'NONE',  ( 4.975610109902397937, -27.50982196586606321, 40.44328253918227034 ) ) ;
#35498=CARTESIAN_POINT ( 'NONE',  ( 2.706805983486680223, -42.95931102688237502, -9.553727514187235315 ) ) ;
#35500=CARTESIAN_POINT ( 'NONE',  ( 0.5987334363312688534, 46.41165631110268919, 16.04746288147003952 ) ) ;
#35504=EDGE_LOOP ( 'NONE', ( #20304, #39940, #4617, #49538 ) ) ;
#35511=CARTESIAN_POINT ( 'NONE',  ( 1.657374760986086493, -41.28420722619999594, -15.37870868949730685 ) ) ;
#35519=CARTESIAN_POINT ( 'NONE',  ( 0.5997462898726536595, 44.01516392039482639, 21.77652348757905898 ) ) ;
#35525=CARTESIAN_POINT ( 'NONE',  ( 4.975610109902397937, 0.000000000000000000, 0.000000000000000000 ) ) ;
#35526=CARTESIAN_POINT ( 'NONE',  ( 5.901764892641307547, 45.37424261077610055, 18.41655708698313632 ) ) ;
#35533=CARTESIAN_POINT ( 'NONE',  ( 0.6029442701453590070, 16.87823742969306551, -46.11583596146973463 ) ) ;
#35538=CARTESIAN_POINT ( 'NONE',  ( 0.6039202388192953519, -30.48176006895493728, 38.50228585353934108 ) ) ;
#35540=FACE_OUTER_BOUND ( 'NONE', #8296, .T. ) ;
#35545=ORIENTED_EDGE ( 'NONE', *, *, #14785, .T. ) ;
#35564=ORIENTED_EDGE ( 'NONE', *, *, #58455, .T. ) ;
#35569=AXIS2_PLACEMENT_3D ( 'NONE', #32730, #3881, #35669 ) ;
#35572=CARTESIAN_POINT ( 'NONE',  ( 0.6027444965799114707, -35.36702213964480279, 34.06922747673207397 ) ) ;
#35578=CARTESIAN_POINT ( 'NONE',  ( -2.739355103387248747, 3.064916856561631597, -14.61005994557795695 ) ) ;
#35582=CARTESIAN_POINT ( 'NONE',  ( -2.739355103387247858, 12.36564479942402350, 8.362917890634497198 ) ) ;
#35585=B_SPLINE_CURVE_WITH_KNOTS ( 'NONE', 3,
 ( #59893, #40515, #45516, #30768, #16373, #44910, #2252, #50803, #54553, #36425, #22313, #7893, #3185, #54875, #45217, #49887, #45830, #41442, #21688, #12011, #27012, #46137, #17613, #36124, #40832 ),
 .UNSPECIFIED., .F., .F.,
 ( 4, 3, 3, 3, 3, 3, 3, 3, 4 ),
 ( 4.670885906470169154E-18, 0.0005656085177311400737, 0.001131215744874499406, 0.001696821861372765699, 0.002262427090022497717, 0.002828031679238745058, 0.003393635864401603995, 0.003977030878808130755, 0.004561030005651157265 ),
 .UNSPECIFIED. ) ;
#35590=CARTESIAN_POINT ( 'NONE',  ( 1.830465331921976802, 36.22942041522664169, 25.05604023494431942 ) ) ;
#35591=CARTESIAN_POINT ( 'NONE',  ( -6.078075953587585900, -19.21681836813551314, 1.228440496412283478 ) ) ;
#35594=CARTESIAN_POINT ( 'NONE',  ( 0.6024113833632039894, 41.27473200771225237, -26.60711120720173639 ) ) ;
#35607=( BOUNDED_SURFACE ( )  B_SPLINE_SURFACE ( 3, 1, ( 
 ( #40282, #25520 ),
 ( #16756, #54623 ),
 ( #36182, #11435 ),
 ( #20835, #2631 ) ),
 .UNSPECIFIED., .F., .F., .F. ) 
 B_SPLINE_SURFACE_WITH_KNOTS ( ( 4, 4 ),
 ( 2, 2 ),
 ( 0.000000000000000000, 1.000000000000000000 ),
 ( 0.000000000000000000, 1.000000000000000000 ),
 .UNSPECIFIED. ) 
 GEOMETRIC_REPRESENTATION_ITEM ( )  RATIONAL_B_SPLINE_SURFACE ( (
 ( 1.000000000000000000, 1.000000000000000000),
 ( 0.9953485035131437453, 0.8621029689291515030),
 ( 0.9953485035131437453, 0.8621029689291515030),
 ( 1.000000000000000000, 1.000000000000000000) ) ) 
 REPRESENTATION_ITEM ( '' )  SURFACE ( )  );
#35608=EDGE_CURVE ( 'NONE', #57221, #52094, #22182, .T. ) ;
#35617=CARTESIAN_POINT ( 'NONE',  ( 0.1119898979215352836, -42.82020512811597968, -10.64853703744787339 ) ) ;
#35620=CARTESIAN_POINT ( 'NONE',  ( 4.553261556744873317, 43.92594400279101308, -0.2258523573157051323 ) ) ;
#35624=ORIENTED_EDGE ( 'NONE', *, *, #18545, .T. ) ;
#35626=CARTESIAN_POINT ( 'NONE',  ( 4.975610109902397937, 42.89797504594920241, 23.49921581872238718 ) ) ;
#35629=EDGE_LOOP ( 'NONE', ( #45286, #27428, #3916, #4087 ) ) ;
#35631=FACE_OUTER_BOUND ( 'NONE', #27292, .T. ) ;
#35634=ADVANCED_FACE ( 'NONE', ( #18071 ), #27531, .F. ) ;
#35635=CARTESIAN_POINT ( 'NONE',  ( 0.1129192098497447394, 33.28205046155626690, -28.96993104685574139 ) ) ;
#35639=CARTESIAN_POINT ( 'NONE',  ( 0.1368894036331272379, -6.411983869493682597, 43.65487130642680569 ) ) ;
#35647=CARTESIAN_POINT ( 'NONE',  ( 4.553261556744875094, 0.000000000000000000, 0.000000000000000000 ) ) ;
#35659=FACE_OUTER_BOUND ( 'NONE', #14367, .T. ) ;
#35662=B_SPLINE_CURVE_WITH_KNOTS ( 'NONE', 3,
 ( #25758, #20757, #39892, #45207 ),
 .UNSPECIFIED., .F., .F.,
 ( 4, 4 ),
 ( 2.096810281905421196E-17, 0.004559932413162185935 ),
 .UNSPECIFIED. ) ;
#35669=DIRECTION ( 'NONE',  ( 0.000000000000000000, 0.000000000000000000, 1.000000000000000000 ) ) ;
#35670=CARTESIAN_POINT ( 'NONE',  ( 0.5997462898726536595, -45.71211507932792273, 17.94308126043545215 ) ) ;
#35672=EDGE_CURVE ( 'NONE', #13219, #14899, #32476, .T. ) ;
#35674=EDGE_CURVE ( 'NONE', #29310, #6759, #18688, .T. ) ;
#35675=DIRECTION ( 'NONE',  ( -0.000000000000000000, 0.000000000000000000, 1.000000000000000000 ) ) ;
#35677=EDGE_CURVE ( 'NONE', #43965, #5254, #37498, .T. ) ;
#35683=FACE_OUTER_BOUND ( 'NONE', #3851, .T. ) ;
#35685=CARTESIAN_POINT ( 'NONE',  ( 0.5997462898726536595, -19.39900779840473888, 45.11352487427402025 ) ) ;
#35689=CARTESIAN_POINT ( 'NONE',  ( 2.299652685299202748, -36.10726366766370887, 33.17449676019164428 ) ) ;
#35701=AXIS2_PLACEMENT_3D ( 'NONE', #60575, #27083, #12694 ) ;
#35703=LINE ( 'NONE', #12505, #43257 ) ;
#35705=VECTOR ( 'NONE', #35342, 999.9999999999998863 ) ;
#35719=FACE_OUTER_BOUND ( 'NONE', #18997, .T. ) ;
#35731=CARTESIAN_POINT ( 'NONE',  ( 0.5980271706414711508, 41.53842981737997775, -26.20320764998554353 ) ) ;
#35734=ORIENTED_EDGE ( 'NONE', *, *, #3125, .F. ) ;
#35736=DIRECTION ( 'NONE',  ( -0.1011922191286467598, 0.9849719771322121842, 0.1399654923617988100 ) ) ;
#35738=ORIENTED_EDGE ( 'NONE', *, *, #23694, .F. ) ;
#35739=ORIENTED_EDGE ( 'NONE', *, *, #34044, .F. ) ;
#35744=CARTESIAN_POINT ( 'NONE',  ( -6.078075953587585900, -16.14115596471627612, -10.50039324834266452 ) ) ;
#35745=FACE_OUTER_BOUND ( 'NONE', #56150, .T. ) ;
#35750=VERTEX_POINT ( 'NONE', #34634 ) ;
#35761=CARTESIAN_POINT ( 'NONE',  ( 0.1145239942831223490, -35.55610539828845162, 26.12869781696891636 ) ) ;
#35768=AXIS2_PLACEMENT_3D ( 'NONE', #61827, #9532, #23644 ) ;
#35772=CARTESIAN_POINT ( 'NONE',  ( 0.8744876279028263033, -19.05609938968970241, -45.24616145519706834 ) ) ;
#35774=CARTESIAN_POINT ( 'NONE',  ( 3.050102900204245682, -42.05946948370080207, 12.90063083448639247 ) ) ;
#35780=CARTESIAN_POINT ( 'NONE',  ( 0.1129192098497455998, 3.754263797494300725, 43.96427289429426821 ) ) ;
#35786=VECTOR ( 'NONE', #14756, 1000.000000000000114 ) ;
#35789=CARTESIAN_POINT ( 'NONE',  ( 0.1129192098497447394, 44.06201484046244587, 2.343210614524684487 ) ) ;
#35797=EDGE_CURVE ( 'NONE', #54460, #16494, #53771, .T. ) ;
#35803=ORIENTED_EDGE ( 'NONE', *, *, #22859, .F. ) ;
#35804=ORIENTED_EDGE ( 'NONE', *, *, #3340, .T. ) ;
#35809=ORIENTED_EDGE ( 'NONE', *, *, #17507, .T. ) ;
#35811=CARTESIAN_POINT ( 'NONE',  ( 0.5997462898726536595, -48.63480578518805686, 6.797594896825438049 ) ) ;
#35812=CARTESIAN_POINT ( 'NONE',  ( 4.060580049360325461, 7.510230244653757659, -43.30201076198999033 ) ) ;
#35816=ORIENTED_EDGE ( 'NONE', *, *, #32130, .F. ) ;
#35818=CARTESIAN_POINT ( 'NONE',  ( 4.975610109902397937, -16.35148546628954236, 46.09857188876348744 ) ) ;
#35819=CARTESIAN_POINT ( 'NONE',  ( 1.657374760986086271, 42.18470164349173501, 12.70202324442172426 ) ) ;
#35824=CARTESIAN_POINT ( 'NONE',  ( 0.3676999524040366896, -13.34038000160327364, -42.04741186726791113 ) ) ;
#35825=CARTESIAN_POINT ( 'NONE',  ( 4.975610109902397937, 20.32389311291169065, 44.49032227207074186 ) ) ;
#35827=CARTESIAN_POINT ( 'NONE',  ( -6.057079549204054558, -12.94019084496092731, 14.26123038155291312 ) ) ;
#35834=CARTESIAN_POINT ( 'NONE',  ( 3.678748215320121862, 44.89637374983790608, 19.56855739226451263 ) ) ;
#35837=CARTESIAN_POINT ( 'NONE',  ( -6.078075953587585900, -4.279696274496966879, 18.77443405392537201 ) ) ;
#35839=CARTESIAN_POINT ( 'NONE',  ( 0.5997462898726536595, 48.29911994996563607, 8.873930482212578852 ) ) ;
#35846=CARTESIAN_POINT ( 'NONE',  ( 0.5997462898726536595, 44.46857747280011353, 20.83500054451363326 ) ) ;
#35851=ORIENTED_EDGE ( 'NONE', *, *, #27426, .T. ) ;
#35855=CARTESIAN_POINT ( 'NONE',  ( 0.8753041380234465318, 46.87455897190349674, -14.62580080072613775 ) ) ;
#35861=CARTESIAN_POINT ( 'NONE',  ( 0.2285344041767098100, 43.97331108839381386, -3.584561649462690625 ) ) ;
#35868=ORIENTED_EDGE ( 'NONE', *, *, #51133, .F. ) ;
#35870=CARTESIAN_POINT ( 'NONE',  ( 0.6008122571543326185, -7.407407791708222611, 48.54569867941606276 ) ) ;
#35880=CARTESIAN_POINT ( 'NONE',  ( -6.063463321072276813, 18.63085535290907302, 4.869464169541593890 ) ) ;
#35882=EDGE_CURVE ( 'NONE', #54794, #60972, #38081, .T. ) ;
#35889=B_SPLINE_CURVE_WITH_KNOTS ( 'NONE', 3,
 ( #18756, #56941, #33162, #52238, #47565, #4604 ),
 .UNSPECIFIED., .F., .F.,
 ( 4, 2, 4 ),
 ( 5.421010862427522170E-19, 0.0002293801035737093178, 0.0004587602071474180935 ),
 .UNSPECIFIED. ) ;
#35896=FACE_OUTER_BOUND ( 'NONE', #35629, .T. ) ;
#35899=CARTESIAN_POINT ( 'NONE',  ( 0.5997462898726536595, -14.47257175146244457, -46.92649887902442885 ) ) ;
#35912=CARTESIAN_POINT ( 'NONE',  ( 1.834102595619085507, 36.18890472896515575, -25.11097209140993414 ) ) ;
#35914=CARTESIAN_POINT ( 'NONE',  ( 4.553261556744875094, 0.000000000000000000, 0.000000000000000000 ) ) ;
#35919=VECTOR ( 'NONE', #34963, 1000.000000000000114 ) ;
#35924=DIRECTION ( 'NONE',  ( 0.000000000000000000, 8.881784197001252323E-16, 1.000000000000000000 ) ) ;
#35931=DIRECTION ( 'NONE',  ( -1.000000000000000000, -0.000000000000000000, -0.000000000000000000 ) ) ;
#35933=ORIENTED_EDGE ( 'NONE', *, *, #34113, .F. ) ;
#35934=EDGE_CURVE ( 'NONE', #40399, #50810, #18649, .T. ) ;
#35936=EDGE_LOOP ( 'NONE', ( #28291, #41360, #5068, #10292 ) ) ;
#35938=CARTESIAN_POINT ( 'NONE',  ( -6.078075953587585900, 9.977648803906024710, -16.46941706901153779 ) ) ;
#35943=CARTESIAN_POINT ( 'NONE',  ( 0.1129192098497447394, 29.30421273086510681, -32.98810246148386227 ) ) ;
#35949=CARTESIAN_POINT ( 'NONE',  ( 0.1129192098497447394, -6.563350895509266536, 43.63340707310824484 ) ) ;
#35958=CARTESIAN_POINT ( 'NONE',  ( 0.1135584504625008762, 39.94012421351568776, -18.75469354439548653 ) ) ;
#35971=CARTESIAN_POINT ( 'NONE',  ( 4.975610109902397937, 45.11887670192763267, -18.88746601040027784 ) ) ;
#35978=CARTESIAN_POINT ( 'NONE',  ( 0.6029442701453591180, 33.07943709324084836, 36.29457351660987285 ) ) ;
#35981=LINE ( 'NONE', #46297, #23805 ) ;
#35982=ORIENTED_EDGE ( 'NONE', *, *, #55697, .F. ) ;
#35989=CARTESIAN_POINT ( 'NONE',  ( 0.6024113833632039894, 44.14939292512354285, 21.50285965735530169 ) ) ;
#35991=EDGE_CURVE ( 'NONE', #16981, #35341, #38274, .T. ) ;
#35992=LINE ( 'NONE', #60073, #10709 ) ;
#35994=CARTESIAN_POINT ( 'NONE',  ( 0.6008122571543325074, 5.148691493768951410, 48.83692789649354182 ) ) ;
#35995=CARTESIAN_POINT ( 'NONE',  ( 0.1145239942831223490, -12.24112153461662444, -42.39222127088197567 ) ) ;
#36000=CARTESIAN_POINT ( 'NONE',  ( 4.975610109902397937, -36.86873347511144772, 32.14258700041067840 ) ) ;
#36005=PRODUCT_DEFINITION ( 'UNKNOWN', '', #48888, #39874 ) ;
#36018=CARTESIAN_POINT ( 'NONE',  ( 0.5997462898726536595, -47.63132954987522538, -11.95023328037962251 ) ) ;
#36020=B_SPLINE_CURVE_WITH_KNOTS ( 'NONE', 3,
 ( #47102, #12668, #31767, #3229, #41487, #4148 ),
 .UNSPECIFIED., .F., .F.,
 ( 4, 2, 4 ),
 ( 2.235140038340936352E-18, 0.0002447193893791689491, 0.0004894387787583368140 ),
 .UNSPECIFIED. ) ;
#36022=ORIENTED_EDGE ( 'NONE', *, *, #20584, .T. ) ;
#36026=ADVANCED_FACE ( 'NONE', ( #43913 ), #18767, .F. ) ;
#36043=CARTESIAN_POINT ( 'NONE',  ( -2.739355103387247858, -6.282164585817087143, 13.54186010368304593 ) ) ;
#36048=CARTESIAN_POINT ( 'NONE',  ( 3.221118495291109163, 6.099796721976346703, 43.56092170297041122 ) ) ;
#36052=ORIENTED_EDGE ( 'NONE', *, *, #4404, .F. ) ;
#36056=VERTEX_POINT ( 'NONE', #15385 ) ;
#36058=CARTESIAN_POINT ( 'NONE',  ( 1.834102595619085507, -34.50568523712564684, 27.37800999295042814 ) ) ;
#36059=B_SPLINE_CURVE_WITH_KNOTS ( 'NONE', 3,
 ( #31740, #59299, #41159, #22035, #54905, #50525 ),
 .UNSPECIFIED., .F., .F.,
 ( 4, 2, 4 ),
 ( 0.000000000000000000, 0.0002447195606305744208, 0.0004894391212611488417 ),
 .UNSPECIFIED. ) ;
#36062=ORIENTED_EDGE ( 'NONE', *, *, #56434, .F. ) ;
#36066=B_SPLINE_CURVE_WITH_KNOTS ( 'NONE', 3,
 ( #21275, #40113, #20969, #1842 ),
 .UNSPECIFIED., .F., .F.,
 ( 4, 4 ),
 ( 0.000000000000000000, 0.005013413432710138971 ),
 .UNSPECIFIED. ) ;
#36067=( NAMED_UNIT ( * ) PLANE_ANGLE_UNIT ( ) SI_UNIT ( $, .RADIAN. ) );
#36072=CARTESIAN_POINT ( 'NONE',  ( 0.1119899015040013712, 20.90518409856474946, -38.85787675616901993 ) ) ;
#36073=CARTESIAN_POINT ( 'NONE',  ( 0.9268187852002115479, -8.013537751244687257, -43.35363359186865040 ) ) ;
#36078=CARTESIAN_POINT ( 'NONE',  ( 4.834790513006555379, 24.88720127704534235, 40.16486715427070209 ) ) ;
#36079=CARTESIAN_POINT ( 'NONE',  ( 0.3676999524040366896, 43.13409918076302318, -9.241215893319285613 ) ) ;
#36081=DIRECTION ( 'NONE',  ( -1.000000000000000000, -0.000000000000000000, -0.000000000000000000 ) ) ;
#36083=CARTESIAN_POINT ( 'NONE',  ( -6.079354080745853928, -11.01762705387090868, 15.79255677051609830 ) ) ;
#36085=CARTESIAN_POINT ( 'NONE',  ( 1.112077966505211624, -2.461812912967866307, -44.01101910101717607 ) ) ;
#36090=CARTESIAN_POINT ( 'NONE',  ( 0.6029443199889047422, 44.24423630359484605, -21.30692835126788509 ) ) ;
#36094=CARTESIAN_POINT ( 'NONE',  ( 1.830465331921979022, 40.20755377393447105, -17.99246162687467532 ) ) ;
#36095=( BOUNDED_SURFACE ( )  B_SPLINE_SURFACE ( 3, 1, ( 
 ( #37255, #46966 ),
 ( #28139, #27836 ),
 ( #13138, #41345 ),
 ( #9031, #55704 ) ),
 .UNSPECIFIED., .F., .F., .F. ) 
 B_SPLINE_SURFACE_WITH_KNOTS ( ( 4, 4 ),
 ( 2, 2 ),
 ( 0.000000000000000000, 1.000000000000000000 ),
 ( 0.000000000000000000, 1.000000000000000000 ),
 .UNSPECIFIED. ) 
 GEOMETRIC_REPRESENTATION_ITEM ( )  RATIONAL_B_SPLINE_SURFACE ( (
 ( 1.000000000000000000, 1.000000000000000000),
 ( 0.7211978278499968642, 0.9934217856018975334),
 ( 0.7211978278499968642, 0.9934217856018975334),
 ( 1.000000000000000000, 1.000000000000000000) ) ) 
 REPRESENTATION_ITEM ( '' )  SURFACE ( )  );
#36106=CARTESIAN_POINT ( 'NONE',  ( 0.1365634738349418842, -13.16346314626551539, 42.11396273945445046 ) ) ;
#36113=EDGE_CURVE ( 'NONE', #26582, #6528, #15788, .T. ) ;
#36114=B_SPLINE_CURVE_WITH_KNOTS ( 'NONE', 3,
 ( #52977, #8840, #13552, #32662, #27954, #47993 ),
 .UNSPECIFIED., .F., .F.,
 ( 4, 2, 4 ),
 ( 2.528804606065167438E-17, 0.0002293755540694318877, 0.0004587511081388384593 ),
 .UNSPECIFIED. ) ;
#36117=ORIENTED_EDGE ( 'NONE', *, *, #59880, .T. ) ;
#36119=ADVANCED_FACE ( 'NONE', ( #20085 ), #36341, .F. ) ;
#36121=CARTESIAN_POINT ( 'NONE',  ( 0.08486401232817714080, 12.80000000000000071, -3.000000000000000000 ) ) ;
#36124=CARTESIAN_POINT ( 'NONE',  ( 0.5549461598389365813, 14.40543502832328926, -41.68574261197179709 ) ) ;
#36125=ORIENTED_EDGE ( 'NONE', *, *, #26293, .F. ) ;
#36128=CARTESIAN_POINT ( 'NONE',  ( 4.553261556744875094, 7.233533384971297941, -43.32684572631779218 ) ) ;
#36131=ORIENTED_EDGE ( 'NONE', *, *, #39922, .F. ) ;
#36137=CARTESIAN_POINT ( 'NONE',  ( 1.296416391601052487, -13.60092540267492467, -41.92042702868174331 ) ) ;
#36140=CARTESIAN_POINT ( 'NONE',  ( 0.3676999524040323597, 43.44964275340426951, -7.620966337964178550 ) ) ;
#36143=CARTESIAN_POINT ( 'NONE',  ( -6.057079549204054558, 5.487289185789611778, -18.45862639773758573 ) ) ;
#36144=CARTESIAN_POINT ( 'NONE',  ( 1.112077966505211402, 41.49149550466378855, -14.88240994983740251 ) ) ;
#36145=CARTESIAN_POINT ( 'NONE',  ( 0.7948884756798504370, 17.76850134148177318, -45.77094061386453916 ) ) ;
#36150=CARTESIAN_POINT ( 'NONE',  ( 0.5997462898726536595, 16.46871699354475993, 46.26373299606117229 ) ) ;
#36153=ORIENTED_EDGE ( 'NONE', *, *, #6897, .F. ) ;
#36155=CARTESIAN_POINT ( 'NONE',  ( 2.706805983486679779, 2.574964235114478583, -43.93342318221557719 ) ) ;
#36158=ORIENTED_EDGE ( 'NONE', *, *, #23975, .T. ) ;
#36159=CARTESIAN_POINT ( 'NONE',  ( 0.6039202388192952409, -30.75412344224365313, 38.28508331123533992 ) ) ;
#36164=B_SPLINE_CURVE_WITH_KNOTS ( 'NONE', 3,
 ( #54447, #21270, #49773, #6833, #25974, #18122, #14052, #36941, #17504, #47553, #51000, #56929, #46953, #9321, #41629, #61616 ),
 .UNSPECIFIED., .F., .F.,
 ( 4, 3, 3, 3, 3, 4 ),
 ( 1.868480190406682863E-17, 0.0002612764279487719702, 0.0003919131003184807630, 0.0005225497727000651474, 0.0007837925190632448122, 0.001045051706266717602 ),
 .UNSPECIFIED. ) ;
#36170=CARTESIAN_POINT ( 'NONE',  ( 4.553261556744875094, 17.98701270972463817, -40.07501640179128799 ) ) ;
#36171=B_SPLINE_CURVE_WITH_KNOTS ( 'NONE', 3,
 ( #28319, #38365, #19555, #99 ),
 .UNSPECIFIED., .F., .F.,
 ( 4, 4 ),
 ( 0.000000000000000000, 0.005013413432710145910 ),
 .UNSPECIFIED. ) ;
#36172=CARTESIAN_POINT ( 'NONE',  ( -6.078457390727109555, 16.78028475769486505, -9.445451523785473924 ) ) ;
#36177=CARTESIAN_POINT ( 'NONE',  ( -6.078457390727109555, 0.6215653986403898434, -19.24599094597939342 ) ) ;
#36180=CARTESIAN_POINT ( 'NONE',  ( -6.078726893082806448, 9.985094725776210822, 16.46486940689163703 ) ) ;
#36182=CARTESIAN_POINT ( 'NONE',  ( -6.078457390727109555, 15.43466132010190961, -11.51371968441379856 ) ) ;
#36184=EDGE_CURVE ( 'NONE', #17426, #10554, #17851, .T. ) ;
#36186=CARTESIAN_POINT ( 'NONE',  ( 4.975610109902397937, -22.11219452748616021, 43.62912170003406942 ) ) ;
#36189=CIRCLE ( 'NONE', #45189, 48.91267123290010943 ) ;
#36190=CARTESIAN_POINT ( 'NONE',  ( 0.1135584504625007096, -31.39461082923043023, -31.00532959051426829 ) ) ;
#36194=CARTESIAN_POINT ( 'NONE',  ( -4.915099999999998914, 0.000000000000000000, 0.000000000000000000 ) ) ;
#36198=CARTESIAN_POINT ( 'NONE',  ( 4.834790513006555379, 38.14091330549777581, 27.89014293880336481 ) ) ;
#36205=CARTESIAN_POINT ( 'NONE',  ( 5.901764892641307547, 47.35677775444503368, 12.46302804922537177 ) ) ;
#36206=CARTESIAN_POINT ( 'NONE',  ( 1.657374760986086493, -32.49590154289041521, -29.74738358523344672 ) ) ;
#36209=EDGE_LOOP ( 'NONE', ( #33161, #17437, #50307, #10297 ) ) ;
#36212=CARTESIAN_POINT ( 'NONE',  ( 0.8744876279028306332, 32.34273794994798834, -36.93639603806098393 ) ) ;
#36214=CARTESIAN_POINT ( 'NONE',  ( 0.1145239942831223490, 44.05326557292652723, -2.501054390828159502 ) ) ;
#36220=CARTESIAN_POINT ( 'NONE',  ( 3.559346040607745287, 35.69064246342631463, -25.68284100503404588 ) ) ;
#36221=B_SPLINE_CURVE_WITH_KNOTS ( 'NONE', 3,
 ( #61956, #34418, #43520, #4953, #19391, #53489 ),
 .UNSPECIFIED., .F., .F.,
 ( 4, 2, 4 ),
 ( 2.223916437056137064E-17, 0.0002293755540694324298, 0.0004587511081388426335 ),
 .UNSPECIFIED. ) ;
#36223=CARTESIAN_POINT ( 'NONE',  ( 0.6000166863083106206, -42.53190469623940118, 24.55321902762372588 ) ) ;
#36227=CARTESIAN_POINT ( 'NONE',  ( 2.009741617377216460, -19.07132956818588809, -39.69620216248254252 ) ) ;
#36229=CARTESIAN_POINT ( 'NONE',  ( 4.975610109902397937, 38.85236532789286201, -29.71435874397630528 ) ) ;
#36237=DIRECTION ( 'NONE',  ( 1.000000000000000000, 0.000000000000000000, 0.000000000000000000 ) ) ;
#36254=CARTESIAN_POINT ( 'NONE',  ( 2.648799415243708655, -44.91402171431691670, 19.67862080369118161 ) ) ;
#36259=VERTEX_POINT ( 'NONE', #57560 ) ;
#36261=CARTESIAN_POINT ( 'NONE',  ( 4.553261556744873317, -20.51767157960462384, -38.84024612145397981 ) ) ;
#36262=ORIENTED_EDGE ( 'NONE', *, *, #38380, .F. ) ;
#36268=CARTESIAN_POINT ( 'NONE',  ( 0.6008122571543327295, -48.75817579134915292, -5.847635758595932209 ) ) ;
#36271=CARTESIAN_POINT ( 'NONE',  ( 0.1158403557922069033, -27.48134092720074051, -34.52124285171061047 ) ) ;
#36278=CARTESIAN_POINT ( 'NONE',  ( -2.601141883200662974, -14.91960803315171269, 0.4480218817239753903 ) ) ;
#36299=CARTESIAN_POINT ( 'NONE',  ( 5.901764892641307547, -10.85461099010599106, -47.75111399426351255 ) ) ;
#36301=B_SPLINE_CURVE_WITH_KNOTS ( 'NONE', 3,
 ( #32838, #47234, #24032, #14041 ),
 .UNSPECIFIED., .F., .F.,
 ( 4, 4 ),
 ( 0.000000000000000000, 0.005013413432710142441 ),
 .UNSPECIFIED. ) ;
#36308=SURFACE_SIDE_STYLE ('',( #16253 ) ) ;
#36312=LINE ( 'NONE', #25345, #57653 ) ;
#36320=VERTEX_POINT ( 'NONE', #23160 ) ;
#36322=CARTESIAN_POINT ( 'NONE',  ( 0.8753041380234530822, -35.88662119133316963, -33.51550010581278372 ) ) ;
#36332=CARTESIAN_POINT ( 'NONE',  ( 1.830465331921977912, -44.03239073142495386, -1.234755989461712389 ) ) ;
#36333=ORIENTED_EDGE ( 'NONE', *, *, #53158, .F. ) ;
#36335=ORIENTED_EDGE ( 'NONE', *, *, #35674, .T. ) ;
#36337=CARTESIAN_POINT ( 'NONE',  ( 0.1135584504625009039, 20.02520167614220981, 39.31848610978152436 ) ) ;
#36339=VERTEX_POINT ( 'NONE', #9050 ) ;
#36341=( BOUNDED_SURFACE ( )  B_SPLINE_SURFACE ( 3, 1, ( 
 ( #58255, #44833 ),
 ( #35113, #48569 ),
 ( #6548, #15074 ),
 ( #16297, #25692 ) ),
 .UNSPECIFIED., .F., .F., .F. ) 
 B_SPLINE_SURFACE_WITH_KNOTS ( ( 4, 4 ),
 ( 2, 2 ),
 ( 0.000000000000000000, 1.000000000000000000 ),
 ( 0.000000000000000000, 1.000000000000000000 ),
 .UNSPECIFIED. ) 
 GEOMETRIC_REPRESENTATION_ITEM ( )  RATIONAL_B_SPLINE_SURFACE ( (
 ( 1.000000000000000000, 1.000000000000000000),
 ( 0.9953485035131437453, 0.8621029689291515030),
 ( 0.9953485035131437453, 0.8621029689291515030),
 ( 1.000000000000000000, 1.000000000000000000) ) ) 
 REPRESENTATION_ITEM ( '' )  SURFACE ( )  );
#36342=ORIENTED_EDGE ( 'NONE', *, *, #17990, .T. ) ;
#36349=CARTESIAN_POINT ( 'NONE',  ( -6.077587904424778920, -16.13490349385135758, 10.51003856501172606 ) ) ;
#36356=CARTESIAN_POINT ( 'NONE',  ( 0.6016117650947688800, 46.49485840376616608, -15.80440433101590969 ) ) ;
#36359=( BOUNDED_SURFACE ( )  B_SPLINE_SURFACE ( 3, 1, ( 
 ( #45467, #2513 ),
 ( #50448, #44854 ),
 ( #59213, #30400 ),
 ( #31346, #40778 ) ),
 .UNSPECIFIED., .F., .F., .F. ) 
 B_SPLINE_SURFACE_WITH_KNOTS ( ( 4, 4 ),
 ( 2, 2 ),
 ( 0.000000000000000000, 1.000000000000000000 ),
 ( 0.000000000000000000, 1.000000000000000000 ),
 .UNSPECIFIED. ) 
 GEOMETRIC_REPRESENTATION_ITEM ( )  RATIONAL_B_SPLINE_SURFACE ( (
 ( 1.000000000000000000, 1.000000000000000000),
 ( 0.7211978278499970862, 0.9934217856018976445),
 ( 0.7211978278499970862, 0.9934217856018976445),
 ( 1.000000000000000000, 1.000000000000000000) ) ) 
 REPRESENTATION_ITEM ( '' )  SURFACE ( )  );
#36361=CARTESIAN_POINT ( 'NONE',  ( -6.063463321072278589, -8.893131869789531407, -17.08018319650008010 ) ) ;
#36366=ORIENTED_EDGE ( 'NONE', *, *, #56390, .T. ) ;
#36374=APPLICATION_CONTEXT ( 'automotive_design' ) ;
#36382=EDGE_CURVE ( 'NONE', #27771, #4535, #14102, .T. ) ;
#36385=CARTESIAN_POINT ( 'NONE',  ( 0.1129192098497447394, 43.21532672376840623, -8.909956450123800664 ) ) ;
#36386=CARTESIAN_POINT ( 'NONE',  ( 0.6008123274975392114, -49.10565096348182124, -0.4354246331507586332 ) ) ;
#36398=CARTESIAN_POINT ( 'NONE',  ( 0.6016117650947688800, 44.09211389101648138, -21.62028091552307174 ) ) ;
#36403=CARTESIAN_POINT ( 'NONE',  ( 3.390910168358336918, -10.61186345626784977, 42.67886468170355840 ) ) ;
#36408=CARTESIAN_POINT ( 'NONE',  ( 0.1158816050234198897, 44.03387193347052886, 2.821376233662789001 ) ) ;
#36415=VERTEX_POINT ( 'NONE', #20923 ) ;
#36418=CARTESIAN_POINT ( 'NONE',  ( 4.553261556744875094, -36.93702150832111641, 23.77385134801386712 ) ) ;
#36425=CARTESIAN_POINT ( 'NONE',  ( 3.050102900204245682, 13.48218373028109340, -41.87667574009432769 ) ) ;
#36428=LINE ( 'NONE', #961, #15304 ) ;
#36429=CARTESIAN_POINT ( 'NONE',  ( 0.6000166863083106206, 48.30184070260992968, 8.874438937090559421 ) ) ;
#36440=CARTESIAN_POINT ( 'NONE',  ( 4.390527457369402420, 12.19251145444202855, 42.20815088418253680 ) ) ;
#36443=CARTESIAN_POINT ( 'NONE',  ( 0.5980271706414711508, 48.96187791475873752, 3.844964746512286258 ) ) ;
#36448=CARTESIAN_POINT ( 'NONE',  ( -6.078726893082806448, 7.791390017580341443, -17.60932374802251132 ) ) ;
#36457=CARTESIAN_POINT ( 'NONE',  ( 4.553261556744875094, 0.000000000000000000, 0.000000000000000000 ) ) ;
#36462=B_SPLINE_CURVE_WITH_KNOTS ( 'NONE', 3,
 ( #47915, #18173, #47001, #52587, #51662, #9680, #52902, #57574, #51973, #32583, #14710, #47599, #42604, #4642, #14101, #56977, #61666, #13476, #56358, #52274, #8756, #23174, #37288, #41996, #4964 ),
 .UNSPECIFIED., .F., .F.,
 ( 4, 3, 3, 3, 3, 3, 3, 3, 4 ),
 ( 4.670885906470169154E-18, 0.0005656085177311383390, 0.001131215744874499622, 0.001696821861372764832, 0.002262427090022497284, 0.002828031679238744624, 0.003393635864401603995, 0.003977030878808131623, 0.004561030005651157265 ),
 .UNSPECIFIED. ) ;
#36473=ORIENTED_EDGE ( 'NONE', *, *, #27271, .T. ) ;
#36477=ORIENTED_EDGE ( 'NONE', *, *, #33831, .T. ) ;
#36479=CARTESIAN_POINT ( 'NONE',  ( 0.3676999524040323597, 25.91024933382809436, -35.70167450949183774 ) ) ;
#36480=VECTOR ( 'NONE', #31280, 999.9999999999998863 ) ;
#36486=ORIENTED_EDGE ( 'NONE', *, *, #48667, .T. ) ;
#36487=CARTESIAN_POINT ( 'NONE',  ( 0.6028777368367059797, -48.71531753957629007, 6.193356628624226978 ) ) ;
#36489=CARTESIAN_POINT ( 'NONE',  ( 0.5997462898726536595, -25.00873172704263325, 42.26245340191598387 ) ) ;
#36497=ORIENTED_EDGE ( 'NONE', *, *, #52915, .F. ) ;
#36499=CARTESIAN_POINT ( 'NONE',  ( 0.1129192098497447394, 30.02178898772887550, 32.33641869102754640 ) ) ;
#36505=LINE ( 'NONE', #17386, #9689 ) ;
#36509=CARTESIAN_POINT ( 'NONE',  ( 0.7242003506639994592, -14.75411309231543022, -46.83297792138777993 ) ) ;
#36522=CARTESIAN_POINT ( 'NONE',  ( 1.830465331921977246, 11.00192678874612895, -42.65364770817919293 ) ) ;
#36523=B_SPLINE_CURVE_WITH_KNOTS ( 'NONE', 3,
 ( #49857, #17280, #3157, #6593, #45487, #26664 ),
 .UNSPECIFIED., .F., .F.,
 ( 4, 2, 4 ),
 ( 5.553824967135426632E-18, 0.0002447193893791698707, 0.0004894387787583342119 ),
 .UNSPECIFIED. ) ;
#36527=CARTESIAN_POINT ( 'NONE',  ( 0.6252788684277219566, -2.260168747266527500, -49.05441843919412293 ) ) ;
#36530=CARTESIAN_POINT ( 'NONE',  ( 1.112077966505211624, 36.35951895807152567, -24.92018672213736963 ) ) ;
#36531=CARTESIAN_POINT ( 'NONE',  ( 0.6016117650947689910, -1.225764908963027366, 49.09224536148712303 ) ) ;
#36535=CARTESIAN_POINT ( 'NONE',  ( 0.7948884756798489937, 27.37439991543159223, 40.75954948070661743 ) ) ;
#36541=CARTESIAN_POINT ( 'NONE',  ( 0.7044674535453004927, -8.668117436800327980, -48.33907801057799247 ) ) ;
#36544=ORIENTED_EDGE ( 'NONE', *, *, #51002, .F. ) ;
#36553=CARTESIAN_POINT ( 'NONE',  ( 0.5987334308729319599, 48.08272117021891034, -9.980722991683057543 ) ) ;
#36555=CARTESIAN_POINT ( 'NONE',  ( 0.1368894036331295694, 33.18070637688693836, -29.08439530494225167 ) ) ;
#36557=ORIENTED_EDGE ( 'NONE', *, *, #7051, .T. ) ;
#36558=CARTESIAN_POINT ( 'NONE',  ( -6.078457390727109555, -4.289140445936591384, 18.77226105914092713 ) ) ;
#36560=VERTEX_POINT ( 'NONE', #54722 ) ;
#36561=CARTESIAN_POINT ( 'NONE',  ( 4.335381028904216727, -44.56680861641540048, 20.33608658056285279 ) ) ;
#36562=CARTESIAN_POINT ( 'NONE',  ( -6.078075953587585900, -17.34679059108030685, -8.359666885489142274 ) ) ;
#36571=ORIENTED_EDGE ( 'NONE', *, *, #43299, .F. ) ;
#36577=CARTESIAN_POINT ( 'NONE',  ( 0.1129192098497447394, -27.88830454350447852, -34.19348267541494124 ) ) ;
#36580=ORIENTED_EDGE ( 'NONE', *, *, #32433, .F. ) ;
#36583=CARTESIAN_POINT ( 'NONE',  ( 0.5997462898726536595, 32.62638226927682439, 36.70246327105753892 ) ) ;
#36586=CONICAL_SURFACE ( 'NONE', #44594, 43.92652462719577500, 1.486293639869522343 ) ;
#36591=ORIENTED_EDGE ( 'NONE', *, *, #44294, .T. ) ;
#36594=DIRECTION ( 'NONE',  ( 1.000000000000000000, 0.000000000000000000, 0.000000000000000000 ) ) ;
#36597=AXIS2_PLACEMENT_3D ( 'NONE', #12623, #13230, #51410 ) ;
#36605=CARTESIAN_POINT ( 'NONE',  ( 0.1158403557922069033, -12.51823201008644659, -42.31115898348171811 ) ) ;
#36610=CARTESIAN_POINT ( 'NONE',  ( -6.063463321072276813, -18.28058862190277267, -6.053142334046738071 ) ) ;
#36613=CARTESIAN_POINT ( 'NONE',  ( 3.894904216938897878, 17.24901631294985904, 40.43013441372400507 ) ) ;
#36614=ADVANCED_FACE ( 'NONE', ( #35659 ), #1905, .F. ) ;
#36615=DIRECTION ( 'NONE',  ( -1.000000000000000000, -0.000000000000000000, -0.000000000000000000 ) ) ;
#36617=ORIENTED_EDGE ( 'NONE', *, *, #29983, .F. ) ;
#36626=CARTESIAN_POINT ( 'NONE',  ( 4.975610109902397937, 35.53430708602585497, -33.61193875773584949 ) ) ;
#36633=CARTESIAN_POINT ( 'NONE',  ( -6.057079549204054558, -1.857573237467230909, 19.16717644221975547 ) ) ;
#36635=VERTEX_POINT ( 'NONE', #13699 ) ;
#36637=CARTESIAN_POINT ( 'NONE',  ( 0.1157991065609915576, 20.33690428145512286, 39.15804757370611355 ) ) ;
#36638=ADVANCED_FACE ( 'NONE', ( #42516 ), #44756, .F. ) ;
#36642=DIRECTION ( 'NONE',  ( 0.09722883295013595717, -0.2904161885395372678, -0.9519479983052239191 ) ) ;
#36651=CARTESIAN_POINT ( 'NONE',  ( 0.6029443449137436017, -25.41969901341494875, -42.01640679604484774 ) ) ;
#36657=CARTESIAN_POINT ( 'NONE',  ( 4.060580049360325461, 0.9058177295226151893, 43.93913049435652596 ) ) ;
#36660=CARTESIAN_POINT ( 'NONE',  ( 0.5987334308729320709, 11.51672212534787576, 47.73811912986572281 ) ) ;
#36663=ORIENTED_EDGE ( 'NONE', *, *, #33478, .T. ) ;
#36664=DIRECTION ( 'NONE',  ( 0.000000000000000000, 0.000000000000000000, 1.000000000000000000 ) ) ;
#36665=CARTESIAN_POINT ( 'NONE',  ( 4.060580049360325461, -33.78822741605884517, 28.10379658408981740 ) ) ;
#36667=EDGE_LOOP ( 'NONE', ( #4735, #57572, #10062, #22823 ) ) ;
#36670=EDGE_CURVE ( 'NONE', #60330, #33022, #7276, .T. ) ;
#36671=CARTESIAN_POINT ( 'NONE',  ( 2.648799415243696664, -21.10807549816198403, 44.26021477640490787 ) ) ;
#36674=CARTESIAN_POINT ( 'NONE',  ( 2.533389852662419894, -43.42454841681725952, 7.194381594627227372 ) ) ;
#36690=B_SPLINE_CURVE_WITH_KNOTS ( 'NONE', 3,
 ( #59382, #16491, #12736, #35620 ),
 .UNSPECIFIED., .F., .F.,
 ( 4, 4 ),
 ( 2.175771182130668512E-17, 0.004559932413162188537 ),
 .UNSPECIFIED. ) ;
#36693=DIRECTION ( 'NONE',  ( 1.000000000000000000, 0.000000000000000000, 0.000000000000000000 ) ) ;
#36700=CARTESIAN_POINT ( 'NONE',  ( 3.559346040607745287, -41.96528360729811169, 13.12803310862003769 ) ) ;
#36705=( BOUNDED_SURFACE ( )  B_SPLINE_SURFACE ( 3, 1, ( 
 ( #24712, #61969 ),
 ( #48825, #28474 ),
 ( #48513, #38839 ),
 ( #33510, #10006 ) ),
 .UNSPECIFIED., .F., .F., .F. ) 
 B_SPLINE_SURFACE_WITH_KNOTS ( ( 4, 4 ),
 ( 2, 2 ),
 ( 0.000000000000000000, 1.000000000000000000 ),
 ( 0.000000000000000000, 1.000000000000000000 ),
 .UNSPECIFIED. ) 
 GEOMETRIC_REPRESENTATION_ITEM ( )  RATIONAL_B_SPLINE_SURFACE ( (
 ( 1.000000000000000000, 1.000000000000000000),
 ( 0.7211978278499968642, 0.9934217856018975334),
 ( 0.7211978278499968642, 0.9934217856018975334),
 ( 1.000000000000000000, 1.000000000000000000) ) ) 
 REPRESENTATION_ITEM ( '' )  SURFACE ( )  );
#36707=CARTESIAN_POINT ( 'NONE',  ( 0.6000166863083106206, -49.10753961887881758, 0.5225268306041193078 ) ) ;
#36729=CARTESIAN_POINT ( 'NONE',  ( 2.648799415243708655, 36.42501529472047395, -32.82888551365973484 ) ) ;
#36738=CARTESIAN_POINT ( 'NONE',  ( 0.1158516988532803244, -12.50734325492080501, 42.31440090012363697 ) ) ;
#36740=CARTESIAN_POINT ( 'NONE',  ( 4.834790513006555379, -26.65333699373609733, 39.01524020203795828 ) ) ;
#36744=CARTESIAN_POINT ( 'NONE',  ( 0.6026112563231247332, 27.95217006345316690, 40.37594808358065279 ) ) ;
#36748=ORIENTED_EDGE ( 'NONE', *, *, #4062, .T. ) ;
#36767=CARTESIAN_POINT ( 'NONE',  ( 0.6026777506516367566, 17.12337608662687671, 46.02538845064920991 ) ) ;
#36768=DIRECTION ( 'NONE',  ( 0.000000000000000000, 0.000000000000000000, 1.000000000000000000 ) ) ;
#36771=ORIENTED_EDGE ( 'NONE', *, *, #56434, .T. ) ;
#36773=VECTOR ( 'NONE', #21002, 1000.000000000000000 ) ;
#36775=CARTESIAN_POINT ( 'NONE',  ( 1.296416391601052487, 3.124427423165220485, -43.96072482743581844 ) ) ;
#36776=VECTOR ( 'NONE', #2083, 1000.000000000000227 ) ;
#36793=EDGE_CURVE ( 'NONE', #50931, #34042, #17703, .T. ) ;
#36800=CARTESIAN_POINT ( 'NONE',  ( 0.1129192098497447394, 3.754263797494919341, -43.96427289429421137 ) ) ;
#36806=CARTESIAN_POINT ( 'NONE',  ( 0.6000166863083090663, -31.02657807334512086, -38.06803035050636197 ) ) ;
#36809=CARTESIAN_POINT ( 'NONE',  ( -6.072942160501519915, 11.99473239968607885, -15.06421444845171287 ) ) ;
#36816=CARTESIAN_POINT ( 'NONE',  ( 2.359973842542475886, -5.532421374462768604, 43.67525853807723735 ) ) ;
#36821=CARTESIAN_POINT ( 'NONE',  ( 0.3676999524040366896, -11.75791688508890331, 42.51707861373098041 ) ) ;
#36823=EDGE_CURVE ( 'NONE', #46958, #51774, #36505, .T. ) ;
#36828=CARTESIAN_POINT ( 'NONE',  ( 2.299746137290199055, 21.52978567797254428, -44.05394041793203996 ) ) ;
#36831=FACE_OUTER_BOUND ( 'NONE', #21590, .T. ) ;
#36834=ORIENTED_EDGE ( 'NONE', *, *, #2892, .F. ) ;
#36837=CARTESIAN_POINT ( 'NONE',  ( 2.648799415243708655, -40.11112523584274925, -28.20664984722818502 ) ) ;
#36839=CARTESIAN_POINT ( 'NONE',  ( 0.5987334363312689645, -13.39119798739007905, -47.24657366343718934 ) ) ;
#36841=CARTESIAN_POINT ( 'NONE',  ( 2.706805983486679779, -24.21343163196654658, -36.74895701817722937 ) ) ;
#36854=CARTESIAN_POINT ( 'NONE',  ( 2.299652685299200972, -9.094837095626216339, 48.18262822908455689 ) ) ;
#36862=AXIS2_PLACEMENT_3D ( 'NONE', #37638, #8174, #8792 ) ;
#36868=B_SPLINE_CURVE_WITH_KNOTS ( 'NONE', 3,
 ( #58018, #42730, #19847, #4775 ),
 .UNSPECIFIED., .F., .F.,
 ( 4, 4 ),
 ( 0.000000000000000000, 0.005013413432710147645 ),
 .UNSPECIFIED. ) ;
#36870=EDGE_CURVE ( 'NONE', #5016, #44428, #12700, .T. ) ;
#36872=CARTESIAN_POINT ( 'NONE',  ( -6.077587904424778920, -4.290907484552348272, 18.77189746277512583 ) ) ;
#36875=ORIENTED_EDGE ( 'NONE', *, *, #14240, .T. ) ;
#36877=CARTESIAN_POINT ( 'NONE',  ( -6.078457390727109555, 16.77598442640661958, -9.453087197443521106 ) ) ;
#36887=ORIENTED_EDGE ( 'NONE', *, *, #5361, .F. ) ;
#36893=B_SPLINE_CURVE_WITH_KNOTS ( 'NONE', 3,
 ( #15295, #20297, #49102, #38189, #38490, #6153 ),
 .UNSPECIFIED., .F., .F.,
 ( 4, 2, 4 ),
 ( 2.538052214298621590E-18, 0.0002447193893791693828, 0.0004894387787583361635 ),
 .UNSPECIFIED. ) ;
#36900=FACE_OUTER_BOUND ( 'NONE', #25628, .T. ) ;
#36901=B_SPLINE_CURVE_WITH_KNOTS ( 'NONE', 3,
 ( #17405, #22409, #36527, #50592, #59371, #59996 ),
 .UNSPECIFIED., .F., .F.,
 ( 4, 2, 4 ),
 ( 0.000000000000000000, 0.0002447195606305751798, 0.0004894391212611503596 ),
 .UNSPECIFIED. ) ;
#36908=CARTESIAN_POINT ( 'NONE',  ( 0.1129192098497455998, 33.28205046155587610, 28.96993104685618547 ) ) ;
#36911=CARTESIAN_POINT ( 'NONE',  ( 0.6252788684277225117, -48.78635097398380793, -5.597882619074505683 ) ) ;
#36920=CARTESIAN_POINT ( 'NONE',  ( 0.6029443199889047422, 4.715466349721216588, 48.88048709821794091 ) ) ;
#36927=CARTESIAN_POINT ( 'NONE',  ( 0.1119898979215348395, -27.94769354442891895, -34.14509823969635960 ) ) ;
#36928=DIRECTION ( 'NONE',  ( 0.000000000000000000, 0.000000000000000000, 1.000000000000000000 ) ) ;
#36929=AXIS2_PLACEMENT_3D ( 'NONE', #51579, #36594, #46011 ) ;
#36931=CARTESIAN_POINT ( 'NONE',  ( 0.6029443449137434907, -1.530470916618504429, -49.08357359399087017 ) ) ;
#36941=CARTESIAN_POINT ( 'NONE',  ( 0.6028777368367060907, -45.48575615302912922, -18.50907389628789090 ) ) ;
#36946=CARTESIAN_POINT ( 'NONE',  ( 2.009741617377216460, -26.37340513181155544, 35.26964104405346490 ) ) ;
#36957=CARTESIAN_POINT ( 'NONE',  ( 4.694002226626920127, -41.22189368134345244, -19.46895612944235765 ) ) ;
#36961=CARTESIAN_POINT ( 'NONE',  ( 5.901764892641307547, -32.95403503760685737, 36.22185862403885892 ) ) ;
#36965=ORIENTED_EDGE ( 'NONE', *, *, #3602, .T. ) ;
#36968=CARTESIAN_POINT ( 'NONE',  ( 0.6008123274975391004, -42.57300165257447588, -24.47639845745999310 ) ) ;
#36973=CARTESIAN_POINT ( 'NONE',  ( 0.1129192098497455998, -7.520259262076605999, 43.47870154933683295 ) ) ;
#36974=VERTEX_POINT ( 'NONE', #42747 ) ;
#36975=CARTESIAN_POINT ( 'NONE',  ( 1.479689385636123067, 5.399678476185347797, 43.73130820843933719 ) ) ;
#36982=CARTESIAN_POINT ( 'NONE',  ( 0.3676999524040323597, -26.85386693986589890, -34.99743438737782242 ) ) ;
#36983=CARTESIAN_POINT ( 'NONE',  ( 4.553261556744873317, 22.57774691820481294, -37.68003330573274923 ) ) ;
#36990=CARTESIAN_POINT ( 'NONE',  ( -6.077587904424778920, 7.788877841491995468, -17.61049128685073129 ) ) ;
#36994=CARTESIAN_POINT ( 'NONE',  ( 3.559346040607745287, -43.29952482140919301, 7.653850781283672688 ) ) ;
#36995=B_SPLINE_CURVE_WITH_KNOTS ( 'NONE', 3,
 ( #221, #57862, #9338, #47569 ),
 .UNSPECIFIED., .F., .F.,
 ( 4, 4 ),
 ( 6.992893892674702526E-18, 0.005013413432710137237 ),
 .UNSPECIFIED. ) ;
#37001=( BOUNDED_SURFACE ( )  B_SPLINE_SURFACE ( 3, 1, ( 
 ( #9033, #56642 ),
 ( #18446, #4937 ),
 ( #52244, #46969 ),
 ( #9341, #23145 ) ),
 .UNSPECIFIED., .F., .F., .F. ) 
 B_SPLINE_SURFACE_WITH_KNOTS ( ( 4, 4 ),
 ( 2, 2 ),
 ( 0.000000000000000000, 1.000000000000000000 ),
 ( 0.000000000000000000, 1.000000000000000000 ),
 .UNSPECIFIED. ) 
 GEOMETRIC_REPRESENTATION_ITEM ( )  RATIONAL_B_SPLINE_SURFACE ( (
 ( 1.000000000000000000, 1.000000000000000000),
 ( 0.9953485035131437453, 0.8621029689291523912),
 ( 0.9953485035131437453, 0.8621029689291523912),
 ( 1.000000000000000000, 1.000000000000000000) ) ) 
 REPRESENTATION_ITEM ( '' )  SURFACE ( )  );
#37006=B_SPLINE_CURVE_WITH_KNOTS ( 'NONE', 3,
 ( #496, #51573, #32815, #42836, #61282, #8987 ),
 .UNSPECIFIED., .F., .F.,
 ( 4, 2, 4 ),
 ( 2.504320737601683728E-17, 0.0002293755540694346795, 0.0004587511081388443140 ),
 .UNSPECIFIED. ) ;
#37012=CARTESIAN_POINT ( 'NONE',  ( 4.335381028904216727, 39.85754067141783707, -28.48040202122537679 ) ) ;
#37014=CARTESIAN_POINT ( 'NONE',  ( -6.077587904424778920, 19.25606354205735116, -0.006185319731011218458 ) ) ;
#37019=ORIENTED_EDGE ( 'NONE', *, *, #5959, .T. ) ;
#37025=CARTESIAN_POINT ( 'NONE',  ( 0.7044674535453004927, -45.83030039157684854, -17.64614090470599805 ) ) ;
#37026=EDGE_CURVE ( 'NONE', #54760, #43185, #51339, .T. ) ;
#37031=FACE_OUTER_BOUND ( 'NONE', #40474, .T. ) ;
#37035=CARTESIAN_POINT ( 'NONE',  ( 0.6000166863083106206, -42.53190469623904590, -24.55321902762431918 ) ) ;
#37038=FACE_OUTER_BOUND ( 'NONE', #54636, .T. ) ;
#37040=ORIENTED_EDGE ( 'NONE', *, *, #21155, .F. ) ;
#37041=CARTESIAN_POINT ( 'NONE',  ( 0.1140933569871964981, 14.88246909729719825, 41.53868153482846992 ) ) ;
#37050=VERTEX_POINT ( 'NONE', #43368 ) ;
#37062=CARTESIAN_POINT ( 'NONE',  ( -6.077587904424778920, -19.21689618909968544, 1.227567615773810239 ) ) ;
#37071=CARTESIAN_POINT ( 'NONE',  ( 0.6253024248130465423, 17.60252607561340099, -45.84315982973894421 ) ) ;
#37083=B_SPLINE_CURVE_WITH_KNOTS ( 'NONE', 3,
 ( #57416, #9518, #51496, #60902, #13626, #18016, #37134, #47750, #14555, #51812, #52120, #42151, #28323, #56202, #3570, #33656, #27395, #61509, #23626 ),
 .UNSPECIFIED., .F., .F.,
 ( 4, 3, 3, 3, 3, 3, 4 ),
 ( 3.469552829456483146E-18, 0.0002612768053151680227, 0.0003919133833142895160, 0.0005225499612322576093, 0.0006531865391693353080, 0.0008112755173415210500, 0.0009693688056799712720 ),
 .UNSPECIFIED. ) ;
#37085=CARTESIAN_POINT ( 'NONE',  ( 0.6000166863083090663, -34.91285637184702040, 34.53861522509602366 ) ) ;
#37086=CARTESIAN_POINT ( 'NONE',  ( -6.072942160501519915, -17.34299816270055317, 8.368068894170592742 ) ) ;
#37087=ADVANCED_FACE ( 'NONE', ( #20169 ), #4650, .F. ) ;
#37091=CARTESIAN_POINT ( 'NONE',  ( 0.9268187852002115479, -30.97276895400849384, 31.37581737947608218 ) ) ;
#37104=CARTESIAN_POINT ( 'NONE',  ( 4.694002226626921015, 36.32786722402816793, -27.54216466437439337 ) ) ;
#37105=B_SPLINE_CURVE_WITH_KNOTS ( 'NONE', 3,
 ( #54618, #44653, #21133, #59330, #45274, #11751 ),
 .UNSPECIFIED., .F., .F.,
 ( 4, 2, 4 ),
 ( 0.000000000000000000, 0.0002447195606305739330, 0.0004894391212611478659 ),
 .UNSPECIFIED. ) ;
#37112=ORIENTED_EDGE ( 'NONE', *, *, #51297, .T. ) ;
#37118=EDGE_CURVE ( 'NONE', #27417, #23299, #15526, .T. ) ;
#37121=CARTESIAN_POINT ( 'NONE',  ( -6.063463321072276813, 18.62294427965544585, -4.899632520538490965 ) ) ;
#37129=CARTESIAN_POINT ( 'NONE',  ( 0.3676999524040323597, 19.66859742988730986, 39.48540057367873857 ) ) ;
#37132=CARTESIAN_POINT ( 'NONE',  ( 0.5997462898726536595, -30.20781297212619165, 38.71743361310707598 ) ) ;
#37133=CARTESIAN_POINT ( 'NONE',  ( 0.8744876279028306332, -13.11369837310865805, 47.31153099782990523 ) ) ;
#37134=CARTESIAN_POINT ( 'NONE',  ( 0.1157506346131639274, -17.94551365393233411, -40.31003844576883921 ) ) ;
#37141=CARTESIAN_POINT ( 'NONE',  ( 0.1129192098497455998, 36.71339784380029414, 24.47607416535571545 ) ) ;
#37145=CARTESIAN_POINT ( 'NONE',  ( 0.1156495703730067437, -35.44308041932243469, -26.28176180587048449 ) ) ;
#37153=CARTESIAN_POINT ( 'NONE',  ( 0.5997462898726536595, -1.051648045107538954, 49.09628974305014992 ) ) ;
#37158=CARTESIAN_POINT ( 'NONE',  ( 0.1158516988532803244, -6.993612654201856849, 43.56640380930912215 ) ) ;
#37160=EDGE_CURVE ( 'NONE', #19013, #3214, #11757, .T. ) ;
#37164=CARTESIAN_POINT ( 'NONE',  ( -6.057079549204054558, -6.658663215492206078, 18.06912934489068334 ) ) ;
#37171=CARTESIAN_POINT ( 'NONE',  ( 2.009741617377216460, -44.01846488356086695, 1.370703074251920173 ) ) ;
#37173=CARTESIAN_POINT ( 'NONE',  ( 0.1152339509894530906, -42.73720773065363687, -10.97605420186156344 ) ) ;
#37176=CARTESIAN_POINT ( 'NONE',  ( 0.1158403557922069033, 33.57359527808708322, 28.63134658529052956 ) ) ;
#37178=CARTESIAN_POINT ( 'NONE',  ( 0.5987334308729321819, 22.17584284255811156, -43.81546417410061167 ) ) ;
#37181=CARTESIAN_POINT ( 'NONE',  ( -6.079354080745853928, 3.074405391879146521, 19.00897121715287241 ) ) ;
#37184=CARTESIAN_POINT ( 'NONE',  ( 0.3676999524040323597, 37.41430475689418245, -23.36921870497780418 ) ) ;
#37195=CARTESIAN_POINT ( 'NONE',  ( 1.112077966505211624, 43.45537587376833955, 7.393282951305692130 ) ) ;
#37196=CARTESIAN_POINT ( 'NONE',  ( 2.299652685299202748, -12.71149381474350371, -47.35714993383671612 ) ) ;
#37197=B_SPLINE_CURVE_WITH_KNOTS ( 'NONE', 3,
 ( #60501, #9133, #3491, #51732 ),
 .UNSPECIFIED., .F., .F.,
 ( 4, 4 ),
 ( 0.000000000000000000, 0.004444103432399266161 ),
 .UNSPECIFIED. ) ;
#37198=CARTESIAN_POINT ( 'NONE',  ( 0.6252788684277238440, 33.51946330543371744, 35.88718310050747107 ) ) ;
#37201=CARTESIAN_POINT ( 'NONE',  ( 0.1157506346131639274, -27.43836492290452256, 34.55541622033160820 ) ) ;
#37218=DIRECTION ( 'NONE',  ( 0.09722883295013597105, 0.4670337431504756887, -0.8788777143619072030 ) ) ;
#37222=CARTESIAN_POINT ( 'NONE',  ( 0.1119898979215351448, 39.50795620750168524, -19.64898736724001083 ) ) ;
#37225=B_SPLINE_CURVE_WITH_KNOTS ( 'NONE', 3,
 ( #46181, #60546, #51155, #12055 ),
 .UNSPECIFIED., .F., .F.,
 ( 4, 4 ),
 ( 0.000000000000000000, 0.005013413432710145910 ),
 .UNSPECIFIED. ) ;
#37226=CARTESIAN_POINT ( 'NONE',  ( 2.648799415243708655, -9.190926635156966285, -48.16683849783750304 ) ) ;
#37227=CARTESIAN_POINT ( 'NONE',  ( 4.694002226626920127, -4.720386398733717570, -45.34316622924322360 ) ) ;
#37230=ORIENTED_EDGE ( 'NONE', *, *, #25088, .F. ) ;
#37237=CARTESIAN_POINT ( 'NONE',  ( 0.3676999524040366896, 33.04872056100262512, -29.21870381457057775 ) ) ;
#37242=CARTESIAN_POINT ( 'NONE',  ( 2.009741617377216460, 28.57895180276246805, -33.50742591543588844 ) ) ;
#37249=CARTESIAN_POINT ( 'NONE',  ( 2.879087469061462734, -26.05926906996272763, 35.45442387520437677 ) ) ;
#37255=CARTESIAN_POINT ( 'NONE',  ( -6.057079549204054558, -14.65763772032089740, -12.48939100034763250 ) ) ;
#37257=CARTESIAN_POINT ( 'NONE',  ( 0.6253024248130445439, -43.12021026963351034, 23.49663153986622177 ) ) ;
#37261=CARTESIAN_POINT ( 'NONE',  ( 0.6008123274975392114, -7.407413473420949579, -48.54569781960332620 ) ) ;
#37264=( BOUNDED_SURFACE ( )  B_SPLINE_SURFACE ( 3, 1, ( 
 ( #19336, #29036 ),
 ( #28107, #23108 ),
 ( #57199, #52833 ),
 ( #47224, #4271 ) ),
 .UNSPECIFIED., .F., .F., .F. ) 
 B_SPLINE_SURFACE_WITH_KNOTS ( ( 4, 4 ),
 ( 2, 2 ),
 ( 0.000000000000000000, 1.000000000000000000 ),
 ( 0.000000000000000000, 1.000000000000000000 ),
 .UNSPECIFIED. ) 
 GEOMETRIC_REPRESENTATION_ITEM ( )  RATIONAL_B_SPLINE_SURFACE ( (
 ( 1.000000000000000000, 1.000000000000000000),
 ( 0.7211978278499970862, 0.9934217856018976445),
 ( 0.7211978278499970862, 0.9934217856018976445),
 ( 1.000000000000000000, 1.000000000000000000) ) ) 
 REPRESENTATION_ITEM ( '' )  SURFACE ( )  );
#37265=AXIS2_PLACEMENT_3D ( 'NONE', #26611, #55411, #31943 ) ;
#37269=DIRECTION ( 'NONE',  ( 0.000000000000000000, 0.000000000000000000, 1.000000000000000000 ) ) ;
#37273=CARTESIAN_POINT ( 'NONE',  ( 4.975610109902397937, 42.33317580307119954, 24.50207406657730047 ) ) ;
#37275=CARTESIAN_POINT ( 'NONE',  ( 2.359973842542475886, 5.726946755930971911, 43.65017726753503524 ) ) ;
#37279=ORIENTED_EDGE ( 'NONE', *, *, #47735, .F. ) ;
#37284=CARTESIAN_POINT ( 'NONE',  ( 3.727782113643637540, -33.91244348195018432, 27.97720416677674393 ) ) ;
#37287=CARTESIAN_POINT ( 'NONE',  ( 3.678834586032790011, 31.53396450442054544, 37.47294293570093515 ) ) ;
#37288=CARTESIAN_POINT ( 'NONE',  ( 0.7413678028165013867, 43.09507536412139217, -9.343477464570760560 ) ) ;
#37289=CARTESIAN_POINT ( 'NONE',  ( 3.559346040607745287, -39.27867776338149497, -19.76400148508467325 ) ) ;
#37290=CARTESIAN_POINT ( 'NONE',  ( 3.221118495291109163, -43.34303269931057656, 7.492859006296892943 ) ) ;
#37291=CARTESIAN_POINT ( 'NONE',  ( 4.553261556744875094, 0.000000000000000000, 0.000000000000000000 ) ) ;
#37292=ORIENTED_EDGE ( 'NONE', *, *, #25474, .F. ) ;
#37303=VECTOR ( 'NONE', #4398, 1000.000000000000000 ) ;
#37308=LINE ( 'NONE', #22585, #27188 ) ;
#37325=CARTESIAN_POINT ( 'NONE',  ( 2.299652685299202748, 47.86636889862017341, 10.63449356195967432 ) ) ;
#37327=PRODUCT_DEFINITION_SHAPE ( 'NONE', 'NONE',  #36005 ) ;
#37331=CARTESIAN_POINT ( 'NONE',  ( 0.7948878604505656975, 40.66950417720534006, -27.50800024136056976 ) ) ;
#37332=( BOUNDED_SURFACE ( )  B_SPLINE_SURFACE ( 3, 1, ( 
 ( #4428, #42695 ),
 ( #60536, #37382 ),
 ( #61757, #14195 ),
 ( #17647, #37085 ) ),
 .UNSPECIFIED., .F., .F., .F. ) 
 B_SPLINE_SURFACE_WITH_KNOTS ( ( 4, 4 ),
 ( 2, 2 ),
 ( 0.000000000000000000, 1.000000000000000000 ),
 ( 0.000000000000000000, 1.000000000000000000 ),
 .UNSPECIFIED. ) 
 GEOMETRIC_REPRESENTATION_ITEM ( )  RATIONAL_B_SPLINE_SURFACE ( (
 ( 1.000000000000000000, 1.000000000000000000),
 ( 0.9953485035131437453, 0.8621029689291515030),
 ( 0.9953485035131437453, 0.8621029689291515030),
 ( 1.000000000000000000, 1.000000000000000000) ) ) 
 REPRESENTATION_ITEM ( '' )  SURFACE ( )  );
#37335=FACE_OUTER_BOUND ( 'NONE', #50102, .T. ) ;
#37336=CARTESIAN_POINT ( 'NONE',  ( 1.834102595619085285, -37.72341624877798694, 22.74074781925867939 ) ) ;
#37337=CARTESIAN_POINT ( 'NONE',  ( 0.6252788684277205133, 27.52863421382489406, -40.66470987840802565 ) ) ;
#37342=AXIS2_PLACEMENT_3D ( 'NONE', #19356, #5828, #44116 ) ;
#37346=CARTESIAN_POINT ( 'NONE',  ( 0.1149546198390367369, -12.81688777603463514, 42.22172370663890462 ) ) ;
#37350=CARTESIAN_POINT ( 'NONE',  ( -6.063463321072278589, 7.809047921946556947, -17.60225051043791922 ) ) ;
#37352=CARTESIAN_POINT ( 'NONE',  ( 4.975610109902397937, 0.000000000000000000, 0.000000000000000000 ) ) ;
#37363=CARTESIAN_POINT ( 'NONE',  ( 4.553261556744875094, 0.000000000000000000, 0.000000000000000000 ) ) ;
#37374=CARTESIAN_POINT ( 'NONE',  ( 0.3676999524040323597, -31.10876963919482563, -31.27610965031216139 ) ) ;
#37380=VERTEX_POINT ( 'NONE', #48822 ) ;
#37381=VERTEX_POINT ( 'NONE', #30323 ) ;
#37382=CARTESIAN_POINT ( 'NONE',  ( 0.7044674535453004927, -34.68719619958527289, 34.76494128604828404 ) ) ;
#37385=ORIENTED_EDGE ( 'NONE', *, *, #51249, .F. ) ;
#37388=CARTESIAN_POINT ( 'NONE',  ( 0.1368894036331306796, -23.41594797177933174, -37.39725533386449996 ) ) ;
#37392=ORIENTED_EDGE ( 'NONE', *, *, #16062, .T. ) ;
#37402=CARTESIAN_POINT ( 'NONE',  ( 4.834790513006553603, 18.70372717509320637, 43.39078163255486942 ) ) ;
#37411=DIRECTION ( 'NONE',  ( -0.1011922191286467460, -0.2338987173090957550, 0.9669806227784399910 ) ) ;
#37413=CARTESIAN_POINT ( 'NONE',  ( 4.390527457369402420, 35.01638428076268639, 26.53371757840531231 ) ) ;
#37426=CARTESIAN_POINT ( 'NONE',  ( 0.1119898979215350893, 30.07795596614133160, 32.28432859996768656 ) ) ;
#37431=ORIENTED_EDGE ( 'NONE', *, *, #13375, .F. ) ;
#37432=ORIENTED_EDGE ( 'NONE', *, *, #21734, .T. ) ;
#37433=CARTESIAN_POINT ( 'NONE',  ( -6.057079549204054558, 17.85280408805613561, 7.218629876453331207 ) ) ;
#37440=( BOUNDED_SURFACE ( )  B_SPLINE_SURFACE ( 3, 1, ( 
 ( #10860, #1420 ),
 ( #59057, #15866 ),
 ( #39688, #30247 ),
 ( #49984, #54044 ) ),
 .UNSPECIFIED., .F., .F., .F. ) 
 B_SPLINE_SURFACE_WITH_KNOTS ( ( 4, 4 ),
 ( 2, 2 ),
 ( 0.000000000000000000, 1.000000000000000000 ),
 ( 0.000000000000000000, 1.000000000000000000 ),
 .UNSPECIFIED. ) 
 GEOMETRIC_REPRESENTATION_ITEM ( )  RATIONAL_B_SPLINE_SURFACE ( (
 ( 1.000000000000000000, 1.000000000000000000),
 ( 0.9754377213608244057, 0.9999580625633939235),
 ( 0.9754377213608244057, 0.9999580625633939235),
 ( 1.000000000000000000, 1.000000000000000000) ) ) 
 REPRESENTATION_ITEM ( '' )  SURFACE ( )  );
#37446=( BOUNDED_SURFACE ( )  B_SPLINE_SURFACE ( 3, 1, ( 
 ( #42641, #9103 ),
 ( #47952, #56704 ),
 ( #43269, #38566 ),
 ( #47329, #61701 ) ),
 .UNSPECIFIED., .F., .F., .F. ) 
 B_SPLINE_SURFACE_WITH_KNOTS ( ( 4, 4 ),
 ( 2, 2 ),
 ( 0.000000000000000000, 1.000000000000000000 ),
 ( 0.000000000000000000, 1.000000000000000000 ),
 .UNSPECIFIED. ) 
 GEOMETRIC_REPRESENTATION_ITEM ( )  RATIONAL_B_SPLINE_SURFACE ( (
 ( 1.000000000000000000, 1.000000000000000000),
 ( 0.9953485035131437453, 0.8621029689291515030),
 ( 0.9953485035131437453, 0.8621029689291515030),
 ( 1.000000000000000000, 1.000000000000000000) ) ) 
 REPRESENTATION_ITEM ( '' )  SURFACE ( )  );
#37447=CARTESIAN_POINT ( 'NONE',  ( 0.1119899015040008994, 36.67093986234336001, 24.53983451054433118 ) ) ;
#37450=CARTESIAN_POINT ( 'NONE',  ( 4.694002226626921015, -44.68037479411228219, -9.052562051916137165 ) ) ;
#37452=CARTESIAN_POINT ( 'NONE',  ( 0.6027444965799114707, -39.27709376116379048, -29.47623486071769960 ) ) ;
#37454=CARTESIAN_POINT ( 'NONE',  ( 2.009741617377216460, -23.99099187825139978, -36.93150939672950983 ) ) ;
#37465=CARTESIAN_POINT ( 'NONE',  ( 0.1155031312995260795, -7.208502386081764080, 43.53135796045952333 ) ) ;
#37466=CARTESIAN_POINT ( 'NONE',  ( -6.078457390727109555, 3.077585051287140772, -19.00849760737554917 ) ) ;
#37469=CARTESIAN_POINT ( 'NONE',  ( 0.6029442701453590070, 10.84250512224628338, -47.89556668244295423 ) ) ;
#37472=ORIENTED_EDGE ( 'NONE', *, *, #37692, .T. ) ;
#37476=CARTESIAN_POINT ( 'NONE',  ( 4.226256110419178924, -39.76716733621343991, 18.69223507344121771 ) ) ;
#37477=CARTESIAN_POINT ( 'NONE',  ( 4.390527457369402420, 38.12195674272248169, 21.83808028959083103 ) ) ;
#37480=CARTESIAN_POINT ( 'NONE',  ( 0.5997462898726536595, 48.97040376101512749, 3.667585803694950464 ) ) ;
#37485=DIRECTION ( 'NONE',  ( 1.000000000000000000, 0.000000000000000000, 0.000000000000000000 ) ) ;
#37488=LINE ( 'NONE', #51547, #45666 ) ;
#37495=CARTESIAN_POINT ( 'NONE',  ( 4.553261556744873317, -39.67390170502044100, -18.85526688551536623 ) ) ;
#37496=CARTESIAN_POINT ( 'NONE',  ( 0.5980271706414711508, 37.84660806146532508, -31.29989618327016743 ) ) ;
#37498=LINE ( 'NONE', #56572, #6134 ) ;
#37505=CARTESIAN_POINT ( 'NONE',  ( 0.3676999524040323597, -23.56959980820351674, 37.28839696479283106 ) ) ;
#37509=ORIENTED_EDGE ( 'NONE', *, *, #4988, .F. ) ;
#37515=CARTESIAN_POINT ( 'NONE',  ( 0.8744876279028263033, -0.6840263623742536270, -49.09055060105834656 ) ) ;
#37518=AXIS2_PLACEMENT_3D ( 'NONE', #18648, #33374, #61527 ) ;
#37525=ORIENTED_EDGE ( 'NONE', *, *, #43030, .F. ) ;
#37536=FACE_OUTER_BOUND ( 'NONE', #12596, .T. ) ;
#37544=AXIS2_PLACEMENT_3D ( 'NONE', #34628, #11753, #34323 ) ;
#37547=CARTESIAN_POINT ( 'NONE',  ( 1.479689385636123067, 32.77795963426115122, -29.44807646489730146 ) ) ;
#37549=ADVANCED_FACE ( 'NONE', ( #42227 ), #53491, .F. ) ;
#37560=FACE_OUTER_BOUND ( 'NONE', #14087, .T. ) ;
#37561=ORIENTED_EDGE ( 'NONE', *, *, #31204, .F. ) ;
#37563=CARTESIAN_POINT ( 'NONE',  ( -2.739355103387247858, -4.498893467419792458, 14.23402699589348686 ) ) ;
#37567=CARTESIAN_POINT ( 'NONE',  ( 0.7242486021783788308, -43.17951146175377630, 23.37822175226863664 ) ) ;
#37584=ORIENTED_EDGE ( 'NONE', *, *, #53365, .T. ) ;
#37596=LINE ( 'NONE', #42598, #47830 ) ;
#37599=EDGE_CURVE ( 'NONE', #11949, #15688, #3629, .T. ) ;
#37600=CARTESIAN_POINT ( 'NONE',  ( 4.834790513006553603, -44.98626621068908094, 14.45078521553053008 ) ) ;
#37602=CARTESIAN_POINT ( 'NONE',  ( 4.390527457369402420, -39.44280170213821890, -19.35072945690735580 ) ) ;
#37615=B_SPLINE_CURVE_WITH_KNOTS ( 'NONE', 3,
 ( #40924, #55274, #60909, #56210 ),
 .UNSPECIFIED., .F., .F.,
 ( 4, 4 ),
 ( 0.000000000000000000, 0.004442905043737217438 ),
 .UNSPECIFIED. ) ;
#37616=( BOUNDED_SURFACE ( )  B_SPLINE_SURFACE ( 3, 1, ( 
 ( #15125, #34236 ),
 ( #49239, #44573 ),
 ( #10422, #1002 ),
 ( #29513, #48621 ) ),
 .UNSPECIFIED., .F., .F., .F. ) 
 B_SPLINE_SURFACE_WITH_KNOTS ( ( 4, 4 ),
 ( 2, 2 ),
 ( 0.000000000000000000, 1.000000000000000000 ),
 ( 0.000000000000000000, 1.000000000000000000 ),
 .UNSPECIFIED. ) 
 GEOMETRIC_REPRESENTATION_ITEM ( )  RATIONAL_B_SPLINE_SURFACE ( (
 ( 1.000000000000000000, 1.000000000000000000),
 ( 0.9953485035131437453, 0.8621029689291515030),
 ( 0.9953485035131437453, 0.8621029689291515030),
 ( 1.000000000000000000, 1.000000000000000000) ) ) 
 REPRESENTATION_ITEM ( '' )  SURFACE ( )  );
#37628=VECTOR ( 'NONE', #22485, 1000.000000000000114 ) ;
#37632=ORIENTED_EDGE ( 'NONE', *, *, #46999, .F. ) ;
#37635=CARTESIAN_POINT ( 'NONE',  ( 5.901764892641288895, 48.96927204603445460, -0.04315925332753958038 ) ) ;
#37637=CIRCLE ( 'NONE', #33648, 43.92652462719577500 ) ;
#37638=CARTESIAN_POINT ( 'NONE',  ( 4.975610109902397937, 0.000000000000000000, 0.000000000000000000 ) ) ;
#37640=ORIENTED_EDGE ( 'NONE', *, *, #40858, .T. ) ;
#37641=CARTESIAN_POINT ( 'NONE',  ( 4.975610109902397937, -11.44439439467527642, -47.55497076097196185 ) ) ;
#37647=CARTESIAN_POINT ( 'NONE',  ( 0.6039202388192952409, 4.888815891286901305, -48.86372061182091642 ) ) ;
#37652=CARTESIAN_POINT ( 'NONE',  ( 0.6039202388192952409, 37.27969488251749652, 31.96541978944418361 ) ) ;
#37654=CARTESIAN_POINT ( 'NONE',  ( 0.8753041380234465318, -6.957149426673734816, -48.60798699522449340 ) ) ;
#37659=VERTEX_POINT ( 'NONE', #15247 ) ;
#37663=CARTESIAN_POINT ( 'NONE',  ( 0.6028777368367060907, 46.63305245651208253, -15.39149920895511059 ) ) ;
#37664=ORIENTED_EDGE ( 'NONE', *, *, #16298, .F. ) ;
#37667=CARTESIAN_POINT ( 'NONE',  ( 1.479689385636123067, 8.655498711569247661, -43.20493244204549654 ) ) ;
#37671=DIRECTION ( 'NONE',  ( 0.000000000000000000, 0.000000000000000000, -1.000000000000000000 ) ) ;
#37680=CARTESIAN_POINT ( 'NONE',  ( 4.975610109902397937, 24.86209007719020647, -42.12274782266053563 ) ) ;
#37689=CARTESIAN_POINT ( 'NONE',  ( 4.553261556744875094, 0.000000000000000000, 0.000000000000000000 ) ) ;
#37692=EDGE_CURVE ( 'NONE', #30308, #2370, #10689, .T. ) ;
#37702=CARTESIAN_POINT ( 'NONE',  ( 4.975610109902397937, -41.30423662854469313, 26.19941685746003301 ) ) ;
#37704=EDGE_CURVE ( 'NONE', #56788, #10029, #14947, .T. ) ;
#37715=VECTOR ( 'NONE', #47717, 999.9999999999998863 ) ;
#37720=DIRECTION ( 'NONE',  ( -0.1011922191286467460, 0.9269080304895044309, -0.3613884859841106634 ) ) ;
#37730=( BOUNDED_SURFACE ( )  B_SPLINE_SURFACE ( 3, 1, ( 
 ( #17441, #21213 ),
 ( #59410, #40350 ),
 ( #16517, #54390 ),
 ( #12764, #16213 ) ),
 .UNSPECIFIED., .F., .F., .F. ) 
 B_SPLINE_SURFACE_WITH_KNOTS ( ( 4, 4 ),
 ( 2, 2 ),
 ( 0.000000000000000000, 1.000000000000000000 ),
 ( 0.000000000000000000, 1.000000000000000000 ),
 .UNSPECIFIED. ) 
 GEOMETRIC_REPRESENTATION_ITEM ( )  RATIONAL_B_SPLINE_SURFACE ( (
 ( 1.000000000000000000, 1.000000000000000000),
 ( 0.7211978278499970862, 0.9934217856018976445),
 ( 0.7211978278499970862, 0.9934217856018976445),
 ( 1.000000000000000000, 1.000000000000000000) ) ) 
 REPRESENTATION_ITEM ( '' )  SURFACE ( )  );
#37731=CARTESIAN_POINT ( 'NONE',  ( 4.553261556744875094, 43.92594400279101308, 0.2258523573163287723 ) ) ;
#37734=CARTESIAN_POINT ( 'NONE',  ( 0.7044674535452954967, -24.73445998053410833, -42.42651543884158372 ) ) ;
#37737=CARTESIAN_POINT ( 'NONE',  ( 0.6253024248130498730, -2.260222131445328131, 49.05441492194326969 ) ) ;
#37742=VECTOR ( 'NONE', #5581, 1000.000000000000227 ) ;
#37746=B_SPLINE_CURVE_WITH_KNOTS ( 'NONE', 3,
 ( #45942, #26490, #45616, #40938 ),
 .UNSPECIFIED., .F., .F.,
 ( 4, 4 ),
 ( 0.000000000000000000, 0.005013413432710147645 ),
 .UNSPECIFIED. ) ;
#37750=CARTESIAN_POINT ( 'NONE',  ( 3.390910168358336918, -5.067088124568913443, 43.68548677159830618 ) ) ;
#37756=EDGE_CURVE ( 'NONE', #38361, #36415, #10938, .T. ) ;
#37757=CARTESIAN_POINT ( 'NONE',  ( -2.739355103387247858, 3.577672767447764635, -14.49302675496321768 ) ) ;
#37761=CARTESIAN_POINT ( 'NONE',  ( 2.648799415243696664, 38.22150636651035427, -30.71862487749745441 ) ) ;
#37769=AXIS2_PLACEMENT_3D ( 'NONE', #42574, #27841, #29076 ) ;
#37771=CARTESIAN_POINT ( 'NONE',  ( 0.6039202388192953519, -1.748061966038592097, -49.07655236680628974 ) ) ;
#37779=B_SPLINE_CURVE_WITH_KNOTS ( 'NONE', 3,
 ( #17430, #36553, #24285, #33089, #28672, #23670 ),
 .UNSPECIFIED., .F., .F.,
 ( 4, 2, 4 ),
 ( 0.000000000000000000, 0.0002447195606305750714, 0.0004894391212611501427 ),
 .UNSPECIFIED. ) ;
#37785=ORIENTED_EDGE ( 'NONE', *, *, #41719, .T. ) ;
#37787=CARTESIAN_POINT ( 'NONE',  ( -6.077587904424778920, 3.079371755031687474, -19.00824797261030241 ) ) ;
#37791=DIRECTION ( 'NONE',  ( -1.000000000000000000, -0.000000000000000000, -0.000000000000000000 ) ) ;
#37795=VERTEX_POINT ( 'NONE', #31808 ) ;
#37796=EDGE_LOOP ( 'NONE', ( #10288, #17596, #61169, #34029 ) ) ;
#37799=VECTOR ( 'NONE', #59456, 1000.000000000000000 ) ;
#37804=CARTESIAN_POINT ( 'NONE',  ( 4.975610109902397937, -41.30423662854430944, -26.19941685746064053 ) ) ;
#37805=CARTESIAN_POINT ( 'NONE',  ( 0.1156495703730067576, 33.68638054895946254, 28.49860906679054295 ) ) ;
#37807=ADVANCED_FACE ( 'NONE', ( #22395 ), #23500, .F. ) ;
#37809=CARTESIAN_POINT ( 'NONE',  ( -6.057079549204054558, 19.09996424292739192, 2.454098005099527580 ) ) ;
#37810=VECTOR ( 'NONE', #28425, 1000.000000000000114 ) ;
#37824=DIRECTION ( 'NONE',  ( 0.09722883295013592941, -0.9646010353641026880, -0.2451354658503246409 ) ) ;
#37827=CARTESIAN_POINT ( 'NONE',  ( 4.553261556744875094, 43.59419396814060832, -5.393126930804686303 ) ) ;
#37828=EDGE_LOOP ( 'NONE', ( #45548, #1762, #6592, #38476 ) ) ;
#37829=CARTESIAN_POINT ( 'NONE',  ( 2.185380717157383135, 43.47195670229825026, 7.000627367651174993 ) ) ;
#37845=VERTEX_POINT ( 'NONE', #51198 ) ;
#37851=CARTESIAN_POINT ( 'NONE',  ( 0.6000166863083106206, 11.43688157230898383, 47.76003791465657144 ) ) ;
#37855=CARTESIAN_POINT ( 'NONE',  ( 4.335381028904216727, -9.909170555160370597, -47.97463065593197484 ) ) ;
#37859=CARTESIAN_POINT ( 'NONE',  ( 0.1119899015040012047, 39.99500458464175523, -18.63762099805095929 ) ) ;
#37861=EDGE_CURVE ( 'NONE', #56788, #40746, #59497, .T. ) ;
#37878=ORIENTED_EDGE ( 'NONE', *, *, #19840, .F. ) ;
#37889=CARTESIAN_POINT ( 'NONE',  ( 4.834790513006555379, -42.76900418948076776, -20.08486050647493570 ) ) ;
#37890=CARTESIAN_POINT ( 'NONE',  ( 0.8744876279028263033, 17.78802839418742110, -45.75954650373051891 ) ) ;
#37893=CARTESIAN_POINT ( 'NONE',  ( 0.5997462898726536595, -7.321308210775074876, -48.55872811583048332 ) ) ;
#37895=CARTESIAN_POINT ( 'NONE',  ( 4.335381028904201628, -46.16199858719154747, 16.39593651184559064 ) ) ;
#37896=B_SPLINE_CURVE_WITH_KNOTS ( 'NONE', 3,
 ( #4748, #61165, #24194, #48015, #57372, #365 ),
 .UNSPECIFIED., .F., .F.,
 ( 4, 2, 4 ),
 ( 2.602085213965210642E-18, 0.0002447193893791707381, 0.0004894387787583388740 ),
 .UNSPECIFIED. ) ;
#37897=ORIENTED_EDGE ( 'NONE', *, *, #24258, .T. ) ;
#37899=CARTESIAN_POINT ( 'NONE',  ( 0.6008122571543325074, -43.00034544187082730, -23.71760616810003697 ) ) ;
#37901=CIRCLE ( 'NONE', #10918, 48.91267123290010943 ) ;
#37903=CARTESIAN_POINT ( 'NONE',  ( 2.706805983486679779, -28.71399201132674861, -33.35090367731014283 ) ) ;
#37905=CARTESIAN_POINT ( 'NONE',  ( 0.6000166863083090663, 4.195342255947408283, -48.93079383234974244 ) ) ;
#37907=CARTESIAN_POINT ( 'NONE',  ( 0.1156867017252034141, -38.50738325018485853, 21.54354294211074716 ) ) ;
#37914=CARTESIAN_POINT ( 'NONE',  ( -6.057079549204054558, -11.01026639367717763, -15.79890075416645701 ) ) ;
#37916=DIRECTION ( 'NONE',  ( -0.1011922191286467321, 0.6302926308031447933, -0.7697345869473909419 ) ) ;
#37917=EDGE_LOOP ( 'NONE', ( #515, #45079, #51462, #23197 ) ) ;
#37922=CARTESIAN_POINT ( 'NONE',  ( 1.834102595619085729, -39.00212455761993624, -20.47027173365282593 ) ) ;
#37924=CARTESIAN_POINT ( 'NONE',  ( -2.601141883200665639, -13.66110686928766249, -6.014115610402755330 ) ) ;
#37935=( BOUNDED_SURFACE ( )  B_SPLINE_SURFACE ( 3, 1, ( 
 ( #27863, #61056 ),
 ( #14397, #19398 ),
 ( #42914, #46994 ),
 ( #52582, #38215 ) ),
 .UNSPECIFIED., .F., .F., .F. ) 
 B_SPLINE_SURFACE_WITH_KNOTS ( ( 4, 4 ),
 ( 2, 2 ),
 ( 0.000000000000000000, 1.000000000000000000 ),
 ( 0.000000000000000000, 1.000000000000000000 ),
 .UNSPECIFIED. ) 
 GEOMETRIC_REPRESENTATION_ITEM ( )  RATIONAL_B_SPLINE_SURFACE ( (
 ( 1.000000000000000000, 1.000000000000000000),
 ( 0.7211978278499970862, 0.9934217856018976445),
 ( 0.7211978278499970862, 0.9934217856018976445),
 ( 1.000000000000000000, 1.000000000000000000) ) ) 
 REPRESENTATION_ITEM ( '' )  SURFACE ( )  );
#37937=EDGE_CURVE ( 'NONE', #48800, #52075, #7589, .T. ) ;
#37939=VECTOR ( 'NONE', #29808, 1000.000000000000000 ) ;
#37942=AXIS2_PLACEMENT_3D ( 'NONE', #38822, #47898, #9991 ) ;
#37946=CARTESIAN_POINT ( 'NONE',  ( 0.3676999524040366896, -40.57213187173863389, 17.31625533148228513 ) ) ;
#37951=ORIENTED_EDGE ( 'NONE', *, *, #28353, .F. ) ;
#37955=CARTESIAN_POINT ( 'NONE',  ( -6.078726893082806448, 17.84743921491351415, 7.229312189875837014 ) ) ;
#37961=ORIENTED_EDGE ( 'NONE', *, *, #46191, .F. ) ;
#37964=VERTEX_POINT ( 'NONE', #2268 ) ;
#37972=CARTESIAN_POINT ( 'NONE',  ( 0.5997462898726536595, -39.66574928371219499, -28.95133786038212875 ) ) ;
#37974=CARTESIAN_POINT ( 'NONE',  ( 0.1135584504625008206, -22.50320180596501984, -37.95468298662583351 ) ) ;
#37977=CARTESIAN_POINT ( 'NONE',  ( 0.1152809850208376535, -31.54231067941225319, -30.85494967575203873 ) ) ;
#37987=CARTESIAN_POINT ( 'NONE',  ( 0.6000166863083106206, 48.97316450298212942, -3.667784109282603122 ) ) ;
#37989=CARTESIAN_POINT ( 'NONE',  ( 0.3676999524040323597, -31.10876963919482563, -31.27610965031216139 ) ) ;
#37998=FACE_OUTER_BOUND ( 'NONE', #28435, .T. ) ;
#38009=( BOUNDED_SURFACE ( )  B_SPLINE_SURFACE ( 3, 1, ( 
 ( #1206, #4649 ),
 ( #9377, #19416 ),
 ( #23799, #29110 ),
 ( #43542, #587 ) ),
 .UNSPECIFIED., .F., .F., .F. ) 
 B_SPLINE_SURFACE_WITH_KNOTS ( ( 4, 4 ),
 ( 2, 2 ),
 ( 0.000000000000000000, 1.000000000000000000 ),
 ( 0.000000000000000000, 1.000000000000000000 ),
 .UNSPECIFIED. ) 
 GEOMETRIC_REPRESENTATION_ITEM ( )  RATIONAL_B_SPLINE_SURFACE ( (
 ( 1.000000000000000000, 1.000000000000000000),
 ( 0.7211978278499970862, 0.9934217856018976445),
 ( 0.7211978278499970862, 0.9934217856018976445),
 ( 1.000000000000000000, 1.000000000000000000) ) ) 
 REPRESENTATION_ITEM ( '' )  SURFACE ( )  );
#38013=CARTESIAN_POINT ( 'NONE',  ( 0.1119898979215348395, 20.90518435893999083, 38.85787661685284888 ) ) ;
#38016=CARTESIAN_POINT ( 'NONE',  ( 0.5987334363312692975, 5.317554374040649456, -48.81891561629772980 ) ) ;
#38018=EDGE_CURVE ( 'NONE', #759, #19623, #21344, .T. ) ;
#38022=B_SPLINE_CURVE_WITH_KNOTS ( 'NONE', 3,
 ( #25138, #26684, #16999, #60189 ),
 .UNSPECIFIED., .F., .F.,
 ( 4, 4 ),
 ( 0.000000000000000000, 0.004442905043737212234 ),
 .UNSPECIFIED. ) ;
#38030=CARTESIAN_POINT ( 'NONE',  ( 4.834790513006553603, -22.26269597880833473, 41.67687258755787383 ) ) ;
#38033=EDGE_LOOP ( 'NONE', ( #26424, #11490, #14633, #17123 ) ) ;
#38035=CARTESIAN_POINT ( 'NONE',  ( -6.078726893082806448, -17.34758611460008382, 8.357948149232223400 ) ) ;
#38036=ADVANCED_FACE ( 'NONE', ( #10668 ), #44039, .F. ) ;
#38038=CARTESIAN_POINT ( 'NONE',  ( 0.1119899015040013435, -23.35186486751172552, 37.43863933694675694 ) ) ;
#38039=CARTESIAN_POINT ( 'NONE',  ( 4.553261556744873317, 35.06776520399894537, -26.45357082552063233 ) ) ;
#38046=CARTESIAN_POINT ( 'NONE',  ( 0.6000166863083106206, 41.44150143800037966, 26.35195325346237283 ) ) ;
#38049=CARTESIAN_POINT ( 'NONE',  ( 2.009741617377216460, 34.40621083346663767, 27.49030253936991741 ) ) ;
#38064=CARTESIAN_POINT ( 'NONE',  ( 4.553261556744875094, 0.000000000000000000, 0.000000000000000000 ) ) ;
#38067=FACE_OUTER_BOUND ( 'NONE', #44758, .T. ) ;
#38073=CARTESIAN_POINT ( 'NONE',  ( 2.648799415243708655, -48.43667485455544863, 7.642381325455785301 ) ) ;
#38074=CARTESIAN_POINT ( 'NONE',  ( 0.1129192098497447394, -22.45785791439742241, 37.98152716363431125 ) ) ;
#38077=CARTESIAN_POINT ( 'NONE',  ( 2.299652685299201860, -38.51197436690490150, -30.34978674094784523 ) ) ;
#38078=CARTESIAN_POINT ( 'NONE',  ( -6.078726893082806448, 0.6205993875982012131, 19.24600991553399254 ) ) ;
#38079=CARTESIAN_POINT ( 'NONE',  ( 0.1157991065609915576, -35.31295772492552487, -26.45632972003714656 ) ) ;
#38081=B_SPLINE_CURVE_WITH_KNOTS ( 'NONE', 3,
 ( #17302, #7564, #26688, #41132 ),
 .UNSPECIFIED., .F., .F.,
 ( 4, 4 ),
 ( 0.000000000000000000, 0.004444103432399267896 ),
 .UNSPECIFIED. ) ;
#38086=CARTESIAN_POINT ( 'NONE',  ( 0.8744876279028263033, 48.35212675551510841, -8.510105087370661181 ) ) ;
#38099=CARTESIAN_POINT ( 'NONE',  ( -6.072942160501519915, -18.89839206595250687, 3.695259072184732929 ) ) ;
#38108=( BOUNDED_SURFACE ( )  B_SPLINE_SURFACE ( 3, 1, ( 
 ( #8177, #21986 ),
 ( #45811, #41419 ),
 ( #16351, #59244 ),
 ( #17593, #35476 ) ),
 .UNSPECIFIED., .F., .F., .F. ) 
 B_SPLINE_SURFACE_WITH_KNOTS ( ( 4, 4 ),
 ( 2, 2 ),
 ( 0.000000000000000000, 1.000000000000000000 ),
 ( 0.000000000000000000, 1.000000000000000000 ),
 .UNSPECIFIED. ) 
 GEOMETRIC_REPRESENTATION_ITEM ( )  RATIONAL_B_SPLINE_SURFACE ( (
 ( 1.000000000000000000, 1.000000000000000000),
 ( 0.7211978278499968642, 0.9934217856018975334),
 ( 0.7211978278499968642, 0.9934217856018975334),
 ( 1.000000000000000000, 1.000000000000000000) ) ) 
 REPRESENTATION_ITEM ( '' )  SURFACE ( )  );
#38115=CARTESIAN_POINT ( 'NONE',  ( 3.727782113643637096, 43.95811118998071976, 0.6798797800101179512 ) ) ;
#38120=CARTESIAN_POINT ( 'NONE',  ( 0.8744876279028306332, 46.30617036199629410, -16.31222353896820110 ) ) ;
#38121=EDGE_LOOP ( 'NONE', ( #37664, #11514, #43557, #28886 ) ) ;
#38130=CARTESIAN_POINT ( 'NONE',  ( 4.834790513006555379, -15.88524143731160088, 44.49998253261117043 ) ) ;
#38131=CARTESIAN_POINT ( 'NONE',  ( 4.975610109902397937, -40.67634447773618689, 27.16402781375239073 ) ) ;
#38134=EDGE_CURVE ( 'NONE', #10258, #48557, #43755, .T. ) ;
#38139=ORIENTED_EDGE ( 'NONE', *, *, #1404, .F. ) ;
#38140=CARTESIAN_POINT ( 'NONE',  ( 0.5997462898726536595, -1.051648045106814422, -49.09628974305016413 ) ) ;
#38142=CARTESIAN_POINT ( 'NONE',  ( -6.078075953587585900, -8.911363828324688541, -17.06993757945125623 ) ) ;
#38143=CARTESIAN_POINT ( 'NONE',  ( 5.901764892641288895, -37.25947723020453850, 31.77613607680373420 ) ) ;
#38146=EDGE_CURVE ( 'NONE', #44906, #2290, #29542, .T. ) ;
#38147=CARTESIAN_POINT ( 'NONE',  ( 2.879087469061463178, -16.21381997011050657, 40.90493513942082160 ) ) ;
#38155=CARTESIAN_POINT ( 'NONE',  ( -6.079354080745853928, -4.283721817891188444, -18.77345686428274618 ) ) ;
#38159=ADVANCED_FACE ( 'NONE', ( #2479 ), #7705, .F. ) ;
#38164=CARTESIAN_POINT ( 'NONE',  ( 0.1129192098497455998, 29.30421273086464140, 32.98810246148426728 ) ) ;
#38169=CARTESIAN_POINT ( 'NONE',  ( 3.390910168358336474, 32.17648676134584917, -29.97950693774952313 ) ) ;
#38172=ORIENTED_EDGE ( 'NONE', *, *, #19888, .T. ) ;
#38181=ORIENTED_EDGE ( 'NONE', *, *, #48205, .T. ) ;
#38182=CARTESIAN_POINT ( 'NONE',  ( 4.975610109902397937, -46.59897809419034331, -14.86555238512655919 ) ) ;
#38187=LINE ( 'NONE', #39112, #43535 ) ;
#38189=CARTESIAN_POINT ( 'NONE',  ( 0.6253024248130484297, -48.61070664296096311, -6.960131255201589262 ) ) ;
#38198=CARTESIAN_POINT ( 'NONE',  ( 0.6026112563231247332, -42.70250234240587162, -24.24948017176923543 ) ) ;
#38215=CARTESIAN_POINT ( 'NONE',  ( 5.901764892641288895, 42.68902166415562505, 23.99247583716464760 ) ) ;
#38218=EDGE_CURVE ( 'NONE', #31834, #31616, #24722, .T. ) ;
#38223=CARTESIAN_POINT ( 'NONE',  ( 1.479689385636123067, -38.95645166531898695, -20.59074352507356664 ) ) ;
#38228=EDGE_CURVE ( 'NONE', #19345, #47387, #4115, .T. ) ;
#38230=CARTESIAN_POINT ( 'NONE',  ( 0.6039202388192952409, 48.99530948556955678, 3.320144765254842145 ) ) ;
#38231=CARTESIAN_POINT ( 'NONE',  ( 2.648799415243696664, 26.90653288552037736, 40.99458441513962725 ) ) ;
#38233=CARTESIAN_POINT ( 'NONE',  ( 0.6039202388192953519, -7.665580222077140071, 48.50569649750317325 ) ) ;
#38234=CARTESIAN_POINT ( 'NONE',  ( 4.694002226626921015, -4.720386398734341959, 45.34316622924319518 ) ) ;
#38239=EDGE_LOOP ( 'NONE', ( #55341, #20255, #35021, #32080 ) ) ;
#38243=CARTESIAN_POINT ( 'NONE',  ( 0.8744876279028263033, -8.712669995482247742, 48.31603700562906312 ) ) ;
#38253=ADVANCED_FACE ( 'NONE', ( #53309 ), #48390, .F. ) ;
#38256=CARTESIAN_POINT ( 'NONE',  ( 0.6000166863083090663, 16.46965316277509217, -46.26633772416342083 ) ) ;
#38258=EDGE_LOOP ( 'NONE', ( #54713, #23652, #17584, #9671 ) ) ;
#38260=ORIENTED_EDGE ( 'NONE', *, *, #12603, .F. ) ;
#38261=CARTESIAN_POINT ( 'NONE',  ( 4.834790513006555379, -10.96306168285373595, -45.96085964668552037 ) ) ;
#38262=CARTESIAN_POINT ( 'NONE',  ( 0.5980271706414711508, -14.64360625457728204, 46.87871626551400794 ) ) ;
#38265=ORIENTED_EDGE ( 'NONE', *, *, #50720, .T. ) ;
#38273=ADVANCED_FACE ( 'NONE', ( #57688 ), #37616, .F. ) ;
#38274=LINE ( 'NONE', #52641, #20790 ) ;
#38278=B_SPLINE_CURVE_WITH_KNOTS ( 'NONE', 3,
 ( #14592, #24279, #13984, #8948 ),
 .UNSPECIFIED., .F., .F.,
 ( 4, 4 ),
 ( 0.000000000000000000, 0.004444103432399267896 ),
 .UNSPECIFIED. ) ;
#38286=CARTESIAN_POINT ( 'NONE',  ( 0.3676999524040366896, 34.11874447324979087, 27.96179284115963171 ) ) ;
#38289=ADVANCED_FACE ( 'NONE', ( #43966 ), #38108, .F. ) ;
#38290=VERTEX_POINT ( 'NONE', #21363 ) ;
#38292=EDGE_CURVE ( 'NONE', #43179, #4300, #12370, .T. ) ;
#38297=CARTESIAN_POINT ( 'NONE',  ( 0.6039202388192953519, -39.45949250020231602, -29.23204003273579588 ) ) ;
#38298=VECTOR ( 'NONE', #51028, 1000.000000000000114 ) ;
#38300=DIRECTION ( 'NONE',  ( 0.000000000000000000, 0.000000000000000000, 1.000000000000000000 ) ) ;
#38301=CARTESIAN_POINT ( 'NONE',  ( 0.7948878604505665857, 46.86364170957251929, 14.64574112208839551 ) ) ;
#38308=LINE ( 'NONE', #11890, #1740 ) ;
#38312=ORIENTED_EDGE ( 'NONE', *, *, #59594, .F. ) ;
#38313=LINE ( 'NONE', #1285, #37939 ) ;
#38318=CARTESIAN_POINT ( 'NONE',  ( 4.975610109902397937, -11.44439439467527642, -47.55497076097196185 ) ) ;
#38320=ORIENTED_EDGE ( 'NONE', *, *, #32356, .T. ) ;
#38323=EDGE_LOOP ( 'NONE', ( #25064, #50467, #15801, #47465 ) ) ;
#38332=B_SPLINE_CURVE_WITH_KNOTS ( 'NONE', 3,
 ( #36229, #55294, #12417, #31507 ),
 .UNSPECIFIED., .F., .F.,
 ( 4, 4 ),
 ( 0.000000000000000000, 0.004444103432399266161 ),
 .UNSPECIFIED. ) ;
#38334=CARTESIAN_POINT ( 'NONE',  ( -6.078726893082806448, 17.84743921491351415, 7.229312189875837014 ) ) ;
#38338=ORIENTED_EDGE ( 'NONE', *, *, #54861, .F. ) ;
#38339=ORIENTED_EDGE ( 'NONE', *, *, #46152, .F. ) ;
#38342=CARTESIAN_POINT ( 'NONE',  ( 4.553261556744875094, 35.06776520399859010, 26.45357082552112260 ) ) ;
#38346=VECTOR ( 'NONE', #29342, 1000.000000000000000 ) ;
#38347=ORIENTED_EDGE ( 'NONE', *, *, #44718, .T. ) ;
#38353=B_SPLINE_CURVE_WITH_KNOTS ( 'NONE', 3,
 ( #47449, #52434, #9527, #28637, #4809, #112, #19262, #14565, #33665, #49909, #21094, #48671, #40238, #34280, #44614, #44929 ),
 .UNSPECIFIED., .F., .F.,
 ( 4, 3, 3, 3, 3, 4 ),
 ( 2.221635811791082109E-17, 0.0002612764279487776080, 0.0003919131003184762635, 0.0005225497727000636295, 0.0007837925190632439448, 0.001045051706266717385 ),
 .UNSPECIFIED. ) ;
#38356=EDGE_CURVE ( 'NONE', #1298, #12205, #54694, .T. ) ;
#38357=CARTESIAN_POINT ( 'NONE',  ( -6.077587904424778920, 12.00112336472165353, 15.05885318935882644 ) ) ;
#38361=VERTEX_POINT ( 'NONE', #4373 ) ;
#38365=CARTESIAN_POINT ( 'NONE',  ( 4.834790513006553603, 37.58952546674443340, 28.62895241026735604 ) ) ;
#38367=CARTESIAN_POINT ( 'NONE',  ( 4.834790513006553603, -42.76900418948107330, 20.08486050647432108 ) ) ;
#38376=ORIENTED_EDGE ( 'NONE', *, *, #11767, .T. ) ;
#38380=EDGE_CURVE ( 'NONE', #26359, #4753, #16808, .T. ) ;
#38381=CARTESIAN_POINT ( 'NONE',  ( 0.2279481005628803680, -26.91014123888646736, -34.96209069229257693 ) ) ;
#38394=CARTESIAN_POINT ( 'NONE',  ( 0.1119898979215352142, 14.71105701693103107, -41.59983304890096889 ) ) ;
#38396=CARTESIAN_POINT ( 'NONE',  ( -6.063463321072276813, -18.89860197674391529, 3.696389563355157559 ) ) ;
#38401=VERTEX_POINT ( 'NONE', #42341 ) ;
#38410=ORIENTED_EDGE ( 'NONE', *, *, #8630, .T. ) ;
#38412=VERTEX_POINT ( 'NONE', #14442 ) ;
#38415=CARTESIAN_POINT ( 'NONE',  ( 2.299746137290198611, -40.05309593391260847, -28.28481648862038966 ) ) ;
#38423=B_SPLINE_CURVE_WITH_KNOTS ( 'NONE', 3,
 ( #44272, #34546, #30750, #20752, #11051, #53611 ),
 .UNSPECIFIED., .F., .F.,
 ( 4, 2, 4 ),
 ( 3.144186300207962859E-18, 0.0002447193893791683528, 0.0004894387787583335614 ),
 .UNSPECIFIED. ) ;
#38433=ADVANCED_FACE ( 'NONE', ( #37031 ), #18034, .F. ) ;
#38440=CARTESIAN_POINT ( 'NONE',  ( 0.2940135542859018680, -43.64383946108019785, 6.438619866623495724 ) ) ;
#38446=CARTESIAN_POINT ( 'NONE',  ( 1.296416391601052265, -16.81764146547304151, 40.73664578257469771 ) ) ;
#38451=CARTESIAN_POINT ( 'NONE',  ( 0.6016118706126977189, 22.40471323146671168, 43.69874002531047097 ) ) ;
#38452=EDGE_CURVE ( 'NONE', #15681, #13767, #19801, .T. ) ;
#38457=CARTESIAN_POINT ( 'NONE',  ( 0.2940135542859017570, 39.39157462944580601, -19.86314166752638499 ) ) ;
#38458=CARTESIAN_POINT ( 'NONE',  ( 4.834790513006553603, 41.39428925248056146, -22.78381351324563298 ) ) ;
#38463=CARTESIAN_POINT ( 'NONE',  ( -2.601141883200662974, -5.629531953699331126, 13.82402971103819667 ) ) ;
#38468=CARTESIAN_POINT ( 'NONE',  ( 0.1156495703730067298, 9.685606167693753932, -43.04801954091968241 ) ) ;
#38474=CARTESIAN_POINT ( 'NONE',  ( 0.8753041380234465318, 28.81806460335508646, -39.75748332565621723 ) ) ;
#38476=ORIENTED_EDGE ( 'NONE', *, *, #17762, .F. ) ;
#38478=EDGE_CURVE ( 'NONE', #1744, #41667, #38880, .T. ) ;
#38479=CARTESIAN_POINT ( 'NONE',  ( 0.1129192098497455998, 20.83764143887614040, -38.89401608281131928 ) ) ;
#38483=CARTESIAN_POINT ( 'NONE',  ( 0.5980271706414734822, 23.33483692714744961, 43.21498152753393640 ) ) ;
#38490=CARTESIAN_POINT ( 'NONE',  ( 0.5987334363312691865, -48.62339724184305112, -6.879545561590992619 ) ) ;
#38494=CARTESIAN_POINT ( 'NONE',  ( 0.6029443449137436017, -7.794573848081279621, -48.48488585642065374 ) ) ;
#38498=B_SPLINE_CURVE_WITH_KNOTS ( 'NONE', 3,
 ( #48389, #131, #42785, #5449, #9551, #5141 ),
 .UNSPECIFIED., .F., .F.,
 ( 4, 2, 4 ),
 ( 0.000000000000000000, 0.0002447195606305752340, 0.0004894391212611504680 ),
 .UNSPECIFIED. ) ;
#38499=ORIENTED_EDGE ( 'NONE', *, *, #51126, .F. ) ;
#38507=EDGE_CURVE ( 'NONE', #20167, #60001, #47415, .T. ) ;
#38509=CARTESIAN_POINT ( 'NONE',  ( -6.057079549204054558, 19.25697688790420159, 0.008499321259854933364 ) ) ;
#38510=ORIENTED_EDGE ( 'NONE', *, *, #15917, .T. ) ;
#38514=DIRECTION ( 'NONE',  ( 0.1011922191286468153, -0.6101824289146793312, 0.7857719377984951903 ) ) ;
#38516=CARTESIAN_POINT ( 'NONE',  ( -2.739355103387247858, -12.11899594566314242, 8.716507570123328108 ) ) ;
#38520=B_SPLINE_CURVE_WITH_KNOTS ( 'NONE', 3,
 ( #2629, #45276, #51470, #12683, #21754, #40893, #8254, #36487, #27068, #46195, #27374, #26139, #2316, #40579, #17368, #55874 ),
 .UNSPECIFIED., .F., .F.,
 ( 4, 3, 3, 3, 3, 4 ),
 ( 2.081781105835003155E-17, 0.0002612764279487750059, 0.0003919131003184785403, 0.0005225497727000651474, 0.0007837925190632448122, 0.001045051706266716084 ),
 .UNSPECIFIED. ) ;
#38523=CARTESIAN_POINT ( 'NONE',  ( 3.240649175237395596, -8.819624127022542837, 43.09848196463181580 ) ) ;
#38532=CARTESIAN_POINT ( 'NONE',  ( 4.335381028904201628, 48.70445384730871297, 5.256712194872322108 ) ) ;
#38536=LINE ( 'NONE', #53519, #31248 ) ;
#38538=CARTESIAN_POINT ( 'NONE',  ( -2.601141883200665639, -0.03040527887379005853, -14.92630238834806811 ) ) ;
#38539=( BOUNDED_SURFACE ( )  B_SPLINE_SURFACE ( 3, 1, ( 
 ( #36448, #2898 ),
 ( #27643, #26714 ),
 ( #22029, #31420 ),
 ( #50518, #46777 ) ),
 .UNSPECIFIED., .F., .F., .F. ) 
 B_SPLINE_SURFACE_WITH_KNOTS ( ( 4, 4 ),
 ( 2, 2 ),
 ( 0.000000000000000000, 1.000000000000000000 ),
 ( 0.000000000000000000, 1.000000000000000000 ),
 .UNSPECIFIED. ) 
 GEOMETRIC_REPRESENTATION_ITEM ( )  RATIONAL_B_SPLINE_SURFACE ( (
 ( 1.000000000000000000, 1.000000000000000000),
 ( 0.9953485035131437453, 0.8621029689291523912),
 ( 0.9953485035131437453, 0.8621029689291523912),
 ( 1.000000000000000000, 1.000000000000000000) ) ) 
 REPRESENTATION_ITEM ( '' )  SURFACE ( )  );
#38543=EDGE_CURVE ( 'NONE', #57626, #7870, #51056, .T. ) ;
#38545=CARTESIAN_POINT ( 'NONE',  ( 0.5997462898726536595, -47.36625756029525292, -12.96106765957508244 ) ) ;
#38550=CARTESIAN_POINT ( 'NONE',  ( 4.975610109902397937, 30.94437158899635776, -37.88001153774755636 ) ) ;
#38552=EDGE_CURVE ( 'NONE', #5530, #40357, #30204, .T. ) ;
#38562=EDGE_LOOP ( 'NONE', ( #31830, #45894, #19863, #1745 ) ) ;
#38566=CARTESIAN_POINT ( 'NONE',  ( 0.5980271706414734822, -48.61493274831096301, 6.974063142735757559 ) ) ;
#38567=ORIENTED_EDGE ( 'NONE', *, *, #7457, .T. ) ;
#38568=CARTESIAN_POINT ( 'NONE',  ( 0.1129192098497447394, 9.345467776859020859, -43.12324222292247811 ) ) ;
#38571=CARTESIAN_POINT ( 'NONE',  ( 0.5997462898726536595, -25.00873172704203640, -42.26245340191634625 ) ) ;
#38582=ORIENTED_EDGE ( 'NONE', *, *, #21786, .F. ) ;
#38587=B_SPLINE_CURVE_WITH_KNOTS ( 'NONE', 3,
 ( #26820, #11188, #12126, #16194 ),
 .UNSPECIFIED., .F., .F.,
 ( 4, 4 ),
 ( 0.000000000000000000, 0.004444103432399267029 ),
 .UNSPECIFIED. ) ;
#38591=CARTESIAN_POINT ( 'NONE',  ( 0.1139756605157202229, 24.91714249760716982, -36.41553555076405502 ) ) ;
#38594=EDGE_LOOP ( 'NONE', ( #24654, #48718, #21057, #22996 ) ) ;
#38596=CARTESIAN_POINT ( 'NONE',  ( -2.739355103387248747, -14.83685109948651260, -1.647852057280288829 ) ) ;
#38602=CARTESIAN_POINT ( 'NONE',  ( 0.7948884756798515472, -35.86813339442895199, 33.52872874714461915 ) ) ;
#38603=CARTESIAN_POINT ( 'NONE',  ( 4.553261556744875094, 0.000000000000000000, 0.000000000000000000 ) ) ;
#38607=CARTESIAN_POINT ( 'NONE',  ( 0.1119899015040009133, 33.95944448262266491, -28.17299129705921601 ) ) ;
#38623=CARTESIAN_POINT ( 'NONE',  ( -6.078075953587585900, 15.42887869085119767, -11.52149628260729308 ) ) ;
#38626=ORIENTED_EDGE ( 'NONE', *, *, #11040, .T. ) ;
#38629=ORIENTED_EDGE ( 'NONE', *, *, #1379, .T. ) ;
#38632=EDGE_CURVE ( 'NONE', #61039, #61495, #7470, .T. ) ;
#38635=CARTESIAN_POINT ( 'NONE',  ( 0.6039202388192953519, -48.72646899558811384, -6.106957677189313038 ) ) ;
#38636=ORIENTED_EDGE ( 'NONE', *, *, #30122, .F. ) ;
#38637=CARTESIAN_POINT ( 'NONE',  ( 0.2940133293162995876, -23.55385447652355424, 37.30223168761883556 ) ) ;
#38659=CARTESIAN_POINT ( 'NONE',  ( 4.694002226626921015, -10.47998749083617653, 44.36726984656654338 ) ) ;
#38660=VERTEX_POINT ( 'NONE', #3391 ) ;
#38662=CARTESIAN_POINT ( 'NONE',  ( 0.5997462898726536595, -14.47257175146244457, -46.92649887902442885 ) ) ;
#38664=CARTESIAN_POINT ( 'NONE',  ( 0.8744876279028263033, -29.90976330662845939, -38.93271258621668096 ) ) ;
#38670=CARTESIAN_POINT ( 'NONE',  ( 3.240649175237396484, -32.84582282638324102, 29.26460046293974315 ) ) ;
#38684=CARTESIAN_POINT ( 'NONE',  ( 0.1365634738349421895, -35.73818327155645846, 25.87749748472385747 ) ) ;
#38692=CARTESIAN_POINT ( 'NONE',  ( 0.5997462898726536595, 48.29911994996575686, -8.873930482211887849 ) ) ;
#38699=VERTEX_POINT ( 'NONE', #46652 ) ;
#38702=VECTOR ( 'NONE', #46662, 1000.000000000000114 ) ;
#38703=CARTESIAN_POINT ( 'NONE',  ( 0.6253024248130484297, -34.79435467495893164, -34.65251953568179033 ) ) ;
#38716=CARTESIAN_POINT ( 'NONE',  ( 3.894904216938897878, -39.85650388126904176, 18.53600363720797262 ) ) ;
#38718=EDGE_CURVE ( 'NONE', #60263, #55634, #28654, .T. ) ;
#38721=CARTESIAN_POINT ( 'NONE',  ( 3.678834586032786458, -41.73552251152050729, -25.62730048832143126 ) ) ;
#38725=ORIENTED_EDGE ( 'NONE', *, *, #41553, .T. ) ;
#38727=EDGE_CURVE ( 'NONE', #42399, #6528, #12261, .T. ) ;
#38730=CARTESIAN_POINT ( 'NONE',  ( 0.1145239942831223490, 41.97809357794537277, -13.59356981318502022 ) ) ;
#38733=CARTESIAN_POINT ( 'NONE',  ( 0.1135584504625007929, -40.73546803870070221, -16.95799798924523927 ) ) ;
#38734=ORIENTED_EDGE ( 'NONE', *, *, #11772, .F. ) ;
#38741=ORIENTED_EDGE ( 'NONE', *, *, #60043, .T. ) ;
#38745=CARTESIAN_POINT ( 'NONE',  ( 0.1147471544378676767, 10.12104602677796272, 42.94783598503057931 ) ) ;
#38748=CIRCLE ( 'NONE', #51673, 43.92652462719577500 ) ;
#38754=CARTESIAN_POINT ( 'NONE',  ( 0.2279481005628792856, -7.789954559295118486, 43.42603015516188947 ) ) ;
#38759=DIRECTION ( 'NONE',  ( -1.000000000000000000, -0.000000000000000000, -0.000000000000000000 ) ) ;
#38761=B_SPLINE_CURVE_WITH_KNOTS ( 'NONE', 3,
 ( #39280, #33647, #1324, #38664 ),
 .UNSPECIFIED., .F., .F.,
 ( 4, 4 ),
 ( 0.000000000000000000, 0.004444103432399266161 ),
 .UNSPECIFIED. ) ;
#38772=DIRECTION ( 'NONE',  ( 0.000000000000000000, 0.000000000000000000, 1.000000000000000000 ) ) ;
#38776=ORIENTED_EDGE ( 'NONE', *, *, #10260, .T. ) ;
#38781=LINE ( 'NONE', #1750, #20505 ) ;
#38785=ORIENTED_EDGE ( 'NONE', *, *, #17289, .T. ) ;
#38796=DIRECTION ( 'NONE',  ( 1.000000000000000000, 0.000000000000000000, 0.000000000000000000 ) ) ;
#38799=ORIENTED_EDGE ( 'NONE', *, *, #12857, .F. ) ;
#38804=ORIENTED_EDGE ( 'NONE', *, *, #8319, .F. ) ;
#38805=CARTESIAN_POINT ( 'NONE',  ( 0.5997462898726536595, 16.46871699354475993, 46.26373299606117229 ) ) ;
#38809=EDGE_CURVE ( 'NONE', #31065, #29981, #34659, .T. ) ;
#38811=ORIENTED_EDGE ( 'NONE', *, *, #21786, .T. ) ;
#38821=ORIENTED_EDGE ( 'NONE', *, *, #56524, .T. ) ;
#38822=CARTESIAN_POINT ( 'NONE',  ( 4.975610109902397937, 0.000000000000000000, 0.000000000000000000 ) ) ;
#38823=CARTESIAN_POINT ( 'NONE',  ( 0.1368894036331269326, -38.12855930276679572, 22.20527620676512726 ) ) ;
#38824=CARTESIAN_POINT ( 'NONE',  ( 4.975610109902397937, -27.50982196586606321, 40.44328253918227034 ) ) ;
#38827=ORIENTED_EDGE ( 'NONE', *, *, #1811, .F. ) ;
#38829=CARTESIAN_POINT ( 'NONE',  ( 0.8753041380234530822, 48.01981714478404939, -10.25843502950054109 ) ) ;
#38839=CARTESIAN_POINT ( 'NONE',  ( 2.648799415243708655, -47.06172439114165229, 13.77358198225216235 ) ) ;
#38841=CARTESIAN_POINT ( 'NONE',  ( 0.1147471544378677044, -42.60137459085243705, 11.49239189390608828 ) ) ;
#38842=DIRECTION ( 'NONE',  ( 1.000000000000000000, 0.000000000000000000, 0.000000000000000000 ) ) ;
#38845=( BOUNDED_SURFACE ( )  B_SPLINE_SURFACE ( 3, 1, ( 
 ( #17142, #53767 ),
 ( #10901, #54082 ),
 ( #6454, #29990 ),
 ( #20903, #49101 ) ),
 .UNSPECIFIED., .F., .F., .F. ) 
 B_SPLINE_SURFACE_WITH_KNOTS ( ( 4, 4 ),
 ( 2, 2 ),
 ( 0.000000000000000000, 1.000000000000000000 ),
 ( 0.000000000000000000, 1.000000000000000000 ),
 .UNSPECIFIED. ) 
 GEOMETRIC_REPRESENTATION_ITEM ( )  RATIONAL_B_SPLINE_SURFACE ( (
 ( 1.000000000000000000, 1.000000000000000000),
 ( 0.9754377213608244057, 0.9999580625633939235),
 ( 0.9754377213608244057, 0.9999580625633939235),
 ( 1.000000000000000000, 1.000000000000000000) ) ) 
 REPRESENTATION_ITEM ( '' )  SURFACE ( )  );
#38852=FILL_AREA_STYLE_COLOUR ( '', #48246 ) ;
#38853=CARTESIAN_POINT ( 'NONE',  ( -6.077587904424778920, 7.800189710370596607, 17.60548385805284255 ) ) ;
#38859=VECTOR ( 'NONE', #61740, 1000.000000000000227 ) ;
#38862=CARTESIAN_POINT ( 'NONE',  ( 2.009741617377216460, 40.25399224802043108, 17.86393533685553336 ) ) ;
#38866=CARTESIAN_POINT ( 'NONE',  ( 0.6253024248130452101, 32.50267139205902822, 36.81060417593644729 ) ) ;
#38877=ORIENTED_EDGE ( 'NONE', *, *, #49242, .T. ) ;
#38880=LINE ( 'NONE', #15059, #30705 ) ;
#38881=CARTESIAN_POINT ( 'NONE',  ( 3.678748215320120973, -48.94071388080758567, 1.849145515207392343 ) ) ;
#38883=CARTESIAN_POINT ( 'NONE',  ( 0.8744876279028306332, 3.827863332835647281, -48.94586308039347955 ) ) ;
#38884=EDGE_CURVE ( 'NONE', #59386, #51399, #36893, .T. ) ;
#38887=CARTESIAN_POINT ( 'NONE',  ( 4.975610109902397937, 48.90928568712962488, -0.5754830253892166958 ) ) ;
#38890=LINE ( 'NONE', #13001, #61375 ) ;
#38897=CARTESIAN_POINT ( 'NONE',  ( 0.1156495703730067298, -17.73599580866132541, 40.40269057756201931 ) ) ;
#38899=DIRECTION ( 'NONE',  ( 1.000000000000000000, 0.000000000000000000, 0.000000000000000000 ) ) ;
#38913=AXIS2_PLACEMENT_3D ( 'NONE', #61602, #51911, #9001 ) ;
#38928=CARTESIAN_POINT ( 'NONE',  ( 0.1147471544378676073, -43.80064347916233913, -5.334399618003720533 ) ) ;
#38929=CARTESIAN_POINT ( 'NONE',  ( 0.1157506346131639274, 39.79465037914078351, 19.06112433737277101 ) ) ;
#38931=CARTESIAN_POINT ( 'NONE',  ( 0.7044674535452954967, -45.19827881396718539, -19.20724642070773669 ) ) ;
#38935=CARTESIAN_POINT ( 'NONE',  ( 0.1365634738349416066, -44.11867064301219443, -0.6368047712308788633 ) ) ;
#38936=CARTESIAN_POINT ( 'NONE',  ( 0.7413678028165013867, 19.56431516233115886, -39.51864957205928874 ) ) ;
#38940=CARTESIAN_POINT ( 'NONE',  ( 2.879087469061463622, 26.57443547924880178, 35.06994519161131052 ) ) ;
#38945=CARTESIAN_POINT ( 'NONE',  ( 0.5980271706414734822, 22.09347986454800861, -43.86259671196490473 ) ) ;
#38947=CARTESIAN_POINT ( 'NONE',  ( 4.975610109902397937, 47.45567470742105343, -11.84940273605426242 ) ) ;
#38948=ORIENTED_EDGE ( 'NONE', *, *, #32508, .F. ) ;
#38954=EDGE_CURVE ( 'NONE', #52762, #57626, #33891, .T. ) ;
#38967=ORIENTED_EDGE ( 'NONE', *, *, #34770, .F. ) ;
#38972=CARTESIAN_POINT ( 'NONE',  ( 0.1149546198390367646, 37.12868760141555668, -23.84129027589972338 ) ) ;
#38984=CARTESIAN_POINT ( 'NONE',  ( 0.1152809850208375425, -31.85007772001079829, 30.53715493819007776 ) ) ;
#38986=CARTESIAN_POINT ( 'NONE',  ( -6.079354080745853928, -17.34954932540436090, -8.353807123313488958 ) ) ;
#38990=( BOUNDED_SURFACE ( )  B_SPLINE_SURFACE ( 3, 1, ( 
 ( #51304, #36322 ),
 ( #8389, #51003 ),
 ( #31600, #27512 ),
 ( #7780, #16904 ) ),
 .UNSPECIFIED., .F., .F., .F. ) 
 B_SPLINE_SURFACE_WITH_KNOTS ( ( 4, 4 ),
 ( 2, 2 ),
 ( 0.000000000000000000, 1.000000000000000000 ),
 ( 0.000000000000000000, 1.000000000000000000 ),
 .UNSPECIFIED. ) 
 GEOMETRIC_REPRESENTATION_ITEM ( )  RATIONAL_B_SPLINE_SURFACE ( (
 ( 1.000000000000000000, 1.000000000000000000),
 ( 0.9953485035131437453, 0.8621029689291515030),
 ( 0.9953485035131437453, 0.8621029689291515030),
 ( 1.000000000000000000, 1.000000000000000000) ) ) 
 REPRESENTATION_ITEM ( '' )  SURFACE ( )  );
#38997=CARTESIAN_POINT ( 'NONE',  ( 2.648799415243708655, -43.38879977521469300, -22.84577679475856371 ) ) ;
#38998=CARTESIAN_POINT ( 'NONE',  ( 0.1119899015040011631, -27.07006270142763782, -34.84498548619703939 ) ) ;
#39001=CARTESIAN_POINT ( 'NONE',  ( 0.6016118706126977189, 33.27208259263638013, -36.11813359979602467 ) ) ;
#39005=CARTESIAN_POINT ( 'NONE',  ( 0.6253024248130506502, 48.32746506278895282, -8.712080579434449135 ) ) ;
#39010=CARTESIAN_POINT ( 'NONE',  ( -6.078457390727109555, 3.068934028528590652, -19.00989623764546721 ) ) ;
#39016=CARTESIAN_POINT ( 'NONE',  ( 3.559346040607745287, 43.70094520706050645, -4.863915043612893285 ) ) ;
#39017=CARTESIAN_POINT ( 'NONE',  ( 0.7242486021783847150, -34.69771184318253887, -34.74306053331289235 ) ) ;
#39018=VERTEX_POINT ( 'NONE', #16212 ) ;
#39022=ORIENTED_EDGE ( 'NONE', *, *, #49831, .T. ) ;
#39029=CARTESIAN_POINT ( 'NONE',  ( 0.1365634738349393862, 14.63942591880842770, 41.62390933575277074 ) ) ;
#39035=VERTEX_POINT ( 'NONE', #50938 ) ;
#39036=ORIENTED_EDGE ( 'NONE', *, *, #10941, .F. ) ;
#39038=CARTESIAN_POINT ( 'NONE',  ( 1.479689385636123067, 44.03253894626729448, 1.649047971753838215 ) ) ;
#39039=ORIENTED_EDGE ( 'NONE', *, *, #24176, .T. ) ;
#39041=CARTESIAN_POINT ( 'NONE',  ( -6.057079549204054558, 17.84642505839074644, 7.234386203056984321 ) ) ;
#39042=CARTESIAN_POINT ( 'NONE',  ( 2.299652685299202748, -21.01913371789099827, 44.29986165449697211 ) ) ;
#39050=CARTESIAN_POINT ( 'NONE',  ( 0.6016117650947689910, 4.368597403151937009, -48.91284505090327883 ) ) ;
#39058=DIRECTION ( 'NONE',  ( -1.000000000000000000, -0.000000000000000000, -0.000000000000000000 ) ) ;
#39063=CARTESIAN_POINT ( 'NONE',  ( 2.185380717157382691, 21.63101079767031010, 38.35256412468753950 ) ) ;
#39067=ORIENTED_EDGE ( 'NONE', *, *, #3125, .T. ) ;
#39071=EDGE_CURVE ( 'NONE', #25523, #31232, #46601, .T. ) ;
#39074=VERTEX_POINT ( 'NONE', #32788 ) ;
#39078=CARTESIAN_POINT ( 'NONE',  ( 0.7948878604505662526, 10.07807612458116253, -48.05341849364687334 ) ) ;
#39091=CARTESIAN_POINT ( 'NONE',  ( 0.1147471544378676767, -22.60761324532118266, 37.89258518263465447 ) ) ;
#39093=CARTESIAN_POINT ( 'NONE',  ( 0.1147471544378676350, 9.515620283457987938, -43.08602046017117004 ) ) ;
#39106=EDGE_CURVE ( 'NONE', #38290, #34547, #51120, .T. ) ;
#39107=CARTESIAN_POINT ( 'NONE',  ( 2.299652685299201416, -47.08666796816785904, -13.67945263940299405 ) ) ;
#39112=CARTESIAN_POINT ( 'NONE',  ( -2.739355103387247858, 5.401627249124374863, -13.91653656670847461 ) ) ;
#39119=CARTESIAN_POINT ( 'NONE',  ( 4.553261556744873317, -33.59363643963353496, -28.30206982864260112 ) ) ;
#39120=ORIENTED_EDGE ( 'NONE', *, *, #3609, .T. ) ;
#39126=CARTESIAN_POINT ( 'NONE',  ( 0.6021447746440204973, -30.82182302570912924, -38.23030688420319478 ) ) ;
#39131=CARTESIAN_POINT ( 'NONE',  ( 0.1129192098497455998, -38.68182264534154058, 21.22895156665764915 ) ) ;
#39142=CARTESIAN_POINT ( 'NONE',  ( 4.694002226626921015, 44.00857453008718778, 11.89664403417603467 ) ) ;
#39148=CARTESIAN_POINT ( 'NONE',  ( 0.2279481005628797297, -42.86255399062842031, 10.45490088300113918 ) ) ;
#39152=CARTESIAN_POINT ( 'NONE',  ( 1.296416391601052487, 10.88712986132706639, 42.70571129789034615 ) ) ;
#39156=DIRECTION ( 'NONE',  ( 0.000000000000000000, 0.000000000000000000, 1.000000000000000000 ) ) ;
#39157=CARTESIAN_POINT ( 'NONE',  ( -6.057079549204054558, 3.081801865088773518, 19.00878029659119761 ) ) ;
#39159=EDGE_CURVE ( 'NONE', #14082, #26555, #14540, .T. ) ;
#39161=EDGE_CURVE ( 'NONE', #42575, #22617, #11540, .T. ) ;
#39162=CARTESIAN_POINT ( 'NONE',  ( -6.072942160501519915, 7.807899065004430206, 17.60229742049949309 ) ) ;
#39172=CARTESIAN_POINT ( 'NONE',  ( 0.5997462898726536595, 37.72933316221968170, 31.43324751403423534 ) ) ;
#39173=CARTESIAN_POINT ( 'NONE',  ( 0.6024113833632038784, 28.27346982169563816, -40.15162230025745771 ) ) ;
#39176=DIRECTION ( 'NONE',  ( 0.1011922191286468153, -0.9589869809184693450, 0.2647717983787155616 ) ) ;
#39180=B_SPLINE_CURVE_WITH_KNOTS ( 'NONE', 3,
 ( #61265, #41277, #22457, #8043 ),
 .UNSPECIFIED., .F., .F.,
 ( 4, 4 ),
 ( 0.000000000000000000, 0.004444103432399269631 ),
 .UNSPECIFIED. ) ;
#39184=CARTESIAN_POINT ( 'NONE',  ( 2.299746137290199055, -38.51195501985936431, 30.34980491262615843 ) ) ;
#39185=ORIENTED_EDGE ( 'NONE', *, *, #25953, .T. ) ;
#39190=VECTOR ( 'NONE', #51555, 1000.000000000000114 ) ;
#39191=VERTEX_POINT ( 'NONE', #34024 ) ;
#39193=CARTESIAN_POINT ( 'NONE',  ( 0.1129192098497447394, -0.9297496242502409913, 44.11448008785053077 ) ) ;
#39199=CARTESIAN_POINT ( 'NONE',  ( -6.072942160501519915, 13.84283391500573224, 13.38581755032494414 ) ) ;
#39201=ORIENTED_EDGE ( 'NONE', *, *, #50453, .T. ) ;
#39202=CARTESIAN_POINT ( 'NONE',  ( 0.5980271706414734822, 27.52111707190191225, -40.67723390247095239 ) ) ;
#39203=CARTESIAN_POINT ( 'NONE',  ( -6.078457390727109555, -1.844660340668231147, 19.16746564533437791 ) ) ;
#39204=B_SPLINE_CURVE_WITH_KNOTS ( 'NONE', 3,
 ( #58692, #44345, #60471, #10495, #39637, #3159 ),
 .UNSPECIFIED., .F., .F.,
 ( 4, 2, 4 ),
 ( 4.553649124439118623E-18, 0.0002447193893791687323, 0.0004894387787583329109 ),
 .UNSPECIFIED. ) ;
#39210=( BOUNDED_SURFACE ( )  B_SPLINE_SURFACE ( 3, 1, ( 
 ( #10498, #34313 ),
 ( #58697, #53390 ),
 ( #2306, #30823 ),
 ( #15821, #39642 ) ),
 .UNSPECIFIED., .F., .F., .F. ) 
 B_SPLINE_SURFACE_WITH_KNOTS ( ( 4, 4 ),
 ( 2, 2 ),
 ( 0.000000000000000000, 1.000000000000000000 ),
 ( 0.000000000000000000, 1.000000000000000000 ),
 .UNSPECIFIED. ) 
 GEOMETRIC_REPRESENTATION_ITEM ( )  RATIONAL_B_SPLINE_SURFACE ( (
 ( 1.000000000000000000, 1.000000000000000000),
 ( 0.9754377213608244057, 0.9999580625633939235),
 ( 0.9754377213608244057, 0.9999580625633939235),
 ( 1.000000000000000000, 1.000000000000000000) ) ) 
 REPRESENTATION_ITEM ( '' )  SURFACE ( )  );
#39213=CARTESIAN_POINT ( 'NONE',  ( 0.08486401232817714080, 0.000000000000000000, 10.00000000000000000 ) ) ;
#39218=ORIENTED_EDGE ( 'NONE', *, *, #29785, .F. ) ;
#39219=CARTESIAN_POINT ( 'NONE',  ( 0.1154773475650540809, -40.83160922148467620, 16.72493104410563447 ) ) ;
#39221=B_SPLINE_CURVE_WITH_KNOTS ( 'NONE', 3,
 ( #19254, #47752, #28628, #28327 ),
 .UNSPECIFIED., .F., .F.,
 ( 4, 4 ),
 ( 0.000000000000000000, 0.005013413432710149380 ),
 .UNSPECIFIED. ) ;
#39225=CARTESIAN_POINT ( 'NONE',  ( 1.296416391601052265, -8.128596768097615666, -43.31550863902941018 ) ) ;
#39229=LINE ( 'NONE', #25404, #49390 ) ;
#39234=VECTOR ( 'NONE', #12641, 1000.000000000000000 ) ;
#39240=CARTESIAN_POINT ( 'NONE',  ( 4.975610109902397937, -43.81605102859474954, 21.73943604138237973 ) ) ;
#39245=CARTESIAN_POINT ( 'NONE',  ( 3.050102900204245682, 26.63270562985675127, 35.01605688839702424 ) ) ;
#39250=VERTEX_POINT ( 'NONE', #20526 ) ;
#39257=LINE ( 'NONE', #53610, #42105 ) ;
#39258=ADVANCED_FACE ( 'NONE', ( #31147 ), #35607, .F. ) ;
#39259=VERTEX_POINT ( 'NONE', #30516 ) ;
#39270=CARTESIAN_POINT ( 'NONE',  ( 0.1140933569871964842, -1.035112909008395476, -44.11211275091581285 ) ) ;
#39271=CARTESIAN_POINT ( 'NONE',  ( 2.299652685299200972, -47.74024202747411039, 11.18709149047902507 ) ) ;
#39272=( BOUNDED_SURFACE ( )  B_SPLINE_SURFACE ( 3, 1, ( 
 ( #61512, #33973 ),
 ( #29863, #44007 ),
 ( #38986, #25164 ),
 ( #54260, #48061 ) ),
 .UNSPECIFIED., .F., .F., .F. ) 
 B_SPLINE_SURFACE_WITH_KNOTS ( ( 4, 4 ),
 ( 2, 2 ),
 ( 0.000000000000000000, 1.000000000000000000 ),
 ( 0.000000000000000000, 1.000000000000000000 ),
 .UNSPECIFIED. ) 
 GEOMETRIC_REPRESENTATION_ITEM ( )  RATIONAL_B_SPLINE_SURFACE ( (
 ( 1.000000000000000000, 1.000000000000000000),
 ( 0.9754377213608244057, 0.9999580625633939235),
 ( 0.9754377213608244057, 0.9999580625633939235),
 ( 1.000000000000000000, 1.000000000000000000) ) ) 
 REPRESENTATION_ITEM ( '' )  SURFACE ( )  );
#39275=CARTESIAN_POINT ( 'NONE',  ( -6.079354080745853928, 9.981161348512202380, 16.46722117975975408 ) ) ;
#39278=CARTESIAN_POINT ( 'NONE',  ( 0.6027444965799114707, -13.84715149815399649, -47.11469952440122455 ) ) ;
#39280=CARTESIAN_POINT ( 'NONE',  ( 4.975610109902397937, -28.45381238669758872, -39.78479568629688856 ) ) ;
#39285=DIRECTION ( 'NONE',  ( 0.000000000000000000, 0.000000000000000000, -1.000000000000000000 ) ) ;
#39287=CARTESIAN_POINT ( 'NONE',  ( 4.553261556744873317, -41.75933753256789771, -13.62707946203816967 ) ) ;
#39296=CARTESIAN_POINT ( 'NONE',  ( 0.1158403557922069033, -7.004826579936690223, -43.56458093186288494 ) ) ;
#39298=CARTESIAN_POINT ( 'NONE',  ( -6.077587904424778920, -8.901182807328959612, 17.07527352707539592 ) ) ;
#39305=CARTESIAN_POINT ( 'NONE',  ( 0.6252788684277205133, 23.32025617012770624, 43.21585337967175633 ) ) ;
#39306=CARTESIAN_POINT ( 'NONE',  ( 4.553261556744873317, 27.56395660609696563, 34.20186927699770507 ) ) ;
#39310=CARTESIAN_POINT ( 'NONE',  ( 4.694002226626920127, -44.68037479411238877, 9.052562051915485242 ) ) ;
#39311=CARTESIAN_POINT ( 'NONE',  ( 0.1129192098497447394, -43.82135468580274562, -5.161459220630158384 ) ) ;
#39312=CARTESIAN_POINT ( 'NONE',  ( 0.1154773475650540809, 41.93263902776148200, 13.73307737594076094 ) ) ;
#39323=CARTESIAN_POINT ( 'NONE',  ( -6.078075953587585900, -17.35139778253833498, -8.350099953848438616 ) ) ;
#39326=EDGE_CURVE ( 'NONE', #26558, #1848, #5511, .T. ) ;
#39328=EDGE_CURVE ( 'NONE', #5134, #38412, #2525, .T. ) ;
#39329=DIRECTION ( 'NONE',  ( 0.1011922191286468153, -0.8049255303601264844, -0.5846836968500909171 ) ) ;
#39331=CARTESIAN_POINT ( 'NONE',  ( 0.1152809850208375148, 15.44635349940774027, -41.33225672596513078 ) ) ;
#39332=VERTEX_POINT ( 'NONE', #3244 ) ;
#39333=ADVANCED_FACE ( 'NONE', ( #18609 ), #20765, .F. ) ;
#39335=ORIENTED_EDGE ( 'NONE', *, *, #34595, .T. ) ;
#39345=CARTESIAN_POINT ( 'NONE',  ( 4.975610109902397937, 48.58133226360784818, -5.683622315980244366 ) ) ;
#39351=CARTESIAN_POINT ( 'NONE',  ( 3.727782113643637540, -29.04977724543226358, -32.99830628830427770 ) ) ;
#39356=( BOUNDED_SURFACE ( )  B_SPLINE_SURFACE ( 3, 1, ( 
 ( #11880, #7122 ),
 ( #60363, #41013 ),
 ( #12483, #3352 ),
 ( #54428, #50066 ) ),
 .UNSPECIFIED., .F., .F., .F. ) 
 B_SPLINE_SURFACE_WITH_KNOTS ( ( 4, 4 ),
 ( 2, 2 ),
 ( 0.000000000000000000, 1.000000000000000000 ),
 ( 0.000000000000000000, 1.000000000000000000 ),
 .UNSPECIFIED. ) 
 GEOMETRIC_REPRESENTATION_ITEM ( )  RATIONAL_B_SPLINE_SURFACE ( (
 ( 1.000000000000000000, 1.000000000000000000),
 ( 0.7211978278499968642, 0.9934217856018975334),
 ( 0.7211978278499968642, 0.9934217856018975334),
 ( 1.000000000000000000, 1.000000000000000000) ) ) 
 REPRESENTATION_ITEM ( '' )  SURFACE ( )  );
#39357=ORIENTED_EDGE ( 'NONE', *, *, #54222, .F. ) ;
#39361=CARTESIAN_POINT ( 'NONE',  ( 4.694002226626920127, 12.64038892846120810, -43.80074587473789904 ) ) ;
#39375=( BOUNDED_SURFACE ( )  B_SPLINE_SURFACE ( 3, 1, ( 
 ( #17446, #51248 ),
 ( #51870, #37496 ),
 ( #13685, #18687 ),
 ( #12768, #28077 ) ),
 .UNSPECIFIED., .F., .F., .F. ) 
 B_SPLINE_SURFACE_WITH_KNOTS ( ( 4, 4 ),
 ( 2, 2 ),
 ( 0.000000000000000000, 1.000000000000000000 ),
 ( 0.000000000000000000, 1.000000000000000000 ),
 .UNSPECIFIED. ) 
 GEOMETRIC_REPRESENTATION_ITEM ( )  RATIONAL_B_SPLINE_SURFACE ( (
 ( 1.000000000000000000, 1.000000000000000000),
 ( 0.9953485035131437453, 0.8621029689291523912),
 ( 0.9953485035131437453, 0.8621029689291523912),
 ( 1.000000000000000000, 1.000000000000000000) ) ) 
 REPRESENTATION_ITEM ( '' )  SURFACE ( )  );
#39378=CARTESIAN_POINT ( 'NONE',  ( 0.6016117650947688800, 23.02239457412811063, 43.37649596633706750 ) ) ;
#39379=CARTESIAN_POINT ( 'NONE',  ( 4.694002226626920127, 28.15356303305734187, -35.85612444185512970 ) ) ;
#39389=DIRECTION ( 'NONE',  ( 0.09722883295013595717, -0.2759265041300154597, 0.9562484605800645188 ) ) ;
#39398=ORIENTED_EDGE ( 'NONE', *, *, #42443, .T. ) ;
#39400=CARTESIAN_POINT ( 'NONE',  ( 4.694002226626921015, 28.69237940071596071, -35.42643272715312719 ) ) ;
#39401=CARTESIAN_POINT ( 'NONE',  ( 0.6028777368367060907, 37.33615699143113886, 31.89907851995540966 ) ) ;
#39424=CARTESIAN_POINT ( 'NONE',  ( 0.8753041380234471980, -26.21158409634572095, 41.52217705074212972 ) ) ;
#39426=EDGE_LOOP ( 'NONE', ( #12910, #35460, #3225, #13712 ) ) ;
#39429=ORIENTED_EDGE ( 'NONE', *, *, #43085, .F. ) ;
#39431=ORIENTED_EDGE ( 'NONE', *, *, #25512, .F. ) ;
#39432=CARTESIAN_POINT ( 'NONE',  ( 0.1129192098497447394, 36.71339784380064231, -24.47607416535520741 ) ) ;
#39433=CARTESIAN_POINT ( 'NONE',  ( 0.6026112563231247332, -30.48163520784209979, -38.50208968303211776 ) ) ;
#39455=CARTESIAN_POINT ( 'NONE',  ( 0.3676999524040366896, 10.61898383218289155, 42.81574203134493928 ) ) ;
#39458=( BOUNDED_SURFACE ( )  B_SPLINE_SURFACE ( 3, 1, ( 
 ( #31358, #55452 ),
 ( #31665, #50758 ),
 ( #7848, #26968 ),
 ( #41397, #60455 ) ),
 .UNSPECIFIED., .F., .F., .F. ) 
 B_SPLINE_SURFACE_WITH_KNOTS ( ( 4, 4 ),
 ( 2, 2 ),
 ( 0.000000000000000000, 1.000000000000000000 ),
 ( 0.000000000000000000, 1.000000000000000000 ),
 .UNSPECIFIED. ) 
 GEOMETRIC_REPRESENTATION_ITEM ( )  RATIONAL_B_SPLINE_SURFACE ( (
 ( 1.000000000000000000, 1.000000000000000000),
 ( 0.9953485035131437453, 0.8621029689291523912),
 ( 0.9953485035131437453, 0.8621029689291523912),
 ( 1.000000000000000000, 1.000000000000000000) ) ) 
 REPRESENTATION_ITEM ( '' )  SURFACE ( )  );
#39461=CARTESIAN_POINT ( 'NONE',  ( 0.3676999524040323597, 30.26295534861902681, -32.09523511193413725 ) ) ;
#39462=CARTESIAN_POINT ( 'NONE',  ( 2.648799415243696664, -6.455064903435647317, -48.60915140569758108 ) ) ;
#39463=( BOUNDED_SURFACE ( )  B_SPLINE_SURFACE ( 3, 1, ( 
 ( #16835, #56251 ),
 ( #17438, #36561 ),
 ( #50323, #36254 ),
 ( #13062, #51545 ) ),
 .UNSPECIFIED., .F., .F., .F. ) 
 B_SPLINE_SURFACE_WITH_KNOTS ( ( 4, 4 ),
 ( 2, 2 ),
 ( 0.000000000000000000, 1.000000000000000000 ),
 ( 0.000000000000000000, 1.000000000000000000 ),
 .UNSPECIFIED. ) 
 GEOMETRIC_REPRESENTATION_ITEM ( )  RATIONAL_B_SPLINE_SURFACE ( (
 ( 1.000000000000000000, 1.000000000000000000),
 ( 0.7211978278499968642, 0.9934217856018975334),
 ( 0.7211978278499968642, 0.9934217856018975334),
 ( 1.000000000000000000, 1.000000000000000000) ) ) 
 REPRESENTATION_ITEM ( '' )  SURFACE ( )  );
#39466=LINE ( 'NONE', #31505, #26147 ) ;
#39467=CIRCLE ( 'NONE', #12444, 48.91267123290010943 ) ;
#39469=LINE ( 'NONE', #38538, #4621 ) ;
#39470=EDGE_LOOP ( 'NONE', ( #11145, #21588, #22346, #61231 ) ) ;
#39471=CARTESIAN_POINT ( 'NONE',  ( 3.240649175237395152, -41.42738255131205705, 14.79989501127953133 ) ) ;
#39474=CARTESIAN_POINT ( 'NONE',  ( 3.221118495291108719, 40.41289623301514666, 17.36546105697460618 ) ) ;
#39478=CARTESIAN_POINT ( 'NONE',  ( 0.6021447746440204973, 27.88050730053805992, -40.42546786065847897 ) ) ;
#39483=CARTESIAN_POINT ( 'NONE',  ( 4.553261556744875094, 0.000000000000000000, 0.000000000000000000 ) ) ;
#39494=ORIENTED_EDGE ( 'NONE', *, *, #52133, .F. ) ;
#39495=CARTESIAN_POINT ( 'NONE',  ( 4.975610109902397937, 48.43414999183889336, 6.825138951393308950 ) ) ;
#39496=CARTESIAN_POINT ( 'NONE',  ( 0.1129192098497447394, 43.99990943031675528, -3.310552508128703497 ) ) ;
#39498=CARTESIAN_POINT ( 'NONE',  ( 4.975610109902397937, -32.45573888811652807, 36.59336579715199633 ) ) ;
#39501=CARTESIAN_POINT ( 'NONE',  ( 4.834790513006555379, 47.24803566211424766, -0.4609414235693951589 ) ) ;
#39505=CARTESIAN_POINT ( 'NONE',  ( 3.559346040607745287, -36.42883594846195194, -24.62458513319633369 ) ) ;
#39513=CARTESIAN_POINT ( 'NONE',  ( 0.1135584504625008623, -18.25492125837011770, 40.17100822715256214 ) ) ;
#39520=CARTESIAN_POINT ( 'NONE',  ( 0.1156867017252034557, 25.14158812297082335, 36.26076879949014398 ) ) ;
#39528=DIRECTION ( 'NONE',  ( 0.09722883295013597105, 0.6635018476521645781, 0.7418300696286974638 ) ) ;
#39530=CARTESIAN_POINT ( 'NONE',  ( 0.6000166863083090663, 46.44114019838971785, 15.97009639238173051 ) ) ;
#39538=CARTESIAN_POINT ( 'NONE',  ( -6.063463321072278589, -1.833563764454256395, -19.16920698414909197 ) ) ;
#39545=CARTESIAN_POINT ( 'NONE',  ( 0.1119899015040012186, -44.12081468926701433, -0.5612658441996505321 ) ) ;
#39547=CARTESIAN_POINT ( 'NONE',  ( 3.221118495291109163, 18.65183604292354147, -39.83554231951222135 ) ) ;
#39549=EDGE_LOOP ( 'NONE', ( #26380, #18752, #24953, #23926 ) ) ;
#39552=CARTESIAN_POINT ( 'NONE',  ( 0.1157506346131639274, 4.329268483212691088, 43.91125247818713717 ) ) ;
#39563=CARTESIAN_POINT ( 'NONE',  ( 0.7242486021783869354, -48.79688800429393325, 5.465819560722072090 ) ) ;
#39575=ADVANCED_FACE ( 'NONE', ( #40431 ), #25269, .F. ) ;
#39581=CARTESIAN_POINT ( 'NONE',  ( -6.078726893082806448, 7.797636468844645563, 17.60655862934219584 ) ) ;
#39584=CARTESIAN_POINT ( 'NONE',  ( 4.975610109902397937, -11.44439439467595143, 47.55497076097179843 ) ) ;
#39586=ORIENTED_EDGE ( 'NONE', *, *, #19186, .T. ) ;
#39587=CARTESIAN_POINT ( 'NONE',  ( 4.226256110419178924, -43.04997224218647034, -8.804949740581237805 ) ) ;
#39590=CARTESIAN_POINT ( 'NONE',  ( 0.7413678028165009426, -6.114974495787087072, 43.67027797811822154 ) ) ;
#39603=EDGE_CURVE ( 'NONE', #31065, #10036, #22538, .T. ) ;
#39607=CARTESIAN_POINT ( 'NONE',  ( -6.072942160501519915, -12.93525546908874624, 14.26475826077785136 ) ) ;
#39611=LINE ( 'NONE', #57744, #21144 ) ;
#39617=CARTESIAN_POINT ( 'NONE',  ( 0.6008123274975391004, 49.03265588904381644, -2.711679852983228223 ) ) ;
#39618=CARTESIAN_POINT ( 'NONE',  ( 0.8744876279028263033, -19.05609938968970241, -45.24616145519706834 ) ) ;
#39620=ORIENTED_EDGE ( 'NONE', *, *, #24185, .F. ) ;
#39622=CARTESIAN_POINT ( 'NONE',  ( 0.1145239942831223490, 41.77227326564666043, 14.21346780081533900 ) ) ;
#39625=CARTESIAN_POINT ( 'NONE',  ( 0.6000166863083090663, -2.096232480231297046, -49.06556115135418850 ) ) ;
#39631=ORIENTED_EDGE ( 'NONE', *, *, #8855, .F. ) ;
#39636=CARTESIAN_POINT ( 'NONE',  ( -6.078726893082806448, -12.94330610022648820, 14.25709887966552003 ) ) ;
#39637=CARTESIAN_POINT ( 'NONE',  ( 0.5987334363312690755, 36.99765863950310774, 32.29142551308128617 ) ) ;
#39638=EDGE_CURVE ( 'NONE', #57068, #60263, #31677, .T. ) ;
#39639=AXIS2_PLACEMENT_3D ( 'NONE', #28510, #52624, #48256 ) ;
#39642=CARTESIAN_POINT ( 'NONE',  ( 0.6000166863083106206, 41.44150143800074204, -26.35195325346179018 ) ) ;
#39645=CARTESIAN_POINT ( 'NONE',  ( 0.1157991065609915438, 15.31532217366139470, -41.38095301288571193 ) ) ;
#39659=CARTESIAN_POINT ( 'NONE',  ( -2.739355103387248747, 14.91194544146094003, 0.6938660547319468463 ) ) ;
#39662=ORIENTED_EDGE ( 'NONE', *, *, #49902, .T. ) ;
#39667=CARTESIAN_POINT ( 'NONE',  ( 4.975610109902397937, -36.86873347511144772, 32.14258700041067840 ) ) ;
#39675=CARTESIAN_POINT ( 'NONE',  ( 0.3676999524040366896, 21.13209774130265473, 38.72189339863005841 ) ) ;
#39677=CARTESIAN_POINT ( 'NONE',  ( 4.975610109902397937, 0.000000000000000000, 0.000000000000000000 ) ) ;
#39678=ORIENTED_EDGE ( 'NONE', *, *, #56524, .F. ) ;
#39683=ORIENTED_EDGE ( 'NONE', *, *, #40543, .T. ) ;
#39684=VECTOR ( 'NONE', #4855, 1000.000000000000000 ) ;
#39686=EDGE_CURVE ( 'NONE', #43289, #19080, #653, .T. ) ;
#39688=CARTESIAN_POINT ( 'NONE',  ( -6.079354080745853928, -14.66163526140127615, 12.48316493161076224 ) ) ;
#39691=CARTESIAN_POINT ( 'NONE',  ( 0.3676999524040323597, -6.224421213753346116, -43.67158302462387098 ) ) ;
#39692=CARTESIAN_POINT ( 'NONE',  ( 2.299746137290200831, -36.10727851862707638, -33.17447476094279324 ) ) ;
#39705=CARTESIAN_POINT ( 'NONE',  ( 4.834790513006555379, -4.078087887156410574, 47.07396881620466189 ) ) ;
#39707=CARTESIAN_POINT ( 'NONE',  ( 0.1129192098497447394, -22.45785791439742241, 37.98152716363431125 ) ) ;
#39709=CARTESIAN_POINT ( 'NONE',  ( 0.1139756605157204034, 9.430567968997152661, -43.10475156496261917 ) ) ;
#39715=CARTESIAN_POINT ( 'NONE',  ( 0.3676999524040323597, -34.85286720109652947, -27.04123205746306979 ) ) ;
#39716=EDGE_CURVE ( 'NONE', #43165, #59959, #27901, .T. ) ;
#39728=CIRCLE ( 'NONE', #59675, 49.35315702047511621 ) ;
#39737=CARTESIAN_POINT ( 'NONE',  ( -4.915099999999998914, 6.044018577294158388E-15, -49.35315702047512332 ) ) ;
#39740=EDGE_LOOP ( 'NONE', ( #4072, #3622, #60408, #31191 ) ) ;
#39742=ORIENTED_EDGE ( 'NONE', *, *, #991, .F. ) ;
#39759=CARTESIAN_POINT ( 'NONE',  ( 0.1129192098497455998, 24.84520063729130612, 36.46461014570008530 ) ) ;
#39763=ORIENTED_EDGE ( 'NONE', *, *, #17062, .F. ) ;
#39769=CARTESIAN_POINT ( 'NONE',  ( -6.078075953587585900, -16.13536320617218323, -10.50929248103985714 ) ) ;
#39770=CARTESIAN_POINT ( 'NONE',  ( 0.6000166863083106206, -47.36892948402883263, 12.96179004788911726 ) ) ;
#39774=CARTESIAN_POINT ( 'NONE',  ( 0.6029442701453591180, 37.33617409675466803, -31.89914307587434550 ) ) ;
#39778=CARTESIAN_POINT ( 'NONE',  ( 0.1145239942831223490, 29.42216488540841368, 32.88284802386364447 ) ) ;
#39779=EDGE_CURVE ( 'NONE', #4631, #41953, #60839, .T. ) ;
#39782=B_SPLINE_CURVE_WITH_KNOTS ( 'NONE', 3,
 ( #51402, #21761, #9122, #46745, #52025, #18857, #42655, #61411, #28228, #56415, #13850, #4390, #61720, #37977, #2325, #3788, #23230, #36190, #8491 ),
 .UNSPECIFIED., .F., .F.,
 ( 4, 3, 3, 3, 3, 3, 4 ),
 ( 1.355252715606880543E-20, 0.0002612768053151653122, 0.0003919133833142877813, 0.0005225499612322621629, 0.0006531865391693346574, 0.0008112755173415177974, 0.0009693688056799715973 ),
 .UNSPECIFIED. ) ;
#39784=EDGE_CURVE ( 'NONE', #37845, #13905, #54845, .T. ) ;
#39786=DIRECTION ( 'NONE',  ( 0.1011922191286468153, -0.5266864627877008154, -0.8440151092865576521 ) ) ;
#39787=CARTESIAN_POINT ( 'NONE',  ( 3.050102900204245682, -19.44795466911843818, -39.46140276733677865 ) ) ;
#39798=CARTESIAN_POINT ( 'NONE',  ( 4.390527457369401532, 40.60156772890515242, 16.78386232616756857 ) ) ;
#39800=ORIENTED_EDGE ( 'NONE', *, *, #815, .F. ) ;
#39801=DIRECTION ( 'NONE',  ( 0.1011922191286468015, -0.4144321176143268559, -0.9044369268652869831 ) ) ;
#39802=CARTESIAN_POINT ( 'NONE',  ( 0.6029443199889047422, 28.09514691971974898, -40.27654852906047722 ) ) ;
#39807=CARTESIAN_POINT ( 'NONE',  ( 2.648799415243696664, 40.32403112341478391, 27.90143324719133844 ) ) ;
#39812=CARTESIAN_POINT ( 'NONE',  ( 0.1145239942831223490, 29.90569479618491755, -32.44371895239680725 ) ) ;
#39814=ORIENTED_EDGE ( 'NONE', *, *, #57658, .T. ) ;
#39823=CARTESIAN_POINT ( 'NONE',  ( 3.050102900204245682, -36.30976962477565451, -24.84000561541360952 ) ) ;
#39832=EDGE_LOOP ( 'NONE', ( #49396, #29137, #37431, #53538 ) ) ;
#39834=( BOUNDED_SURFACE ( )  B_SPLINE_SURFACE ( 3, 1, ( 
 ( #61050, #17852 ),
 ( #18159, #8741 ),
 ( #28157, #51960 ),
 ( #61345, #22850 ) ),
 .UNSPECIFIED., .F., .F., .F. ) 
 B_SPLINE_SURFACE_WITH_KNOTS ( ( 4, 4 ),
 ( 2, 2 ),
 ( 0.000000000000000000, 1.000000000000000000 ),
 ( 0.000000000000000000, 1.000000000000000000 ),
 .UNSPECIFIED. ) 
 GEOMETRIC_REPRESENTATION_ITEM ( )  RATIONAL_B_SPLINE_SURFACE ( (
 ( 1.000000000000000000, 1.000000000000000000),
 ( 0.9953485035131437453, 0.8621029689291523912),
 ( 0.9953485035131437453, 0.8621029689291523912),
 ( 1.000000000000000000, 1.000000000000000000) ) ) 
 REPRESENTATION_ITEM ( '' )  SURFACE ( )  );
#39840=CARTESIAN_POINT ( 'NONE',  ( 4.553261556744875094, 0.000000000000000000, 0.000000000000000000 ) ) ;
#39846=CARTESIAN_POINT ( 'NONE',  ( -6.078075953587585900, 18.62761703674214075, -4.879247665328125372 ) ) ;
#39848=B_SPLINE_CURVE_WITH_KNOTS ( 'NONE', 3,
 ( #8670, #22475, #36911, #32192, #17472, #3048 ),
 .UNSPECIFIED., .F., .F.,
 ( 4, 2, 4 ),
 ( 0.000000000000000000, 0.0002447195606305747461, 0.0004894391212611494922 ),
 .UNSPECIFIED. ) ;
#39852=CARTESIAN_POINT ( 'NONE',  ( 0.5549461598389363592, -7.904200586800755879, -43.39056704573498280 ) ) ;
#39854=CARTESIAN_POINT ( 'NONE',  ( 0.7044674535453004927, -47.71057267246421674, -11.64061759858214273 ) ) ;
#39859=CARTESIAN_POINT ( 'NONE',  ( 0.2940135542859021456, -26.87228822145753426, 34.98743595112873095 ) ) ;
#39860=CARTESIAN_POINT ( 'NONE',  ( 0.8744876279028306332, -45.16590161815026505, 19.24555484778404590 ) ) ;
#39863=CARTESIAN_POINT ( 'NONE',  ( 0.1157991065609915715, 36.93546633102171484, 24.13946338358953980 ) ) ;
#39865=ORIENTED_EDGE ( 'NONE', *, *, #30200, .T. ) ;
#39871=CARTESIAN_POINT ( 'NONE',  ( 0.1129192098497447394, 39.54191224844646513, -19.58032082273713570 ) ) ;
#39872=CARTESIAN_POINT ( 'NONE',  ( 0.1152339509894530906, 4.459257806557805459, 43.89826545855652284 ) ) ;
#39874=PRODUCT_DEFINITION_CONTEXT ( 'detailed design', #60057, 'design' ) ;
#39877=CARTESIAN_POINT ( 'NONE',  ( -6.078457390727109555, -8.910533588204446076, 17.07035155499113444 ) ) ;
#39879=CARTESIAN_POINT ( 'NONE',  ( 0.6026112563231247332, 10.75757372951007973, 47.91467001199488607 ) ) ;
#39883=ORIENTED_EDGE ( 'NONE', *, *, #49575, .T. ) ;
#39890=VECTOR ( 'NONE', #51976, 1000.000000000000114 ) ;
#39892=CARTESIAN_POINT ( 'NONE',  ( 3.240649175237395596, 34.65332694999099772, -27.10003410873642693 ) ) ;
#39894=CARTESIAN_POINT ( 'NONE',  ( 0.1129192098497455998, 10.29049805561888498, -42.90754522869442411 ) ) ;
#39899=CARTESIAN_POINT ( 'NONE',  ( -6.078457390727109555, 17.84708778612959890, -7.230212209312498750 ) ) ;
#39901=ORIENTED_EDGE ( 'NONE', *, *, #51450, .F. ) ;
#39902=CARTESIAN_POINT ( 'NONE',  ( 3.894904216938898323, -43.02812409911978619, -8.983588870098012436 ) ) ;
#39903=CARTESIAN_POINT ( 'NONE',  ( 0.5997462898726536595, 48.09935696025624452, 9.899671214447447909 ) ) ;
#39913=EDGE_CURVE ( 'NONE', #23672, #39035, #56293, .T. ) ;
#39915=CARTESIAN_POINT ( 'NONE',  ( 0.2940135542859014794, 15.98885814221885937, 41.11686957927879149 ) ) ;
#39917=B_SPLINE_CURVE_WITH_KNOTS ( 'NONE', 3,
 ( #16463, #61131, #25858, #54652 ),
 .UNSPECIFIED., .F., .F.,
 ( 4, 4 ),
 ( 0.000000000000000000, 0.004444103432399267029 ),
 .UNSPECIFIED. ) ;
#39918=B_SPLINE_CURVE_WITH_KNOTS ( 'NONE', 3,
 ( #45005, #40612, #54661, #2040 ),
 .UNSPECIFIED., .F., .F.,
 ( 4, 4 ),
 ( 0.000000000000000000, 0.005013413432710143308 ),
 .UNSPECIFIED. ) ;
#39919=CARTESIAN_POINT ( 'NONE',  ( 0.8753041380234465318, 16.12068986424767658, 46.38169559399183584 ) ) ;
#39922=EDGE_CURVE ( 'NONE', #8036, #31957, #7727, .T. ) ;
#39925=VECTOR ( 'NONE', #35736, 1000.000000000000227 ) ;
#39927=FACE_OUTER_BOUND ( 'NONE', #13781, .T. ) ;
#39937=CARTESIAN_POINT ( 'NONE',  ( 0.7948878604505646983, 23.47568002599128434, 43.12297641183513974 ) ) ;
#39938=CARTESIAN_POINT ( 'NONE',  ( 0.6026112563231247332, 49.01739703219963928, -2.972504515036971551 ) ) ;
#39939=LINE ( 'NONE', #52761, #15355 ) ;
#39940=ORIENTED_EDGE ( 'NONE', *, *, #12473, .F. ) ;
#39943=CARTESIAN_POINT ( 'NONE',  ( 1.657374760986086271, 43.86835707583708199, -4.056808440030005514 ) ) ;
#39949=CARTESIAN_POINT ( 'NONE',  ( -6.057079549204054558, -4.293366707802514171, 18.77227299535331539 ) ) ;
#39957=CARTESIAN_POINT ( 'NONE',  ( 0.8744876279028306332, -0.6840263623749832655, 49.09055060105833235 ) ) ;
#39959=CARTESIAN_POINT ( 'NONE',  ( -6.077587904424778920, -19.21610359950803115, -1.239912838430589970 ) ) ;
#39966=CARTESIAN_POINT ( 'NONE',  ( 0.1129192098497455998, 15.69290830752535726, -41.23935519181593889 ) ) ;
#39967=ORIENTED_EDGE ( 'NONE', *, *, #6532, .F. ) ;
#39971=AXIS2_PLACEMENT_3D ( 'NONE', #5332, #34190, #14466 ) ;
#39986=CARTESIAN_POINT ( 'NONE',  ( 0.1156867017252034419, 9.696689235465189682, 43.04552270731533525 ) ) ;
#39990=CARTESIAN_POINT ( 'NONE',  ( 4.975610109902397937, 13.36434394399761949, -47.05150069959838532 ) ) ;
#39991=B_SPLINE_CURVE_WITH_KNOTS ( 'NONE', 3,
 ( #53387, #23668, #42795, #14906 ),
 .UNSPECIFIED., .F., .F.,
 ( 4, 4 ),
 ( 0.000000000000000000, 0.005013413432710138104 ),
 .UNSPECIFIED. ) ;
#39992=CARTESIAN_POINT ( 'NONE',  ( 2.533389852662419894, 21.74902146992863905, 38.26787943999772779 ) ) ;
#39994=CARTESIAN_POINT ( 'NONE',  ( 4.834790513006553603, -47.18049212391683511, 2.567197668549032308 ) ) ;
#39997=DIRECTION ( 'NONE',  ( -1.000000000000000000, 0.000000000000000000, 0.000000000000000000 ) ) ;
#40018=CARTESIAN_POINT ( 'NONE',  ( 4.335381028904201628, -3.692956800737033696, 48.84791620665343004 ) ) ;
#40021=CARTESIAN_POINT ( 'NONE',  ( 4.553261556744873317, -3.993093339917161977, 43.74465420371208069 ) ) ;
#40022=CARTESIAN_POINT ( 'NONE',  ( 4.975610109902397937, -27.50982196586548412, -40.44328253918266824 ) ) ;
#40025=CARTESIAN_POINT ( 'NONE',  ( 0.1152339509894530906, -22.68230489146504425, 37.84779696714015529 ) ) ;
#40034=VERTEX_POINT ( 'NONE', #27461 ) ;
#40037=DIRECTION ( 'NONE',  ( 0.000000000000000000, 0.000000000000000000, 1.000000000000000000 ) ) ;
#40041=CARTESIAN_POINT ( 'NONE',  ( 0.6000166863083106206, -14.47337940799656586, -46.92914627628159252 ) ) ;
#40048=CARTESIAN_POINT ( 'NONE',  ( -6.078726893082806448, 3.069885851706299462, 19.00973019603943825 ) ) ;
#40054=EDGE_CURVE ( 'NONE', #7870, #49156, #54064, .T. ) ;
#40057=ORIENTED_EDGE ( 'NONE', *, *, #38718, .F. ) ;
#40061=EDGE_CURVE ( 'NONE', #885, #43681, #28671, .T. ) ;
#40065=VECTOR ( 'NONE', #3053, 1000.000000000000227 ) ;
#40074=CARTESIAN_POINT ( 'NONE',  ( -6.077587904424778920, -18.90214787454608469, 3.674891443665150970 ) ) ;
#40075=CARTESIAN_POINT ( 'NONE',  ( 0.6026112563231247332, 32.88584477487121660, 36.47001793730409247 ) ) ;
#40078=CARTESIAN_POINT ( 'NONE',  ( 0.6000166863083090663, 40.87138819217380359, -27.22780029589407036 ) ) ;
#40088=CARTESIAN_POINT ( 'NONE',  ( 4.335381028904216727, 12.96255624111825888, 47.24117889469092546 ) ) ;
#40089=CARTESIAN_POINT ( 'NONE',  ( 2.533389852662419894, 11.33089370753568303, 42.53306219310039182 ) ) ;
#40098=DIRECTION ( 'NONE',  ( 0.000000000000000000, 0.000000000000000000, -1.000000000000000000 ) ) ;
#40112=EDGE_LOOP ( 'NONE', ( #29158, #47130, #38785, #59194 ) ) ;
#40113=CARTESIAN_POINT ( 'NONE',  ( 4.834790513006553603, -15.88524143731098448, -44.49998253261139780 ) ) ;
#40114=CARTESIAN_POINT ( 'NONE',  ( 0.6026112563231248442, 28.23784955160265753, -40.17667043951328765 ) ) ;
#40117=CARTESIAN_POINT ( 'NONE',  ( 0.3676999524040366896, -44.10520818713899871, 0.8253448321555690859 ) ) ;
#40123=CARTESIAN_POINT ( 'NONE',  ( -6.078726893082806448, 13.83016815118539000, -13.39852567182887455 ) ) ;
#40126=CARTESIAN_POINT ( 'NONE',  ( 0.1139756605157204866, 20.76085607197808613, 38.93510080703057952 ) ) ;
#40127=ADVANCED_FACE ( 'NONE', ( #14310 ), #16639, .T. ) ;
#40130=ORIENTED_EDGE ( 'NONE', *, *, #9977, .F. ) ;
#40133=CARTESIAN_POINT ( 'NONE',  ( 4.975610109902397937, 0.000000000000000000, 0.000000000000000000 ) ) ;
#40136=ORIENTED_EDGE ( 'NONE', *, *, #26369, .T. ) ;
#40138=CARTESIAN_POINT ( 'NONE',  ( -6.077587904424778920, -17.35179747939703887, 8.349320069797363075 ) ) ;
#40141=CARTESIAN_POINT ( 'NONE',  ( 0.1119898979215348811, -32.08462161508800392, -30.29089572905457928 ) ) ;
#40154=DIRECTION ( 'NONE',  ( -0.1011922191286467460, -0.3314939457937330358, -0.9380148712520081089 ) ) ;
#40164=CARTESIAN_POINT ( 'NONE',  ( -6.078726893082806448, -18.27610589745688330, -6.064486333867170842 ) ) ;
#40171=DIRECTION ( 'NONE',  ( 0.000000000000000000, 0.000000000000000000, 1.000000000000000000 ) ) ;
#40174=CARTESIAN_POINT ( 'NONE',  ( 0.1158816050234198897, 36.98303739194169992, 24.06651172420720997 ) ) ;
#40176=CARTESIAN_POINT ( 'NONE',  ( 0.6253024248130512053, -19.24752319158097436, -45.17717430746637319 ) ) ;
#40178=CARTESIAN_POINT ( 'NONE',  ( 2.009741617377216460, -42.23114984276965345, 12.49135943684998473 ) ) ;
#40185=EDGE_LOOP ( 'NONE', ( #22972, #52827, #20672, #23827 ) ) ;
#40192=CARTESIAN_POINT ( 'NONE',  ( 0.1157506346131639274, 44.03933932887103708, 2.734456304164842866 ) ) ;
#40194=EDGE_LOOP ( 'NONE', ( #21669, #56972, #23681, #15497 ) ) ;
#40195=CARTESIAN_POINT ( 'NONE',  ( 0.1129192098497455998, -13.01845098534629486, 42.16007260106758281 ) ) ;
#40205=CARTESIAN_POINT ( 'NONE',  ( 0.1158516988532803660, 43.30104365222493357, -8.483028790526823570 ) ) ;
#40215=CARTESIAN_POINT ( 'NONE',  ( -6.078726893082806448, -6.653559303940370206, 18.06998035022918359 ) ) ;
#40217=CARTESIAN_POINT ( 'NONE',  ( 4.694002226626920127, -25.79840873770053733, 37.58625916540072609 ) ) ;
#40218=EDGE_LOOP ( 'NONE', ( #54281, #56611, #2050, #44264 ) ) ;
#40222=EDGE_LOOP ( 'NONE', ( #4868, #18129, #51252, #48619 ) ) ;
#40223=ORIENTED_EDGE ( 'NONE', *, *, #55926, .T. ) ;
#40232=CARTESIAN_POINT ( 'NONE',  ( 0.3676999524040366896, -41.19158123804976412, -15.78620342045500280 ) ) ;
#40238=CARTESIAN_POINT ( 'NONE',  ( 0.6021447746440204973, 41.29831215267225275, 26.57048272856424020 ) ) ;
#40241=CARTESIAN_POINT ( 'NONE',  ( 2.359973842542475886, 41.28141064895650914, -15.29643845686700843 ) ) ;
#40248=CARTESIAN_POINT ( 'NONE',  ( 3.240649175237397372, 28.19680434710399553, 33.76692378658126614 ) ) ;
#40249=ORIENTED_EDGE ( 'NONE', *, *, #27670, .T. ) ;
#40251=CARTESIAN_POINT ( 'NONE',  ( 0.6029443449137436017, 17.00082651214890817, -46.07072211163124109 ) ) ;
#40252=CARTESIAN_POINT ( 'NONE',  ( 2.009741617377216460, 2.862416983765094791, -43.94667958599486468 ) ) ;
#40264=VERTEX_POINT ( 'NONE', #31160 ) ;
#40266=CARTESIAN_POINT ( 'NONE',  ( 0.3676999524040366896, 5.056646555325087000, 43.82215089355334925 ) ) ;
#40269=EDGE_CURVE ( 'NONE', #17907, #56898, #12943, .T. ) ;
#40273=EDGE_CURVE ( 'NONE', #1309, #4904, #34959, .T. ) ;
#40282=CARTESIAN_POINT ( 'NONE',  ( -6.077587904424778920, 15.43577113102541887, -11.51229738082424348 ) ) ;
#40298=CARTESIAN_POINT ( 'NONE',  ( 0.2279481005628794799, -42.47734836628340105, -11.92385687780218184 ) ) ;
#40304=CARTESIAN_POINT ( 'NONE',  ( -6.077587904424778920, -19.21689618909968544, 1.227567615773810239 ) ) ;
#40305=CARTESIAN_POINT ( 'NONE',  ( -6.072942160501519027, -19.21763696748628547, 1.219258657924985334 ) ) ;
#40310=CARTESIAN_POINT ( 'NONE',  ( -6.057079549204054558, -14.66865672308385804, -12.47644745270323874 ) ) ;
#40311=CARTESIAN_POINT ( 'NONE',  ( 0.6000166863083090663, 5.235566842224464779, 48.83044461756470866 ) ) ;
#40312=CARTESIAN_POINT ( 'NONE',  ( 0.6000166863083106206, -47.63401213562553949, -11.95091500980295685 ) ) ;
#40315=CARTESIAN_POINT ( 'NONE',  ( 0.8744876279028306332, 23.49358985382604459, 43.10917867646859492 ) ) ;
#40317=CARTESIAN_POINT ( 'NONE',  ( 2.706805983486679779, 35.95399731719180636, -25.37885320961369828 ) ) ;
#40320=VERTEX_POINT ( 'NONE', #18317 ) ;
#40321=ORIENTED_EDGE ( 'NONE', *, *, #37026, .F. ) ;
#40325=VERTEX_POINT ( 'NONE', #41512 ) ;
#40329=ORIENTED_EDGE ( 'NONE', *, *, #27779, .T. ) ;
#40339=FACE_OUTER_BOUND ( 'NONE', #13619, .T. ) ;
#40341=EDGE_CURVE ( 'NONE', #60557, #2175, #8577, .T. ) ;
#40344=CARTESIAN_POINT ( 'NONE',  ( 0.1119898979215349782, -6.487605684152662811, 43.64484254455250323 ) ) ;
#40346=CARTESIAN_POINT ( 'NONE',  ( 5.901764892641307547, 25.42221402738085700, -41.85334516362722468 ) ) ;
#40348=ADVANCED_FACE ( 'NONE', ( #51185 ), #50871, .F. ) ;
#40349=CARTESIAN_POINT ( 'NONE',  ( 2.299746137290199943, 48.35891443790075783, 8.105352063540024687 ) ) ;
#40350=CARTESIAN_POINT ( 'NONE',  ( 2.648799415243696664, -42.02883204265787498, -25.26053721557904552 ) ) ;
#40354=CARTESIAN_POINT ( 'NONE',  ( 0.1158516988532803660, 39.73311795087249010, -19.18909838254134925 ) ) ;
#40356=CARTESIAN_POINT ( 'NONE',  ( 0.6039202388192952409, -30.48176006895440082, -38.50228585353977451 ) ) ;
#40357=VERTEX_POINT ( 'NONE', #22694 ) ;
#40360=CARTESIAN_POINT ( 'NONE',  ( -2.739355103387247858, 13.33354922980902302, 6.712974891005939249 ) ) ;
#40363=ORIENTED_EDGE ( 'NONE', *, *, #23657, .T. ) ;
#40366=CARTESIAN_POINT ( 'NONE',  ( 4.553261556744873317, -36.69060082144796553, 24.15241969627054530 ) ) ;
#40368=AXIS2_PLACEMENT_3D ( 'NONE', #11479, #43793, #43472 ) ;
#40372=CARTESIAN_POINT ( 'NONE',  ( -6.063463321072278589, -18.90456390296430200, 3.665776332267008275 ) ) ;
#40376=CARTESIAN_POINT ( 'NONE',  ( 0.6253024248130498730, -45.77087648984584689, 17.78963441920380717 ) ) ;
#40379=FACE_BOUND ( 'NONE', #5053, .T. ) ;
#40382=CARTESIAN_POINT ( 'NONE',  ( 0.6008122571543323964, 44.43158886499384153, 20.91383421081539140 ) ) ;
#40384=B_SPLINE_CURVE_WITH_KNOTS ( 'NONE', 3,
 ( #18907, #38030, #23897, #43027 ),
 .UNSPECIFIED., .F., .F.,
 ( 4, 4 ),
 ( 0.000000000000000000, 0.005013413432710142441 ),
 .UNSPECIFIED. ) ;
#40386=CARTESIAN_POINT ( 'NONE',  ( 0.5997462898726536595, 46.43852004798843325, 15.96920429754989890 ) ) ;
#40391=CARTESIAN_POINT ( 'NONE',  ( 0.6016118706126977189, 23.02238442462318702, -43.37650135947801999 ) ) ;
#40394=CARTESIAN_POINT ( 'NONE',  ( -2.739355103387248747, 14.60025052884540209, -3.111310245855684720 ) ) ;
#40399=VERTEX_POINT ( 'NONE', #50881 ) ;
#40404=CARTESIAN_POINT ( 'NONE',  ( 2.648799415243708655, 31.92790172191037712, -37.21728838759792524 ) ) ;
#40410=CARTESIAN_POINT ( 'NONE',  ( 0.8744876279028263033, -42.33402326122615733, -24.86323641237110493 ) ) ;
#40412=CARTESIAN_POINT ( 'NONE',  ( -6.057079549204054558, -16.14367994231336567, -10.49822980410923812 ) ) ;
#40418=CARTESIAN_POINT ( 'NONE',  ( 4.335381028904216727, -27.18827219542376383, -40.74990432739557633 ) ) ;
#40422=CARTESIAN_POINT ( 'NONE',  ( 0.1156867017252034696, 20.29825183744268458, 39.17810331829427639 ) ) ;
#40431=FACE_OUTER_BOUND ( 'NONE', #11008, .T. ) ;
#40434=CARTESIAN_POINT ( 'NONE',  ( 0.1129192098497447394, -32.03190746134960420, -30.34647742609823595 ) ) ;
#40445=CARTESIAN_POINT ( 'NONE',  ( 0.8753041380234465318, -35.88662119133365280, 33.51550010581227212 ) ) ;
#40446=LINE ( 'NONE', #49502, #23976 ) ;
#40452=CARTESIAN_POINT ( 'NONE',  ( 4.694002226626921015, -43.15593359350871339, 14.69184015427610923 ) ) ;
#40453=EDGE_LOOP ( 'NONE', ( #17163, #19430, #45497, #14143 ) ) ;
#40454=CARTESIAN_POINT ( 'NONE',  ( 0.7044674535453004927, -47.28336972574665964, 13.26972758534445340 ) ) ;
#40463=CARTESIAN_POINT ( 'NONE',  ( 0.1158516988532803382, -35.33224402766282424, 26.43056357330432604 ) ) ;
#40470=ADVANCED_FACE ( 'NONE', ( #53631 ), #5184, .F. ) ;
#40472=DIRECTION ( 'NONE',  ( 0.000000000000000000, 0.000000000000000000, -1.000000000000000000 ) ) ;
#40474=EDGE_LOOP ( 'NONE', ( #30999, #11829, #9292, #283 ) ) ;
#40475=CARTESIAN_POINT ( 'NONE',  ( 3.894904216938898323, -3.630410452522087272, -43.80575821079255405 ) ) ;
#40486=VECTOR ( 'NONE', #16444, 1000.000000000000114 ) ;
#40487=ADVANCED_FACE ( 'NONE', ( #43994 ), #58788, .F. ) ;
#40490=B_SPLINE_CURVE_WITH_KNOTS ( 'NONE', 3,
 ( #29260, #24883, #119, #53975, #29879, #19892, #5128, #44322, #48076, #33675, #30181, #15184, #25481, #52757, #6042, #20487 ),
 .UNSPECIFIED., .F., .F.,
 ( 4, 3, 3, 3, 3, 4 ),
 ( 1.962735358247463844E-17, 0.0002612764279487724581, 0.0003919131003184757214, 0.0005225497727000657979, 0.0007837925190632480648, 0.001045051706266718252 ),
 .UNSPECIFIED. ) ;
#40493=ORIENTED_EDGE ( 'NONE', *, *, #26383, .F. ) ;
#40494=CARTESIAN_POINT ( 'NONE',  ( 0.1156495703730067298, 44.04204243056376100, 2.690994569948411907 ) ) ;
#40496=CARTESIAN_POINT ( 'NONE',  ( -6.077587904424778920, 19.25606354205735116, -0.006185319731011218458 ) ) ;
#40510=ORIENTED_EDGE ( 'NONE', *, *, #34754, .T. ) ;
#40515=CARTESIAN_POINT ( 'NONE',  ( 4.390527457369401532, 12.80762060415681525, -42.02558971732101156 ) ) ;
#40524=CARTESIAN_POINT ( 'NONE',  ( 2.879087469061463178, 42.27281810937363815, 12.21108209272179401 ) ) ;
#40538=CARTESIAN_POINT ( 'NONE',  ( 3.727782113643637540, 41.00064633199524877, -15.86583676534648824 ) ) ;
#40540=CARTESIAN_POINT ( 'NONE',  ( 4.975610109902397937, 45.11887670192734134, 18.88746601040093154 ) ) ;
#40541=CARTESIAN_POINT ( 'NONE',  ( 2.955597489168904524, 0.3322054216400753268, -43.99767708311318160 ) ) ;
#40543=EDGE_CURVE ( 'NONE', #34863, #1980, #28547, .T. ) ;
#40547=CARTESIAN_POINT ( 'NONE',  ( 0.6021448801613057400, 48.15124027138728025, 9.643609228607319395 ) ) ;
#40553=CARTESIAN_POINT ( 'NONE',  ( 0.7413678028165010536, 3.304446308179310954, -43.97234046951110287 ) ) ;
#40558=CARTESIAN_POINT ( 'NONE',  ( 3.894904216938897434, -29.98771076940676750, 32.13816322204189646 ) ) ;
#40572=CARTESIAN_POINT ( 'NONE',  ( 0.3676999524040366896, 43.96170928169366476, -3.649479463524768263 ) ) ;
#40575=CARTESIAN_POINT ( 'NONE',  ( -6.078726893082806448, -1.852420388636693227, 19.16670498475111373 ) ) ;
#40576=CARTESIAN_POINT ( 'NONE',  ( 0.1365634738349428001, -40.65536331164525308, -17.14654640507459149 ) ) ;
#40579=CARTESIAN_POINT ( 'NONE',  ( 0.6016117650947689910, -48.65860227857874776, 6.625064417769112701 ) ) ;
#40580=CARTESIAN_POINT ( 'NONE',  ( 0.1368894036331304576, 37.32310111198702884, 23.53396373983203915 ) ) ;
#40582=CARTESIAN_POINT ( 'NONE',  ( 3.050102900204245682, -43.82680816383815880, -3.825720239143000523 ) ) ;
#40584=EDGE_CURVE ( 'NONE', #43185, #7798, #4670, .T. ) ;
#40594=DIRECTION ( 'NONE',  ( 0.09722883295013592941, 0.2140925343086658994, -0.9719624173785975652 ) ) ;
#40596=ORIENTED_EDGE ( 'NONE', *, *, #45528, .F. ) ;
#40597=B_SPLINE_CURVE_WITH_KNOTS ( 'NONE', 3,
 ( #34711, #53775, #10907, #6158 ),
 .UNSPECIFIED., .F., .F.,
 ( 4, 4 ),
 ( 0.000000000000000000, 0.004444103432399266161 ),
 .UNSPECIFIED. ) ;
#40598=CARTESIAN_POINT ( 'NONE',  ( -6.072942160501519915, 15.42355008158977192, -11.52901839575739373 ) ) ;
#40607=FACE_OUTER_BOUND ( 'NONE', #31752, .T. ) ;
#40612=CARTESIAN_POINT ( 'NONE',  ( 4.834790513006553603, -4.078087887155715130, -47.07396881620473295 ) ) ;
#40617=CARTESIAN_POINT ( 'NONE',  ( 4.975610109902397937, 24.86209007718959185, 42.12274782266089801 ) ) ;
#40619=CARTESIAN_POINT ( 'NONE',  ( 4.226256110419178924, 35.46064522245336548, -25.94937167629463204 ) ) ;
#40621=DIRECTION ( 'NONE',  ( -0.1011922191286467460, -0.8407325376063348177, 0.5319106456895111856 ) ) ;
#40622=ADVANCED_FACE ( 'NONE', ( #31404 ), #57254, .F. ) ;
#40629=EDGE_CURVE ( 'NONE', #8248, #14950, #14373, .T. ) ;
#40631=AXIS2_PLACEMENT_3D ( 'NONE', #32053, #61748, #41774 ) ;
#40643=VERTEX_POINT ( 'NONE', #56118 ) ;
#40645=CARTESIAN_POINT ( 'NONE',  ( -6.077587904424778920, 9.976910903713122281, -16.46988980574249695 ) ) ;
#40647=ORIENTED_EDGE ( 'NONE', *, *, #36870, .F. ) ;
#40649=CARTESIAN_POINT ( 'NONE',  ( 0.6000166863083090663, 28.52380356231368097, 39.97769518177598513 ) ) ;
#40654=ORIENTED_EDGE ( 'NONE', *, *, #53441, .F. ) ;
#40668=ORIENTED_EDGE ( 'NONE', *, *, #44729, .F. ) ;
#40670=CARTESIAN_POINT ( 'NONE',  ( 0.5997462898726536595, -48.76843890605300658, -5.761162800241320880 ) ) ;
#40682=CARTESIAN_POINT ( 'NONE',  ( 0.6024113833632039894, 32.85349838899362851, 36.49917139751612893 ) ) ;
#40683=CARTESIAN_POINT ( 'NONE',  ( 0.8744876279028306332, -14.81965677137948489, -46.80521149998148900 ) ) ;
#40698=CARTESIAN_POINT ( 'NONE',  ( 0.6029443449137436017, 4.672121757583973967, 48.88466851954346737 ) ) ;
#40699=CARTESIAN_POINT ( 'NONE',  ( 0.1155031312995260795, -12.39291212668941355, -42.34805026860106381 ) ) ;
#40700=EDGE_CURVE ( 'NONE', #40643, #30048, #22670, .T. ) ;
#40703=CARTESIAN_POINT ( 'NONE',  ( 0.3676999524040366896, -28.14442808720893296, -33.96824621564622504 ) ) ;
#40709=CARTESIAN_POINT ( 'NONE',  ( 0.7948878604505658085, -45.82899947609774216, -17.61821370963155786 ) ) ;
#40713=CARTESIAN_POINT ( 'NONE',  ( 0.1129192098497455998, 43.40062318508800843, -7.958498283668546947 ) ) ;
#40714=EDGE_CURVE ( 'NONE', #31634, #44906, #35353, .T. ) ;
#40716=AXIS2_PLACEMENT_3D ( 'NONE', #21352, #26662, #11979 ) ;
#40717=CARTESIAN_POINT ( 'NONE',  ( 0.1157506346131639274, -38.49163757259893259, -21.57161321696930401 ) ) ;
#40718=CARTESIAN_POINT ( 'NONE',  ( 4.335381028904216727, 31.32980982056223951, -37.65899446708247211 ) ) ;
#40719=B_SPLINE_CURVE_WITH_KNOTS ( 'NONE', 3,
 ( #40572, #49946, #35861, #11427, #49019, #59326 ),
 .UNSPECIFIED., .F., .F.,
 ( 4, 2, 4 ),
 ( 5.421010862427522170E-19, 0.0002293801035737090739, 0.0004587602071474176056 ),
 .UNSPECIFIED. ) ;
#40723=EDGE_CURVE ( 'NONE', #26600, #24074, #46741, .T. ) ;
#40725=CARTESIAN_POINT ( 'NONE',  ( 0.6029443449137436017, -14.01413519038458055, 47.06531156647066183 ) ) ;
#40734=CARTESIAN_POINT ( 'NONE',  ( -6.072942160501519027, 9.969886825815823528, 16.47438979050345864 ) ) ;
#40737=CARTESIAN_POINT ( 'NONE',  ( 4.834790513006555379, 1.053669480798880009, -47.23853428663524312 ) ) ;
#40738=AXIS2_PLACEMENT_3D ( 'NONE', #29042, #14961, #38772 ) ;
#40741=CARTESIAN_POINT ( 'NONE',  ( 4.834790513006553603, 1.975078679466633957, -47.20898648704818612 ) ) ;
#40746=VERTEX_POINT ( 'NONE', #647 ) ;
#40747=VERTEX_POINT ( 'NONE', #48581 ) ;
#40752=ORIENTED_EDGE ( 'NONE', *, *, #34200, .F. ) ;
#40754=CARTESIAN_POINT ( 'NONE',  ( -2.739355103387247858, -13.93362462427449167, 5.357394122222905786 ) ) ;
#40756=VERTEX_POINT ( 'NONE', #38286 ) ;
#40760=CARTESIAN_POINT ( 'NONE',  ( 4.975610109902397937, 7.237810502494091303, 48.37420290059321104 ) ) ;
#40764=CARTESIAN_POINT ( 'NONE',  ( 2.706805983486680223, -34.25409726565154500, 27.63029015111926867 ) ) ;
#40774=CARTESIAN_POINT ( 'NONE',  ( 2.299746137290199499, -18.66300477064106289, 45.34284497709828088 ) ) ;
#40775=CARTESIAN_POINT ( 'NONE',  ( 0.5997462898726536595, -45.71211507932792273, 17.94308126043545215 ) ) ;
#40778=CARTESIAN_POINT ( 'NONE',  ( 5.901764892641288895, 1.526405342808391463, -48.94549574954905324 ) ) ;
#40779=EDGE_CURVE ( 'NONE', #57626, #15681, #11726, .T. ) ;
#40782=CARTESIAN_POINT ( 'NONE',  ( 0.8753041380234465318, 3.828530797420660381, 48.95386276695825956 ) ) ;
#40788=FACE_OUTER_BOUND ( 'NONE', #42482, .T. ) ;
#40794=CARTESIAN_POINT ( 'NONE',  ( 0.7948884756798498818, -19.07805331891001188, -45.24076177697474321 ) ) ;
#40796=CARTESIAN_POINT ( 'NONE',  ( 2.359973842542475886, -42.17663974021382955, 12.62010122212638485 ) ) ;
#40797=VERTEX_POINT ( 'NONE', #43925 ) ;
#40800=CARTESIAN_POINT ( 'NONE',  ( 0.5997462898726536595, 44.46857747280041195, -20.83500054451300088 ) ) ;
#40804=DIRECTION ( 'NONE',  ( 0.000000000000000000, 0.000000000000000000, -1.000000000000000000 ) ) ;
#40808=CIRCLE ( 'NONE', #59776, 43.92652462719577500 ) ;
#40819=CARTESIAN_POINT ( 'NONE',  ( 0.6252788684277233999, 40.77687624000223821, -27.36221290906875225 ) ) ;
#40821=CARTESIAN_POINT ( 'NONE',  ( 0.1154773475650540532, 15.40762055515278384, 41.34669102690751430 ) ) ;
#40829=CARTESIAN_POINT ( 'NONE',  ( -6.078075953587585900, 17.84675544569240557, -7.231078364171170669 ) ) ;
#40831=CARTESIAN_POINT ( 'NONE',  ( 0.1145239942831223490, -12.86729789440911986, 42.20637541416234484 ) ) ;
#40832=CARTESIAN_POINT ( 'NONE',  ( 0.3676999524040366896, 14.45783756353458216, -41.67639039443420756 ) ) ;
#40841=ORIENTED_EDGE ( 'NONE', *, *, #38292, .F. ) ;
#40854=CARTESIAN_POINT ( 'NONE',  ( 4.390527457369401532, 40.84234994305386834, -16.18912560201280826 ) ) ;
#40856=CARTESIAN_POINT ( 'NONE',  ( 4.553261556744875094, 6.787618719203488915, 43.39893775135925580 ) ) ;
#40858=EDGE_CURVE ( 'NONE', #11409, #26359, #38748, .T. ) ;
#40863=ORIENTED_EDGE ( 'NONE', *, *, #49575, .F. ) ;
#40866=CARTESIAN_POINT ( 'NONE',  ( 0.6026112563231247332, 17.12333019133003376, -46.02534690866429656 ) ) ;
#40869=ORIENTED_EDGE ( 'NONE', *, *, #46693, .F. ) ;
#40871=ORIENTED_EDGE ( 'NONE', *, *, #18296, .T. ) ;
#40872=CARTESIAN_POINT ( 'NONE',  ( -2.601141883200662974, 14.55883463511898057, -3.291771792917696171 ) ) ;
#40893=CARTESIAN_POINT ( 'NONE',  ( 0.6026112563231248442, -48.72623651472557782, 6.106952596445339942 ) ) ;
#40896=CARTESIAN_POINT ( 'NONE',  ( 0.7948884756798504370, -8.691324955621483994, 48.32348823414908168 ) ) ;
#40903=DIRECTION ( 'NONE',  ( 0.09722883295013592941, 0.2288279796715218528, 0.9685991481322931973 ) ) ;
#40909=ADVANCED_FACE ( 'NONE', ( #4599 ), #61675, .F. ) ;
#40923=CARTESIAN_POINT ( 'NONE',  ( 0.6026112563231247332, 41.25111472265821533, -26.64369585928908535 ) ) ;
#40924=CARTESIAN_POINT ( 'NONE',  ( 0.8744876279028306332, -13.11369837310865805, 47.31153099782990523 ) ) ;
#40928=CARTESIAN_POINT ( 'NONE',  ( 0.1140933569871965536, 44.05627166033247732, -2.448443888450706485 ) ) ;
#40933=( BOUNDED_SURFACE ( )  B_SPLINE_SURFACE ( 3, 1, ( 
 ( #19280, #3911 ),
 ( #38099, #51839 ),
 ( #38396, #52455 ),
 ( #57443, #14583 ) ),
 .UNSPECIFIED., .F., .F., .F. ) 
 B_SPLINE_SURFACE_WITH_KNOTS ( ( 4, 4 ),
 ( 2, 2 ),
 ( 0.000000000000000000, 1.000000000000000000 ),
 ( 0.000000000000000000, 1.000000000000000000 ),
 .UNSPECIFIED. ) 
 GEOMETRIC_REPRESENTATION_ITEM ( )  RATIONAL_B_SPLINE_SURFACE ( (
 ( 1.000000000000000000, 1.000000000000000000),
 ( 0.7211978278499970862, 0.9934217856018976445),
 ( 0.7211978278499970862, 0.9934217856018976445),
 ( 1.000000000000000000, 1.000000000000000000) ) ) 
 REPRESENTATION_ITEM ( '' )  SURFACE ( )  );
#40935=B_SPLINE_CURVE_WITH_KNOTS ( 'NONE', 3,
 ( #5289, #25041, #24417, #54134 ),
 .UNSPECIFIED., .F., .F.,
 ( 4, 4 ),
 ( 2.183987964099527011E-17, 0.004559932413162189405 ),
 .UNSPECIFIED. ) ;
#40938=CARTESIAN_POINT ( 'NONE',  ( 4.975610109902397937, 24.86209007719020647, -42.12274782266053563 ) ) ;
#40943=CARTESIAN_POINT ( 'NONE',  ( 0.7413678028165012757, -18.69877339599409893, -39.93547251824506361 ) ) ;
#40955=CONICAL_SURFACE ( 'NONE', #36929, 43.92652462719577500, 1.486293639869522343 ) ;
#40959=CARTESIAN_POINT ( 'NONE',  ( 0.1154773475650540532, -42.72636521210627336, -11.01822788872314440 ) ) ;
#40963=CARTESIAN_POINT ( 'NONE',  ( -6.079354080745853928, 5.479977851902066099, 18.45976159084468549 ) ) ;
#40966=CARTESIAN_POINT ( 'NONE',  ( 0.6000166863083090663, 10.41802958826996317, -47.99258423138293495 ) ) ;
#40970=CARTESIAN_POINT ( 'NONE',  ( 0.8744876279028263033, 11.79038800009220722, -47.65854384249244191 ) ) ;
#40973=VERTEX_POINT ( 'NONE', #43182 ) ;
#40975=CARTESIAN_POINT ( 'NONE',  ( 0.1154773475650540809, 39.67614629000453164, -19.30665806451962041 ) ) ;
#40978=DIRECTION ( 'NONE',  ( -1.000000000000000000, -0.000000000000000000, -0.000000000000000000 ) ) ;
#40988=CARTESIAN_POINT ( 'NONE',  ( 0.1152809850208376119, -43.78968008214310004, 5.423025059255664360 ) ) ;
#40991=ADVANCED_FACE ( 'NONE', ( #24054 ), #34704, .F. ) ;
#40993=CARTESIAN_POINT ( 'NONE',  ( -6.057079549204054558, 0.6257114429647351317, -19.24681054850079320 ) ) ;
#40996=ORIENTED_EDGE ( 'NONE', *, *, #12365, .T. ) ;
#40997=CARTESIAN_POINT ( 'NONE',  ( 0.1129192098497455998, 29.30421273086464140, 32.98810246148426728 ) ) ;
#41006=AXIS2_PLACEMENT_3D ( 'NONE', #51771, #18586, #18283 ) ;
#41010=CARTESIAN_POINT ( 'NONE',  ( 0.6029443199889047422, 44.24425750603113983, 21.30688432395522369 ) ) ;
#41011=CARTESIAN_POINT ( 'NONE',  ( 0.1152809850208375841, -42.73668636166265600, 10.97820209846000772 ) ) ;
#41013=CARTESIAN_POINT ( 'NONE',  ( 4.335381028904216727, -23.55321997556169222, 42.95349434501397923 ) ) ;
#41017=CARTESIAN_POINT ( 'NONE',  ( -6.057079549204054558, 3.065021114850542627, 19.01149327815305412 ) ) ;
#41018=DIRECTION ( 'NONE',  ( -1.000000000000000000, -0.000000000000000000, -0.000000000000000000 ) ) ;
#41019=( BOUNDED_SURFACE ( )  B_SPLINE_SURFACE ( 3, 1, ( 
 ( #47246, #20511 ),
 ( #778, #4295 ),
 ( #1371, #5757 ),
 ( #39636, #34933 ) ),
 .UNSPECIFIED., .F., .F., .F. ) 
 B_SPLINE_SURFACE_WITH_KNOTS ( ( 4, 4 ),
 ( 2, 2 ),
 ( 0.000000000000000000, 1.000000000000000000 ),
 ( 0.000000000000000000, 1.000000000000000000 ),
 .UNSPECIFIED. ) 
 GEOMETRIC_REPRESENTATION_ITEM ( )  RATIONAL_B_SPLINE_SURFACE ( (
 ( 1.000000000000000000, 1.000000000000000000),
 ( 0.9754377213608244057, 0.9999580625633939235),
 ( 0.9754377213608244057, 0.9999580625633939235),
 ( 1.000000000000000000, 1.000000000000000000) ) ) 
 REPRESENTATION_ITEM ( '' )  SURFACE ( )  );
#41020=CARTESIAN_POINT ( 'NONE',  ( 0.7948884756798505480, 3.850400318513474751, 48.94765634825986211 ) ) ;
#41022=CARTESIAN_POINT ( 'NONE',  ( -2.739355103387247858, -14.92576340101414800, -0.2629711922692861692 ) ) ;
#41031=CARTESIAN_POINT ( 'NONE',  ( 0.1149546198390367091, -38.31111110369499784, -21.89075903260455647 ) ) ;
#41047=CARTESIAN_POINT ( 'NONE',  ( 0.1149546198390368618, 20.16591343492030930, 39.24643296350026134 ) ) ;
#41049=ORIENTED_EDGE ( 'NONE', *, *, #32042, .T. ) ;
#41056=EDGE_CURVE ( 'NONE', #21415, #2779, #49700, .T. ) ;
#41057=VERTEX_POINT ( 'NONE', #53759 ) ;
#41059=B_SPLINE_CURVE_WITH_KNOTS ( 'NONE', 3,
 ( #15180, #48988, #39001, #25477, #58665, #53656, #5122, #44019, #10787, #10161, #428, #34284, #15483, #748, #52752, #20483 ),
 .UNSPECIFIED., .F., .F.,
 ( 4, 3, 3, 3, 3, 4 ),
 ( 1.962735358247463844E-17, 0.0002612764279487723496, 0.0003919131003184841782, 0.0005225497727000665569, 0.0007837925190632412343, 0.001045051706266714349 ),
 .UNSPECIFIED. ) ;
#41065=ORIENTED_EDGE ( 'NONE', *, *, #6632, .F. ) ;
#41079=ORIENTED_EDGE ( 'NONE', *, *, #36870, .T. ) ;
#41083=DIRECTION ( 'NONE',  ( 0.09722883295013598492, -0.7930735330831429897, -0.6013159944373470678 ) ) ;
#41086=CARTESIAN_POINT ( 'NONE',  ( -2.601141883200665639, 11.65089574274779949, -9.330169122851405206 ) ) ;
#41088=ORIENTED_EDGE ( 'NONE', *, *, #53441, .T. ) ;
#41091=CARTESIAN_POINT ( 'NONE',  ( 0.3676999524040366896, 33.04872056100262512, -29.21870381457057775 ) ) ;
#41096=CARTESIAN_POINT ( 'NONE',  ( 2.299746137290199055, 33.90759634673861456, 35.41971552218871722 ) ) ;
#41098=CARTESIAN_POINT ( 'NONE',  ( 4.553261556744875094, 0.000000000000000000, 0.000000000000000000 ) ) ;
#41099=EDGE_CURVE ( 'NONE', #53021, #26015, #55687, .T. ) ;
#41106=CARTESIAN_POINT ( 'NONE',  ( 0.8753041380234530822, 48.36002538446245325, 8.511537621788884067 ) ) ;
#41117=CARTESIAN_POINT ( 'NONE',  ( 0.1149546198390368201, 44.01516278036778829, 3.100324247711259584 ) ) ;
#41120=EDGE_LOOP ( 'NONE', ( #49813, #21111, #3421, #33264 ) ) ;
#41128=CARTESIAN_POINT ( 'NONE',  ( 4.226256110419178924, -37.05036947536322600, 23.62408456906341669 ) ) ;
#41130=VERTEX_POINT ( 'NONE', #49091 ) ;
#41132=CARTESIAN_POINT ( 'NONE',  ( 0.8744876279028263033, 3.827863332834932297, 48.94586308039354350 ) ) ;
#41140=ORIENTED_EDGE ( 'NONE', *, *, #33638, .T. ) ;
#41143=CARTESIAN_POINT ( 'NONE',  ( 2.185380717157383135, 42.21983218090981183, 12.50222274969580383 ) ) ;
#41144=DIRECTION ( 'NONE',  ( 1.000000000000000000, 0.000000000000000000, 0.000000000000000000 ) ) ;
#41145=B_SPLINE_CURVE_WITH_KNOTS ( 'NONE', 3,
 ( #223, #28141, #37567, #37257, #32553, #33169 ),
 .UNSPECIFIED., .F., .F.,
 ( 4, 2, 4 ),
 ( 1.951563910473907981E-18, 0.0002447193893791718765, 0.0004894387787583418014 ),
 .UNSPECIFIED. ) ;
#41154=CARTESIAN_POINT ( 'NONE',  ( 4.060580049360325461, 40.92264867182483812, -16.02512152969835668 ) ) ;
#41156=B_SPLINE_CURVE_WITH_KNOTS ( 'NONE', 3,
 ( #52079, #4443, #8869, #32689 ),
 .UNSPECIFIED., .F., .F.,
 ( 4, 4 ),
 ( 0.000000000000000000, 0.005013413432710147645 ),
 .UNSPECIFIED. ) ;
#41159=CARTESIAN_POINT ( 'NONE',  ( 0.6252788684277231779, -38.93999277421796279, 29.91857773888190053 ) ) ;
#41161=CARTESIAN_POINT ( 'NONE',  ( 0.6026112563231247332, 16.79644620207902861, 46.14564323839112348 ) ) ;
#41162=CARTESIAN_POINT ( 'NONE',  ( 0.6028777368367060907, -47.52337658901180362, 12.37208579383598206 ) ) ;
#41166=VERTEX_POINT ( 'NONE', #23587 ) ;
#41169=CARTESIAN_POINT ( 'NONE',  ( 0.8744876279028306332, 44.61213666265828692, 20.49651952824657286 ) ) ;
#41172=CARTESIAN_POINT ( 'NONE',  ( 4.553261556744875094, 27.21079963941838997, 34.48350256002230196 ) ) ;
#41178=ADVANCED_FACE ( 'NONE', ( #33011 ), #7951, .F. ) ;
#41193=CARTESIAN_POINT ( 'NONE',  ( 0.7242003506639999033, 16.18715005828274300, -46.35717686741356403 ) ) ;
#41195=ADVANCED_FACE ( 'NONE', ( #5071 ), #48689, .F. ) ;
#41196=B_SPLINE_CURVE_WITH_KNOTS ( 'NONE', 3,
 ( #8211, #36440, #12636, #50817, #7910, #27330, #3500, #1503, #35062, #10944, #1203, #11239, #40089, #43537, #20335, #30025, #49137, #48518, #30329, #39152, #20636, #29103, #54117, #49441, #39455 ),
 .UNSPECIFIED., .F., .F.,
 ( 4, 3, 3, 3, 3, 3, 3, 3, 4 ),
 ( 4.670885906470169154E-18, 0.0005656085177311393148, 0.001131215744874498755, 0.001696821861372766567, 0.002262427090022498151, 0.002828031679238745925, 0.003393635864401605730, 0.003977030878808132490, 0.004561030005651159000 ),
 .UNSPECIFIED. ) ;
#41198=DIRECTION ( 'NONE',  ( 0.09722883295013594329, 0.3508110149947525902, 0.9313850899609172895 ) ) ;
#41202=CARTESIAN_POINT ( 'NONE',  ( 0.8753041380234471980, -8.714053517584197550, 48.32394436680080219 ) ) ;
#41205=FACE_OUTER_BOUND ( 'NONE', #19832, .T. ) ;
#41221=CARTESIAN_POINT ( 'NONE',  ( 0.6016118706126977189, 41.34544472431174711, -26.49726882780209891 ) ) ;
#41223=VERTEX_POINT ( 'NONE', #17130 ) ;
#41238=CARTESIAN_POINT ( 'NONE',  ( 0.5987334363312691865, 27.59677704409741139, 40.61995572684014633 ) ) ;
#41251=ADVANCED_FACE ( 'NONE', ( #53315 ), #50755, .F. ) ;
#41255=ORIENTED_EDGE ( 'NONE', *, *, #2970, .F. ) ;
#41256=CARTESIAN_POINT ( 'NONE',  ( 0.8744876279028306332, 43.84003649649945089, -22.09980204357244560 ) ) ;
#41257=CARTESIAN_POINT ( 'NONE',  ( 0.1135584504625007513, -42.56957105991563139, -11.60963702748914628 ) ) ;
#41258=CARTESIAN_POINT ( 'NONE',  ( -6.078726893082806448, 5.482141236671949969, 18.45914864585853721 ) ) ;
#41260=VERTEX_POINT ( 'NONE', #24512 ) ;
#41261=EDGE_CURVE ( 'NONE', #473, #29981, #58009, .T. ) ;
#41262=CARTESIAN_POINT ( 'NONE',  ( -6.078075953587585900, -4.290048539733580135, 18.77207121693995973 ) ) ;
#41268=CARTESIAN_POINT ( 'NONE',  ( 0.7413678028165009426, 39.31562913345087651, -19.96916116443533440 ) ) ;
#41272=LINE ( 'NONE', #4547, #48017 ) ;
#41277=CARTESIAN_POINT ( 'NONE',  ( 3.678834586032788234, -40.32777138951392715, 27.78998424582957227 ) ) ;
#41283=CARTESIAN_POINT ( 'NONE',  ( 0.1156495703730067437, -27.61742026461291744, -34.41251300266834079 ) ) ;
#41286=EDGE_CURVE ( 'NONE', #21723, #52990, #35230, .T. ) ;
#41290=( BOUNDED_SURFACE ( )  B_SPLINE_SURFACE ( 3, 1, ( 
 ( #268, #19415 ),
 ( #47605, #33211 ),
 ( #47922, #38532 ),
 ( #29109, #42926 ) ),
 .UNSPECIFIED., .F., .F., .F. ) 
 B_SPLINE_SURFACE_WITH_KNOTS ( ( 4, 4 ),
 ( 2, 2 ),
 ( 0.000000000000000000, 1.000000000000000000 ),
 ( 0.000000000000000000, 1.000000000000000000 ),
 .UNSPECIFIED. ) 
 GEOMETRIC_REPRESENTATION_ITEM ( )  RATIONAL_B_SPLINE_SURFACE ( (
 ( 1.000000000000000000, 1.000000000000000000),
 ( 0.7211978278499970862, 0.9934217856018976445),
 ( 0.7211978278499970862, 0.9934217856018976445),
 ( 1.000000000000000000, 1.000000000000000000) ) ) 
 REPRESENTATION_ITEM ( '' )  SURFACE ( )  );
#41308=CARTESIAN_POINT ( 'NONE',  ( 0.5997462898726536595, 32.62638226927682439, 36.70246327105753892 ) ) ;
#41313=CARTESIAN_POINT ( 'NONE',  ( 0.7242486021783841599, 3.898994070056987393, 48.94700509342359851 ) ) ;
#41314=CARTESIAN_POINT ( 'NONE',  ( 1.830465331921977468, 43.86281037434080332, 4.053384011293614364 ) ) ;
#41320=CARTESIAN_POINT ( 'NONE',  ( 0.8744876279028306332, -45.83369275826206746, -17.59609782084448071 ) ) ;
#41333=CARTESIAN_POINT ( 'NONE',  ( 1.296416391601052265, -40.42071545795151621, 17.56340331323853476 ) ) ;
#41337=B_SPLINE_CURVE_WITH_KNOTS ( 'NONE', 3,
 ( #52681, #39545, #38935, #53906, #57987, #9779 ),
 .UNSPECIFIED., .F., .F.,
 ( 4, 2, 4 ),
 ( 1.910620358896493634E-17, 0.0002293755540694311830, 0.0004587511081388432298 ),
 .UNSPECIFIED. ) ;
#41345=CARTESIAN_POINT ( 'NONE',  ( 2.648799415243708655, 38.22150636650994926, 30.71862487749798731 ) ) ;
#41351=CARTESIAN_POINT ( 'NONE',  ( 0.8753041380234524160, -34.64850320773157222, 34.79395857525835822 ) ) ;
#41353=CARTESIAN_POINT ( 'NONE',  ( 0.1158516988532803799, -1.365047127049809239, 44.10304757240399454 ) ) ;
#41354=EDGE_LOOP ( 'NONE', ( #35396, #9830, #15427, #28909 ) ) ;
#41360=ORIENTED_EDGE ( 'NONE', *, *, #4928, .F. ) ;
#41361=CARTESIAN_POINT ( 'NONE',  ( 4.553261556744875094, 6.787618719203488915, 43.39893775135925580 ) ) ;
#41363=CARTESIAN_POINT ( 'NONE',  ( 2.879087469061463178, 0.3214110636685244549, 43.99998149671804271 ) ) ;
#41365=ORIENTED_EDGE ( 'NONE', *, *, #9528, .F. ) ;
#41366=CARTESIAN_POINT ( 'NONE',  ( -6.077587904424778920, -17.34643006009198274, 8.360465630828690209 ) ) ;
#41367=CARTESIAN_POINT ( 'NONE',  ( 0.8744876279028306332, 5.599149760997630842, 48.77498920895230583 ) ) ;
#41371=CARTESIAN_POINT ( 'NONE',  ( 4.553261556744875094, 0.000000000000000000, 0.000000000000000000 ) ) ;
#41374=VERTEX_POINT ( 'NONE', #16057 ) ;
#41377=CARTESIAN_POINT ( 'NONE',  ( 0.8744876279028263033, 32.34273794994744833, 36.93639603806145288 ) ) ;
#41381=CARTESIAN_POINT ( 'NONE',  ( 3.894904216938897878, -43.25473375298778933, 7.819996191453038037 ) ) ;
#41384=CARTESIAN_POINT ( 'NONE',  ( -4.915099999999998914, 0.000000000000000000, 0.000000000000000000 ) ) ;
#41391=( BOUNDED_SURFACE ( )  B_SPLINE_SURFACE ( 3, 1, ( 
 ( #887, #20027 ),
 ( #48817, #44462 ),
 ( #5871, #1189 ),
 ( #20323, #58812 ) ),
 .UNSPECIFIED., .F., .F., .F. ) 
 B_SPLINE_SURFACE_WITH_KNOTS ( ( 4, 4 ),
 ( 2, 2 ),
 ( 0.000000000000000000, 1.000000000000000000 ),
 ( 0.000000000000000000, 1.000000000000000000 ),
 .UNSPECIFIED. ) 
 GEOMETRIC_REPRESENTATION_ITEM ( )  RATIONAL_B_SPLINE_SURFACE ( (
 ( 1.000000000000000000, 1.000000000000000000),
 ( 0.9953485035131437453, 0.8621029689291523912),
 ( 0.9953485035131437453, 0.8621029689291523912),
 ( 1.000000000000000000, 1.000000000000000000) ) ) 
 REPRESENTATION_ITEM ( '' )  SURFACE ( )  );
#41397=CARTESIAN_POINT ( 'NONE',  ( -6.077587904424778920, -4.290907484552072049, -18.77189746277518623 ) ) ;
#41407=ORIENTED_EDGE ( 'NONE', *, *, #815, .T. ) ;
#41408=CARTESIAN_POINT ( 'NONE',  ( 0.6026777506516368677, 44.16847194355625561, -21.46374796741015345 ) ) ;
#41415=EDGE_CURVE ( 'NONE', #27238, #49921, #23697, .T. ) ;
#41417=VERTEX_POINT ( 'NONE', #49549 ) ;
#41419=CARTESIAN_POINT ( 'NONE',  ( 4.335381028904216727, -21.75407475222698750, -43.89210725562018922 ) ) ;
#41420=EDGE_CURVE ( 'NONE', #37050, #9776, #2231, .T. ) ;
#41422=FACE_OUTER_BOUND ( 'NONE', #6679, .T. ) ;
#41427=CARTESIAN_POINT ( 'NONE',  ( 1.112077966505211624, -0.3630408210682974923, 44.07832263699236108 ) ) ;
#41429=CARTESIAN_POINT ( 'NONE',  ( 0.1129192098497455998, 43.40062318508800843, -7.958498283668546947 ) ) ;
#41430=FACE_OUTER_BOUND ( 'NONE', #36667, .T. ) ;
#41431=CARTESIAN_POINT ( 'NONE',  ( 1.479689385636123067, -37.80276034141566299, 22.63923929457843087 ) ) ;
#41433=ORIENTED_EDGE ( 'NONE', *, *, #24314, .F. ) ;
#41436=ORIENTED_EDGE ( 'NONE', *, *, #48926, .T. ) ;
#41442=CARTESIAN_POINT ( 'NONE',  ( 1.657374760986086271, 14.04758338772360915, -41.75590794387299809 ) ) ;
#41447=LINE ( 'NONE', #61731, #61412 ) ;
#41448=VERTEX_POINT ( 'NONE', #44895 ) ;
#41457=CARTESIAN_POINT ( 'NONE',  ( 0.7948884756798504370, 43.85325300242502067, 22.08145932010500800 ) ) ;
#41458=CARTESIAN_POINT ( 'NONE',  ( -6.063463321072278589, 13.82218400051372598, 13.40774708649489355 ) ) ;
#41459=FACE_OUTER_BOUND ( 'NONE', #3297, .T. ) ;
#41474=CARTESIAN_POINT ( 'NONE',  ( 3.727782113643637096, 2.088457279502629493, -43.91373500509456562 ) ) ;
#41479=DIRECTION ( 'NONE',  ( 0.1011922191286468292, 0.9739806266819530656, -0.2027852894961811869 ) ) ;
#41481=CARTESIAN_POINT ( 'NONE',  ( 4.226256110419178924, 27.07260893061330620, 34.61070781820654929 ) ) ;
#41483=ORIENTED_EDGE ( 'NONE', *, *, #49552, .T. ) ;
#41487=CARTESIAN_POINT ( 'NONE',  ( 0.5987334363312694085, 48.96426925486512971, 3.750099039911617194 ) ) ;
#41495=FACE_OUTER_BOUND ( 'NONE', #26060, .T. ) ;
#41504=CARTESIAN_POINT ( 'NONE',  ( -6.077587904424778920, 19.09718056542708453, -2.468545289316033120 ) ) ;
#41512=CARTESIAN_POINT ( 'NONE',  ( 4.553261556744873317, -36.69060082144796553, 24.15241969627054530 ) ) ;
#41516=ORIENTED_EDGE ( 'NONE', *, *, #38552, .F. ) ;
#41523=CARTESIAN_POINT ( 'NONE',  ( 4.975610109902397937, 20.32389311291233724, -44.49032227207044343 ) ) ;
#41531=CARTESIAN_POINT ( 'NONE',  ( 4.553261556744873317, 12.28162544311275006, -42.17465165592624032 ) ) ;
#41532=B_SPLINE_CURVE_WITH_KNOTS ( 'NONE', 3,
 ( #55313, #45643, #22130, #36555, #26202, #35635 ),
 .UNSPECIFIED., .F., .F.,
 ( 4, 2, 4 ),
 ( 7.047314121155778821E-19, 0.0002293801035737096431, 0.0004587602071474185814 ),
 .UNSPECIFIED. ) ;
#41533=CARTESIAN_POINT ( 'NONE',  ( -6.079354080745853928, 7.795569227099167442, -17.60744318956237464 ) ) ;
#41548=ADVANCED_FACE ( 'NONE', ( #60793 ), #50392, .F. ) ;
#41550=CARTESIAN_POINT ( 'NONE',  ( 0.8744876279028263033, -47.25615711918255357, -13.31186180466976587 ) ) ;
#41551=CARTESIAN_POINT ( 'NONE',  ( -6.078075953587585900, 3.068021059656498295, 19.01006104736752889 ) ) ;
#41553=EDGE_CURVE ( 'NONE', #15459, #39035, #3470, .T. ) ;
#41558=CARTESIAN_POINT ( 'NONE',  ( 2.359973842542476330, 37.69777570118016996, 22.73793310342894358 ) ) ;
#41562=CARTESIAN_POINT ( 'NONE',  ( 0.6029443449137436017, 49.00372439284071646, 3.189754475479290363 ) ) ;
#41563=CARTESIAN_POINT ( 'NONE',  ( -6.078726893082806448, -11.01948708261720178, -15.79129335123480971 ) ) ;
#41564=CARTESIAN_POINT ( 'NONE',  ( 0.1155031312995260795, 33.48869165808871173, 28.73063110273194454 ) ) ;
#41565=ORIENTED_EDGE ( 'NONE', *, *, #9528, .T. ) ;
#41566=CARTESIAN_POINT ( 'NONE',  ( 0.8744876279028306332, 21.91587810745098963, -43.93226988397984911 ) ) ;
#41571=CARTESIAN_POINT ( 'NONE',  ( 1.657374760986086493, 39.13992893817287211, -20.22267069323491029 ) ) ;
#41572=CARTESIAN_POINT ( 'NONE',  ( 0.7948884756798516582, 23.47568016441766758, -43.12297630519164215 ) ) ;
#41574=VERTEX_POINT ( 'NONE', #26366 ) ;
#41578=CARTESIAN_POINT ( 'NONE',  ( 0.6039202388192953519, 17.12343321804663177, 46.02555537607436520 ) ) ;
#41582=VERTEX_POINT ( 'NONE', #55479 ) ;
#41583=CARTESIAN_POINT ( 'NONE',  ( 4.060580049360325461, 43.52047761765033584, 6.118473853078531199 ) ) ;
#41587=CARTESIAN_POINT ( 'NONE',  ( 0.1155031312995260795, -27.37902390932426755, -34.60246641938199019 ) ) ;
#41588=EDGE_CURVE ( 'NONE', #46515, #33349, #20248, .T. ) ;
#41596=CARTESIAN_POINT ( 'NONE',  ( 0.3676999524040366896, 41.59822836379080968, -14.68121181363270367 ) ) ;
#41597=ORIENTED_EDGE ( 'NONE', *, *, #51852, .T. ) ;
#41602=AXIS2_PLACEMENT_3D ( 'NONE', #2621, #51461, #45886 ) ;
#41603=CARTESIAN_POINT ( 'NONE',  ( 0.5980271706414734822, -43.13192993667226460, -23.48799401353080540 ) ) ;
#41604=CARTESIAN_POINT ( 'NONE',  ( -6.057079549204054558, -18.27862279149374203, 6.059965341982067599 ) ) ;
#41605=CARTESIAN_POINT ( 'NONE',  ( 0.6016118706126977189, 44.09211895607887755, 21.62027059837412679 ) ) ;
#41611=CARTESIAN_POINT ( 'NONE',  ( 0.1158516988532803521, -12.60172690908452076, -42.28638832699774497 ) ) ;
#41613=CARTESIAN_POINT ( 'NONE',  ( -6.079354080745853928, 13.83171223607736167, 13.39689112691858419 ) ) ;
#41622=CARTESIAN_POINT ( 'NONE',  ( 2.359973842542475442, 32.52418265237010786, -29.67007646481159711 ) ) ;
#41624=ORIENTED_EDGE ( 'NONE', *, *, #20400, .F. ) ;
#41625=CARTESIAN_POINT ( 'NONE',  ( 0.3676999524040323597, 39.37931578712994707, 19.88014264185084912 ) ) ;
#41627=CARTESIAN_POINT ( 'NONE',  ( 3.221118495291108719, -32.88209193446716938, -29.21522633277039560 ) ) ;
#41628=CARTESIAN_POINT ( 'NONE',  ( 3.727782113643637540, 27.93898545223054697, -33.94393712883089620 ) ) ;
#41629=CARTESIAN_POINT ( 'NONE',  ( 0.6008122571543325074, -45.68025335892497907, -18.02412282275449584 ) ) ;
#41637=CARTESIAN_POINT ( 'NONE',  ( 4.226256110419179812, -25.47726887332619583, 35.80134104671822115 ) ) ;
#41639=CARTESIAN_POINT ( 'NONE',  ( -6.063463321072276813, 12.01854346922034722, 15.04576569530214059 ) ) ;
#41657=AXIS2_PLACEMENT_3D ( 'NONE', #32834, #51913, #51287 ) ;
#41661=ORIENTED_EDGE ( 'NONE', *, *, #11978, .T. ) ;
#41662=CARTESIAN_POINT ( 'NONE',  ( 4.226256110419178924, 6.604788716987348707, 43.44196146574351758 ) ) ;
#41666=B_SPLINE_CURVE_WITH_KNOTS ( 'NONE', 3,
 ( #20994, #34485, #58561, #15691, #40141, #6864 ),
 .UNSPECIFIED., .F., .F.,
 ( 4, 2, 4 ),
 ( 1.246832498358330099E-18, 0.0002293801035737093178, 0.0004587602071474173888 ),
 .UNSPECIFIED. ) ;
#41667=VERTEX_POINT ( 'NONE', #38571 ) ;
#41671=CARTESIAN_POINT ( 'NONE',  ( 2.299746137290199943, 5.989104756252149997, 48.66633294079981198 ) ) ;
#41681=EDGE_CURVE ( 'NONE', #21596, #23436, #57623, .T. ) ;
#41682=B_SPLINE_CURVE_WITH_KNOTS ( 'NONE', 3,
 ( #483, #48727, #38745, #29312, #1400, #49340, #14933, #20847, #48421, #6393, #29010, #39986, #53414, #25229, #48124, #5177, #34339, #57800, #34040 ),
 .UNSPECIFIED., .F., .F.,
 ( 4, 3, 3, 3, 3, 3, 4 ),
 ( 1.734776414728241573E-18, 0.0002612768053151712754, 0.0003919133833142901665, 0.0005225499612322610787, 0.0006531865391693348743, 0.0008112755173415197489, 0.0009693688056799721394 ),
 .UNSPECIFIED. ) ;
#41693=VECTOR ( 'NONE', #26464, 1000.000000000000114 ) ;
#41694=EDGE_CURVE ( 'NONE', #54562, #4022, #52013, .T. ) ;
#41699=CARTESIAN_POINT ( 'NONE',  ( 0.2285344041767085055, 43.15390724259560074, -9.178314659724513547 ) ) ;
#41700=CARTESIAN_POINT ( 'NONE',  ( 0.5997462898726536595, -49.10477184366966696, -0.5225058138009923692 ) ) ;
#41701=B_SPLINE_CURVE_WITH_KNOTS ( 'NONE', 3,
 ( #43153, #39379, #5807, #57503 ),
 .UNSPECIFIED., .F., .F.,
 ( 4, 4 ),
 ( 0.000000000000000000, 0.005013413432710150247 ),
 .UNSPECIFIED. ) ;
#41708=CARTESIAN_POINT ( 'NONE',  ( -6.057079549204054558, 19.25697688790420159, -0.008499321259853864774 ) ) ;
#41712=ORIENTED_EDGE ( 'NONE', *, *, #6711, .F. ) ;
#41716=VECTOR ( 'NONE', #52595, 1000.000000000000114 ) ;
#41717=EDGE_LOOP ( 'NONE', ( #15143, #14913, #32221, #42637 ) ) ;
#41719=EDGE_CURVE ( 'NONE', #58860, #11856, #44122, .T. ) ;
#41724=VERTEX_POINT ( 'NONE', #33558 ) ;
#41730=CARTESIAN_POINT ( 'NONE',  ( 3.598860563414087554, 0.2887493804703922251, 48.97398519332762845 ) ) ;
#41734=EDGE_LOOP ( 'NONE', ( #38626, #3910, #37584, #466 ) ) ;
#41735=CARTESIAN_POINT ( 'NONE',  ( 0.1157991065609915854, 15.16251859759399778, 41.43718614137927858 ) ) ;
#41737=CARTESIAN_POINT ( 'NONE',  ( 0.8744876279028263033, 28.81338721758142896, -39.75095932715596092 ) ) ;
#41743=EDGE_LOOP ( 'NONE', ( #57689, #46099, #55978, #18815 ) ) ;
#41749=EDGE_LOOP ( 'NONE', ( #2936, #35734, #36342, #48280 ) ) ;
#41752=CARTESIAN_POINT ( 'NONE',  ( -6.079354080745853928, -18.90111140843025694, -3.679802002047057652 ) ) ;
#41753=CARTESIAN_POINT ( 'NONE',  ( -6.078726893082806448, -18.27395335922926378, 6.070969436048390122 ) ) ;
#41758=DIRECTION ( 'NONE',  ( 1.000000000000000000, 0.000000000000000000, 0.000000000000000000 ) ) ;
#41761=( BOUNDED_SURFACE ( )  B_SPLINE_SURFACE ( 3, 1, ( 
 ( #58022, #34870 ),
 ( #14839, #53027 ),
 ( #20451, #10128 ),
 ( #39581, #29842 ) ),
 .UNSPECIFIED., .F., .F., .F. ) 
 B_SPLINE_SURFACE_WITH_KNOTS ( ( 4, 4 ),
 ( 2, 2 ),
 ( 0.000000000000000000, 1.000000000000000000 ),
 ( 0.000000000000000000, 1.000000000000000000 ),
 .UNSPECIFIED. ) 
 GEOMETRIC_REPRESENTATION_ITEM ( )  RATIONAL_B_SPLINE_SURFACE ( (
 ( 1.000000000000000000, 1.000000000000000000),
 ( 0.9754377213608244057, 0.9999580625633939235),
 ( 0.9754377213608244057, 0.9999580625633939235),
 ( 1.000000000000000000, 1.000000000000000000) ) ) 
 REPRESENTATION_ITEM ( '' )  SURFACE ( )  );
#41763=CARTESIAN_POINT ( 'NONE',  ( 0.3676999524040366896, -18.60775935196311082, -39.99627326667158655 ) ) ;
#41769=CARTESIAN_POINT ( 'NONE',  ( 0.7044674535452954967, 48.94804745615587649, 3.986398505019110416 ) ) ;
#41774=DIRECTION ( 'NONE',  ( 0.000000000000000000, 0.000000000000000000, 1.000000000000000000 ) ) ;
#41778=B_SPLINE_CURVE_WITH_KNOTS ( 'NONE', 3,
 ( #27810, #37859, #46942, #51921, #3977, #56920 ),
 .UNSPECIFIED., .F., .F.,
 ( 4, 2, 4 ),
 ( 2.196947838360372653E-17, 0.0002293755540694311017, 0.0004587511081388401940 ),
 .UNSPECIFIED. ) ;
#41782=CARTESIAN_POINT ( 'NONE',  ( 0.6029442701453590070, -47.47924998016712550, 12.54057600268335548 ) ) ;
#41787=AXIS2_PLACEMENT_3D ( 'NONE', #19933, #474, #15528 ) ;
#41791=CARTESIAN_POINT ( 'NONE',  ( 0.7413678028165008316, -31.02027698649011711, 31.34052500280865772 ) ) ;
#41793=B_SPLINE_CURVE_WITH_KNOTS ( 'NONE', 3,
 ( #2609, #17046, #50845, #11410, #7936, #21113 ),
 .UNSPECIFIED., .F., .F.,
 ( 4, 2, 4 ),
 ( 0.000000000000000000, 0.0002447195606305737161, 0.0004894391212611474322 ),
 .UNSPECIFIED. ) ;
#41799=FACE_OUTER_BOUND ( 'NONE', #27350, .T. ) ;
#41800=CARTESIAN_POINT ( 'NONE',  ( 2.299746137290199055, 48.99837783518191259, 1.854806514677992624 ) ) ;
#41802=ORIENTED_EDGE ( 'NONE', *, *, #24644, .T. ) ;
#41817=ORIENTED_EDGE ( 'NONE', *, *, #41694, .T. ) ;
#41819=CARTESIAN_POINT ( 'NONE',  ( -6.057079549204054558, 18.62501892953343585, -4.892841809650052554 ) ) ;
#41822=VERTEX_POINT ( 'NONE', #15990 ) ;
#41826=CARTESIAN_POINT ( 'NONE',  ( -6.057079549204054558, 12.01317374117834902, -15.05041154799434011 ) ) ;
#41833=CARTESIAN_POINT ( 'NONE',  ( -6.078457390727109555, 0.6128065477899394820, -19.24627182527810021 ) ) ;
#41843=ADVANCED_FACE ( 'NONE', ( #15064 ), #3729, .F. ) ;
#41846=CARTESIAN_POINT ( 'NONE',  ( 0.1140933569871964426, -35.13362084938451346, -26.69416857846670865 ) ) ;
#41851=AXIS2_PLACEMENT_3D ( 'NONE', #14712, #29406, #19111 ) ;
#41853=SHAPE_DEFINITION_REPRESENTATION ( #37327, #2385 ) ;
#41856=CONICAL_SURFACE ( 'NONE', #48842, 43.92652462719577500, 1.486293639869522343 ) ;
#41876=CARTESIAN_POINT ( 'NONE',  ( 1.112077966505211624, -44.06731193995874918, 1.049925480652556198 ) ) ;
#41878=CARTESIAN_POINT ( 'NONE',  ( 0.6027444965799114707, 48.99797994875344642, 3.276656348932040164 ) ) ;
#41880=CARTESIAN_POINT ( 'NONE',  ( 0.1129192098497447394, 33.91039995638862337, 28.23183597612653983 ) ) ;
#41882=CARTESIAN_POINT ( 'NONE',  ( 4.694002226626921015, 44.18338616738627422, -11.23001149731177328 ) ) ;
#41883=CARTESIAN_POINT ( 'NONE',  ( -6.072942160501519915, -6.636811946999699785, 18.07641804863957091 ) ) ;
#41886=CARTESIAN_POINT ( 'NONE',  ( 0.5987334363312690755, -20.42989704442242171, 44.65626734542841803 ) ) ;
#41888=CARTESIAN_POINT ( 'NONE',  ( 2.879087469061462734, 38.86168815156121781, -20.63663903822967427 ) ) ;
#41889=CARTESIAN_POINT ( 'NONE',  ( 0.5997462898726536595, 23.17609050332929854, -43.29457771044543080 ) ) ;
#41892=VERTEX_POINT ( 'NONE', #26601 ) ;
#41894=CARTESIAN_POINT ( 'NONE',  ( 0.7044674535452954967, -47.28336972574645358, -13.26972758534514618 ) ) ;
#41898=EDGE_CURVE ( 'NONE', #53021, #11949, #50082, .T. ) ;
#41901=CARTESIAN_POINT ( 'NONE',  ( 0.6029443449137436017, -25.49413300155796591, 41.97128447500987392 ) ) ;
#41904=CARTESIAN_POINT ( 'NONE',  ( 0.7948878604505664747, -8.691324790642898535, -48.32348829174041072 ) ) ;
#41911=CARTESIAN_POINT ( 'NONE',  ( 0.2285344041767085332, -43.65329955122442129, 6.394576497824234984 ) ) ;
#41920=CARTESIAN_POINT ( 'NONE',  ( 0.6000166863083090663, -43.04473087057990455, -23.64264422580097502 ) ) ;
#41923=EDGE_CURVE ( 'NONE', #60001, #27320, #50408, .T. ) ;
#41932=ORIENTED_EDGE ( 'NONE', *, *, #49273, .F. ) ;
#41935=CARTESIAN_POINT ( 'NONE',  ( 4.975610109902397937, 24.86209007718959185, 42.12274782266089801 ) ) ;
#41937=CARTESIAN_POINT ( 'NONE',  ( 4.553261556744875094, 0.000000000000000000, 0.000000000000000000 ) ) ;
#41942=EDGE_LOOP ( 'NONE', ( #52636, #33387, #31610, #54410, #18675, #31035, #34305, #53561, #36477, #20031, #47427, #33663, #22466, #5213, #32013, #36125, #15767, #1185, #60185, #21294, #55974, #45630, #36473, #20662, #6477, #21130, #37392, #15994, #3398, #47352, #4446, #48433, #27916, #28069, #3296, #18378, #10369, #53762, #41088, #8095, #37432, #54520, #33789, #9897, #22748, #11481, #40871, #36486, #28597, #21664, #56775, #47034, #58933, #11990, #11175, #4379, #60298, #7889, #52491, #28298, #21916, #56569, #56983, #52571, #8786, #20287, #39039, #30131, #5746, #33113, #33854, #47235, #51517, #37785, #5558, #37961, #45451, #11403, #8180, #39120, #25134, #27682, #33942, #10205, #16697, #48020, #11522, #50925, #19899, #41661, #1570, #25574, #56029, #53179, #18902, #40363, #18975, #12864, #36748, #17451, #60934, #47103, #52693, #20361, #42870, #19176, #29236, #53184, #48929, #46971, #12511, #48120, #34319, #9349, #60541, #34251, #12342, #30650, #20986, #15848, #53480, #24416, #9717, #35739, #18289, #38811, #60430, #51145, #32327, #12431, #4770, #54737, #26533, #27837, #15527, #51476, #29541, #15079, #27455, #4334, #37897, #43173, #57302, #45123, #30904, #61501, #61115, #40596, #16972, #1284, #7152, #22340 ) ) ;
#41946=CARTESIAN_POINT ( 'NONE',  ( 2.533389852662419894, 28.40184444967290034, -33.62715812539327231 ) ) ;
#41953=VERTEX_POINT ( 'NONE', #7474 ) ;
#41955=ADVANCED_FACE ( 'NONE', ( #27530 ), #1525, .F. ) ;
#41956=CARTESIAN_POINT ( 'NONE',  ( 1.296416391601052487, -26.60065513383224456, 35.13847635466117936 ) ) ;
#41957=ORIENTED_EDGE ( 'NONE', *, *, #35677, .F. ) ;
#41960=CARTESIAN_POINT ( 'NONE',  ( 0.6252788684277220677, 17.60247651936639102, 45.84317998959954110 ) ) ;
#41968=CARTESIAN_POINT ( 'NONE',  ( 0.6021448801613057400, -7.579532981145714388, -48.51898410328343658 ) ) ;
#41970=CARTESIAN_POINT ( 'NONE',  ( -6.072942160501519915, 17.84350912780789500, -7.239706091745485850 ) ) ;
#41974=CARTESIAN_POINT ( 'NONE',  ( 0.6026777506516366456, -42.87348921357890674, -23.94598741523000740 ) ) ;
#41977=CIRCLE ( 'NONE', #39971, 43.92652462719577500 ) ;
#41979=CARTESIAN_POINT ( 'NONE',  ( 3.390910168358337806, -28.93279679135903848, -33.12084549590425553 ) ) ;
#41981=CARTESIAN_POINT ( 'NONE',  ( 3.050102900204245682, 6.022580839601601177, 43.57928142143379802 ) ) ;
#41984=CARTESIAN_POINT ( 'NONE',  ( 2.254628338793795983, 0.05544974030731342207, 44.02889495774882533 ) ) ;
#41988=CARTESIAN_POINT ( 'NONE',  ( 0.7948878604505678069, 11.76956405680572892, 47.66734741110693108 ) ) ;
#41989=FACE_OUTER_BOUND ( 'NONE', #36209, .T. ) ;
#41990=CARTESIAN_POINT ( 'NONE',  ( 4.335381028904216727, 29.74326630871418331, 38.92422069808531404 ) ) ;
#41996=CARTESIAN_POINT ( 'NONE',  ( 0.5549461598389361372, 43.11493157709418966, -9.290875662137066726 ) ) ;
#41997=EDGE_CURVE ( 'NONE', #11842, #9433, #35117, .T. ) ;
#41999=B_SPLINE_CURVE_WITH_KNOTS ( 'NONE', 3,
 ( #12276, #26047, #31671, #3151, #60461, #21655 ),
 .UNSPECIFIED., .F., .F.,
 ( 4, 2, 4 ),
 ( 1.870761316369714769E-17, 0.0002293755540694314540, 0.0004587511081388442056 ),
 .UNSPECIFIED. ) ;
#42000=CARTESIAN_POINT ( 'NONE',  ( 0.9268187852002115479, -43.58820572414531114, 6.619868175289538748 ) ) ;
#42002=CIRCLE ( 'NONE', #11996, 48.91267123290010943 ) ;
#42004=CARTESIAN_POINT ( 'NONE',  ( 0.2279481005628782586, 21.07700012148384516, -38.75904478895067484 ) ) ;
#42011=CARTESIAN_POINT ( 'NONE',  ( 0.6026777506516367566, -49.10718938754244789, 0.1741869491615331278 ) ) ;
#42024=EDGE_LOOP ( 'NONE', ( #3703, #54073, #11581, #50701 ) ) ;
#42039=VERTEX_POINT ( 'NONE', #13442 ) ;
#42041=CARTESIAN_POINT ( 'NONE',  ( -4.915099999999999802, 0.000000000000000000, -3.000000000000000000 ) ) ;
#42048=ADVANCED_FACE ( 'NONE', ( #23448 ), #24768, .F. ) ;
#42051=CARTESIAN_POINT ( 'NONE',  ( -6.057079549204054558, -11.01026639367740501, 15.79890075416629713 ) ) ;
#42055=EDGE_CURVE ( 'NONE', #28087, #43207, #56707, .T. ) ;
#42056=DIRECTION ( 'NONE',  ( 0.000000000000000000, 0.000000000000000000, 1.000000000000000000 ) ) ;
#42063=CARTESIAN_POINT ( 'NONE',  ( 0.1129192098497447394, -12.08918212651769686, 42.43587472053614817 ) ) ;
#42064=CARTESIAN_POINT ( 'NONE',  ( 0.5997462898726536595, 46.76781179977627545, -14.97743000668059210 ) ) ;
#42067=CARTESIAN_POINT ( 'NONE',  ( 0.3676999524040323597, 34.11874447325018167, -27.96179284115914854 ) ) ;
#42068=CARTESIAN_POINT ( 'NONE',  ( 0.6029442701453591180, 28.16660832611681542, 40.22670009535214319 ) ) ;
#42073=FACE_BOUND ( 'NONE', #56395, .T. ) ;
#42084=CARTESIAN_POINT ( 'NONE',  ( -2.601141883200662974, -11.02917173973125919, -10.05747474294128985 ) ) ;
#42085=CARTESIAN_POINT ( 'NONE',  ( -6.063463321072278589, 5.494009911919311762, -18.45633516078428826 ) ) ;
#42087=CARTESIAN_POINT ( 'NONE',  ( 0.5997462898726536595, 17.44942740672471260, -45.90282249842328355 ) ) ;
#42089=CARTESIAN_POINT ( 'NONE',  ( 0.1365634738349401633, -31.24960441609707829, -31.15003761571876950 ) ) ;
#42095=ORIENTED_EDGE ( 'NONE', *, *, #22912, .F. ) ;
#42098=CARTESIAN_POINT ( 'NONE',  ( -2.739355103387248747, 9.839932234830028435, -11.22601000199848365 ) ) ;
#42103=CARTESIAN_POINT ( 'NONE',  ( 0.7044674535453004927, -39.85538961151615212, -28.69408722585818339 ) ) ;
#42105=VECTOR ( 'NONE', #58619, 1000.000000000000000 ) ;
#42106=ORIENTED_EDGE ( 'NONE', *, *, #685, .T. ) ;
#42120=CARTESIAN_POINT ( 'NONE',  ( 4.553261556744875094, 22.57774691820428714, 37.68003330573307608 ) ) ;
#42127=ORIENTED_EDGE ( 'NONE', *, *, #43872, .F. ) ;
#42130=CARTESIAN_POINT ( 'NONE',  ( 2.185380717157382691, 34.44259825520901330, 27.43222973980556390 ) ) ;
#42133=CARTESIAN_POINT ( 'NONE',  ( -6.078457390727109555, 12.00250936636376231, 15.05769836156436092 ) ) ;
#42134=CARTESIAN_POINT ( 'NONE',  ( 1.834102595619085507, -43.83354038710950817, -4.338027430679048280 ) ) ;
#42143=CARTESIAN_POINT ( 'NONE',  ( 0.2279481005628774537, 15.94756160462533501, -41.13610051936851164 ) ) ;
#42147=CARTESIAN_POINT ( 'NONE',  ( 0.1365634738349410515, 19.84198381844869274, 39.41012938029597024 ) ) ;
#42151=CARTESIAN_POINT ( 'NONE',  ( 0.1156867017252034557, -17.74639720403204990, -40.39812116363717820 ) ) ;
#42152=CARTESIAN_POINT ( 'NONE',  ( 0.6021447746440204973, -42.65942225007028554, 24.32518925679092092 ) ) ;
#42156=CARTESIAN_POINT ( 'NONE',  ( -6.079354080745853928, -8.905595498587096870, -17.07288271100423316 ) ) ;
#42161=B_SPLINE_CURVE_WITH_KNOTS ( 'NONE', 3,
 ( #41880, #32778, #47184, #4230, #50930, #37805, #12434, #31527, #7704, #37176, #3306, #22439, #41564, #146, #57157, #47486, #4534, #19293, #48401 ),
 .UNSPECIFIED., .F., .F.,
 ( 4, 3, 3, 3, 3, 3, 4 ),
 ( 1.355252715606880543E-20, 0.0002612768053151737690, 0.0003919133833142954791, 0.0005225499612322595609, 0.0006531865391693357416, 0.0008112755173415181226, 0.0009693688056799743078 ),
 .UNSPECIFIED. ) ;
#42164=CARTESIAN_POINT ( 'NONE',  ( 0.1149546198390367924, -35.19724927890863597, -26.61015235246850352 ) ) ;
#42170=CARTESIAN_POINT ( 'NONE',  ( -6.078726893082806448, 16.77980020642716141, -9.446287434813061878 ) ) ;
#42172=ORIENTED_EDGE ( 'NONE', *, *, #60209, .T. ) ;
#42175=CARTESIAN_POINT ( 'NONE',  ( -6.078075953587585900, 3.078503442539607615, -19.00836633699508482 ) ) ;
#42178=CARTESIAN_POINT ( 'NONE',  ( 0.6026112563231247332, 11.09715715893446841, -47.83716231021774234 ) ) ;
#42179=CARTESIAN_POINT ( 'NONE',  ( 0.6000166863083090663, -8.353387137038088994, -48.39467331274403961 ) ) ;
#42186=ADVANCED_FACE ( 'NONE', ( #25001 ), #46038, .F. ) ;
#42189=EDGE_CURVE ( 'NONE', #48274, #8195, #27549, .T. ) ;
#42193=AXIS2_PLACEMENT_3D ( 'NONE', #28805, #29113, #47301 ) ;
#42194=CARTESIAN_POINT ( 'NONE',  ( 0.7242003506640006805, -24.75021972573795992, 42.40799803873931495 ) ) ;
#42199=CARTESIAN_POINT ( 'NONE',  ( 0.6039202388192952409, -7.665580222076482819, -48.50569649750325851 ) ) ;
#42201=CARTESIAN_POINT ( 'NONE',  ( 0.3676999524040323597, -34.85286720109652947, -27.04123205746306979 ) ) ;
#42204=ORIENTED_EDGE ( 'NONE', *, *, #38809, .T. ) ;
#42206=CARTESIAN_POINT ( 'NONE',  ( 0.1129192098497455998, -44.12161472487017733, -0.4846667466135657909 ) ) ;
#42207=DIRECTION ( 'NONE',  ( 0.000000000000000000, 0.000000000000000000, 1.000000000000000000 ) ) ;
#42208=CARTESIAN_POINT ( 'NONE',  ( 0.6000166863083106206, 17.45040302316584757, 45.90541270958728148 ) ) ;
#42213=CARTESIAN_POINT ( 'NONE',  ( 2.706805983486679779, 43.48315593847570426, 6.781685848663358662 ) ) ;
#42215=CARTESIAN_POINT ( 'NONE',  ( 0.5987334308729320709, 33.46066835468740663, 35.94365840906223752 ) ) ;
#42218=CARTESIAN_POINT ( 'NONE',  ( 0.1135584504625007374, -27.84745193548719655, 34.22676544513054608 ) ) ;
#42221=CARTESIAN_POINT ( 'NONE',  ( 0.2285344041767061740, 24.61438786917755905, -36.61465662984072367 ) ) ;
#42227=FACE_OUTER_BOUND ( 'NONE', #61398, .T. ) ;
#42233=CARTESIAN_POINT ( 'NONE',  ( 0.8744876279028263033, -26.20733431478184983, 41.51536677536103070 ) ) ;
#42250=CARTESIAN_POINT ( 'NONE',  ( 3.894904216938898323, 31.98519698887119489, -30.15081269318135782 ) ) ;
#42253=B_SPLINE_CURVE_WITH_KNOTS ( 'NONE', 3,
 ( #31481, #50577, #26784, #60275, #22391, #13019, #47440, #52121, #23940, #32732, #5109, #43064, #42152, #19252, #42450, #8913 ),
 .UNSPECIFIED., .F., .F.,
 ( 4, 3, 3, 3, 3, 4 ),
 ( 1.868480190406682863E-17, 0.0002612764279487752770, 0.0003919131003184815219, 0.0005225497727000692674, 0.0007837925190632515342, 0.001045051706266716084 ),
 .UNSPECIFIED. ) ;
#42257=CARTESIAN_POINT ( 'NONE',  ( 1.834102595619085507, 28.63582846592697351, -33.46919588110372956 ) ) ;
#42260=EDGE_CURVE ( 'NONE', #21937, #26819, #55325, .T. ) ;
#42264=CARTESIAN_POINT ( 'NONE',  ( 3.050102900204245682, -25.99102862069139519, 35.49495288652262559 ) ) ;
#42265=EDGE_LOOP ( 'NONE', ( #59023, #18431, #20129, #402 ) ) ;
#42269=CARTESIAN_POINT ( 'NONE',  ( 0.8753041380234524160, 3.828530797421371812, -48.95386276695819561 ) ) ;
#42277=CARTESIAN_POINT ( 'NONE',  ( 0.8753041380234471980, -45.84117188851855929, 17.59901382919725066 ) ) ;
#42278=B_SPLINE_CURVE_WITH_KNOTS ( 'NONE', 3,
 ( #27895, #8781, #23813, #27582, #8162, #57001 ),
 .UNSPECIFIED., .F., .F.,
 ( 4, 2, 4 ),
 ( 1.843143693225357538E-18, 0.0002447193893791693828, 0.0004894387787583369225 ),
 .UNSPECIFIED. ) ;
#42288=CARTESIAN_POINT ( 'NONE',  ( 4.553261556744875094, 1.182159483579356074, 43.91061448874314976 ) ) ;
#42299=ORIENTED_EDGE ( 'NONE', *, *, #21660, .T. ) ;
#42302=CARTESIAN_POINT ( 'NONE',  ( 3.894904216938897878, -39.34215491042563428, -19.60406028046930516 ) ) ;
#42303=CARTESIAN_POINT ( 'NONE',  ( 2.185380717157383135, -41.33206684581055157, -15.18156952757675349 ) ) ;
#42306=LINE ( 'NONE', #24099, #52823 ) ;
#42308=CARTESIAN_POINT ( 'NONE',  ( 0.6000166863083106206, 48.97316450298206547, 3.667784109283283911 ) ) ;
#42311=CARTESIAN_POINT ( 'NONE',  ( -6.079354080745853928, 3.072100940895990284, -19.00934378291655236 ) ) ;
#42315=CARTESIAN_POINT ( 'NONE',  ( 0.6029443449137434907, -49.10740925637109200, -0.04352138108543880668 ) ) ;
#42319=( BOUNDED_SURFACE ( )  B_SPLINE_SURFACE ( 3, 1, ( 
 ( #14152, #25005 ),
 ( #44144, #42650 ),
 ( #29686, #22925 ),
 ( #58181, #18526 ) ),
 .UNSPECIFIED., .F., .F., .F. ) 
 B_SPLINE_SURFACE_WITH_KNOTS ( ( 4, 4 ),
 ( 2, 2 ),
 ( 0.000000000000000000, 1.000000000000000000 ),
 ( 0.000000000000000000, 1.000000000000000000 ),
 .UNSPECIFIED. ) 
 GEOMETRIC_REPRESENTATION_ITEM ( )  RATIONAL_B_SPLINE_SURFACE ( (
 ( 1.000000000000000000, 1.000000000000000000),
 ( 0.7211978278499968642, 0.9934217856018975334),
 ( 0.7211978278499968642, 0.9934217856018975334),
 ( 1.000000000000000000, 1.000000000000000000) ) ) 
 REPRESENTATION_ITEM ( '' )  SURFACE ( )  );
#42321=CARTESIAN_POINT ( 'NONE',  ( 4.553261556744873317, -41.75933753256789771, -13.62707946203816967 ) ) ;
#42330=CARTESIAN_POINT ( 'NONE',  ( 0.6027444965799114707, 44.30076917591773622, -21.18915680978122751 ) ) ;
#42335=CARTESIAN_POINT ( 'NONE',  ( 4.975610109902397937, 35.53430708602537891, 33.61193875773635398 ) ) ;
#42337=ORIENTED_EDGE ( 'NONE', *, *, #50283, .T. ) ;
#42341=CARTESIAN_POINT ( 'NONE',  ( 4.553261556744873317, 22.96401893593727550, 37.44587293859699173 ) ) ;
#42346=ORIENTED_EDGE ( 'NONE', *, *, #13686, .F. ) ;
#42348=DIRECTION ( 'NONE',  ( 0.1011922191286468153, 0.8267003359790527917, -0.5534678755627476798 ) ) ;
#42350=VERTEX_POINT ( 'NONE', #42506 ) ;
#42352=CARTESIAN_POINT ( 'NONE',  ( -6.078726893082806448, -14.66019907464893635, -12.48489504803234418 ) ) ;
#42354=CARTESIAN_POINT ( 'NONE',  ( 0.5987334308729319599, 27.59677667583599714, -40.61995597823517556 ) ) ;
#42363=CARTESIAN_POINT ( 'NONE',  ( 0.6024113833632039894, 46.67385196666943159, -15.26739701764171997 ) ) ;
#42366=CARTESIAN_POINT ( 'NONE',  ( 0.8753041380234524160, -19.05925361776951021, 45.25354328012912219 ) ) ;
#42368=FACE_OUTER_BOUND ( 'NONE', #42720, .T. ) ;
#42369=ORIENTED_EDGE ( 'NONE', *, *, #46693, .T. ) ;
#42370=CARTESIAN_POINT ( 'NONE',  ( 0.1152339509894530906, -40.81507403732233286, 16.76521463576112225 ) ) ;
#42372=EDGE_CURVE ( 'NONE', #30901, #49479, #6646, .T. ) ;
#42376=( BOUNDED_SURFACE ( )  B_SPLINE_SURFACE ( 3, 1, ( 
 ( #56758, #57667 ),
 ( #52989, #43628 ),
 ( #19199, #9157 ),
 ( #5052, #671 ) ),
 .UNSPECIFIED., .F., .F., .F. ) 
 B_SPLINE_SURFACE_WITH_KNOTS ( ( 4, 4 ),
 ( 2, 2 ),
 ( 0.000000000000000000, 1.000000000000000000 ),
 ( 0.000000000000000000, 1.000000000000000000 ),
 .UNSPECIFIED. ) 
 GEOMETRIC_REPRESENTATION_ITEM ( )  RATIONAL_B_SPLINE_SURFACE ( (
 ( 1.000000000000000000, 1.000000000000000000),
 ( 0.9754377213608244057, 0.9999580625633939235),
 ( 0.9754377213608244057, 0.9999580625633939235),
 ( 1.000000000000000000, 1.000000000000000000) ) ) 
 REPRESENTATION_ITEM ( '' )  SURFACE ( )  );
#42381=LINE ( 'NONE', #52053, #55843 ) ;
#42384=CARTESIAN_POINT ( 'NONE',  ( 2.648799415243708655, -12.61806922346209348, 47.38461556625227189 ) ) ;
#42392=CARTESIAN_POINT ( 'NONE',  ( 0.7948878604505672518, -39.86121510370232102, -28.66674341034903861 ) ) ;
#42399=VERTEX_POINT ( 'NONE', #37495 ) ;
#42401=CARTESIAN_POINT ( 'NONE',  ( 0.5549461598389366923, -31.06561436148498956, 31.30727231507564312 ) ) ;
#42413=ORIENTED_EDGE ( 'NONE', *, *, #28577, .T. ) ;
#42414=CARTESIAN_POINT ( 'NONE',  ( 4.553261556744875094, 0.000000000000000000, 0.000000000000000000 ) ) ;
#42422=ORIENTED_EDGE ( 'NONE', *, *, #35797, .T. ) ;
#42426=FACE_OUTER_BOUND ( 'NONE', #11198, .T. ) ;
#42428=CARTESIAN_POINT ( 'NONE',  ( 0.7948878604505656975, 16.14027002511539877, -46.37014482201644938 ) ) ;
#42436=CARTESIAN_POINT ( 'NONE',  ( 0.7242003506639983490, 41.59292590893083030, 26.09674670261058438 ) ) ;
#42437=CARTESIAN_POINT ( 'NONE',  ( 0.8753041380234524160, -29.91468680897855492, 38.93905290314216927 ) ) ;
#42438=CARTESIAN_POINT ( 'NONE',  ( 2.879087469061463178, -5.307820464692313500, 43.67984339140849670 ) ) ;
#42441=CARTESIAN_POINT ( 'NONE',  ( 2.299746137290199055, -47.08665685429843251, 13.67947674334394392 ) ) ;
#42443=EDGE_CURVE ( 'NONE', #17526, #10258, #29101, .T. ) ;
#42444=CARTESIAN_POINT ( 'NONE',  ( -2.601141883200662974, 1.878577531911864718, 14.80764579283231619 ) ) ;
#42446=CIRCLE ( 'NONE', #7380, 43.92652462719577500 ) ;
#42448=ADVANCED_FACE ( 'NONE', ( #796 ), #43749, .F. ) ;
#42450=CARTESIAN_POINT ( 'NONE',  ( 0.6008122571543325074, -42.57299878231319212, 24.47640343568631494 ) ) ;
#42454=CARTESIAN_POINT ( 'NONE',  ( -6.063463321072276813, -4.300220425534933888, -18.77041706439369761 ) ) ;
#42463=CARTESIAN_POINT ( 'NONE',  ( 3.678748215320119197, 9.087549784784737739, -48.12514159156878435 ) ) ;
#42465=CARTESIAN_POINT ( 'NONE',  ( 0.5549461598389364703, -23.60958411260055456, -37.25325802526328545 ) ) ;
#42479=CARTESIAN_POINT ( 'NONE',  ( 0.6027444965799114707, 11.05472791484353579, -47.84695922016592107 ) ) ;
#42482=EDGE_LOOP ( 'NONE', ( #11272, #23662, #9177, #8190, #9887, #34380, #27578, #45764, #1019, #22216, #22198, #33221, #22045, #51236, #61181, #15137, #24617, #50950, #25056, #44794, #50873, #61614, #9025, #55664, #16446, #40329, #24710, #38410, #29685, #46115, #27684, #15351, #837, #45748, #33611, #16467, #26238, #23442, #59894, #20022, #43072, #54170, #16118, #31447, #60345, #41802, #7735, #20769, #58687, #23163, #7777, #16861, #15547, #44654, #42790, #50711, #21438, #58296, #4174, #53380, #58778, #32560, #44517, #26996, #13413, #324, #25880, #38776, #16674, #51956, #29123, #35545, #39814, #13272, #59019, #20506, #52941, #18281, #31057, #60439, #50795, #34802, #61283, #8798, #5156, #18854, #59406, #53688, #48065, #19171, #23984, #22544, #5985, #13426, #7072, #58402, #11344, #36965, #38265, #2544, #57240, #53757, #43713, #59331, #57755, #43833, #36022, #14620, #4372, #44816, #28045, #44195, #42670, #11111, #5395, #43335, #24838, #46551, #607, #24927, #2233, #39185, #52908, #46911, #25809, #59381, #11041, #14623, #59343, #20753, #30089, #61177, #15586, #46898, #21106, #61388, #40223, #21044, #55100, #24583, #37112, #51213, #31872, #24110, #57722, #49108, #42578, #31826, #31118, #53549, #12386, #11215 ) ) ;
#42486=CARTESIAN_POINT ( 'NONE',  ( 3.390910168358336918, -39.98406868784916668, 18.31314794618874942 ) ) ;
#42492=EDGE_CURVE ( 'NONE', #27686, #30599, #22074, .T. ) ;
#42494=ORIENTED_EDGE ( 'NONE', *, *, #7195, .F. ) ;
#42496=CARTESIAN_POINT ( 'NONE',  ( -6.057079549204054558, -6.642710526269747007, 18.07500008198958952 ) ) ;
#42499=CARTESIAN_POINT ( 'NONE',  ( 0.6000166863083090663, -43.04473087058024561, 23.64264422580035330 ) ) ;
#42500=CARTESIAN_POINT ( 'NONE',  ( 1.479689385636123067, 39.17559155776038438, -20.17069337844452903 ) ) ;
#42504=EDGE_LOOP ( 'NONE', ( #61909, #23400, #35809, #50717 ) ) ;
#42506=CARTESIAN_POINT ( 'NONE',  ( 0.5997462898726536595, -31.02483596213004091, -38.06587952047387091 ) ) ;
#42516=FACE_OUTER_BOUND ( 'NONE', #18073, .T. ) ;
#42522=VECTOR ( 'NONE', #22196, 1000.000000000000227 ) ;
#42533=DIRECTION ( 'NONE',  ( 1.000000000000000000, 0.000000000000000000, 0.000000000000000000 ) ) ;
#42540=CARTESIAN_POINT ( 'NONE',  ( 4.694002226626921015, 13.30107597157399368, -43.60465742835910419 ) ) ;
#42552=CARTESIAN_POINT ( 'NONE',  ( 4.975610109902397937, 0.000000000000000000, 0.000000000000000000 ) ) ;
#42562=ADVANCED_FACE ( 'NONE', ( #45582 ), #52149, .F. ) ;
#42567=B_SPLINE_CURVE_WITH_KNOTS ( 'NONE', 3,
 ( #48357, #33968, #43686, #15162 ),
 .UNSPECIFIED., .F., .F.,
 ( 4, 4 ),
 ( 2.178848519881467304E-17, 0.004559932413162187670 ),
 .UNSPECIFIED. ) ;
#42573=ORIENTED_EDGE ( 'NONE', *, *, #526, .F. ) ;
#42574=CARTESIAN_POINT ( 'NONE',  ( 4.553261556744875094, 0.000000000000000000, 0.000000000000000000 ) ) ;
#42575=VERTEX_POINT ( 'NONE', #36186 ) ;
#42578=ORIENTED_EDGE ( 'NONE', *, *, #51454, .T. ) ;
#42585=ORIENTED_EDGE ( 'NONE', *, *, #196, .F. ) ;
#42591=B_SPLINE_CURVE_WITH_KNOTS ( 'NONE', 3,
 ( #55270, #36828, #46842, #41523 ),
 .UNSPECIFIED., .F., .F.,
 ( 4, 4 ),
 ( 0.000000000000000000, 0.004442905043737213101 ),
 .UNSPECIFIED. ) ;
#42593=ORIENTED_EDGE ( 'NONE', *, *, #44332, .T. ) ;
#42597=CARTESIAN_POINT ( 'NONE',  ( 4.834790513006555379, 46.80118606150062277, -6.499101796493102157 ) ) ;
#42598=CARTESIAN_POINT ( 'NONE',  ( -2.739355103387248747, -7.512526911499135096, 12.89998086645938535 ) ) ;
#42599=ORIENTED_EDGE ( 'NONE', *, *, #15513, .F. ) ;
#42601=ORIENTED_EDGE ( 'NONE', *, *, #38543, .T. ) ;
#42604=CARTESIAN_POINT ( 'NONE',  ( 2.533389852662419894, 42.87438241343366485, -9.961820335674985927 ) ) ;
#42613=CARTESIAN_POINT ( 'NONE',  ( -6.079354080745853928, -8.907665152502962869, 17.07180297388200074 ) ) ;
#42623=CARTESIAN_POINT ( 'NONE',  ( 4.553261556744875094, 22.96401893593780841, -37.44587293859667199 ) ) ;
#42628=CIRCLE ( 'NONE', #15621, 48.91267123290010943 ) ;
#42630=ORIENTED_EDGE ( 'NONE', *, *, #21466, .T. ) ;
#42636=CARTESIAN_POINT ( 'NONE',  ( 0.1119899015040011075, 41.69625326363821927, 14.43550386952412268 ) ) ;
#42637=ORIENTED_EDGE ( 'NONE', *, *, #32284, .F. ) ;
#42641=CARTESIAN_POINT ( 'NONE',  ( -6.077587904424778920, 19.09876248768971152, -2.456276212632990674 ) ) ;
#42650=CARTESIAN_POINT ( 'NONE',  ( 4.335381028904216727, -47.87967504119340134, -10.35826074271485275 ) ) ;
#42652=CARTESIAN_POINT ( 'NONE',  ( 0.1145239942831223490, -22.59375522573645867, -37.90076127868911016 ) ) ;
#42655=CARTESIAN_POINT ( 'NONE',  ( 0.1157506346131639274, -31.76102471912784608, -30.62969096471239894 ) ) ;
#42656=ORIENTED_EDGE ( 'NONE', *, *, #33289, .F. ) ;
#42662=ORIENTED_EDGE ( 'NONE', *, *, #37756, .T. ) ;
#42666=DIRECTION ( 'NONE',  ( -1.000000000000000000, -0.000000000000000000, -0.000000000000000000 ) ) ;
#42670=ORIENTED_EDGE ( 'NONE', *, *, #32612, .T. ) ;
#42682=CARTESIAN_POINT ( 'NONE',  ( 0.8744876279028306332, 46.86690837902563089, 14.62336997314605469 ) ) ;
#42692=CARTESIAN_POINT ( 'NONE',  ( 0.1147471544378675656, 37.14850691661145277, 23.81051495326627077 ) ) ;
#42695=CARTESIAN_POINT ( 'NONE',  ( 0.8753041380234530822, -34.64850320773157932, 34.79395857525835822 ) ) ;
#42696=CARTESIAN_POINT ( 'NONE',  ( 0.8744876279028263033, 5.599149760998344050, -48.77498920895221346 ) ) ;
#42699=CARTESIAN_POINT ( 'NONE',  ( 2.706805983486679779, -30.43958851955885692, 31.78376258531540799 ) ) ;
#42705=AXIS2_PLACEMENT_3D ( 'NONE', #45295, #2647, #30538 ) ;
#42708=AXIS2_PLACEMENT_3D ( 'NONE', #60166, #2217, #31679 ) ;
#42712=ADVANCED_FACE ( 'NONE', ( #55880 ), #31305, .F. ) ;
#42716=CARTESIAN_POINT ( 'NONE',  ( -6.078726893082806448, -12.94330610022648820, 14.25709887966552003 ) ) ;
#42720=EDGE_LOOP ( 'NONE', ( #29391, #47497, #1769, #14164 ) ) ;
#42721=CARTESIAN_POINT ( 'NONE',  ( 0.1129192098497447394, -7.520259262076021578, -43.47870154933693243 ) ) ;
#42730=CARTESIAN_POINT ( 'NONE',  ( 4.694002226626921015, 28.69237940071545268, 35.42643272715351799 ) ) ;
#42742=CARTESIAN_POINT ( 'NONE',  ( 0.1129192098497447394, -41.07894348801345075, -16.10814047907924973 ) ) ;
#42746=CARTESIAN_POINT ( 'NONE',  ( 0.1129192098497455998, 19.97823103613628248, 39.34236993944205807 ) ) ;
#42747=CARTESIAN_POINT ( 'NONE',  ( 4.975610109902397937, 30.94437158899580353, 37.88001153774800400 ) ) ;
#42748=ADVANCED_FACE ( 'NONE', ( #34252 ), #10875, .F. ) ;
#42750=CARTESIAN_POINT ( 'NONE',  ( 4.553261556744873317, 43.59419396814051595, 5.393126930805304475 ) ) ;
#42752=ADVANCED_FACE ( 'NONE', ( #33949 ), #41761, .F. ) ;
#42753=CARTESIAN_POINT ( 'NONE',  ( 4.975610109902397937, 19.27143522741721426, -44.95621415792522413 ) ) ;
#42755=( BOUNDED_SURFACE ( )  B_SPLINE_SURFACE ( 3, 1, ( 
 ( #37164, #17118 ),
 ( #60613, #17418 ),
 ( #51221, #56233 ),
 ( #32447, #23357 ) ),
 .UNSPECIFIED., .F., .F., .F. ) 
 B_SPLINE_SURFACE_WITH_KNOTS ( ( 4, 4 ),
 ( 2, 2 ),
 ( 0.000000000000000000, 1.000000000000000000 ),
 ( 0.000000000000000000, 1.000000000000000000 ),
 .UNSPECIFIED. ) 
 GEOMETRIC_REPRESENTATION_ITEM ( )  RATIONAL_B_SPLINE_SURFACE ( (
 ( 1.000000000000000000, 1.000000000000000000),
 ( 0.7211978278499968642, 0.9934217856018975334),
 ( 0.7211978278499968642, 0.9934217856018975334),
 ( 1.000000000000000000, 1.000000000000000000) ) ) 
 REPRESENTATION_ITEM ( '' )  SURFACE ( )  );
#42760=CARTESIAN_POINT ( 'NONE',  ( 0.1368894036331286812, -22.32560810002344809, 38.05822577167124621 ) ) ;
#42765=CARTESIAN_POINT ( 'NONE',  ( 1.830465331921978134, 19.27193292033265237, 39.61020900465671701 ) ) ;
#42769=CARTESIAN_POINT ( 'NONE',  ( 4.975610109902397937, -27.50982196586548412, -40.44328253918266824 ) ) ;
#42773=B_SPLINE_CURVE_WITH_KNOTS ( 'NONE', 3,
 ( #27580, #31987, #8160, #56381, #46398, #60458 ),
 .UNSPECIFIED., .F., .F.,
 ( 4, 2, 4 ),
 ( 0.000000000000000000, 0.0002447195606305738787, 0.0004894391212611477575 ),
 .UNSPECIFIED. ) ;
#42778=EDGE_LOOP ( 'NONE', ( #52679, #32242, #37878, #50032 ) ) ;
#42785=CARTESIAN_POINT ( 'NONE',  ( 0.6252788684277219566, -47.32158689167658849, 13.11913660372399093 ) ) ;
#42789=ORIENTED_EDGE ( 'NONE', *, *, #18882, .T. ) ;
#42790=ORIENTED_EDGE ( 'NONE', *, *, #36113, .T. ) ;
#42791=B_SPLINE_CURVE_WITH_KNOTS ( 'NONE', 3,
 ( #45172, #6896, #36078, #26644 ),
 .UNSPECIFIED., .F., .F.,
 ( 4, 4 ),
 ( 0.000000000000000000, 0.005013413432710150247 ),
 .UNSPECIFIED. ) ;
#42794=CARTESIAN_POINT ( 'NONE',  ( 2.359973842542475442, -40.21654738650805427, 17.90991934491199444 ) ) ;
#42795=CARTESIAN_POINT ( 'NONE',  ( 4.694002226626921015, 28.15356303305684804, 35.85612444185553471 ) ) ;
#42796=EDGE_CURVE ( 'NONE', #29310, #46130, #566, .T. ) ;
#42797=EDGE_CURVE ( 'NONE', #56636, #15927, #50121, .T. ) ;
#42804=CARTESIAN_POINT ( 'NONE',  ( 4.335381028904201628, 18.89720170524701004, -45.19571456870170323 ) ) ;
#42815=CARTESIAN_POINT ( 'NONE',  ( 0.1152809850208376119, -44.12364846630579507, -0.2211979014933812271 ) ) ;
#42818=EDGE_CURVE ( 'NONE', #14283, #26948, #26764, .T. ) ;
#42823=CARTESIAN_POINT ( 'NONE',  ( 0.6021448801613057400, -25.67997845241691834, 41.85785285117177779 ) ) ;
#42825=VECTOR ( 'NONE', #34, 1000.000000000000227 ) ;
#42828=CARTESIAN_POINT ( 'NONE',  ( 0.6000166863083090663, -49.10753961887881758, 0.5225268306041207511 ) ) ;
#42830=VECTOR ( 'NONE', #53643, 999.9999999999998863 ) ;
#42835=CARTESIAN_POINT ( 'NONE',  ( -6.063463321072276813, 13.82218400051391960, -13.40774708649469105 ) ) ;
#42836=CARTESIAN_POINT ( 'NONE',  ( 0.2279481005628835044, -38.80879475857510386, 20.98525521550088513 ) ) ;
#42839=B_SPLINE_CURVE_WITH_KNOTS ( 'NONE', 3,
 ( #43992, #15454, #39587, #34566, #39902, #30453, #21073, #25771, #15768, #1632, #11068, #35498, #1948, #1025, #34259, #6013, #30150, #48963, #25146, #58029, #44292, #59268, #30770, #49889, #6947 ),
 .UNSPECIFIED., .F., .F.,
 ( 4, 3, 3, 3, 3, 3, 3, 3, 4 ),
 ( 4.670885906470169154E-18, 0.0005656085177311397484, 0.001131215744874499406, 0.001696821861372765266, 0.002262427090022498151, 0.002828031679238745925, 0.003393635864401604862, 0.003977030878808131623, 0.004561030005651158133 ),
 .UNSPECIFIED. ) ;
#42844=CARTESIAN_POINT ( 'NONE',  ( 0.2285344041767131407, -34.89800547056871238, 26.99315440017360146 ) ) ;
#42846=ADVANCED_FACE ( 'NONE', ( #31630 ), #16489, .F. ) ;
#42847=CARTESIAN_POINT ( 'NONE',  ( 4.975610109902397937, 48.90928568712962488, -0.5754830253892166958 ) ) ;
#42853=CARTESIAN_POINT ( 'NONE',  ( 0.7044674535453004927, -29.95677278048795600, 38.91522179545072646 ) ) ;
#42859=CARTESIAN_POINT ( 'NONE',  ( 0.3676999524040366896, -28.14442808720893296, -33.96824621564622504 ) ) ;
#42866=ORIENTED_EDGE ( 'NONE', *, *, #16028, .F. ) ;
#42869=LINE ( 'NONE', #14977, #32840 ) ;
#42870=ORIENTED_EDGE ( 'NONE', *, *, #18323, .T. ) ;
#42873=EDGE_CURVE ( 'NONE', #46397, #8504, #55872, .T. ) ;
#42878=LINE ( 'NONE', #48784, #53934 ) ;
#42907=CARTESIAN_POINT ( 'NONE',  ( 0.1154773475650540532, -38.35764556291236005, 21.80904988568074288 ) ) ;
#42910=ORIENTED_EDGE ( 'NONE', *, *, #39161, .F. ) ;
#42914=CARTESIAN_POINT ( 'NONE',  ( -6.063463321072276813, -17.35644658106379623, -8.341115906049296314 ) ) ;
#42919=CARTESIAN_POINT ( 'NONE',  ( 3.050102900204245682, -39.18813633240142025, -19.99287923164596847 ) ) ;
#42926=CARTESIAN_POINT ( 'NONE',  ( 5.901764892641288895, 48.57275408226675495, 6.219246602548982317 ) ) ;
#42927=FACE_OUTER_BOUND ( 'NONE', #41734, .T. ) ;
#42929=CARTESIAN_POINT ( 'NONE',  ( 0.6039202388192952409, 22.86846745447396501, -43.45799016444105689 ) ) ;
#42934=( BOUNDED_SURFACE ( )  B_SPLINE_SURFACE ( 3, 1, ( 
 ( #25101, #49839 ),
 ( #11635, #44859 ),
 ( #54198, #20111 ),
 ( #20410, #30721 ) ),
 .UNSPECIFIED., .F., .F., .F. ) 
 B_SPLINE_SURFACE_WITH_KNOTS ( ( 4, 4 ),
 ( 2, 2 ),
 ( 0.000000000000000000, 1.000000000000000000 ),
 ( 0.000000000000000000, 1.000000000000000000 ),
 .UNSPECIFIED. ) 
 GEOMETRIC_REPRESENTATION_ITEM ( )  RATIONAL_B_SPLINE_SURFACE ( (
 ( 1.000000000000000000, 1.000000000000000000),
 ( 0.9953485035131437453, 0.8621029689291523912),
 ( 0.9953485035131437453, 0.8621029689291523912),
 ( 1.000000000000000000, 1.000000000000000000) ) ) 
 REPRESENTATION_ITEM ( '' )  SURFACE ( )  );
#42937=ORIENTED_EDGE ( 'NONE', *, *, #24176, .F. ) ;
#42940=CARTESIAN_POINT ( 'NONE',  ( 2.533389852662419894, 23.86852016275539157, -36.98302687684928713 ) ) ;
#42949=CARTESIAN_POINT ( 'NONE',  ( -6.078726893082806448, 19.25601281685051802, 0.003415553934478593023 ) ) ;
#42952=CARTESIAN_POINT ( 'NONE',  ( -6.057079549204054558, -19.21686681020091214, 1.242280603864163835 ) ) ;
#42954=EDGE_CURVE ( 'NONE', #22153, #1157, #37901, .T. ) ;
#42960=ORIENTED_EDGE ( 'NONE', *, *, #14240, .F. ) ;
#42968=ORIENTED_EDGE ( 'NONE', *, *, #21326, .T. ) ;
#42969=CARTESIAN_POINT ( 'NONE',  ( 0.1135584504625007513, 14.83285864174382418, 41.55644783483421634 ) ) ;
#42970=EDGE_CURVE ( 'NONE', #33616, #20911, #25204, .T. ) ;
#42977=B_SPLINE_CURVE_WITH_KNOTS ( 'NONE', 3,
 ( #60137, #21322, #45763, #54817 ),
 .UNSPECIFIED., .F., .F.,
 ( 4, 4 ),
 ( 2.308109569601360422E-17, 0.004559932413162187670 ),
 .UNSPECIFIED. ) ;
#42980=ORIENTED_EDGE ( 'NONE', *, *, #61613, .F. ) ;
#42987=CARTESIAN_POINT ( 'NONE',  ( 0.8753041380234530822, 33.66554281472423327, 35.74590263041275762 ) ) ;
#42994=B_SPLINE_CURVE_WITH_KNOTS ( 'NONE', 3,
 ( #11369, #21074, #30454, #16376, #54878, #39903 ),
 .UNSPECIFIED., .F., .F.,
 ( 4, 2, 4 ),
 ( 3.127317220692750759E-18, 0.0002447193893791696538, 0.0004894387787583361635 ),
 .UNSPECIFIED. ) ;
#42998=DIRECTION ( 'NONE',  ( -1.000000000000000000, -0.000000000000000000, -0.000000000000000000 ) ) ;
#43002=DIRECTION ( 'NONE',  ( 0.09722883295013595717, -0.9196625129306750246, -0.3804831354386032372 ) ) ;
#43005=CARTESIAN_POINT ( 'NONE',  ( 0.1145239942831223490, -43.71898434612356965, -5.966228997287612579 ) ) ;
#43006=CARTESIAN_POINT ( 'NONE',  ( 0.1154773475650540393, 39.83222568495971672, 18.98255586133109318 ) ) ;
#43008=DIRECTION ( 'NONE',  ( 1.000000000000000000, 0.000000000000000000, 0.000000000000000000 ) ) ;
#43012=CARTESIAN_POINT ( 'NONE',  ( 0.2285344041767100598, 21.07743229076804425, 38.75877988693069653 ) ) ;
#43019=B_SPLINE_CURVE_WITH_KNOTS ( 'NONE', 3,
 ( #60197, #40217, #36740, #35496 ),
 .UNSPECIFIED., .F., .F.,
 ( 4, 4 ),
 ( 0.000000000000000000, 0.005013413432710149380 ),
 .UNSPECIFIED. ) ;
#43021=VERTEX_POINT ( 'NONE', #15618 ) ;
#43022=ORIENTED_EDGE ( 'NONE', *, *, #5684, .T. ) ;
#43024=EDGE_CURVE ( 'NONE', #18600, #15275, #58148, .T. ) ;
#43027=CARTESIAN_POINT ( 'NONE',  ( 4.553261556744875094, -20.51767157960516741, 38.84024612145369559 ) ) ;
#43028=CARTESIAN_POINT ( 'NONE',  ( 4.694002226626920127, 44.00857453008735121, -11.89664403417540939 ) ) ;
#43030=EDGE_CURVE ( 'NONE', #5480, #59176, #18561, .T. ) ;
#43031=ORIENTED_EDGE ( 'NONE', *, *, #30338, .T. ) ;
#43034=CARTESIAN_POINT ( 'NONE',  ( 4.694002226626921015, 23.33724324709813658, 39.16194388780908753 ) ) ;
#43051=CARTESIAN_POINT ( 'NONE',  ( -2.739355103387248747, 6.670587007382340339, -13.35480572408145861 ) ) ;
#43052=FACE_OUTER_BOUND ( 'NONE', #53501, .T. ) ;
#43055=LINE ( 'NONE', #395, #23515 ) ;
#43057=ORIENTED_EDGE ( 'NONE', *, *, #53686, .F. ) ;
#43059=CARTESIAN_POINT ( 'NONE',  ( -6.072942160501519915, 17.85441038494885646, 7.212779775845826968 ) ) ;
#43064=CARTESIAN_POINT ( 'NONE',  ( 0.6026777506516368677, -42.70253602701208706, 24.24953210886665644 ) ) ;
#43067=EDGE_CURVE ( 'NONE', #47719, #36320, #8013, .T. ) ;
#43070=CARTESIAN_POINT ( 'NONE',  ( 2.648799415243696664, 9.556201303926476598, 48.09570126246661204 ) ) ;
#43071=DIRECTION ( 'NONE',  ( 0.09722883295013594329, -0.9196625129306804647, 0.3804831354385900810 ) ) ;
#43072=ORIENTED_EDGE ( 'NONE', *, *, #15280, .T. ) ;
#43077=B_SPLINE_CURVE_WITH_KNOTS ( 'NONE', 3,
 ( #59150, #2758, #45099, #54129 ),
 .UNSPECIFIED., .F., .F.,
 ( 4, 4 ),
 ( 0.000000000000000000, 0.004444103432399269631 ),
 .UNSPECIFIED. ) ;
#43085=EDGE_CURVE ( 'NONE', #43207, #54066, #2782, .T. ) ;
#43086=CARTESIAN_POINT ( 'NONE',  ( 0.6000166863083090663, -8.353387137038760457, 48.39467331274393302 ) ) ;
#43095=CARTESIAN_POINT ( 'NONE',  ( 0.3676999524040366896, 29.04098611012985742, -33.20499524279568249 ) ) ;
#43103=CARTESIAN_POINT ( 'NONE',  ( 0.1129192098497455998, 14.78321943369591196, 41.57412910645692961 ) ) ;
#43109=( BOUNDED_SURFACE ( )  B_SPLINE_SURFACE ( 3, 1, ( 
 ( #55905, #50897 ),
 ( #21473, #46228 ),
 ( #60593, #36837 ),
 ( #2975, #49983 ) ),
 .UNSPECIFIED., .F., .F., .F. ) 
 B_SPLINE_SURFACE_WITH_KNOTS ( ( 4, 4 ),
 ( 2, 2 ),
 ( 0.000000000000000000, 1.000000000000000000 ),
 ( 0.000000000000000000, 1.000000000000000000 ),
 .UNSPECIFIED. ) 
 GEOMETRIC_REPRESENTATION_ITEM ( )  RATIONAL_B_SPLINE_SURFACE ( (
 ( 1.000000000000000000, 1.000000000000000000),
 ( 0.7211978278499968642, 0.9934217856018975334),
 ( 0.7211978278499968642, 0.9934217856018975334),
 ( 1.000000000000000000, 1.000000000000000000) ) ) 
 REPRESENTATION_ITEM ( '' )  SURFACE ( )  );
#43113=CARTESIAN_POINT ( 'NONE',  ( 2.009741617377216460, 44.01584547398758218, 1.452385910524921497 ) ) ;
#43117=CARTESIAN_POINT ( 'NONE',  ( 0.8744876279028263033, -39.87136468799916145, 28.64654129726773846 ) ) ;
#43118=CARTESIAN_POINT ( 'NONE',  ( 0.1129192098497447394, -41.07894348801345075, -16.10814047907924973 ) ) ;
#43128=ORIENTED_EDGE ( 'NONE', *, *, #55388, .T. ) ;
#43132=LINE ( 'NONE', #47823, #8390 ) ;
#43147=CARTESIAN_POINT ( 'NONE',  ( 0.5549461598389363592, -17.04665221628824057, 40.67713539181095683 ) ) ;
#43152=CARTESIAN_POINT ( 'NONE',  ( 0.1129192098497447394, -35.06977877439262414, 26.77802092202325213 ) ) ;
#43153=CARTESIAN_POINT ( 'NONE',  ( 4.553261556744873317, 27.21079963941887314, -34.48350256002191117 ) ) ;
#43155=CARTESIAN_POINT ( 'NONE',  ( 0.6039202388192953519, 11.09723268158243492, 47.83738224087738189 ) ) ;
#43160=CARTESIAN_POINT ( 'NONE',  ( 0.5980271706414734822, -30.07077130958565192, 38.83037413788673575 ) ) ;
#43165=VERTEX_POINT ( 'NONE', #8656 ) ;
#43173=ORIENTED_EDGE ( 'NONE', *, *, #40858, .F. ) ;
#43174=CARTESIAN_POINT ( 'NONE',  ( 0.08486401232817714080, 5.403818426594913263E-15, -44.12552607296456131 ) ) ;
#43176=CARTESIAN_POINT ( 'NONE',  ( 4.834790513006553603, 29.81904690970663196, -36.65260948856298029 ) ) ;
#43179=VERTEX_POINT ( 'NONE', #28700 ) ;
#43180=CARTESIAN_POINT ( 'NONE',  ( 0.3676999524040323597, -35.84016207189440451, 25.71834687500696859 ) ) ;
#43182=CARTESIAN_POINT ( 'NONE',  ( 4.975610109902397937, -27.50982196586606321, 40.44328253918227034 ) ) ;
#43185=VERTEX_POINT ( 'NONE', #30233 ) ;
#43195=ORIENTED_EDGE ( 'NONE', *, *, #59946, .F. ) ;
#43196=CARTESIAN_POINT ( 'NONE',  ( 0.6024113833632038784, -7.622554341288246604, -48.51225138472728560 ) ) ;
#43206=CARTESIAN_POINT ( 'NONE',  ( 0.3676999524040323597, -43.63756228305270213, -6.458617600968101335 ) ) ;
#43207=VERTEX_POINT ( 'NONE', #11149 ) ;
#43217=CARTESIAN_POINT ( 'NONE',  ( -6.077587904424778920, -12.95044751835546393, 14.25068175450744157 ) ) ;
#43233=CARTESIAN_POINT ( 'NONE',  ( 4.553261556744875094, 43.59419396814060832, -5.393126930804686303 ) ) ;
#43236=EDGE_CURVE ( 'NONE', #45831, #15748, #58415, .T. ) ;
#43241=B_SPLINE_CURVE_WITH_KNOTS ( 'NONE', 3,
 ( #3552, #28001, #22686, #37737, #60882, #8893 ),
 .UNSPECIFIED., .F., .F.,
 ( 4, 2, 4 ),
 ( 2.335442953235084577E-18, 0.0002447193893791693828, 0.0004894387787583364888 ),
 .UNSPECIFIED. ) ;
#43246=CARTESIAN_POINT ( 'NONE',  ( 0.3676999524040366896, 39.37931578713023839, -19.88014264185028068 ) ) ;
#43250=CARTESIAN_POINT ( 'NONE',  ( 0.1365634738349418564, 4.870270422476211891, -43.85365532809326083 ) ) ;
#43257=VECTOR ( 'NONE', #54765, 1000.000000000000227 ) ;
#43269=CARTESIAN_POINT ( 'NONE',  ( -6.078457390727109555, 19.09849343800969734, -2.458060096053082511 ) ) ;
#43280=CARTESIAN_POINT ( 'NONE',  ( 0.1139756605157203201, -23.21278114026133466, -37.52495185112634601 ) ) ;
#43283=CARTESIAN_POINT ( 'NONE',  ( 0.1155031312995260795, -18.01467581873768609, 40.27918926291336987 ) ) ;
#43284=ORIENTED_EDGE ( 'NONE', *, *, #16481, .T. ) ;
#43286=VERTEX_POINT ( 'NONE', #48731 ) ;
#43289=VERTEX_POINT ( 'NONE', #44377 ) ;
#43291=CARTESIAN_POINT ( 'NONE',  ( -6.078726893082806448, -19.21666810860935470, 1.230328440814298041 ) ) ;
#43292=CARTESIAN_POINT ( 'NONE',  ( 0.1119898979215348395, -0.8531639444010161721, 44.11613559159281550 ) ) ;
#43299=EDGE_CURVE ( 'NONE', #18471, #46940, #52047, .T. ) ;
#43301=CARTESIAN_POINT ( 'NONE',  ( -6.078726893082806448, 15.42998809551227879, 11.51996131248145439 ) ) ;
#43308=ADVANCED_FACE ( 'NONE', ( #27089 ), #1275, .F. ) ;
#43314=CARTESIAN_POINT ( 'NONE',  ( 4.975610109902397937, 0.000000000000000000, 0.000000000000000000 ) ) ;
#43323=CARTESIAN_POINT ( 'NONE',  ( 4.060580049360325461, 18.24836065817153496, -39.98080824156142654 ) ) ;
#43324=ORIENTED_EDGE ( 'NONE', *, *, #12925, .F. ) ;
#43327=CARTESIAN_POINT ( 'NONE',  ( 1.112077966505211846, 26.07276307627627432, 35.54210672845545815 ) ) ;
#43335=ORIENTED_EDGE ( 'NONE', *, *, #19809, .T. ) ;
#43342=CARTESIAN_POINT ( 'NONE',  ( 0.1119898979215352836, 9.270610865333816619, -43.13950721131830335 ) ) ;
#43346=ORIENTED_EDGE ( 'NONE', *, *, #35934, .T. ) ;
#43349=ORIENTED_EDGE ( 'NONE', *, *, #44998, .F. ) ;
#43350=CARTESIAN_POINT ( 'NONE',  ( 0.7413678028165007206, 34.17436483739517428, 27.86752374594578185 ) ) ;
#43354=AXIS2_PLACEMENT_3D ( 'NONE', #21721, #22039, #25801 ) ;
#43362=CARTESIAN_POINT ( 'NONE',  ( 0.1152339509894530906, 36.85759422494557214, -24.25820352797176938 ) ) ;
#43363=CARTESIAN_POINT ( 'NONE',  ( -6.077587904424778920, 9.987489566522819828, -16.46347695818013435 ) ) ;
#43364=CARTESIAN_POINT ( 'NONE',  ( 2.009741617377216460, -5.672209269575592572, 43.67299073369244411 ) ) ;
#43365=ORIENTED_EDGE ( 'NONE', *, *, #8917, .T. ) ;
#43366=VERTEX_POINT ( 'NONE', #11770 ) ;
#43368=CARTESIAN_POINT ( 'NONE',  ( 0.1129192098497455998, 37.24220309526837980, -23.66368729500826618 ) ) ;
#43370=CARTESIAN_POINT ( 'NONE',  ( 3.240649175237395596, 42.79365579596336744, 10.19646708493989706 ) ) ;
#43374=CARTESIAN_POINT ( 'NONE',  ( 4.975610109902397937, -47.89734868211986907, 9.914302615978730415 ) ) ;
#43377=B_SPLINE_CURVE_WITH_KNOTS ( 'NONE', 3,
 ( #31418, #54576, #50516, #46156, #59290, #30788 ),
 .UNSPECIFIED., .F., .F.,
 ( 4, 2, 4 ),
 ( 0.000000000000000000, 0.0002447195606305742582, 0.0004894391212611485164 ),
 .UNSPECIFIED. ) ;
#43378=EDGE_CURVE ( 'NONE', #2222, #6486, #25868, .T. ) ;
#43386=CARTESIAN_POINT ( 'NONE',  ( 0.1129192098497447394, -35.06977877439262414, 26.77802092202325213 ) ) ;
#43389=VECTOR ( 'NONE', #41083, 999.9999999999998863 ) ;
#43397=( BOUNDED_SURFACE ( )  B_SPLINE_SURFACE ( 3, 1, ( 
 ( #10861, #33749 ),
 ( #52831, #30556 ),
 ( #20866, #27105 ),
 ( #40310, #31814 ) ),
 .UNSPECIFIED., .F., .F., .F. ) 
 B_SPLINE_SURFACE_WITH_KNOTS ( ( 4, 4 ),
 ( 2, 2 ),
 ( 0.000000000000000000, 1.000000000000000000 ),
 ( 0.000000000000000000, 1.000000000000000000 ),
 .UNSPECIFIED. ) 
 GEOMETRIC_REPRESENTATION_ITEM ( )  RATIONAL_B_SPLINE_SURFACE ( (
 ( 1.000000000000000000, 1.000000000000000000),
 ( 0.7211978278499970862, 0.9934217856018976445),
 ( 0.7211978278499970862, 0.9934217856018976445),
 ( 1.000000000000000000, 1.000000000000000000) ) ) 
 REPRESENTATION_ITEM ( '' )  SURFACE ( )  );
#43399=ORIENTED_EDGE ( 'NONE', *, *, #49877, .T. ) ;
#43412=CARTESIAN_POINT ( 'NONE',  ( 4.694002226626920127, 44.18338616738611080, 11.23001149731239678 ) ) ;
#43416=CARTESIAN_POINT ( 'NONE',  ( 0.1129192098497455998, 19.97823103613628248, 39.34236993944205807 ) ) ;
#43419=EDGE_CURVE ( 'NONE', #473, #10036, #29639, .T. ) ;
#43424=CARTESIAN_POINT ( 'NONE',  ( 2.879087469061463178, 43.98767675069456118, 1.089022892222180072 ) ) ;
#43426=ORIENTED_EDGE ( 'NONE', *, *, #3872, .T. ) ;
#43427=CARTESIAN_POINT ( 'NONE',  ( 0.1157991065609915715, 41.90187902746315984, -13.82660115522040378 ) ) ;
#43430=LINE ( 'NONE', #19931, #11362 ) ;
#43439=CARTESIAN_POINT ( 'NONE',  ( 0.6008123274975391004, 5.148685779782010030, -48.83692850599358337 ) ) ;
#43443=ORIENTED_EDGE ( 'NONE', *, *, #15635, .F. ) ;
#43447=VECTOR ( 'NONE', #28696, 1000.000000000000114 ) ;
#43459=EDGE_CURVE ( 'NONE', #39250, #8721, #55038, .T. ) ;
#43461=CARTESIAN_POINT ( 'NONE',  ( 4.553261556744875094, 0.000000000000000000, 0.000000000000000000 ) ) ;
#43465=CARTESIAN_POINT ( 'NONE',  ( 0.6021448801613057400, -20.11648276748766762, 44.79808321448942365 ) ) ;
#43472=DIRECTION ( 'NONE',  ( 0.000000000000000000, 0.000000000000000000, 1.000000000000000000 ) ) ;
#43475=CARTESIAN_POINT ( 'NONE',  ( 0.8753041380234465318, -47.71532843791173661, 11.59248721953970573 ) ) ;
#43478=ADVANCED_FACE ( 'NONE', ( #28015 ), #7684, .F. ) ;
#43481=CARTESIAN_POINT ( 'NONE',  ( 0.1158816050234198619, 9.813012560525406158, -43.01914487518472185 ) ) ;
#43483=ORIENTED_EDGE ( 'NONE', *, *, #59237, .F. ) ;
#43498=CARTESIAN_POINT ( 'NONE',  ( 4.335381028904201628, 2.583895202257807888, 48.91912032373532071 ) ) ;
#43499=ORIENTED_EDGE ( 'NONE', *, *, #26243, .T. ) ;
#43501=CARTESIAN_POINT ( 'NONE',  ( 4.553261556744873317, 1.633632119646958980, 43.89613664004264848 ) ) ;
#43507=CARTESIAN_POINT ( 'NONE',  ( 5.901764892641288895, -27.98073834948296934, 40.18793038783474714 ) ) ;
#43508=EDGE_LOOP ( 'NONE', ( #30376, #58737, #27229, #19823 ) ) ;
#43515=CARTESIAN_POINT ( 'NONE',  ( 3.678834586032787346, 40.00782562460102554, 28.24865055927222102 ) ) ;
#43520=CARTESIAN_POINT ( 'NONE',  ( 0.1365634738349439103, -28.00541523581697589, 34.09632439270718152 ) ) ;
#43522=B_SPLINE_CURVE_WITH_KNOTS ( 'NONE', 3,
 ( #30483, #1660, #48993, #40547, #30797, #16406, #49597, #53662, #59301, #1061, #29881, #49919, #59611, #26108, #16719, #35839 ),
 .UNSPECIFIED., .F., .F.,
 ( 4, 3, 3, 3, 3, 4 ),
 ( 2.194378057379452627E-17, 0.0002612764279487758733, 0.0003919131003184795161, 0.0005225497727000660148, 0.0007837925190632443785, 0.001045051706266715867 ),
 .UNSPECIFIED. ) ;
#43523=ORIENTED_EDGE ( 'NONE', *, *, #17343, .T. ) ;
#43525=DIRECTION ( 'NONE',  ( 1.000000000000000000, 0.000000000000000000, 0.000000000000000000 ) ) ;
#43526=CARTESIAN_POINT ( 'NONE',  ( -6.078726893082806448, -12.94836301907752585, 14.25250631976375004 ) ) ;
#43533=CIRCLE ( 'NONE', #56502, 48.91267123290010943 ) ;
#43535=VECTOR ( 'NONE', #47568, 1000.000000000000000 ) ;
#43536=CARTESIAN_POINT ( 'NONE',  ( 0.3676999524040323597, -32.25712563511804376, 30.09033780274075198 ) ) ;
#43537=CARTESIAN_POINT ( 'NONE',  ( 2.359973842542475886, 11.26178937822771253, 42.55946421928896228 ) ) ;
#43538=ADVANCED_FACE ( 'NONE', ( #28317 ), #8887, .F. ) ;
#43542=CARTESIAN_POINT ( 'NONE',  ( -6.057079549204054558, 9.989941839882863661, 16.46305843807571989 ) ) ;
#43545=CARTESIAN_POINT ( 'NONE',  ( -2.601141883200665639, -8.951945844433334187, -11.94395634066540701 ) ) ;
#43553=CARTESIAN_POINT ( 'NONE',  ( 0.5997462898726536595, 49.03735788587803768, -2.624721264558313560 ) ) ;
#43555=CARTESIAN_POINT ( 'NONE',  ( 3.727782113643637096, 40.49037343455033522, 17.12622068749071857 ) ) ;
#43557=ORIENTED_EDGE ( 'NONE', *, *, #57053, .T. ) ;
#43562=CARTESIAN_POINT ( 'NONE',  ( 4.335381028904216727, 18.89720170524636700, 45.19571456870197323 ) ) ;
#43568=CARTESIAN_POINT ( 'NONE',  ( 0.3676999524040323597, 41.59822836379060362, 14.68121181363330408 ) ) ;
#43573=CARTESIAN_POINT ( 'NONE',  ( 0.8744876279028263033, 48.92939099258497038, 4.032957658374010101 ) ) ;
#43574=CARTESIAN_POINT ( 'NONE',  ( 4.553261556744875094, 0.000000000000000000, 0.000000000000000000 ) ) ;
#43584=EDGE_CURVE ( 'NONE', #21723, #54066, #20776, .T. ) ;
#43587=CARTESIAN_POINT ( 'NONE',  ( 1.112077966505210957, -35.94411555399670988, -25.51569873958945678 ) ) ;
#43591=EDGE_CURVE ( 'NONE', #9433, #50250, #57235, .T. ) ;
#43596=CARTESIAN_POINT ( 'NONE',  ( 4.553261556744875094, 0.000000000000000000, 0.000000000000000000 ) ) ;
#43600=( BOUNDED_SURFACE ( )  B_SPLINE_SURFACE ( 3, 1, ( 
 ( #8535, #17966 ),
 ( #37086, #18272 ),
 ( #56153, #51442 ),
 ( #27658, #46792 ) ),
 .UNSPECIFIED., .F., .F., .F. ) 
 B_SPLINE_SURFACE_WITH_KNOTS ( ( 4, 4 ),
 ( 2, 2 ),
 ( 0.000000000000000000, 1.000000000000000000 ),
 ( 0.000000000000000000, 1.000000000000000000 ),
 .UNSPECIFIED. ) 
 GEOMETRIC_REPRESENTATION_ITEM ( )  RATIONAL_B_SPLINE_SURFACE ( (
 ( 1.000000000000000000, 1.000000000000000000),
 ( 0.7211978278499970862, 0.9934217856018976445),
 ( 0.7211978278499970862, 0.9934217856018976445),
 ( 1.000000000000000000, 1.000000000000000000) ) ) 
 REPRESENTATION_ITEM ( '' )  SURFACE ( )  );
#43602=ORIENTED_EDGE ( 'NONE', *, *, #15721, .T. ) ;
#43613=CARTESIAN_POINT ( 'NONE',  ( -6.079354080745853928, 15.43131048252502069, 11.51814273396867705 ) ) ;
#43624=CARTESIAN_POINT ( 'NONE',  ( 0.1158516988532803244, 39.77583507406630758, 19.10039536222936007 ) ) ;
#43628=CARTESIAN_POINT ( 'NONE',  ( 0.6039202388192953519, -48.68192096202343322, 6.452463428512738908 ) ) ;
#43634=ORIENTED_EDGE ( 'NONE', *, *, #17656, .F. ) ;
#43639=ORIENTED_EDGE ( 'NONE', *, *, #13225, .F. ) ;
#43645=ORIENTED_EDGE ( 'NONE', *, *, #54861, .T. ) ;
#43646=DIRECTION ( 'NONE',  ( -1.000000000000000000, -0.000000000000000000, -0.000000000000000000 ) ) ;
#43648=EDGE_LOOP ( 'NONE', ( #45356, #13567, #38741, #14071 ) ) ;
#43652=ORIENTED_EDGE ( 'NONE', *, *, #1404, .T. ) ;
#43655=B_SPLINE_CURVE_WITH_KNOTS ( 'NONE', 3,
 ( #38824, #15007, #57881, #43841 ),
 .UNSPECIFIED., .F., .F.,
 ( 4, 4 ),
 ( 0.000000000000000000, 0.004444103432399267896 ),
 .UNSPECIFIED. ) ;
#43670=CARTESIAN_POINT ( 'NONE',  ( 0.1158403557922069033, -1.376402091003258166, -44.10267366575070724 ) ) ;
#43674=LINE ( 'NONE', #1630, #3031 ) ;
#43677=CARTESIAN_POINT ( 'NONE',  ( 0.1157506346131639274, 36.92923354691153293, -24.14896207791336380 ) ) ;
#43681=VERTEX_POINT ( 'NONE', #35818 ) ;
#43684=DIRECTION ( 'NONE',  ( 1.000000000000000000, 0.000000000000000000, 0.000000000000000000 ) ) ;
#43686=CARTESIAN_POINT ( 'NONE',  ( 3.240649175237396484, 43.49255432869266258, -6.607770831632137742 ) ) ;
#43696=CARTESIAN_POINT ( 'NONE',  ( 0.1129192098497447394, -7.520259262076021578, -43.47870154933693243 ) ) ;
#43705=CARTESIAN_POINT ( 'NONE',  ( 0.6029442701453592290, 22.63682954516835011, -43.57888448895027267 ) ) ;
#43708=AXIS2_PLACEMENT_3D ( 'NONE', #58735, #24636, #6108 ) ;
#43711=CARTESIAN_POINT ( 'NONE',  ( 3.678834586032786458, -18.11945796638148209, -45.50052321273776812 ) ) ;
#43713=ORIENTED_EDGE ( 'NONE', *, *, #35608, .T. ) ;
#43719=ORIENTED_EDGE ( 'NONE', *, *, #40723, .T. ) ;
#43726=CARTESIAN_POINT ( 'NONE',  ( 0.9268187852002115479, 28.89887655679548573, -33.29578451791941518 ) ) ;
#43727=CARTESIAN_POINT ( 'NONE',  ( 4.975610109902397937, 42.33317580307119954, 24.50207406657730047 ) ) ;
#43732=AXIS2_PLACEMENT_3D ( 'NONE', #41384, #60440, #17562 ) ;
#43735=CARTESIAN_POINT ( 'NONE',  ( 0.8744876279028306332, -34.64280934553560343, 34.78829991575276637 ) ) ;
#43749=CYLINDRICAL_SURFACE ( 'NONE', #41787, 10.00000000000000000 ) ;
#43751=CARTESIAN_POINT ( 'NONE',  ( 0.5997462898726536595, 28.52220283460682282, -39.97543715340528081 ) ) ;
#43755=CIRCLE ( 'NONE', #51712, 48.91267123290010943 ) ;
#43759=( BOUNDED_SURFACE ( )  B_SPLINE_SURFACE ( 3, 1, ( 
 ( #37014, #32919 ),
 ( #61379, #22582 ),
 ( #13188, #17574 ),
 ( #41708, #23491 ) ),
 .UNSPECIFIED., .F., .F., .F. ) 
 B_SPLINE_SURFACE_WITH_KNOTS ( ( 4, 4 ),
 ( 2, 2 ),
 ( 0.000000000000000000, 1.000000000000000000 ),
 ( 0.000000000000000000, 1.000000000000000000 ),
 .UNSPECIFIED. ) 
 GEOMETRIC_REPRESENTATION_ITEM ( )  RATIONAL_B_SPLINE_SURFACE ( (
 ( 1.000000000000000000, 1.000000000000000000),
 ( 0.7211978278499970862, 0.9934217856018976445),
 ( 0.7211978278499970862, 0.9934217856018976445),
 ( 1.000000000000000000, 1.000000000000000000) ) ) 
 REPRESENTATION_ITEM ( '' )  SURFACE ( )  );
#43768=CARTESIAN_POINT ( 'NONE',  ( 4.553261556744873317, 43.53643125131393532, -5.841123155973635406 ) ) ;
#43769=CARTESIAN_POINT ( 'NONE',  ( 0.1135584504625008206, 33.87666299352049748, -28.27231431203839307 ) ) ;
#43773=ORIENTED_EDGE ( 'NONE', *, *, #45871, .T. ) ;
#43779=ORIENTED_EDGE ( 'NONE', *, *, #57903, .F. ) ;
#43780=( BOUNDED_SURFACE ( )  B_SPLINE_SURFACE ( 3, 1, ( 
 ( #3305, #40041 ),
 ( #59091, #21204 ),
 ( #40963, #45963 ),
 ( #41258, #16202 ) ),
 .UNSPECIFIED., .F., .F., .F. ) 
 B_SPLINE_SURFACE_WITH_KNOTS ( ( 4, 4 ),
 ( 2, 2 ),
 ( 0.000000000000000000, 1.000000000000000000 ),
 ( 0.000000000000000000, 1.000000000000000000 ),
 .UNSPECIFIED. ) 
 GEOMETRIC_REPRESENTATION_ITEM ( )  RATIONAL_B_SPLINE_SURFACE ( (
 ( 1.000000000000000000, 1.000000000000000000),
 ( 0.9754377213608244057, 0.9999580625633939235),
 ( 0.9754377213608244057, 0.9999580625633939235),
 ( 1.000000000000000000, 1.000000000000000000) ) ) 
 REPRESENTATION_ITEM ( '' )  SURFACE ( )  );
#43782=CARTESIAN_POINT ( 'NONE',  ( 4.694002226626921015, 39.88981857773250539, 22.07005086722095299 ) ) ;
#43783=CARTESIAN_POINT ( 'NONE',  ( 0.6028777368367060907, 22.63683791566365500, 43.57881823192369097 ) ) ;
#43793=DIRECTION ( 'NONE',  ( -1.000000000000000000, -0.000000000000000000, -0.000000000000000000 ) ) ;
#43810=B_SPLINE_CURVE_WITH_KNOTS ( 'NONE', 3,
 ( #36079, #46389, #41699, #55137, #31354, #36385 ),
 .UNSPECIFIED., .F., .F.,
 ( 4, 2, 4 ),
 ( 1.246832498358330292E-18, 0.0002293801035737089925, 0.0004587602071474167383 ),
 .UNSPECIFIED. ) ;
#43822=EDGE_CURVE ( 'NONE', #45706, #9797, #13236, .T. ) ;
#43823=CARTESIAN_POINT ( 'NONE',  ( 0.7242486021783808292, 21.98223893955317010, 43.90663541628263289 ) ) ;
#43831=CARTESIAN_POINT ( 'NONE',  ( -6.079354080745853928, -14.66314846858153054, -12.48138743235291059 ) ) ;
#43833=ORIENTED_EDGE ( 'NONE', *, *, #3537, .T. ) ;
#43836=CARTESIAN_POINT ( 'NONE',  ( 0.2940133293163007533, 10.59968119980750423, -42.82391047114322902 ) ) ;
#43839=CARTESIAN_POINT ( 'NONE',  ( 0.2285344041767068402, -38.06330129766492831, 22.30888308765448258 ) ) ;
#43841=CARTESIAN_POINT ( 'NONE',  ( 0.8744876279028263033, -26.20733431478184983, 41.51536677536103070 ) ) ;
#43845=CARTESIAN_POINT ( 'NONE',  ( 4.553261556744875094, 0.000000000000000000, 0.000000000000000000 ) ) ;
#43846=CARTESIAN_POINT ( 'NONE',  ( 0.7044674535453004927, 32.38853019898915164, -36.91592927666964385 ) ) ;
#43847=CARTESIAN_POINT ( 'NONE',  ( 0.7242003506639982380, -13.18377730284193028, 47.29904534084272427 ) ) ;
#43854=CARTESIAN_POINT ( 'NONE',  ( 4.975610109902397937, 0.000000000000000000, 0.000000000000000000 ) ) ;
#43857=CARTESIAN_POINT ( 'NONE',  ( -6.078457390727109555, 19.09849343800966182, 2.458060096053366284 ) ) ;
#43860=CARTESIAN_POINT ( 'NONE',  ( 0.1140933569871964010, 20.74467474435255809, -38.94365699102905864 ) ) ;
#43862=CARTESIAN_POINT ( 'NONE',  ( -6.077587904424778920, 3.079371755031420133, 19.00824797261034149 ) ) ;
#43866=DIRECTION ( 'NONE',  ( -1.000000000000000000, -0.000000000000000000, -0.000000000000000000 ) ) ;
#43867=CARTESIAN_POINT ( 'NONE',  ( 2.648799415243696664, -18.57388519568332086, -45.38202564922784177 ) ) ;
#43872=EDGE_CURVE ( 'NONE', #56645, #47069, #9442, .T. ) ;
#43875=CARTESIAN_POINT ( 'NONE',  ( 0.6029442701453591180, -47.52343932222595413, -12.37206288963105116 ) ) ;
#43882=FACE_OUTER_BOUND ( 'NONE', #16228, .T. ) ;
#43884=B_SPLINE_CURVE_WITH_KNOTS ( 'NONE', 3,
 ( #32611, #23821, #4366, #42335 ),
 .UNSPECIFIED., .F., .F.,
 ( 4, 4 ),
 ( 0.000000000000000000, 0.005013413432710141573 ),
 .UNSPECIFIED. ) ;
#43885=CARTESIAN_POINT ( 'NONE',  ( 4.553261556744873317, -29.69864478935373242, -32.36556910513746743 ) ) ;
#43887=EDGE_CURVE ( 'NONE', #55761, #17913, #4987, .T. ) ;
#43891=CIRCLE ( 'NONE', #57837, 48.91267123290010943 ) ;
#43895=EDGE_LOOP ( 'NONE', ( #35933, #4822, #42346, #35868 ) ) ;
#43896=CARTESIAN_POINT ( 'NONE',  ( 0.1152339509894530906, 29.49895703548700965, -32.81393338619639621 ) ) ;
#43907=CARTESIAN_POINT ( 'NONE',  ( 1.479689385636123067, -36.00353389669128745, -25.40333427362427088 ) ) ;
#43913=FACE_OUTER_BOUND ( 'NONE', #61333, .T. ) ;
#43925=CARTESIAN_POINT ( 'NONE',  ( 0.3676999524040323597, -42.45338881270421894, -11.98584004733086061 ) ) ;
#43926=CARTESIAN_POINT ( 'NONE',  ( -6.072942160501519027, 15.44092479507881421, -11.50573786255104913 ) ) ;
#43932=CARTESIAN_POINT ( 'NONE',  ( 3.221118495291109607, -8.878221871482150362, -43.08060579962272385 ) ) ;
#43933=CIRCLE ( 'NONE', #26910, 43.92652462719577500 ) ;
#43942=CARTESIAN_POINT ( 'NONE',  ( 0.1155031312995260795, 39.68109568858822911, 19.29643172933567996 ) ) ;
#43945=ADVANCED_FACE ( 'NONE', ( #4104, #42073 ), #18243, .F. ) ;
#43947=CARTESIAN_POINT ( 'NONE',  ( -2.601141883200665639, 14.86024923780642304, 1.403003941427925394 ) ) ;
#43948=ADVANCED_FACE ( 'NONE', ( #60820 ), #17940, .T. ) ;
#43960=EDGE_CURVE ( 'NONE', #14660, #17426, #13130, .T. ) ;
#43965=VERTEX_POINT ( 'NONE', #19791 ) ;
#43966=FACE_OUTER_BOUND ( 'NONE', #15898, .T. ) ;
#43985=VERTEX_POINT ( 'NONE', #15709 ) ;
#43986=CARTESIAN_POINT ( 'NONE',  ( 0.1145239942831223490, -1.087792730805732466, -44.11079445758689843 ) ) ;
#43988=EDGE_CURVE ( 'NONE', #55501, #45566, #10112, .T. ) ;
#43992=CARTESIAN_POINT ( 'NONE',  ( 4.553261556744875094, -43.07273893850278768, -8.618510669438375515 ) ) ;
#43994=FACE_OUTER_BOUND ( 'NONE', #12794, .T. ) ;
#44007=CARTESIAN_POINT ( 'NONE',  ( 0.6039202388192953519, 44.31978288059509907, 21.14995409607076837 ) ) ;
#44010=DIRECTION ( 'NONE',  ( -1.000000000000000000, -0.000000000000000000, -0.000000000000000000 ) ) ;
#44015=CARTESIAN_POINT ( 'NONE',  ( 0.1147471544378677044, -35.17521250930997212, 26.63938087490264195 ) ) ;
#44019=CARTESIAN_POINT ( 'NONE',  ( 0.6028777368367060907, 33.07937202223710216, -36.29455848919381111 ) ) ;
#44032=CARTESIAN_POINT ( 'NONE',  ( 0.2285344041767096157, -43.84762605143654213, -4.887418536286803672 ) ) ;
#44037=CARTESIAN_POINT ( 'NONE',  ( 0.8753041380234524160, 10.05717963662871561, -48.06237057854679051 ) ) ;
#44039=( BOUNDED_SURFACE ( )  B_SPLINE_SURFACE ( 3, 1, ( 
 ( #1546, #53551 ),
 ( #58245, #20683 ),
 ( #5614, #29758 ),
 ( #6229, #24759 ) ),
 .UNSPECIFIED., .F., .F., .F. ) 
 B_SPLINE_SURFACE_WITH_KNOTS ( ( 4, 4 ),
 ( 2, 2 ),
 ( 0.000000000000000000, 1.000000000000000000 ),
 ( 0.000000000000000000, 1.000000000000000000 ),
 .UNSPECIFIED. ) 
 GEOMETRIC_REPRESENTATION_ITEM ( )  RATIONAL_B_SPLINE_SURFACE ( (
 ( 1.000000000000000000, 1.000000000000000000),
 ( 0.9754377213608244057, 0.9999580625633939235),
 ( 0.9754377213608244057, 0.9999580625633939235),
 ( 1.000000000000000000, 1.000000000000000000) ) ) 
 REPRESENTATION_ITEM ( '' )  SURFACE ( )  );
#44048=CARTESIAN_POINT ( 'NONE',  ( 2.009741617377216460, -11.21041860717905791, 42.58909006159744592 ) ) ;
#44052=( BOUNDED_SURFACE ( )  B_SPLINE_SURFACE ( 3, 1, ( 
 ( #48893, #49198 ),
 ( #6247, #59202 ),
 ( #44229, #20394 ),
 ( #10686, #44536 ) ),
 .UNSPECIFIED., .F., .F., .F. ) 
 B_SPLINE_SURFACE_WITH_KNOTS ( ( 4, 4 ),
 ( 2, 2 ),
 ( 0.000000000000000000, 1.000000000000000000 ),
 ( 0.000000000000000000, 1.000000000000000000 ),
 .UNSPECIFIED. ) 
 GEOMETRIC_REPRESENTATION_ITEM ( )  RATIONAL_B_SPLINE_SURFACE ( (
 ( 1.000000000000000000, 1.000000000000000000),
 ( 0.9953485035131437453, 0.8621029689291515030),
 ( 0.9953485035131437453, 0.8621029689291515030),
 ( 1.000000000000000000, 1.000000000000000000) ) ) 
 REPRESENTATION_ITEM ( '' )  SURFACE ( )  );
#44057=CARTESIAN_POINT ( 'NONE',  ( 0.1129192098497447394, 33.91039995638862337, 28.23183597612653983 ) ) ;
#44062=CARTESIAN_POINT ( 'NONE',  ( 0.5987334363312691865, -39.71456561150246500, 28.88453192907479306 ) ) ;
#44068=EDGE_CURVE ( 'NONE', #59959, #988, #42977, .T. ) ;
#44088=CARTESIAN_POINT ( 'NONE',  ( 1.112077966505211846, -16.87764873673971167, 40.72069864636144132 ) ) ;
#44109=EDGE_CURVE ( 'NONE', #49527, #8500, #54916, .T. ) ;
#44115=ORIENTED_EDGE ( 'NONE', *, *, #51133, .T. ) ;
#44116=DIRECTION ( 'NONE',  ( 0.000000000000000000, 0.000000000000000000, -1.000000000000000000 ) ) ;
#44119=CARTESIAN_POINT ( 'NONE',  ( -2.601141883200665639, -13.21958573851854268, 6.930943685483663685 ) ) ;
#44122=B_SPLINE_CURVE_WITH_KNOTS ( 'NONE', 3,
 ( #47645, #28216, #4689, #307, #23835, #24134 ),
 .UNSPECIFIED., .F., .F.,
 ( 4, 2, 4 ),
 ( 1.910758783386232924E-17, 0.0002293755540694306951, 0.0004587511081388422540 ),
 .UNSPECIFIED. ) ;
#44127=CARTESIAN_POINT ( 'NONE',  ( 4.553261556744875094, 0.000000000000000000, 0.000000000000000000 ) ) ;
#44139=CARTESIAN_POINT ( 'NONE',  ( 0.5549461598389365813, -0.5360408303695749499, 44.10136455592935079 ) ) ;
#44141=CARTESIAN_POINT ( 'NONE',  ( 0.5997462898726536595, 5.235280152387000285, 48.82769165002921596 ) ) ;
#44144=CARTESIAN_POINT ( 'NONE',  ( -6.063463321072278589, 18.62294427965537835, 4.899632520538766300 ) ) ;
#44147=CARTESIAN_POINT ( 'NONE',  ( 0.6016118706126976079, -48.65860383458689853, -6.625053030176840885 ) ) ;
#44149=CARTESIAN_POINT ( 'NONE',  ( -6.078726893082806448, 16.77980020642702641, 9.446287434813308792 ) ) ;
#44160=CARTESIAN_POINT ( 'NONE',  ( 0.2279481005628741785, 24.61482262596651438, 36.61439599618051943 ) ) ;
#44161=CARTESIAN_POINT ( 'NONE',  ( -2.739355103387247858, -14.50431811309224095, 3.531617621606463864 ) ) ;
#44168=CARTESIAN_POINT ( 'NONE',  ( 0.1129192098497447394, 24.84520063729181416, -36.46461014569973713 ) ) ;
#44169=CARTESIAN_POINT ( 'NONE',  ( 0.1152339509894530906, -42.62387090632541486, 11.40825663351544073 ) ) ;
#44173=AXIS2_PLACEMENT_3D ( 'NONE', #44616, #45242, #45539 ) ;
#44174=CARTESIAN_POINT ( 'NONE',  ( 0.6029443449137436017, 37.42085009926554307, -31.79967792024990914 ) ) ;
#44175=CARTESIAN_POINT ( 'NONE',  ( -6.057079549204054558, -11.02420820863765449, -15.78917554758146835 ) ) ;
#44178=CARTESIAN_POINT ( 'NONE',  ( 0.2940135542859016460, -2.218054204175251787, -44.06042197072970623 ) ) ;
#44179=CARTESIAN_POINT ( 'NONE',  ( 4.553261556744875094, 0.000000000000000000, 0.000000000000000000 ) ) ;
#44180=EDGE_CURVE ( 'NONE', #40399, #6110, #33320, .T. ) ;
#44181=CARTESIAN_POINT ( 'NONE',  ( 3.390910168358336918, -19.58529142663901013, -39.37656023914808401 ) ) ;
#44183=DIRECTION ( 'NONE',  ( -0.1011922191286467460, 0.01903003979491558334, 0.9946848708878726075 ) ) ;
#44185=CARTESIAN_POINT ( 'NONE',  ( 0.3676999524040323597, -41.19158123804999860, 15.78620342045440239 ) ) ;
#44191=EDGE_CURVE ( 'NONE', #55165, #8492, #32581, .T. ) ;
#44195=ORIENTED_EDGE ( 'NONE', *, *, #46529, .T. ) ;
#44198=ORIENTED_EDGE ( 'NONE', *, *, #14387, .T. ) ;
#44201=CARTESIAN_POINT ( 'NONE',  ( 0.6000166863083106206, -35.63988196839385125, 33.78790160674984833 ) ) ;
#44203=CARTESIAN_POINT ( 'NONE',  ( 4.553261556744875094, 43.53643125131386427, 5.841123155974254466 ) ) ;
#44210=CONICAL_SURFACE ( 'NONE', #60167, 43.92652462719577500, 1.486293639869522343 ) ;
#44212=VERTEX_POINT ( 'NONE', #51349 ) ;
#44214=CARTESIAN_POINT ( 'NONE',  ( 2.879087469061463178, -36.27144865066016877, -24.90951002259781433 ) ) ;
#44216=CARTESIAN_POINT ( 'NONE',  ( -6.077587904424778920, 17.85108912406252912, -7.220432014686311462 ) ) ;
#44222=( BOUNDED_SURFACE ( )  B_SPLINE_SURFACE ( 3, 1, ( 
 ( #54479, #6868 ),
 ( #16614, #7491 ),
 ( #50424, #11938 ),
 ( #31014, #50123 ) ),
 .UNSPECIFIED., .F., .F., .F. ) 
 B_SPLINE_SURFACE_WITH_KNOTS ( ( 4, 4 ),
 ( 2, 2 ),
 ( 0.000000000000000000, 1.000000000000000000 ),
 ( 0.000000000000000000, 1.000000000000000000 ),
 .UNSPECIFIED. ) 
 GEOMETRIC_REPRESENTATION_ITEM ( )  RATIONAL_B_SPLINE_SURFACE ( (
 ( 1.000000000000000000, 1.000000000000000000),
 ( 0.7211978278499968642, 0.9934217856018975334),
 ( 0.7211978278499968642, 0.9934217856018975334),
 ( 1.000000000000000000, 1.000000000000000000) ) ) 
 REPRESENTATION_ITEM ( '' )  SURFACE ( )  );
#44229=CARTESIAN_POINT ( 'NONE',  ( -6.078457390727109555, 5.474669697363819587, 18.46137867934771393 ) ) ;
#44231=CARTESIAN_POINT ( 'NONE',  ( 2.648799415243708655, -38.45353011080888450, 30.42767630475112028 ) ) ;
#44238=CARTESIAN_POINT ( 'NONE',  ( 4.975610109902397937, 0.000000000000000000, 0.000000000000000000 ) ) ;
#44245=CARTESIAN_POINT ( 'NONE',  ( 0.1149546198390368756, -43.72609045126175431, -5.914015460860355233 ) ) ;
#44247=CIRCLE ( 'NONE', #10238, 43.92652462719577500 ) ;
#44248=CARTESIAN_POINT ( 'NONE',  ( 4.553261556744873317, 17.57396821678933563, -40.25785894628420181 ) ) ;
#44251=LINE ( 'NONE', #30110, #11261 ) ;
#44252=CARTESIAN_POINT ( 'NONE',  ( 0.1156495703730067298, 37.05413706972513666, 23.95691714827038865 ) ) ;
#44254=CARTESIAN_POINT ( 'NONE',  ( 4.390527457369401532, -3.899219021785376160, -43.76050077008678585 ) ) ;
#44262=ORIENTED_EDGE ( 'NONE', *, *, #51678, .F. ) ;
#44264=ORIENTED_EDGE ( 'NONE', *, *, #31196, .F. ) ;
#44265=CARTESIAN_POINT ( 'NONE',  ( 0.8744876279028306332, 48.01195819035234535, -10.25679877482985169 ) ) ;
#44272=CARTESIAN_POINT ( 'NONE',  ( 0.8744876279028263033, 41.62483489565955352, -26.03311679934954626 ) ) ;
#44274=CARTESIAN_POINT ( 'NONE',  ( 0.1365634738349418009, 37.32273229751332622, -23.53457612686919020 ) ) ;
#44276=VERTEX_POINT ( 'NONE', #30906 ) ;
#44277=EDGE_LOOP ( 'NONE', ( #33350, #28905, #8905, #1880 ) ) ;
#44282=EDGE_CURVE ( 'NONE', #30382, #1638, #44956, .T. ) ;
#44289=CARTESIAN_POINT ( 'NONE',  ( -6.078075953587585900, -18.90195907099236905, -3.675747206441904780 ) ) ;
#44292=CARTESIAN_POINT ( 'NONE',  ( 1.112077966505211624, -42.89240287839150056, -10.16228815013172770 ) ) ;
#44294=EDGE_CURVE ( 'NONE', #21415, #5530, #10904, .T. ) ;
#44296=CARTESIAN_POINT ( 'NONE',  ( 0.9268187852002115479, -6.055792169277320447, 43.67014671501740963 ) ) ;
#44302=CARTESIAN_POINT ( 'NONE',  ( -6.079354080745853928, -12.94495173828241441, -14.25556662296175148 ) ) ;
#44305=CARTESIAN_POINT ( 'NONE',  ( 0.1157506346131639274, -31.63194487325750259, 30.76297650322595700 ) ) ;
#44306=B_SPLINE_CURVE_WITH_KNOTS ( 'NONE', 3,
 ( #15832, #1386, #11434, #21136, #7317, #54939, #11133, #20834, #16755, #44971, #2007, #1695, #6691, #53694, #35870, #54009 ),
 .UNSPECIFIED., .F., .F.,
 ( 4, 3, 3, 3, 3, 4 ),
 ( 2.081781105835003155E-17, 0.0002612764279487734338, 0.0003919131003184793535, 0.0005225497727000639548, 0.0007837925190632447038, 0.001045051706266716951 ),
 .UNSPECIFIED. ) ;
#44310=ADVANCED_FACE ( 'NONE', ( #40339 ), #16125, .F. ) ;
#44312=CARTESIAN_POINT ( 'NONE',  ( -6.077587904424778920, -12.94128980615197477, 14.25899854643086329 ) ) ;
#44313=EDGE_CURVE ( 'NONE', #27771, #26826, #2070, .T. ) ;
#44314=CARTESIAN_POINT ( 'NONE',  ( 0.1139756605157203756, -7.434439534098977731, -43.49349754283792890 ) ) ;
#44322=CARTESIAN_POINT ( 'NONE',  ( 0.6028777368367060907, -30.68600655816066336, 38.33939006848692088 ) ) ;
#44325=LINE ( 'NONE', #19897, #58320 ) ;
#44326=ORIENTED_EDGE ( 'NONE', *, *, #9120, .T. ) ;
#44328=CARTESIAN_POINT ( 'NONE',  ( 4.553261556744873317, -43.07273893850290136, 8.618510669437750238 ) ) ;
#44329=CARTESIAN_POINT ( 'NONE',  ( 1.112077966505211846, 43.90950196486499379, -3.871170666099937652 ) ) ;
#44332=EDGE_CURVE ( 'NONE', #28177, #55165, #41532, .T. ) ;
#44334=CARTESIAN_POINT ( 'NONE',  ( -6.078726893082806448, 0.6137717894417996645, 19.24622886331775717 ) ) ;
#44338=B_SPLINE_CURVE_WITH_KNOTS ( 'NONE', 3,
 ( #22969, #17965, #56456, #13570, #51142, #56762, #51441, #28266, #8228, #18572, #33300, #57066, #47090, #47383, #23569, #47693 ),
 .UNSPECIFIED., .F., .F.,
 ( 4, 3, 3, 3, 3, 4 ),
 ( 1.962735358247463844E-17, 0.0002612764279487806980, 0.0003919131003184837445, 0.0005225497727000715442, 0.0007837925190632499079, 0.001045051706266720637 ),
 .UNSPECIFIED. ) ;
#44345=CARTESIAN_POINT ( 'NONE',  ( 0.7948884756798514362, 36.81796298084067587, 32.48286081215135823 ) ) ;
#44346=CARTESIAN_POINT ( 'NONE',  ( 0.3676999524040323597, -2.238562284876542741, 44.05609404179593724 ) ) ;
#44347=CARTESIAN_POINT ( 'NONE',  ( -6.078457390727109555, 5.483070842475943785, 18.45888526357694559 ) ) ;
#44353=CARTESIAN_POINT ( 'NONE',  ( -6.078726893082806448, 7.797636468844896918, -17.60655862934208216 ) ) ;
#44354=DIRECTION ( 'NONE',  ( 0.000000000000000000, 0.000000000000000000, 1.000000000000000000 ) ) ;
#44356=CARTESIAN_POINT ( 'NONE',  ( 0.8744876279028306332, -8.712669995481570950, -48.31603700562917680 ) ) ;
#44359=DIRECTION ( 'NONE',  ( 0.000000000000000000, 0.000000000000000000, 1.000000000000000000 ) ) ;
#44364=ADVANCED_FACE ( 'NONE', ( #12138 ), #43780, .F. ) ;
#44367=EDGE_LOOP ( 'NONE', ( #59242, #17911, #34219, #19143 ) ) ;
#44376=B_SPLINE_CURVE_WITH_KNOTS ( 'NONE', 3,
 ( #59636, #54000, #58389, #20517, #31139, #7310, #26436, #49625, #15823, #34938, #39645, #53687, #2622, #39331, #15514, #34621, #29905, #11126, #39966 ),
 .UNSPECIFIED., .F., .F.,
 ( 4, 3, 3, 3, 3, 3, 4 ),
 ( 0.000000000000000000, 0.0002612768053151710585, 0.0003919133833142919012, 0.0005225499612322616208, 0.0006531865391693383437, 0.0008112755173415223510, 0.0009693688056799709468 ),
 .UNSPECIFIED. ) ;
#44377=CARTESIAN_POINT ( 'NONE',  ( 4.553261556744875094, -39.67390170502071811, 18.85526688551479424 ) ) ;
#44382=DIRECTION ( 'NONE',  ( 0.1011922191286468153, 0.7658109114536828521, 0.6350541572860533002 ) ) ;
#44383=CARTESIAN_POINT ( 'NONE',  ( 1.657374760986086715, 21.46677708116468253, 38.47165097834802339 ) ) ;
#44409=CARTESIAN_POINT ( 'NONE',  ( 4.975610109902397937, 48.43414999183889336, 6.825138951393308950 ) ) ;
#44415=CARTESIAN_POINT ( 'NONE',  ( 0.1129192098497455998, 10.29049805561888498, -42.90754522869442411 ) ) ;
#44416=( BOUNDED_SURFACE ( )  B_SPLINE_SURFACE ( 3, 1, ( 
 ( #39949, #15500 ),
 ( #59311, #16418 ),
 ( #3150, #51068 ),
 ( #24896, #44037 ) ),
 .UNSPECIFIED., .F., .F., .F. ) 
 B_SPLINE_SURFACE_WITH_KNOTS ( ( 4, 4 ),
 ( 2, 2 ),
 ( 0.000000000000000000, 1.000000000000000000 ),
 ( 0.000000000000000000, 1.000000000000000000 ),
 .UNSPECIFIED. ) 
 GEOMETRIC_REPRESENTATION_ITEM ( )  RATIONAL_B_SPLINE_SURFACE ( (
 ( 1.000000000000000000, 1.000000000000000000),
 ( 0.7211978278499968642, 0.9934217856018975334),
 ( 0.7211978278499968642, 0.9934217856018975334),
 ( 1.000000000000000000, 1.000000000000000000) ) ) 
 REPRESENTATION_ITEM ( '' )  SURFACE ( )  );
#44418=EDGE_CURVE ( 'NONE', #18802, #22171, #55691, .T. ) ;
#44422=CARTESIAN_POINT ( 'NONE',  ( 0.6008122571543325074, 37.67355775107387217, 31.50012058455996211 ) ) ;
#44428=VERTEX_POINT ( 'NONE', #21197 ) ;
#44430=CARTESIAN_POINT ( 'NONE',  ( 4.834790513006555379, -21.44535528597729979, 42.10327870347612134 ) ) ;
#44436=CARTESIAN_POINT ( 'NONE',  ( 0.5987334363312695196, 22.17584323994378082, 43.81546397186176023 ) ) ;
#44437=CARTESIAN_POINT ( 'NONE',  ( 0.08486401232817714080, 1.224646799147353256E-15, -10.00000000000000000 ) ) ;
#44445=DIRECTION ( 'NONE',  ( 0.1011922191286468153, 0.4715280952439158124, 0.8760259072558667093 ) ) ;
#44449=CARTESIAN_POINT ( 'NONE',  ( 0.5997462898726536595, -30.20781297212564454, -38.71743361310750231 ) ) ;
#44451=CARTESIAN_POINT ( 'NONE',  ( 0.6000166863083090663, -42.53190469623903880, -24.55321902762434050 ) ) ;
#44454=EDGE_CURVE ( 'NONE', #9995, #46120, #32536, .T. ) ;
#44462=CARTESIAN_POINT ( 'NONE',  ( 0.5980271706414711508, -19.23780022038679505, -45.18801041783260075 ) ) ;
#44477=CARTESIAN_POINT ( 'NONE',  ( 0.1152809850208375841, 20.60499082682811434, -39.01768362571110060 ) ) ;
#44479=CARTESIAN_POINT ( 'NONE',  ( 0.1158516988532803244, 29.70113990798797943, 32.63103502800547062 ) ) ;
#44481=CARTESIAN_POINT ( 'NONE',  ( 3.678834586032787346, -5.985442328740523621, -48.60850594039765582 ) ) ;
#44483=CARTESIAN_POINT ( 'NONE',  ( 0.9268187852002115479, -18.74830179125902774, -39.90307648355574344 ) ) ;
#44486=ORIENTED_EDGE ( 'NONE', *, *, #6040, .F. ) ;
#44487=DIRECTION ( 'NONE',  ( -1.000000000000000000, -0.000000000000000000, -0.000000000000000000 ) ) ;
#44488=CARTESIAN_POINT ( 'NONE',  ( 0.8753041380234471980, -14.82204010568781172, 46.81287702094758174 ) ) ;
#44490=CARTESIAN_POINT ( 'NONE',  ( 3.050102900204245682, 40.38856827381131609, 17.44100920158413359 ) ) ;
#44497=CARTESIAN_POINT ( 'NONE',  ( 0.7242003506640029009, 43.87790776620104083, -22.03953003552434708 ) ) ;
#44502=B_SPLINE_CURVE_WITH_KNOTS ( 'NONE', 3,
 ( #36908, #21860, #2423, #31881, #50966, #26864 ),
 .UNSPECIFIED., .F., .F.,
 ( 4, 2, 4 ),
 ( 1.964591557601686678E-17, 0.0002293755540694308577, 0.0004587511081388420371 ),
 .UNSPECIFIED. ) ;
#44506=CARTESIAN_POINT ( 'NONE',  ( 0.1157991065609915715, 29.72493506311960942, -32.60936370171949505 ) ) ;
#44515=AXIS2_PLACEMENT_3D ( 'NONE', #59569, #3473, #11999 ) ;
#44517=ORIENTED_EDGE ( 'NONE', *, *, #21284, .T. ) ;
#44523=CARTESIAN_POINT ( 'NONE',  ( 0.7044674535453004927, -45.19827881396748381, 19.20724642070708654 ) ) ;
#44529=ORIENTED_EDGE ( 'NONE', *, *, #43024, .F. ) ;
#44533=DIRECTION ( 'NONE',  ( -0.1011922191286467321, 0.8604626000150104037, 0.4993638440688594193 ) ) ;
#44536=CARTESIAN_POINT ( 'NONE',  ( 0.6000166863083090663, -14.47337940799656764, -46.92914627628159252 ) ) ;
#44540=VERTEX_POINT ( 'NONE', #27750 ) ;
#44541=CARTESIAN_POINT ( 'NONE',  ( 4.975610109902397937, 45.11887670192734134, 18.88746601040093154 ) ) ;
#44551=DIRECTION ( 'NONE',  ( 0.09722883295013592941, -0.4097642837406412220, -0.9069949205004809167 ) ) ;
#44553=CARTESIAN_POINT ( 'NONE',  ( 0.1140933569871963454, -43.71187804725383330, -6.018443957196380367 ) ) ;
#44557=CARTESIAN_POINT ( 'NONE',  ( 0.1156867017252034557, 36.91162943948151565, 24.17590576167908267 ) ) ;
#44560=CARTESIAN_POINT ( 'NONE',  ( 0.5549461598389362482, 19.61782105380045849, -39.50137709710722334 ) ) ;
#44564=CARTESIAN_POINT ( 'NONE',  ( 0.1129192098497447394, 4.719118110134695954, 43.87119455916095490 ) ) ;
#44568=CARTESIAN_POINT ( 'NONE',  ( 0.7242003506640006805, 37.91427066463845819, 31.20127808431195149 ) ) ;
#44573=CARTESIAN_POINT ( 'NONE',  ( 0.7044674535453004927, -20.64605418817839677, -44.55943412196466369 ) ) ;
#44591=ADVANCED_FACE ( 'NONE', ( #48097 ), #50154, .F. ) ;
#44593=CARTESIAN_POINT ( 'NONE',  ( 0.6000166863083106206, -25.90381862410858460, -41.72308308835457069 ) ) ;
#44594=AXIS2_PLACEMENT_3D ( 'NONE', #60030, #37485, #17436 ) ;
#44603=CARTESIAN_POINT ( 'NONE',  ( 4.390527457369401532, 42.41450209547013372, 11.45405380736354850 ) ) ;
#44606=VECTOR ( 'NONE', #54182, 1000.000000000000114 ) ;
#44607=CARTESIAN_POINT ( 'NONE',  ( -6.078457390727109555, -19.21618051603929445, 1.238110420156431246 ) ) ;
#44610=CARTESIAN_POINT ( 'NONE',  ( 1.834102595619085507, -13.77633997718277392, -41.83790388739330979 ) ) ;
#44614=CARTESIAN_POINT ( 'NONE',  ( 0.6008122571543326185, 41.39240437578163068, 26.42391739423000274 ) ) ;
#44616=CARTESIAN_POINT ( 'NONE',  ( 4.553261556744875094, 0.000000000000000000, 0.000000000000000000 ) ) ;
#44623=CARTESIAN_POINT ( 'NONE',  ( 4.975610109902397937, 7.237810502494805398, -48.37420290059309025 ) ) ;
#44625=ORIENTED_EDGE ( 'NONE', *, *, #33721, .T. ) ;
#44627=CARTESIAN_POINT ( 'NONE',  ( 1.834102595619085729, 43.85446432522261517, -4.121128923664326038 ) ) ;
#44628=CARTESIAN_POINT ( 'NONE',  ( 0.1129192098497447394, 42.02659449688918869, 13.44310763102032702 ) ) ;
#44629=EDGE_CURVE ( 'NONE', #55688, #11233, #58565, .T. ) ;
#44631=ORIENTED_EDGE ( 'NONE', *, *, #12603, .T. ) ;
#44639=EDGE_CURVE ( 'NONE', #19741, #30901, #33204, .T. ) ;
#44642=CARTESIAN_POINT ( 'NONE',  ( -6.078726893082806448, -19.21623043802544828, -1.237145513439781075 ) ) ;
#44649=EDGE_CURVE ( 'NONE', #52565, #19604, #39991, .T. ) ;
#44653=CARTESIAN_POINT ( 'NONE',  ( 0.5987334308729317378, -19.32301376689503769, 45.14625173294140126 ) ) ;
#44654=ORIENTED_EDGE ( 'NONE', *, *, #17002, .T. ) ;
#44656=CARTESIAN_POINT ( 'NONE',  ( 0.1129192098497447394, 37.24220309526806005, 23.66368729500878842 ) ) ;
#44664=DIRECTION ( 'NONE',  ( -1.000000000000000000, -0.000000000000000000, -0.000000000000000000 ) ) ;
#44669=ORIENTED_EDGE ( 'NONE', *, *, #56975, .T. ) ;
#44672=B_SPLINE_CURVE_WITH_KNOTS ( 'NONE', 3,
 ( #23105, #13098, #42844, #56289, #13715, #43152 ),
 .UNSPECIFIED., .F., .F.,
 ( 4, 2, 4 ),
 ( 0.000000000000000000, 0.0002293801035737121909, 0.0004587602071474243819 ),
 .UNSPECIFIED. ) ;
#44677=CARTESIAN_POINT ( 'NONE',  ( 4.553261556744873317, -9.994631851593151595, -42.77437199977056537 ) ) ;
#44678=ADVANCED_FACE ( 'NONE', ( #20820 ), #18501, .F. ) ;
#44680=CARTESIAN_POINT ( 'NONE',  ( 0.2940135542859018680, -31.12576111067042106, 31.26383763988192754 ) ) ;
#44681=CARTESIAN_POINT ( 'NONE',  ( 0.1368894036331279318, -41.13355190018849328, -15.96534478167740900 ) ) ;
#44686=CARTESIAN_POINT ( 'NONE',  ( 4.553261556744873317, 17.57396821678933563, -40.25785894628420181 ) ) ;
#44692=CARTESIAN_POINT ( 'NONE',  ( 0.6021448801613057400, 22.48212995651498858, 43.65884757120048221 ) ) ;
#44703=CARTESIAN_POINT ( 'NONE',  ( 0.6252788684277211795, 48.32745661275763638, 8.712133407822351572 ) ) ;
#44708=CARTESIAN_POINT ( 'NONE',  ( 0.3676999524040366896, -42.87209381266877983, -10.38913641457107673 ) ) ;
#44718=EDGE_CURVE ( 'NONE', #50189, #33142, #28914, .T. ) ;
#44725=EDGE_CURVE ( 'NONE', #57409, #18802, #39204, .T. ) ;
#44729=EDGE_CURVE ( 'NONE', #30775, #2222, #17556, .T. ) ;
#44738=B_SPLINE_CURVE_WITH_KNOTS ( 'NONE', 3,
 ( #59863, #28203, #47319, #27592, #27284, #56694, #8788, #17903, #23820, #32927, #61087, #47026, #17585, #28502, #13504, #14133, #13824, #4365, #8169 ),
 .UNSPECIFIED., .F., .F.,
 ( 4, 3, 3, 3, 3, 3, 4 ),
 ( 1.734776414728241573E-18, 0.0002612768053151701911, 0.0003919133833142903834, 0.0005225499612322601030, 0.0006531865391693342238, 0.0008112755173415183395, 0.0009693688056799714889 ),
 .UNSPECIFIED. ) ;
#44741=CARTESIAN_POINT ( 'NONE',  ( 0.1156867017252034696, 39.80856523685828563, -19.03210290687776762 ) ) ;
#44748=CARTESIAN_POINT ( 'NONE',  ( 2.299652685299201860, 40.37736489803184980, 27.81995917950526476 ) ) ;
#44749=B_SPLINE_CURVE_WITH_KNOTS ( 'NONE', 3,
 ( #30231, #1709, #29615, #19625 ),
 .UNSPECIFIED., .F., .F.,
 ( 4, 4 ),
 ( 2.177303646125455536E-17, 0.004559932413162186803 ),
 .UNSPECIFIED. ) ;
#44750=FACE_OUTER_BOUND ( 'NONE', #24749, .T. ) ;
#44752=CARTESIAN_POINT ( 'NONE',  ( 0.3676999524040366896, -38.02468164711607557, 22.36233818182511257 ) ) ;
#44756=( BOUNDED_SURFACE ( )  B_SPLINE_SURFACE ( 3, 1, ( 
 ( #52189, #32807 ),
 ( #4254, #28702 ),
 ( #32488, #55965 ),
 ( #51885, #28090 ) ),
 .UNSPECIFIED., .F., .F., .F. ) 
 B_SPLINE_SURFACE_WITH_KNOTS ( ( 4, 4 ),
 ( 2, 2 ),
 ( 0.000000000000000000, 1.000000000000000000 ),
 ( 0.000000000000000000, 1.000000000000000000 ),
 .UNSPECIFIED. ) 
 GEOMETRIC_REPRESENTATION_ITEM ( )  RATIONAL_B_SPLINE_SURFACE ( (
 ( 1.000000000000000000, 1.000000000000000000),
 ( 0.9754377213608244057, 0.9999580625633939235),
 ( 0.9754377213608244057, 0.9999580625633939235),
 ( 1.000000000000000000, 1.000000000000000000) ) ) 
 REPRESENTATION_ITEM ( '' )  SURFACE ( )  );
#44757=B_SPLINE_CURVE_WITH_KNOTS ( 'NONE', 3,
 ( #18560, #55833, #60836, #27032, #31736, #3508 ),
 .UNSPECIFIED., .F., .F.,
 ( 4, 2, 4 ),
 ( 2.059984127722458810E-18, 0.0002447193893791709549, 0.0004894387787583398498 ),
 .UNSPECIFIED. ) ;
#44758=EDGE_LOOP ( 'NONE', ( #19856, #13841, #18362, #36333 ) ) ;
#44760=CARTESIAN_POINT ( 'NONE',  ( 1.479689385636123067, 30.48353183614671735, 31.81726154247598615 ) ) ;
#44761=DIRECTION ( 'NONE',  ( -1.000000000000000000, -0.000000000000000000, -0.000000000000000000 ) ) ;
#44764=DIRECTION ( 'NONE',  ( 0.09722883295013598492, -0.8021136117729557036, 0.5892031125611089104 ) ) ;
#44771=CARTESIAN_POINT ( 'NONE',  ( 0.6024113833632039894, -19.67861259707041910, -44.99215570913765561 ) ) ;
#44779=CARTESIAN_POINT ( 'NONE',  ( 0.1157991065609915576, 20.48126240941084930, -39.08273603081740077 ) ) ;
#44786=SURFACE_STYLE_USAGE ( .BOTH. , #36308 ) ;
#44787=CARTESIAN_POINT ( 'NONE',  ( 0.2940135542859017570, -17.11870284647595852, 40.65944615394406014 ) ) ;
#44788=ADVANCED_FACE ( 'NONE', ( #18510 ), #14126, .F. ) ;
#44789=CARTESIAN_POINT ( 'NONE',  ( 0.1139756605157203756, -6.649460940698757483, 43.62040679421897238 ) ) ;
#44792=ADVANCED_FACE ( 'NONE', ( #27286 ), #7304, .F. ) ;
#44794=ORIENTED_EDGE ( 'NONE', *, *, #50182, .T. ) ;
#44806=CARTESIAN_POINT ( 'NONE',  ( 0.5997462898726536595, 28.52220283460682282, -39.97543715340528081 ) ) ;
#44807=CARTESIAN_POINT ( 'NONE',  ( 4.694002226626921015, 23.92658369670245833, -38.80468224391004384 ) ) ;
#44808=VERTEX_POINT ( 'NONE', #18207 ) ;
#44812=ORIENTED_EDGE ( 'NONE', *, *, #28427, .T. ) ;
#44815=CARTESIAN_POINT ( 'NONE',  ( -6.077587904424778920, 9.976910903712887801, 16.46988980574263906 ) ) ;
#44816=ORIENTED_EDGE ( 'NONE', *, *, #28422, .T. ) ;
#44818=CARTESIAN_POINT ( 'NONE',  ( 0.8744876279028306332, -49.08725279547490317, 0.8897546699139438076 ) ) ;
#44827=FACE_OUTER_BOUND ( 'NONE', #13976, .T. ) ;
#44828=CARTESIAN_POINT ( 'NONE',  ( 0.7413678028165011646, -35.88962831636828099, -25.62070785679388152 ) ) ;
#44831=FACE_OUTER_BOUND ( 'NONE', #14058, .T. ) ;
#44833=CARTESIAN_POINT ( 'NONE',  ( 0.8753041380234530822, 46.87455897190329068, 14.62580080072681099 ) ) ;
#44846=AXIS2_PLACEMENT_3D ( 'NONE', #22019, #41144, #51115 ) ;
#44854=CARTESIAN_POINT ( 'NONE',  ( 2.648799415243696664, -0.1860685961553510681, -49.03552632293368418 ) ) ;
#44856=CARTESIAN_POINT ( 'NONE',  ( 0.6000166863083090663, -47.63401213562553949, -11.95091500980295507 ) ) ;
#44859=CARTESIAN_POINT ( 'NONE',  ( 0.5980271706414711508, 32.49685829779699731, 36.82395203688170682 ) ) ;
#44865=CARTESIAN_POINT ( 'NONE',  ( 0.6026777506516368677, -45.45291013477714159, 18.58976468159541895 ) ) ;
#44866=CIRCLE ( 'NONE', #33858, 48.91267123290010943 ) ;
#44870=CARTESIAN_POINT ( 'NONE',  ( 0.7413678028165010536, -2.345741242198491339, -44.03389137692570898 ) ) ;
#44872=CARTESIAN_POINT ( 'NONE',  ( 4.553261556744875094, -41.75933753256810377, 13.62707946203756393 ) ) ;
#44876=CARTESIAN_POINT ( 'NONE',  ( 2.299652685299201860, 26.98654338430133848, 40.93907914237171752 ) ) ;
#44880=CARTESIAN_POINT ( 'NONE',  ( 0.1365634738349403854, 3.602546085856351610, 43.97595117018536826 ) ) ;
#44886=VECTOR ( 'NONE', #14868, 1000.000000000000000 ) ;
#44887=ORIENTED_EDGE ( 'NONE', *, *, #26645, .T. ) ;
#44895=CARTESIAN_POINT ( 'NONE',  ( 0.3676999524040323597, -44.10520818713899871, -0.8253448321555690859 ) ) ;
#44898=CARTESIAN_POINT ( 'NONE',  ( -2.739355103387248747, -9.100462108390502181, 11.83339158334438324 ) ) ;
#44900=CARTESIAN_POINT ( 'NONE',  ( 0.1129192098497447394, 43.21532672376840623, -8.909956450123800664 ) ) ;
#44906=VERTEX_POINT ( 'NONE', #610 ) ;
#44908=CARTESIAN_POINT ( 'NONE',  ( -6.077587904424778920, -18.90214787454603851, -3.674891443665424973 ) ) ;
#44910=CARTESIAN_POINT ( 'NONE',  ( 3.727782113643637096, 13.15907417876901242, -41.94778352504015828 ) ) ;
#44922=CARTESIAN_POINT ( 'NONE',  ( 4.553261556744875094, -41.61700166486733110, -14.05577241741153216 ) ) ;
#44923=CARTESIAN_POINT ( 'NONE',  ( 4.226256110419179812, -14.78729662703991465, -41.37829272035182981 ) ) ;
#44929=CARTESIAN_POINT ( 'NONE',  ( 0.5997462898726536595, 41.43917033312096265, 26.35046094941977302 ) ) ;
#44931=CARTESIAN_POINT ( 'NONE',  ( 1.296416391601052709, 41.46295787682408474, -14.93755328629393198 ) ) ;
#44934=FACE_OUTER_BOUND ( 'NONE', #2056, .T. ) ;
#44939=CARTESIAN_POINT ( 'NONE',  ( 0.6008122571543326185, 48.97685995893719024, -3.580745596656180307 ) ) ;
#44945=EDGE_CURVE ( 'NONE', #25014, #29362, #24188, .T. ) ;
#44949=CARTESIAN_POINT ( 'NONE',  ( 4.553261556744873317, 1.182159483579998449, -43.91061448874312845 ) ) ;
#44956=CIRCLE ( 'NONE', #45945, 43.92652462719577500 ) ;
#44959=EDGE_LOOP ( 'NONE', ( #49429, #14765, #30273, #10043 ) ) ;
#44963=CARTESIAN_POINT ( 'NONE',  ( -4.915099999999999802, 12.80000000000000071, 0.000000000000000000 ) ) ;
#44967=FACE_OUTER_BOUND ( 'NONE', #53466, .T. ) ;
#44968=VECTOR ( 'NONE', #1190, 1000.000000000000000 ) ;
#44971=CARTESIAN_POINT ( 'NONE',  ( 0.6029443199889047422, -7.837513239273773635, 48.47794372782958305 ) ) ;
#44977=LINE ( 'NONE', #39659, #19771 ) ;
#44986=CARTESIAN_POINT ( 'NONE',  ( 4.553261556744873317, -9.554252317234828595, 42.87488575474283437 ) ) ;
#44989=CARTESIAN_POINT ( 'NONE',  ( 5.901764892641288895, -41.01701952799378859, 26.75061824481547035 ) ) ;
#44994=CARTESIAN_POINT ( 'NONE',  ( 1.112077966505211846, 21.31368232310758515, 38.58441746298893804 ) ) ;
#44998=EDGE_CURVE ( 'NONE', #46130, #28495, #18217, .T. ) ;
#45005=CARTESIAN_POINT ( 'NONE',  ( 4.975610109902397937, -4.123593823331679786, -48.73854102369041641 ) ) ;
#45007=CARTESIAN_POINT ( 'NONE',  ( 0.1154773475650540115, 44.02163660921988964, -3.006516304947005391 ) ) ;
#45008=DIRECTION ( 'NONE',  ( -1.000000000000000000, -0.000000000000000000, -0.000000000000000000 ) ) ;
#45009=CARTESIAN_POINT ( 'NONE',  ( 4.975610109902397937, 45.55079628452135410, -17.82061629079668919 ) ) ;
#45012=B_SPLINE_CURVE_WITH_KNOTS ( 'NONE', 3,
 ( #1294, #30124, #30742, #21359, #2223, #39879, #20430, #49539, #58613, #16664, #15742, #35162, #1603, #35473, #6596, #20743 ),
 .UNSPECIFIED., .F., .F.,
 ( 4, 3, 3, 3, 3, 4 ),
 ( 2.194378057379452319E-17, 0.0002612764279487727291, 0.0003919131003184784861, 0.0005225497727000646053, 0.0007837925190632442701, 0.001045051706266716951 ),
 .UNSPECIFIED. ) ;
#45013=CARTESIAN_POINT ( 'NONE',  ( 2.359973842542475442, 36.05128472766631376, -25.26738538347871454 ) ) ;
#45015=CARTESIAN_POINT ( 'NONE',  ( 0.1129192098497455998, 24.84520063729130612, 36.46461014570008530 ) ) ;
#45017=ORIENTED_EDGE ( 'NONE', *, *, #1734, .F. ) ;
#45025=CARTESIAN_POINT ( 'NONE',  ( 0.1139756605157203617, -22.53279618253801786, 37.93716272853338012 ) ) ;
#45028=EDGE_CURVE ( 'NONE', #26582, #35321, #48127, .T. ) ;
#45030=ORIENTED_EDGE ( 'NONE', *, *, #38478, .T. ) ;
#45033=CARTESIAN_POINT ( 'NONE',  ( -6.079354080745853928, -18.90066517279539582, 3.682093327720148412 ) ) ;
#45034=CARTESIAN_POINT ( 'NONE',  ( 0.6029443449137436017, 37.36442650921991770, 31.86595627971074052 ) ) ;
#45035=ORIENTED_EDGE ( 'NONE', *, *, #12400, .T. ) ;
#45041=CARTESIAN_POINT ( 'NONE',  ( 0.7044674535453004927, 28.78324386660388257, 39.79104918604833330 ) ) ;
#45046=CARTESIAN_POINT ( 'NONE',  ( 0.6039202388192953519, -39.25113122883277583, 29.51122515426866499 ) ) ;
#45047=VERTEX_POINT ( 'NONE', #20976 ) ;
#45049=CARTESIAN_POINT ( 'NONE',  ( 0.5997462898726536595, 11.43624519451716992, -47.75734421002901797 ) ) ;
#45058=ORIENTED_EDGE ( 'NONE', *, *, #16358, .F. ) ;
#45065=CARTESIAN_POINT ( 'NONE',  ( 0.1156867017252034141, -43.77771965051793757, 5.518520587606961847 ) ) ;
#45072=ADVANCED_FACE ( 'NONE', ( #7462 ), #56538, .F. ) ;
#45074=CARTESIAN_POINT ( 'NONE',  ( 0.2279481005628716528, 29.09488030924818247, 33.16611865840550166 ) ) ;
#45075=CARTESIAN_POINT ( 'NONE',  ( 0.9268187852002115479, 30.36697088607808936, 31.96250009171234296 ) ) ;
#45079=ORIENTED_EDGE ( 'NONE', *, *, #5955, .F. ) ;
#45084=CARTESIAN_POINT ( 'NONE',  ( 4.975610109902397937, 20.32389311291233724, -44.49032227207044343 ) ) ;
#45099=CARTESIAN_POINT ( 'NONE',  ( 2.299652685299203192, -34.31474700355062879, -35.02541738424348949 ) ) ;
#45114=DIRECTION ( 'NONE',  ( 0.09722883295013597105, 0.5631913828983523551, 0.8205863880617298989 ) ) ;
#45116=ADVANCED_FACE ( 'NONE', ( #37560 ), #22529, .F. ) ;
#45118=ORIENTED_EDGE ( 'NONE', *, *, #25639, .F. ) ;
#45121=ORIENTED_EDGE ( 'NONE', *, *, #9870, .T. ) ;
#45122=CARTESIAN_POINT ( 'NONE',  ( -6.079354080745853928, 13.83333621898001375, -13.39521423124011612 ) ) ;
#45123=ORIENTED_EDGE ( 'NONE', *, *, #41286, .T. ) ;
#45127=VERTEX_POINT ( 'NONE', #56629 ) ;
#45131=VERTEX_POINT ( 'NONE', #36626 ) ;
#45135=CARTESIAN_POINT ( 'NONE',  ( 0.6008123274975392114, -25.08365429764632282, -42.21806293797273213 ) ) ;
#45136=CARTESIAN_POINT ( 'NONE',  ( 4.335381028904201628, -33.67825942593249522, -35.57431221687826906 ) ) ;
#45142=ORIENTED_EDGE ( 'NONE', *, *, #1619, .F. ) ;
#45146=( BOUNDED_SURFACE ( )  B_SPLINE_SURFACE ( 3, 1, ( 
 ( #4111, #16167 ),
 ( #23250, #59051 ),
 ( #35279, #11462 ),
 ( #51118, #30546 ) ),
 .UNSPECIFIED., .F., .F., .F. ) 
 B_SPLINE_SURFACE_WITH_KNOTS ( ( 4, 4 ),
 ( 2, 2 ),
 ( 0.000000000000000000, 1.000000000000000000 ),
 ( 0.000000000000000000, 1.000000000000000000 ),
 .UNSPECIFIED. ) 
 GEOMETRIC_REPRESENTATION_ITEM ( )  RATIONAL_B_SPLINE_SURFACE ( (
 ( 1.000000000000000000, 1.000000000000000000),
 ( 0.7211978278499968642, 0.9934217856018975334),
 ( 0.7211978278499968642, 0.9934217856018975334),
 ( 1.000000000000000000, 1.000000000000000000) ) ) 
 REPRESENTATION_ITEM ( '' )  SURFACE ( )  );
#45147=CARTESIAN_POINT ( 'NONE',  ( 4.553261556744873317, 38.38432632180467863, 21.35844232721216684 ) ) ;
#45148=CARTESIAN_POINT ( 'NONE',  ( -6.078457390727109555, 13.82950465835804188, -13.39922803529968931 ) ) ;
#45150=ORIENTED_EDGE ( 'NONE', *, *, #48881, .F. ) ;
#45161=EDGE_CURVE ( 'NONE', #28569, #5258, #22711, .T. ) ;
#45162=CARTESIAN_POINT ( 'NONE',  ( 0.1365634738349413013, 39.47324950736464189, 19.71611505729723746 ) ) ;
#45164=( LENGTH_UNIT ( ) NAMED_UNIT ( * ) SI_UNIT ( .MILLI., .METRE. ) );
#45169=CARTESIAN_POINT ( 'NONE',  ( 0.1152809850208375703, -35.49359372161672610, 26.21354778000421959 ) ) ;
#45170=B_SPLINE_CURVE_WITH_KNOTS ( 'NONE', 3,
 ( #17557, #56668, #25783, #11703, #41381, #17869, #36994, #30782, #37290, #3128, #22257, #60435, #36674, #55745, #31966, #51046, #8144, #27260, #46685, #3734, #22868, #42000, #61063, #18175, #47290 ),
 .UNSPECIFIED., .F., .F.,
 ( 4, 3, 3, 3, 3, 3, 3, 3, 4 ),
 ( 4.670885906470169154E-18, 0.0005656085177311388811, 0.001131215744874498755, 0.001696821861372765049, 0.002262427090022497284, 0.002828031679238745925, 0.003393635864401604862, 0.003977030878808131623, 0.004561030005651159000 ),
 .UNSPECIFIED. ) ;
#45172=CARTESIAN_POINT ( 'NONE',  ( 4.553261556744873317, 22.96401893593727550, 37.44587293859699173 ) ) ;
#45175=DIRECTION ( 'NONE',  ( 0.000000000000000000, 0.000000000000000000, 1.000000000000000000 ) ) ;
#45178=CARTESIAN_POINT ( 'NONE',  ( 0.1149546198390367924, 36.82985107031473859, 24.30038343651506949 ) ) ;
#45181=CARTESIAN_POINT ( 'NONE',  ( 2.533389852662419894, -2.991380632221138924, -43.91471477360168052 ) ) ;
#45185=CARTESIAN_POINT ( 'NONE',  ( 0.5997462898726536595, -20.35457962188229430, 44.69052157405150183 ) ) ;
#45186=CARTESIAN_POINT ( 'NONE',  ( 0.1129192098497447394, -31.35755906439637641, 31.04279751098549056 ) ) ;
#45189=AXIS2_PLACEMENT_3D ( 'NONE', #3446, #9087, #46712 ) ;
#45195=ORIENTED_EDGE ( 'NONE', *, *, #8855, .T. ) ;
#45198=EDGE_LOOP ( 'NONE', ( #36771, #35409, #51683, #11148 ) ) ;
#45203=ORIENTED_EDGE ( 'NONE', *, *, #48881, .T. ) ;
#45207=CARTESIAN_POINT ( 'NONE',  ( 4.553261556744873317, 35.06776520399894537, -26.45357082552063233 ) ) ;
#45215=EDGE_CURVE ( 'NONE', #13981, #60643, #13082, .T. ) ;
#45216=CARTESIAN_POINT ( 'NONE',  ( 0.6000166863083106206, 17.45040302316649061, -45.90541270958705411 ) ) ;
#45217=CARTESIAN_POINT ( 'NONE',  ( 2.185380717157383135, 13.84901153640016425, -41.79742435284565971 ) ) ;
#45230=CARTESIAN_POINT ( 'NONE',  ( 3.727782113643637096, 42.34800052025986616, 11.80782062203034322 ) ) ;
#45234=CARTESIAN_POINT ( 'NONE',  ( 2.706805983486680223, -14.09998663259384344, -41.68892527135270143 ) ) ;
#45235=CARTESIAN_POINT ( 'NONE',  ( 0.2940135542859007023, 25.89542279162153093, 35.71648956902944150 ) ) ;
#45242=DIRECTION ( 'NONE',  ( -1.000000000000000000, -0.000000000000000000, -0.000000000000000000 ) ) ;
#45251=VERTEX_POINT ( 'NONE', #24988 ) ;
#45254=CARTESIAN_POINT ( 'NONE',  ( 4.390527457369401532, 1.728762144854961935, -43.89984872496869883 ) ) ;
#45261=ORIENTED_EDGE ( 'NONE', *, *, #12026, .T. ) ;
#45274=CARTESIAN_POINT ( 'NONE',  ( 0.7948878604505662526, -19.07805348859470129, 45.24076173523978639 ) ) ;
#45275=VERTEX_POINT ( 'NONE', #24366 ) ;
#45276=CARTESIAN_POINT ( 'NONE',  ( 0.6008123274975389894, -48.75817511408605043, 5.847641464947805012 ) ) ;
#45280=ORIENTED_EDGE ( 'NONE', *, *, #15808, .T. ) ;
#45286=ORIENTED_EDGE ( 'NONE', *, *, #46334, .T. ) ;
#45288=ADVANCED_FACE ( 'NONE', ( #10895 ), #33006, .F. ) ;
#45294=EDGE_CURVE ( 'NONE', #2310, #44540, #29668, .T. ) ;
#45295=CARTESIAN_POINT ( 'NONE',  ( 0.08486401232817714080, 0.000000000000000000, 0.000000000000000000 ) ) ;
#45297=CARTESIAN_POINT ( 'NONE',  ( 0.5987334308729317378, -14.55165157869310377, -46.90215712418830663 ) ) ;
#45298=FACE_OUTER_BOUND ( 'NONE', #50238, .T. ) ;
#45301=CARTESIAN_POINT ( 'NONE',  ( 0.3676999524040366896, -32.25712563511761743, -30.09033780274121739 ) ) ;
#45305=EDGE_CURVE ( 'NONE', #14671, #17907, #42878, .T. ) ;
#45310=ADVANCED_FACE ( 'NONE', ( #10271 ), #13764, .F. ) ;
#45337=CARTESIAN_POINT ( 'NONE',  ( 0.5997462898726536595, 37.05192695178125462, 32.22896739432052016 ) ) ;
#45342=ORIENTED_EDGE ( 'NONE', *, *, #52746, .F. ) ;
#45347=CARTESIAN_POINT ( 'NONE',  ( 0.2940135542859018680, -6.245378429118067842, 43.67191084631547682 ) ) ;
#45353=EDGE_LOOP ( 'NONE', ( #30315, #60336, #39865, #54913 ) ) ;
#45356=ORIENTED_EDGE ( 'NONE', *, *, #42873, .F. ) ;
#45358=B_SPLINE_CURVE_WITH_KNOTS ( 'NONE', 3,
 ( #58119, #25544, #6714, #54032, #11155, #1718, #35273, #6103, #49971, #49654, #25854, #2029, #39992, #11457, #39063, #30541, #26161, #44383, #11778, #1411, #44994, #58422, #34348, #21159, #39675 ),
 .UNSPECIFIED., .F., .F.,
 ( 4, 3, 3, 3, 3, 3, 3, 3, 4 ),
 ( 6.254634441385502288E-18, 0.0005656085177311393148, 0.001131215744874498755, 0.001696821861372764615, 0.002262427090022497284, 0.002828031679238743323, 0.003393635864401603128, 0.003977030878808130755, 0.004561030005651158133 ),
 .UNSPECIFIED. ) ;
#45362=EDGE_LOOP ( 'NONE', ( #44198, #13160, #5878, #25986 ) ) ;
#45364=LINE ( 'NONE', #22155, #48427 ) ;
#45365=CARTESIAN_POINT ( 'NONE',  ( 0.1158403557922069033, -43.76671389845916593, 5.604914068408183958 ) ) ;
#45376=CARTESIAN_POINT ( 'NONE',  ( 0.3676999524040366896, 30.26295534861856495, 32.09523511193457068 ) ) ;
#45382=DIRECTION ( 'NONE',  ( -1.000000000000000000, 0.000000000000000000, -0.000000000000000000 ) ) ;
#45389=FACE_OUTER_BOUND ( 'NONE', #21790, .T. ) ;
#45390=CARTESIAN_POINT ( 'NONE',  ( 0.6021447746440204973, 4.975436559605085129, 48.85474562547464217 ) ) ;
#45392=CARTESIAN_POINT ( 'NONE',  ( 0.1129192098497447394, -13.01845098534572820, -42.16007260106777466 ) ) ;
#45395=( BOUNDED_SURFACE ( )  B_SPLINE_SURFACE ( 3, 1, ( 
 ( #32159, #27442 ),
 ( #41883, #60951 ),
 ( #47802, #42804 ),
 ( #42496, #14294 ) ),
 .UNSPECIFIED., .F., .F., .F. ) 
 B_SPLINE_SURFACE_WITH_KNOTS ( ( 4, 4 ),
 ( 2, 2 ),
 ( 0.000000000000000000, 1.000000000000000000 ),
 ( 0.000000000000000000, 1.000000000000000000 ),
 .UNSPECIFIED. ) 
 GEOMETRIC_REPRESENTATION_ITEM ( )  RATIONAL_B_SPLINE_SURFACE ( (
 ( 1.000000000000000000, 1.000000000000000000),
 ( 0.7211978278499970862, 0.9934217856018976445),
 ( 0.7211978278499970862, 0.9934217856018976445),
 ( 1.000000000000000000, 1.000000000000000000) ) ) 
 REPRESENTATION_ITEM ( '' )  SURFACE ( )  );
#45400=CARTESIAN_POINT ( 'NONE',  ( 0.7242486021783829386, 40.69929259474984207, 27.46960219335028697 ) ) ;
#45414=CARTESIAN_POINT ( 'NONE',  ( 0.6028777368367060907, -14.05586561488587272, 47.05286889369597247 ) ) ;
#45425=CARTESIAN_POINT ( 'NONE',  ( 0.1158816050234199313, 20.41415249631641515, 39.11782738295033823 ) ) ;
#45429=B_SPLINE_CURVE_WITH_KNOTS ( 'NONE', 3,
 ( #61775, #38038, #9798, #56474, #38637, #47404 ),
 .UNSPECIFIED., .F., .F.,
 ( 4, 2, 4 ),
 ( 1.553373257785006303E-17, 0.0002293755540694304511, 0.0004587511081388453982 ),
 .UNSPECIFIED. ) ;
#45435=CARTESIAN_POINT ( 'NONE',  ( 2.648799415243696664, 12.25810282899351300, -47.47900987092526748 ) ) ;
#45446=EDGE_CURVE ( 'NONE', #54914, #42575, #16724, .T. ) ;
#45448=CARTESIAN_POINT ( 'NONE',  ( 0.8744876279028306332, 11.79038800009151089, 47.65854384249261244 ) ) ;
#45451=ORIENTED_EDGE ( 'NONE', *, *, #419, .T. ) ;
#45455=B_SPLINE_CURVE_WITH_KNOTS ( 'NONE', 3,
 ( #30631, #21250, #41605, #50363, #35989, #21559, #59763, #31892, #12178, #41010, #11553, #16874, #46304, #2114, #40382, #16552 ),
 .UNSPECIFIED., .F., .F.,
 ( 4, 3, 3, 3, 3, 4 ),
 ( 2.194378057379452319E-17, 0.0002612764279487742470, 0.0003919131003184743662, 0.0005225497727000644969, 0.0007837925190632463301, 0.001045051706266715650 ),
 .UNSPECIFIED. ) ;
#45459=CARTESIAN_POINT ( 'NONE',  ( -6.078726893082806448, 18.62710865126535253, -4.881072071038842886 ) ) ;
#45465=EDGE_LOOP ( 'NONE', ( #2165, #24620, #54605, #26420 ) ) ;
#45467=CARTESIAN_POINT ( 'NONE',  ( -6.077587904424778920, 0.6233693561568425245, 19.24597183931575373 ) ) ;
#45468=CARTESIAN_POINT ( 'NONE',  ( 0.1365634738349421895, 9.196489050310102442, 43.15422585067162942 ) ) ;
#45471=FACE_OUTER_BOUND ( 'NONE', #17170, .T. ) ;
#45478=DIRECTION ( 'NONE',  ( 0.000000000000000000, 0.000000000000000000, 1.000000000000000000 ) ) ;
#45479=CARTESIAN_POINT ( 'NONE',  ( 0.5549461598389365813, -42.43107887862065297, 12.03416971224342014 ) ) ;
#45483=CARTESIAN_POINT ( 'NONE',  ( 0.8744876279028263033, 44.61213666265857825, -20.49651952824592982 ) ) ;
#45487=CARTESIAN_POINT ( 'NONE',  ( 0.5987334363312687424, -45.28813410862901634, -18.98809667741633334 ) ) ;
#45490=EDGE_CURVE ( 'NONE', #60982, #10029, #29473, .T. ) ;
#45492=CARTESIAN_POINT ( 'NONE',  ( 0.7044674535453004927, 11.74740322167597029, 47.68439199946104878 ) ) ;
#45494=ORIENTED_EDGE ( 'NONE', *, *, #44332, .F. ) ;
#45497=ORIENTED_EDGE ( 'NONE', *, *, #7195, .T. ) ;
#45505=ADVANCED_FACE ( 'NONE', ( #56556 ), #27280, .F. ) ;
#45509=CARTESIAN_POINT ( 'NONE',  ( 2.009741617377216460, -37.68148372272431601, 22.79495255702692091 ) ) ;
#45516=CARTESIAN_POINT ( 'NONE',  ( 4.226256110419179812, 12.89805166227863253, -42.00556526585945960 ) ) ;
#45519=CARTESIAN_POINT ( 'NONE',  ( 2.706805983486679779, 8.171905273964574334, -43.24345126736654521 ) ) ;
#45521=ORIENTED_EDGE ( 'NONE', *, *, #42372, .F. ) ;
#45522=ORIENTED_EDGE ( 'NONE', *, *, #21466, .F. ) ;
#45524=CARTESIAN_POINT ( 'NONE',  ( 1.296416391601052709, 42.16328716573016777, 12.82827305042783550 ) ) ;
#45527=EDGE_CURVE ( 'NONE', #17512, #3481, #42161, .T. ) ;
#45528=EDGE_CURVE ( 'NONE', #60472, #45275, #7945, .T. ) ;
#45530=VECTOR ( 'NONE', #1878, 1000.000000000000000 ) ;
#45539=DIRECTION ( 'NONE',  ( 0.000000000000000000, 0.000000000000000000, 1.000000000000000000 ) ) ;
#45540=CARTESIAN_POINT ( 'NONE',  ( 0.8744876279028263033, 10.05549467470504865, 48.05452192277508061 ) ) ;
#45541=CARTESIAN_POINT ( 'NONE',  ( 4.975610109902397937, 47.16372689271652519, 12.96272628450595832 ) ) ;
#45548=ORIENTED_EDGE ( 'NONE', *, *, #25512, .T. ) ;
#45551=CARTESIAN_POINT ( 'NONE',  ( 1.112077966505211624, 3.186402742498017027, -43.96449889048157189 ) ) ;
#45554=VERTEX_POINT ( 'NONE', #5155 ) ;
#45564=CARTESIAN_POINT ( 'NONE',  ( 0.5980271706414711508, 46.82647351461041296, -14.80981502339418476 ) ) ;
#45565=EDGE_CURVE ( 'NONE', #47165, #18280, #9279, .T. ) ;
#45566=VERTEX_POINT ( 'NONE', #13989 ) ;
#45572=DIRECTION ( 'NONE',  ( -0.1011922191286467460, 0.2707140367831962213, 0.9573265091265185101 ) ) ;
#45577=DIRECTION ( 'NONE',  ( -1.000000000000000000, -0.000000000000000000, -0.000000000000000000 ) ) ;
#45579=CARTESIAN_POINT ( 'NONE',  ( 2.185380717157383135, -43.83117064034907173, -4.200985999000810267 ) ) ;
#45582=FACE_OUTER_BOUND ( 'NONE', #27529, .T. ) ;
#45594=CARTESIAN_POINT ( 'NONE',  ( -6.077587904424778920, 0.6110050725292486273, -19.24636833782607681 ) ) ;
#45602=CARTESIAN_POINT ( 'NONE',  ( 1.479689385636123067, -32.45943909685134798, -29.79880297571515513 ) ) ;
#45610=CARTESIAN_POINT ( 'NONE',  ( 0.6039202388192953519, -47.54548494440594197, -12.28782219314147639 ) ) ;
#45616=CARTESIAN_POINT ( 'NONE',  ( 4.834790513006555379, 24.09885983197582249, -40.64276437108040341 ) ) ;
#45620=VECTOR ( 'NONE', #39329, 1000.000000000000114 ) ;
#45622=DIRECTION ( 'NONE',  ( -0.1011922191286467598, -0.4715280952439284690, 0.8760259072558600479 ) ) ;
#45623=EDGE_CURVE ( 'NONE', #30625, #50534, #40719, .T. ) ;
#45626=CARTESIAN_POINT ( 'NONE',  ( -2.601141883200662974, 8.903211435100862658, 11.98032777561940776 ) ) ;
#45630=ORIENTED_EDGE ( 'NONE', *, *, #57053, .F. ) ;
#45637=VERTEX_POINT ( 'NONE', #50249 ) ;
#45640=CARTESIAN_POINT ( 'NONE',  ( 0.6029443199889047422, 49.00651436223474633, 3.146298129307232294 ) ) ;
#45643=CARTESIAN_POINT ( 'NONE',  ( 0.2940135542859022566, 33.06489085126945326, -29.20536837098717342 ) ) ;
#45647=EDGE_CURVE ( 'NONE', #26055, #7202, #44376, .T. ) ;
#45648=CARTESIAN_POINT ( 'NONE',  ( 0.3676999524040366896, -6.224421213753956295, 43.67158302462379282 ) ) ;
#45650=CARTESIAN_POINT ( 'NONE',  ( 0.6039202388192953519, -8.009480623389540810, -48.45009734760640896 ) ) ;
#45653=EDGE_CURVE ( 'NONE', #44540, #51774, #30210, .T. ) ;
#45660=ORIENTED_EDGE ( 'NONE', *, *, #12560, .T. ) ;
#45666=VECTOR ( 'NONE', #8326, 1000.000000000000227 ) ;
#45681=DIRECTION ( 'NONE',  ( 0.1011922191286468153, 0.9400526519483254351, -0.3256703031483533795 ) ) ;
#45697=CARTESIAN_POINT ( 'NONE',  ( -6.078726893082806448, -11.01948708261720178, -15.79129335123480971 ) ) ;
#45698=CARTESIAN_POINT ( 'NONE',  ( 0.2940133293163018635, 30.25014500077257651, -32.11182456682082176 ) ) ;
#45699=CARTESIAN_POINT ( 'NONE',  ( 0.5987334363312688534, 4.112662775261645365, 48.93515005973777932 ) ) ;
#45700=CARTESIAN_POINT ( 'NONE',  ( -6.077587904424778920, -18.27702681447043886, -6.061873655649631765 ) ) ;
#45706=VERTEX_POINT ( 'NONE', #25510 ) ;
#45712=CARTESIAN_POINT ( 'NONE',  ( -6.077587904424778920, 5.472951620448720078, -18.46192898789718129 ) ) ;
#45715=CARTESIAN_POINT ( 'NONE',  ( -6.063463321072278589, -12.95783560055447658, 14.24482183210702679 ) ) ;
#45717=ORIENTED_EDGE ( 'NONE', *, *, #21092, .T. ) ;
#45721=CARTESIAN_POINT ( 'NONE',  ( 0.1365634738349423560, 43.98722388068600253, 3.462189320886016386 ) ) ;
#45723=CARTESIAN_POINT ( 'NONE',  ( 0.8753041380234471980, 40.66072100792138144, 27.52896828776844629 ) ) ;
#45728=CARTESIAN_POINT ( 'NONE',  ( 5.901764892641307547, 1.612679500413873201, -48.94272910523709896 ) ) ;
#45730=DIRECTION ( 'NONE',  ( 0.09722883295013595717, -0.7096678276952366193, -0.6977951908529310687 ) ) ;
#45737=CARTESIAN_POINT ( 'NONE',  ( 4.553261556744875094, 0.000000000000000000, 0.000000000000000000 ) ) ;
#45743=CARTESIAN_POINT ( 'NONE',  ( 4.975610109902397937, 0.9924324126403755164, 48.90260202733708894 ) ) ;
#45746=CARTESIAN_POINT ( 'NONE',  ( 1.296416391601052709, 5.336661527168872432, 43.74731326402337572 ) ) ;
#45748=ORIENTED_EDGE ( 'NONE', *, *, #51915, .T. ) ;
#45749=B_SPLINE_CURVE_WITH_KNOTS ( 'NONE', 3,
 ( #25202, #6369, #20823, #11423, #1998, #44346 ),
 .UNSPECIFIED., .F., .F.,
 ( 4, 2, 4 ),
 ( 1.910620358896493634E-17, 0.0002293755540694310746, 0.0004587511081388430129 ),
 .UNSPECIFIED. ) ;
#45751=CARTESIAN_POINT ( 'NONE',  ( 0.6000166863083090663, 44.47108027094633087, -20.83618250168446195 ) ) ;
#45756=CARTESIAN_POINT ( 'NONE',  ( 0.9268187852002115479, -34.73073342105909944, 27.15751256915762113 ) ) ;
#45759=( GEOMETRIC_REPRESENTATION_CONTEXT ( 3 ) GLOBAL_UNCERTAINTY_ASSIGNED_CONTEXT ( ( #18581 ) ) GLOBAL_UNIT_ASSIGNED_CONTEXT ( ( #15714, #11014, #7831 ) ) REPRESENTATION_CONTEXT ( 'NONE', 'WORKASPACE' ) );
#45760=B_SPLINE_CURVE_WITH_KNOTS ( 'NONE', 3,
 ( #14482, #39, #57350, #51741, #38301, #42682 ),
 .UNSPECIFIED., .F., .F.,
 ( 4, 2, 4 ),
 ( 0.000000000000000000, 0.0002447195606305744751, 0.0004894391212611489501 ),
 .UNSPECIFIED. ) ;
#45761=ORIENTED_EDGE ( 'NONE', *, *, #38552, .T. ) ;
#45763=CARTESIAN_POINT ( 'NONE',  ( 3.240649175237396484, 26.64593727015325086, -35.00369901014332186 ) ) ;
#45764=ORIENTED_EDGE ( 'NONE', *, *, #30191, .T. ) ;
#45766=CARTESIAN_POINT ( 'NONE',  ( 0.1119899015040011353, 39.50795633840085941, 19.64898710253324410 ) ) ;
#45771=LINE ( 'NONE', #41086, #58793 ) ;
#45773=CARTESIAN_POINT ( 'NONE',  ( 0.1365634738349407185, 20.97116515538588999, -38.82103620009102940 ) ) ;
#45794=CARTESIAN_POINT ( 'NONE',  ( 1.479689385636123067, -42.30896271024097643, 12.30997642772440415 ) ) ;
#45798=CARTESIAN_POINT ( 'NONE',  ( 0.6021448801613057400, 44.35700409489896145, -21.07124406275206141 ) ) ;
#45804=CARTESIAN_POINT ( 'NONE',  ( 0.7044674535453004927, 49.05595398932692319, 2.305667150294545831 ) ) ;
#45805=ORIENTED_EDGE ( 'NONE', *, *, #18323, .F. ) ;
#45809=ORIENTED_EDGE ( 'NONE', *, *, #17307, .F. ) ;
#45811=CARTESIAN_POINT ( 'NONE',  ( -6.063463321072278589, 7.780528881867136093, 17.61487504349381794 ) ) ;
#45819=CARTESIAN_POINT ( 'NONE',  ( 0.1157506346131639274, 15.32596964082831903, 41.37699015601839392 ) ) ;
#45821=CARTESIAN_POINT ( 'NONE',  ( 0.8753041380234524160, 36.80657072176735056, -32.50253343320360244 ) ) ;
#45823=DIRECTION ( 'NONE',  ( 0.1011922191286467876, 0.9788975924247106386, 0.1775377096081985073 ) ) ;
#45830=CARTESIAN_POINT ( 'NONE',  ( 1.834102595619085507, 13.98314437153100975, -41.76924009773946267 ) ) ;
#45831=VERTEX_POINT ( 'NONE', #52090 ) ;
#45836=VECTOR ( 'NONE', #20573, 1000.000000000000000 ) ;
#45839=ORIENTED_EDGE ( 'NONE', *, *, #25746, .T. ) ;
#45848=EDGE_CURVE ( 'NONE', #48557, #16242, #46572, .T. ) ;
#45850=CARTESIAN_POINT ( 'NONE',  ( 0.6000166863083090663, 48.97316450298206547, 3.667784109283304783 ) ) ;
#45855=CARTESIAN_POINT ( 'NONE',  ( 3.894904216938897434, 40.96222025004743017, -15.94430445842042232 ) ) ;
#45858=LINE ( 'NONE', #35216, #22878 ) ;
#45859=( BOUNDED_SURFACE ( )  B_SPLINE_SURFACE ( 3, 1, ( 
 ( #2895, #22027 ),
 ( #17325, #7916 ),
 ( #21093, #50213 ),
 ( #17026, #16392 ) ),
 .UNSPECIFIED., .F., .F., .F. ) 
 B_SPLINE_SURFACE_WITH_KNOTS ( ( 4, 4 ),
 ( 2, 2 ),
 ( 0.000000000000000000, 1.000000000000000000 ),
 ( 0.000000000000000000, 1.000000000000000000 ),
 .UNSPECIFIED. ) 
 GEOMETRIC_REPRESENTATION_ITEM ( )  RATIONAL_B_SPLINE_SURFACE ( (
 ( 1.000000000000000000, 1.000000000000000000),
 ( 0.9953485035131437453, 0.8621029689291515030),
 ( 0.9953485035131437453, 0.8621029689291515030),
 ( 1.000000000000000000, 1.000000000000000000) ) ) 
 REPRESENTATION_ITEM ( '' )  SURFACE ( )  );
#45860=CARTESIAN_POINT ( 'NONE',  ( 0.6000166863083090663, 11.43688157230968017, -47.76003791465640091 ) ) ;
#45865=ORIENTED_EDGE ( 'NONE', *, *, #21326, .F. ) ;
#45868=CARTESIAN_POINT ( 'NONE',  ( 0.6016117650947689910, 16.63268918597161772, -46.20502899779809525 ) ) ;
#45869=CARTESIAN_POINT ( 'NONE',  ( 3.390910168358336918, 2.257738501152356303, -43.92037970457509033 ) ) ;
#45871=EDGE_CURVE ( 'NONE', #60330, #26558, #33326, .T. ) ;
#45875=CARTESIAN_POINT ( 'NONE',  ( -6.078457390727109555, 15.42941986619899097, 11.52074275513744261 ) ) ;
#45879=CARTESIAN_POINT ( 'NONE',  ( 0.3676999524040366896, -17.09834788623584600, 40.66444494744877858 ) ) ;
#45882=ORIENTED_EDGE ( 'NONE', *, *, #22859, .T. ) ;
#45883=CARTESIAN_POINT ( 'NONE',  ( 4.694002226626921015, 18.76791414987520668, -41.54575995103530772 ) ) ;
#45886=DIRECTION ( 'NONE',  ( 0.000000000000000000, 0.000000000000000000, 1.000000000000000000 ) ) ;
#45894=ORIENTED_EDGE ( 'NONE', *, *, #52376, .F. ) ;
#45898=CARTESIAN_POINT ( 'NONE',  ( 0.5997462898726536595, 16.46871699354542429, -46.26373299606095202 ) ) ;
#45900=VERTEX_POINT ( 'NONE', #6301 ) ;
#45902=CARTESIAN_POINT ( 'NONE',  ( 3.678834586032788234, -47.80915124093738200, 10.62532010103831581 ) ) ;
#45910=CONICAL_SURFACE ( 'NONE', #18894, 43.92652462719577500, 1.486293639869522343 ) ;
#45912=CARTESIAN_POINT ( 'NONE',  ( 0.1119898979215348395, -12.01552111793010091, 42.45690238955739204 ) ) ;
#45927=ORIENTED_EDGE ( 'NONE', *, *, #16479, .F. ) ;
#45934=LINE ( 'NONE', #33367, #7076 ) ;
#45939=CARTESIAN_POINT ( 'NONE',  ( 3.050102900204245682, 35.85168643609029004, -25.49670231356046202 ) ) ;
#45941=CARTESIAN_POINT ( 'NONE',  ( 0.6029443449137436017, -1.617468957629060400, 49.08078373614706891 ) ) ;
#45942=CARTESIAN_POINT ( 'NONE',  ( 4.553261556744873317, 22.57774691820481294, -37.68003330573274923 ) ) ;
#45945=AXIS2_PLACEMENT_3D ( 'NONE', #31526, #60024, #17432 ) ;
#45950=CARTESIAN_POINT ( 'NONE',  ( -2.739355103387248747, 14.87824819718638736, -1.218727834234153207 ) ) ;
#45960=CARTESIAN_POINT ( 'NONE',  ( 0.7413678028165009426, -44.08645218430292800, 0.9331803531016585884 ) ) ;
#45961=CARTESIAN_POINT ( 'NONE',  ( 0.1145239942831223490, -42.59710765884724282, -11.50790596960418100 ) ) ;
#45963=CARTESIAN_POINT ( 'NONE',  ( 0.6039202388192952409, -13.80541670804725740, -47.12721275830092083 ) ) ;
#45966=CARTESIAN_POINT ( 'NONE',  ( -6.078457390727109555, 12.00250936636397903, -15.05769836156418684 ) ) ;
#45971=CARTESIAN_POINT ( 'NONE',  ( 0.5549461598389365813, 39.34817863456808595, -19.92331633059426110 ) ) ;
#45974=VERTEX_POINT ( 'NONE', #20755 ) ;
#45976=B_SPLINE_CURVE_WITH_KNOTS ( 'NONE', 3,
 ( #20379, #5321, #57945, #29763, #25070, #24765, #39505, #58560, #53255, #39823, #44214, #35108, #10366, #1244, #25377, #24449, #53862, #15690, #43907, #58250, #43587, #948, #44828, #54167, #11286 ),
 .UNSPECIFIED., .F., .F.,
 ( 4, 3, 3, 3, 3, 3, 3, 3, 4 ),
 ( 5.553824967135426632E-18, 0.0005656085177311402905, 0.001131215744874499839, 0.001696821861372766567, 0.002262427090022498585, 0.002828031679238745925, 0.003393635864401606597, 0.003977030878808131623, 0.004561030005651159000 ),
 .UNSPECIFIED. ) ;
#45980=B_SPLINE_CURVE_WITH_KNOTS ( 'NONE', 3,
 ( #55310, #12429, #51538, #3922 ),
 .UNSPECIFIED., .F., .F.,
 ( 4, 4 ),
 ( 0.000000000000000000, 0.004442905043737213101 ),
 .UNSPECIFIED. ) ;
#45983=ORIENTED_EDGE ( 'NONE', *, *, #24454, .T. ) ;
#45987=CARTESIAN_POINT ( 'NONE',  ( 0.6024113833632039894, -48.67596287166193036, -6.495576003516191577 ) ) ;
#45991=CARTESIAN_POINT ( 'NONE',  ( 0.1135584504625007235, 43.22593930884824687, 8.858342000793420823 ) ) ;
#45994=B_SPLINE_CURVE_WITH_KNOTS ( 'NONE', 3,
 ( #54490, #21010, #1257, #30702 ),
 .UNSPECIFIED., .F., .F.,
 ( 4, 4 ),
 ( 0.000000000000000000, 0.005013413432710151114 ),
 .UNSPECIFIED. ) ;
#46010=EDGE_CURVE ( 'NONE', #36415, #25125, #27925, .T. ) ;
#46011=DIRECTION ( 'NONE',  ( 0.000000000000000000, 0.000000000000000000, -1.000000000000000000 ) ) ;
#46012=CARTESIAN_POINT ( 'NONE',  ( 0.8753041380234524160, 43.84722337925243352, -22.10337824412637175 ) ) ;
#46019=CARTESIAN_POINT ( 'NONE',  ( -6.079354080745853928, -11.01762705387068131, -15.79255677051625817 ) ) ;
#46021=CARTESIAN_POINT ( 'NONE',  ( 0.5997462898726536595, 23.17609050332929854, -43.29457771044543080 ) ) ;
#46026=CARTESIAN_POINT ( 'NONE',  ( 2.185380717157383579, 16.54900345444415066, 40.80380236855377518 ) ) ;
#46038=( BOUNDED_SURFACE ( )  B_SPLINE_SURFACE ( 3, 1, ( 
 ( #20301, #39424 ),
 ( #58476, #29995 ),
 ( #6157, #25294 ),
 ( #20604, #43507 ) ),
 .UNSPECIFIED., .F., .F., .F. ) 
 B_SPLINE_SURFACE_WITH_KNOTS ( ( 4, 4 ),
 ( 2, 2 ),
 ( 0.000000000000000000, 1.000000000000000000 ),
 ( 0.000000000000000000, 1.000000000000000000 ),
 .UNSPECIFIED. ) 
 GEOMETRIC_REPRESENTATION_ITEM ( )  RATIONAL_B_SPLINE_SURFACE ( (
 ( 1.000000000000000000, 1.000000000000000000),
 ( 0.7211978278499970862, 0.9934217856018976445),
 ( 0.7211978278499970862, 0.9934217856018976445),
 ( 1.000000000000000000, 1.000000000000000000) ) ) 
 REPRESENTATION_ITEM ( '' )  SURFACE ( )  );
#46041=ADVANCED_FACE ( 'NONE', ( #3779 ), #26543, .F. ) ;
#46042=CARTESIAN_POINT ( 'NONE',  ( -6.077587904424778920, -16.14165210942803341, -10.49967087922893150 ) ) ;
#46048=CARTESIAN_POINT ( 'NONE',  ( 2.648799415243696664, 41.83591888777205270, -25.57876764242867296 ) ) ;
#46051=CARTESIAN_POINT ( 'NONE',  ( 0.1157506346131639274, 20.49131570213115694, 39.07744414106975483 ) ) ;
#46053=CARTESIAN_POINT ( 'NONE',  ( 1.830465331921978356, 5.457173717480057640, -43.71035702091250386 ) ) ;
#46056=( BOUNDED_SURFACE ( )  B_SPLINE_SURFACE ( 3, 1, ( 
 ( #44149, #44451 ),
 ( #15616, #1791 ),
 ( #53785, #20919 ),
 ( #35345, #10601 ) ),
 .UNSPECIFIED., .F., .F., .F. ) 
 B_SPLINE_SURFACE_WITH_KNOTS ( ( 4, 4 ),
 ( 2, 2 ),
 ( 0.000000000000000000, 1.000000000000000000 ),
 ( 0.000000000000000000, 1.000000000000000000 ),
 .UNSPECIFIED. ) 
 GEOMETRIC_REPRESENTATION_ITEM ( )  RATIONAL_B_SPLINE_SURFACE ( (
 ( 1.000000000000000000, 1.000000000000000000),
 ( 0.9953485035131437453, 0.8621029689291523912),
 ( 0.9953485035131437453, 0.8621029689291523912),
 ( 1.000000000000000000, 1.000000000000000000) ) ) 
 REPRESENTATION_ITEM ( '' )  SURFACE ( )  );
#46061=CARTESIAN_POINT ( 'NONE',  ( 0.5997462898726536595, -25.00873172704203640, -42.26245340191634625 ) ) ;
#46065=CARTESIAN_POINT ( 'NONE',  ( -6.077587904424778920, -1.855182226446173921, 19.16648951426965652 ) ) ;
#46068=ORIENTED_EDGE ( 'NONE', *, *, #17706, .T. ) ;
#46071=CARTESIAN_POINT ( 'NONE',  ( -6.077587904424778920, -8.901182807328710922, -17.07527352707552382 ) ) ;
#46077=B_SPLINE_CURVE_WITH_KNOTS ( 'NONE', 3,
 ( #53714, #10846, #35272, #29939 ),
 .UNSPECIFIED., .F., .F.,
 ( 4, 4 ),
 ( 0.000000000000000000, 0.005013413432710140706 ),
 .UNSPECIFIED. ) ;
#46078=ORIENTED_EDGE ( 'NONE', *, *, #45305, .T. ) ;
#46081=EDGE_CURVE ( 'NONE', #23235, #31634, #52539, .T. ) ;
#46095=CARTESIAN_POINT ( 'NONE',  ( 0.6024113833632039894, -49.10696971218104068, -0.2177034400287303217 ) ) ;
#46099=ORIENTED_EDGE ( 'NONE', *, *, #22448, .F. ) ;
#46112=CARTESIAN_POINT ( 'NONE',  ( 0.9268187852002115479, -11.59048861154065513, 42.53721789979185530 ) ) ;
#46113=ORIENTED_EDGE ( 'NONE', *, *, #35882, .F. ) ;
#46115=ORIENTED_EDGE ( 'NONE', *, *, #11958, .T. ) ;
#46117=CARTESIAN_POINT ( 'NONE',  ( 0.1152809850208375703, 44.01881950007733479, 3.047755290269537287 ) ) ;
#46120=VERTEX_POINT ( 'NONE', #39119 ) ;
#46122=CIRCLE ( 'NONE', #10063, 48.91267123290010943 ) ;
#46123=CARTESIAN_POINT ( 'NONE',  ( 2.009741617377216460, -0.04086241258242288843, 44.03978210534519633 ) ) ;
#46126=CARTESIAN_POINT ( 'NONE',  ( 0.1147471544378676767, 15.52999974506124481, 41.30098420608936749 ) ) ;
#46127=CARTESIAN_POINT ( 'NONE',  ( 4.335381028904216727, 35.88831783935810193, -33.34344748710841344 ) ) ;
#46128=CARTESIAN_POINT ( 'NONE',  ( 2.706805983486679779, -37.50615468164787103, 23.02312911652235528 ) ) ;
#46130=VERTEX_POINT ( 'NONE', #23519 ) ;
#46132=B_SPLINE_CURVE_WITH_KNOTS ( 'NONE', 3,
 ( #13957, #55908, #23336, #61522, #27406, #18028, #37452, #56523, #18642, #46533, #33062, #47155, #52134, #26794, #27726, #22717 ),
 .UNSPECIFIED., .F., .F.,
 ( 4, 3, 3, 3, 3, 4 ),
 ( 2.221635811791082109E-17, 0.0002612764279487730002, 0.0003919131003184738241, 0.0005225497727000642800, 0.0007837925190632422101, 0.001045051706266712397 ),
 .UNSPECIFIED. ) ;
#46137=CARTESIAN_POINT ( 'NONE',  ( 0.9268187852002115479, 14.29204361781913946, -41.70721546848916006 ) ) ;
#46138=ORIENTED_EDGE ( 'NONE', *, *, #13745, .F. ) ;
#46141=CARTESIAN_POINT ( 'NONE',  ( 0.6027444965799114707, 27.98794771890257849, 40.35112511902756438 ) ) ;
#46142=CARTESIAN_POINT ( 'NONE',  ( -6.079354080745853928, -18.27537090945910947, 6.066611358069499360 ) ) ;
#46152=EDGE_CURVE ( 'NONE', #8500, #61919, #40597, .T. ) ;
#46153=CARTESIAN_POINT ( 'NONE',  ( 2.225817577893341337, -0.2642321622234031220, 49.03513408093338199 ) ) ;
#46154=CARTESIAN_POINT ( 'NONE',  ( 4.694002226626920127, 18.76791414987460982, 41.54575995103556352 ) ) ;
#46156=CARTESIAN_POINT ( 'NONE',  ( 0.7242003506639906885, -42.37567836115716347, 24.80551466020780538 ) ) ;
#46169=VERTEX_POINT ( 'NONE', #39737 ) ;
#46170=CARTESIAN_POINT ( 'NONE',  ( 0.6008123274975392114, 17.36800808579142341, -45.93372232130052879 ) ) ;
#46172=CARTESIAN_POINT ( 'NONE',  ( 0.6252788684277243991, 44.53702795073676413, 20.68568279001112842 ) ) ;
#46174=ORIENTED_EDGE ( 'NONE', *, *, #14308, .F. ) ;
#46175=CARTESIAN_POINT ( 'NONE',  ( -6.079354080745853928, 12.00682274379690817, -15.05420747987762020 ) ) ;
#46181=CARTESIAN_POINT ( 'NONE',  ( 4.553261556744873317, -25.31600221269608397, -35.89762663172042068 ) ) ;
#46182=CARTESIAN_POINT ( 'NONE',  ( 0.1129192098497447394, 43.40062318508790895, 7.958498283669150020 ) ) ;
#46183=ADVANCED_FACE ( 'NONE', ( #4382 ), #18024, .F. ) ;
#46184=ORIENTED_EDGE ( 'NONE', *, *, #54267, .T. ) ;
#46186=EDGE_CURVE ( 'NONE', #21995, #50764, #53964, .T. ) ;
#46187=CARTESIAN_POINT ( 'NONE',  ( 0.7044674535453004927, -42.37103341363683739, 24.82938280085469884 ) ) ;
#46188=B_SPLINE_CURVE_WITH_KNOTS ( 'NONE', 3,
 ( #44328, #39310, #14891, #14579 ),
 .UNSPECIFIED., .F., .F.,
 ( 4, 4 ),
 ( 0.000000000000000000, 0.005013413432710144176 ),
 .UNSPECIFIED. ) ;
#46191=EDGE_CURVE ( 'NONE', #16304, #27102, #35018, .T. ) ;
#46192=ORIENTED_EDGE ( 'NONE', *, *, #13368, .F. ) ;
#46195=CARTESIAN_POINT ( 'NONE',  ( 0.6029443199889047422, -48.70423496034977973, 6.279740343473172004 ) ) ;
#46198=CARTESIAN_POINT ( 'NONE',  ( 0.8744876279028306332, -29.90976330662902427, 38.93271258621624042 ) ) ;
#46201=VERTEX_POINT ( 'NONE', #36261 ) ;
#46204=CARTESIAN_POINT ( 'NONE',  ( 4.335381028904201628, 6.815065961880899970, -48.51094436928184450 ) ) ;
#46207=VERTEX_POINT ( 'NONE', #59415 ) ;
#46224=CARTESIAN_POINT ( 'NONE',  ( 4.975610109902397937, 0.000000000000000000, 0.000000000000000000 ) ) ;
#46228=CARTESIAN_POINT ( 'NONE',  ( 4.335381028904216727, -40.49335964728600601, -27.56890770668824686 ) ) ;
#46234=CARTESIAN_POINT ( 'NONE',  ( 0.8744876279028306332, 46.30617036199629410, -16.31222353896820110 ) ) ;
#46237=CARTESIAN_POINT ( 'NONE',  ( 2.009741617377216460, 36.14358544831069509, -25.16237883356238569 ) ) ;
#46243=DIRECTION ( 'NONE',  ( 0.000000000000000000, 0.000000000000000000, 1.000000000000000000 ) ) ;
#46246=CARTESIAN_POINT ( 'NONE',  ( 0.7948884756798506590, -47.26562353173273578, -13.29133088733651036 ) ) ;
#46252=ORIENTED_EDGE ( 'NONE', *, *, #5792, .F. ) ;
#46255=CARTESIAN_POINT ( 'NONE',  ( 3.390910168358337362, 37.89548767558103748, 22.31656672437592448 ) ) ;
#46263=CARTESIAN_POINT ( 'NONE',  ( -6.078075953587585900, -6.645381366291554848, 18.07302079741184286 ) ) ;
#46266=ADVANCED_FACE ( 'NONE', ( #13374 ), #39375, .F. ) ;
#46269=ORIENTED_EDGE ( 'NONE', *, *, #27506, .T. ) ;
#46279=CARTESIAN_POINT ( 'NONE',  ( -6.079354080745853928, -6.649248899792234546, -18.07153685541917909 ) ) ;
#46281=ORIENTED_EDGE ( 'NONE', *, *, #52915, .T. ) ;
#46289=CARTESIAN_POINT ( 'NONE',  ( 0.1140933569871965536, 43.23646427744231602, 8.806708060868194465 ) ) ;
#46291=CARTESIAN_POINT ( 'NONE',  ( 2.648799415243708655, -0.1860685961560771262, 49.03552632293369129 ) ) ;
#46292=ORIENTED_EDGE ( 'NONE', *, *, #46945, .F. ) ;
#46294=CARTESIAN_POINT ( 'NONE',  ( 4.834790513006555379, 46.91907382339837085, 5.584787594785887599 ) ) ;
#46297=CARTESIAN_POINT ( 'NONE',  ( -2.601141883200665639, 0.9866742854873818969, 14.89368662634428730 ) ) ;
#46298=ORIENTED_EDGE ( 'NONE', *, *, #49432, .F. ) ;
#46304=CARTESIAN_POINT ( 'NONE',  ( 0.6021447746440204973, 44.35701149669154120, 21.07122849220856153 ) ) ;
#46306=B_SPLINE_CURVE_WITH_KNOTS ( 'NONE', 3,
 ( #35066, #21567, #16559, #54747, #45698, #39461 ),
 .UNSPECIFIED., .F., .F.,
 ( 4, 2, 4 ),
 ( 2.224307874377020740E-17, 0.0002293755540694337851, 0.0004587511081388452898 ),
 .UNSPECIFIED. ) ;
#46312=EDGE_CURVE ( 'NONE', #55549, #50931, #24003, .T. ) ;
#46313=CARTESIAN_POINT ( 'NONE',  ( 0.6000166863083106206, 28.52380356231368097, 39.97769518177598513 ) ) ;
#46314=CARTESIAN_POINT ( 'NONE',  ( 0.8744876279028306332, -39.87136468799875644, -28.64654129726831044 ) ) ;
#46315=CARTESIAN_POINT ( 'NONE',  ( 0.1368894036331272379, -28.00595822950079494, -34.09585941974172840 ) ) ;
#46319=CARTESIAN_POINT ( 'NONE',  ( 2.706805983486679779, 16.74203531073313655, 40.69988165798421420 ) ) ;
#46327=CARTESIAN_POINT ( 'NONE',  ( 3.390910168358337362, -32.93065864425445710, -29.14907987894689612 ) ) ;
#46328=CARTESIAN_POINT ( 'NONE',  ( 4.834790513006555379, 45.81970208965012148, 11.53881455523459643 ) ) ;
#46334=EDGE_CURVE ( 'NONE', #30625, #17526, #41272, .T. ) ;
#46337=( BOUNDED_SURFACE ( )  B_SPLINE_SURFACE ( 3, 1, ( 
 ( #12217, #31301 ),
 ( #45122, #16592 ),
 ( #11915, #1852 ),
 ( #40123, #44201 ) ),
 .UNSPECIFIED., .F., .F., .F. ) 
 B_SPLINE_SURFACE_WITH_KNOTS ( ( 4, 4 ),
 ( 2, 2 ),
 ( 0.000000000000000000, 1.000000000000000000 ),
 ( 0.000000000000000000, 1.000000000000000000 ),
 .UNSPECIFIED. ) 
 GEOMETRIC_REPRESENTATION_ITEM ( )  RATIONAL_B_SPLINE_SURFACE ( (
 ( 1.000000000000000000, 1.000000000000000000),
 ( 0.9754377213608244057, 0.9999580625633939235),
 ( 0.9754377213608244057, 0.9999580625633939235),
 ( 1.000000000000000000, 1.000000000000000000) ) ) 
 REPRESENTATION_ITEM ( '' )  SURFACE ( )  );
#46340=ADVANCED_FACE ( 'NONE', ( #56874 ), #61287, .F. ) ;
#46343=CARTESIAN_POINT ( 'NONE',  ( 4.335381028904216727, 2.583895202258514878, -48.91912032373529939 ) ) ;
#46349=CONICAL_SURFACE ( 'NONE', #19335, 43.92652462719577500, 1.486293639869522343 ) ;
#46351=EDGE_LOOP ( 'NONE', ( #5987, #46174, #18575, #4704 ) ) ;
#46352=CARTESIAN_POINT ( 'NONE',  ( 0.1129192098497455998, -1.898585089632445433, 44.08341142019953907 ) ) ;
#46355=CARTESIAN_POINT ( 'NONE',  ( -6.077587904424778920, -4.278847002849283321, 18.77465018902185179 ) ) ;
#46357=CARTESIAN_POINT ( 'NONE',  ( 0.6021448801613057400, -25.23316997730999134, -42.12871077451965363 ) ) ;
#46367=FACE_OUTER_BOUND ( 'NONE', #13649, .T. ) ;
#46372=B_SPLINE_CURVE_WITH_KNOTS ( 'NONE', 3,
 ( #59215, #12263, #16320, #21027 ),
 .UNSPECIFIED., .F., .F.,
 ( 4, 4 ),
 ( 0.000000000000000000, 0.005013413432710150247 ),
 .UNSPECIFIED. ) ;
#46376=CARTESIAN_POINT ( 'NONE',  ( 4.553261556744875094, 0.000000000000000000, 0.000000000000000000 ) ) ;
#46385=CARTESIAN_POINT ( 'NONE',  ( 0.8753041380234471980, 46.87455897190349674, -14.62580080072613242 ) ) ;
#46387=CARTESIAN_POINT ( 'NONE',  ( -6.078457390727109555, -1.853383199521488445, -19.16662416163158156 ) ) ;
#46388=CARTESIAN_POINT ( 'NONE',  ( 4.975610109902397937, 47.45567470742089000, 11.84940273605495520 ) ) ;
#46389=CARTESIAN_POINT ( 'NONE',  ( 0.2940135542859016460, 43.14164472089348834, -9.221661426642361548 ) ) ;
#46390=FACE_OUTER_BOUND ( 'NONE', #61124, .T. ) ;
#46397=VERTEX_POINT ( 'NONE', #57791 ) ;
#46398=CARTESIAN_POINT ( 'NONE',  ( 0.7948878604505671408, 46.31693282836004499, -16.29234116606942706 ) ) ;
#46405=CARTESIAN_POINT ( 'NONE',  ( 0.6016118706126976079, 44.39439472474408177, -20.99258849707547725 ) ) ;
#46407=( BOUNDED_SURFACE ( )  B_SPLINE_SURFACE ( 3, 1, ( 
 ( #56368, #46385 ),
 ( #3431, #32277 ),
 ( #61367, #4344 ),
 ( #27263, #17563 ) ),
 .UNSPECIFIED., .F., .F., .F. ) 
 B_SPLINE_SURFACE_WITH_KNOTS ( ( 4, 4 ),
 ( 2, 2 ),
 ( 0.000000000000000000, 1.000000000000000000 ),
 ( 0.000000000000000000, 1.000000000000000000 ),
 .UNSPECIFIED. ) 
 GEOMETRIC_REPRESENTATION_ITEM ( )  RATIONAL_B_SPLINE_SURFACE ( (
 ( 1.000000000000000000, 1.000000000000000000),
 ( 0.7211978278499970862, 0.9934217856018976445),
 ( 0.7211978278499970862, 0.9934217856018976445),
 ( 1.000000000000000000, 1.000000000000000000) ) ) 
 REPRESENTATION_ITEM ( '' )  SURFACE ( )  );
#46409=LINE ( 'NONE', #18506, #15039 ) ;
#46414=B_SPLINE_CURVE_WITH_KNOTS ( 'NONE', 3,
 ( #25034, #1207, #53214, #24410, #57904, #49447 ),
 .UNSPECIFIED., .F., .F.,
 ( 4, 2, 4 ),
 ( 2.949348774913697507E-18, 0.0002447193893791696538, 0.0004894387787583363804 ),
 .UNSPECIFIED. ) ;
#46427=CARTESIAN_POINT ( 'NONE',  ( 0.1156495703730067576, 15.36680576975396306, 41.36186932025348995 ) ) ;
#46428=EDGE_CURVE ( 'NONE', #8350, #36635, #40808, .T. ) ;
#46439=CARTESIAN_POINT ( 'NONE',  ( 0.1129192098497455998, -13.01845098534629486, 42.16007260106758281 ) ) ;
#46446=CARTESIAN_POINT ( 'NONE',  ( -6.078726893082806448, -18.27610589745697567, 6.064486333866907053 ) ) ;
#46449=CARTESIAN_POINT ( 'NONE',  ( 4.694002226626921015, -20.78018001817150306, -40.57670378257112276 ) ) ;
#46456=FACE_OUTER_BOUND ( 'NONE', #38239, .T. ) ;
#46466=CARTESIAN_POINT ( 'NONE',  ( 3.894904216938898323, -20.85496616184445173, 38.69360048980352929 ) ) ;
#46471=ORIENTED_EDGE ( 'NONE', *, *, #5521, .F. ) ;
#46472=ORIENTED_EDGE ( 'NONE', *, *, #32433, .T. ) ;
#46480=CARTESIAN_POINT ( 'NONE',  ( 0.7948878604505664747, 5.577371006631278050, 48.78105759362752991 ) ) ;
#46481=ORIENTED_EDGE ( 'NONE', *, *, #4928, .T. ) ;
#46486=DIRECTION ( 'NONE',  ( -1.000000000000000000, -0.000000000000000000, -0.000000000000000000 ) ) ;
#46487=ORIENTED_EDGE ( 'NONE', *, *, #34391, .F. ) ;
#46491=CARTESIAN_POINT ( 'NONE',  ( 3.678748215320120973, -31.95975617982332295, -37.11046751559092627 ) ) ;
#46503=EDGE_CURVE ( 'NONE', #43179, #52266, #44977, .T. ) ;
#46509=EDGE_LOOP ( 'NONE', ( #24933, #59799, #48949, #33517 ) ) ;
#46512=DIRECTION ( 'NONE',  ( -0.1011922191286467598, 0.1460712814909170820, 0.9840850143719399590 ) ) ;
#46513=CARTESIAN_POINT ( 'NONE',  ( 0.6253024248130486518, -24.86663011560634118, -42.34495169570114825 ) ) ;
#46515=VERTEX_POINT ( 'NONE', #21141 ) ;
#46516=CARTESIAN_POINT ( 'NONE',  ( 0.8753041380234471980, -45.17330286263774752, -19.24866323549208502 ) ) ;
#46518=CARTESIAN_POINT ( 'NONE',  ( 0.6000166863083090663, -2.096232480232020912, 49.06556115135416007 ) ) ;
#46524=CARTESIAN_POINT ( 'NONE',  ( 0.3676999524040323597, 36.51379593394458567, 24.75264207750540635 ) ) ;
#46529=EDGE_CURVE ( 'NONE', #462, #60714, #11389, .T. ) ;
#46533=CARTESIAN_POINT ( 'NONE',  ( 0.6029443199889047422, -39.35536131004970883, -29.37163900789067839 ) ) ;
#46534=B_SPLINE_CURVE_WITH_KNOTS ( 'NONE', 3,
 ( #32360, #61750, #42089, #28259, #51748, #37374 ),
 .UNSPECIFIED., .F., .F.,
 ( 4, 2, 4 ),
 ( 1.736890526760486189E-17, 0.0002293755540694303698, 0.0004587511081388433382 ),
 .UNSPECIFIED. ) ;
#46544=CARTESIAN_POINT ( 'NONE',  ( 0.6028777368367060907, -1.660990723866983432, 49.07933311615287408 ) ) ;
#46551=ORIENTED_EDGE ( 'NONE', *, *, #20503, .T. ) ;
#46554=LINE ( 'NONE', #8617, #57910 ) ;
#46564=CIRCLE ( 'NONE', #35569, 43.92652462719577500 ) ;
#46565=CARTESIAN_POINT ( 'NONE',  ( 0.8744876279028263033, -0.6840263623742536270, -49.09055060105834656 ) ) ;
#46566=CARTESIAN_POINT ( 'NONE',  ( 0.5997462898726536595, 49.03735788587799505, 2.624721264559015221 ) ) ;
#46570=CARTESIAN_POINT ( 'NONE',  ( 4.975610109902397937, 47.45567470742105343, -11.84940273605426242 ) ) ;
#46572=B_SPLINE_CURVE_WITH_KNOTS ( 'NONE', 3,
 ( #15134, #33628, #34242, #4766 ),
 .UNSPECIFIED., .F., .F.,
 ( 4, 4 ),
 ( 0.000000000000000000, 0.004444103432399266161 ),
 .UNSPECIFIED. ) ;
#46575=CARTESIAN_POINT ( 'NONE',  ( -6.077587904424778920, 16.77513308702641837, -9.454677747363051665 ) ) ;
#46576=CARTESIAN_POINT ( 'NONE',  ( 4.390527457369402420, 38.43681538245588314, -21.27901689184964340 ) ) ;
#46577=CARTESIAN_POINT ( 'NONE',  ( 4.553261556744873317, 38.16266689001211887, -21.75202109381124771 ) ) ;
#46579=ORIENTED_EDGE ( 'NONE', *, *, #14513, .F. ) ;
#46582=DIRECTION ( 'NONE',  ( 0.1011922191286468015, 0.9919158664526106506, -0.07657054699678347842 ) ) ;
#46591=CARTESIAN_POINT ( 'NONE',  ( 0.6026112563231248442, -13.80537458850877641, -47.12698406831444942 ) ) ;
#46593=CARTESIAN_POINT ( 'NONE',  ( 0.5997462898726536595, -8.352924653000044941, -48.39194436975655123 ) ) ;
#46594=CARTESIAN_POINT ( 'NONE',  ( 0.1157991065609915715, -27.57457289024313951, 34.44684739505731841 ) ) ;
#46601=B_SPLINE_CURVE_WITH_KNOTS ( 'NONE', 3,
 ( #31856, #46576, #22754, #8639, #17752, #56566, #13680, #27764, #32163, #9265, #41888, #8327, #60956, #52172, #22141, #61256, #22446, #41571, #42500, #18065, #46894, #56253, #41268, #45971, #60326 ),
 .UNSPECIFIED., .F., .F.,
 ( 4, 3, 3, 3, 3, 3, 3, 3, 4 ),
 ( 6.254634441385502288E-18, 0.0005656085177311393148, 0.001131215744874500056, 0.001696821861372765266, 0.002262427090022498585, 0.002828031679238745058, 0.003393635864401605296, 0.003977030878808130755, 0.004561030005651158133 ),
 .UNSPECIFIED. ) ;
#46603=CONICAL_SURFACE ( 'NONE', #28470, 43.92652462719577500, 1.486293639869522343 ) ;
#46604=ORIENTED_EDGE ( 'NONE', *, *, #50835, .T. ) ;
#46607=CARTESIAN_POINT ( 'NONE',  ( 4.975610109902397937, 14.46773809681615575, -46.72401910687593585 ) ) ;
#46618=CARTESIAN_POINT ( 'NONE',  ( 0.6016118706126977189, 4.368608851477891797, 48.91284403392140234 ) ) ;
#46619=ADVANCED_FACE ( 'NONE', ( #51177 ), #33703, .F. ) ;
#46621=CARTESIAN_POINT ( 'NONE',  ( 0.8753041380234524160, -8.714053517583520758, -48.32394436680091587 ) ) ;
#46622=CARTESIAN_POINT ( 'NONE',  ( 4.975610109902397937, -5.269241389990889424, -48.62802178077758697 ) ) ;
#46623=ADVANCED_FACE ( 'NONE', ( #50565 ), #33338, .F. ) ;
#46627=CARTESIAN_POINT ( 'NONE',  ( 0.6027444965799114707, -1.443419008004065640, -49.08620027517687845 ) ) ;
#46631=CARTESIAN_POINT ( 'NONE',  ( 4.553261556744875094, 31.71129487083167220, -30.39627186743139831 ) ) ;
#46635=CARTESIAN_POINT ( 'NONE',  ( 4.226256110419178924, -33.18950264439402531, -28.79729439035807559 ) ) ;
#46636=CARTESIAN_POINT ( 'NONE',  ( 2.879087469061463622, 28.27730024378419671, -33.71195585702882624 ) ) ;
#46647=CONICAL_SURFACE ( 'NONE', #21641, 43.92652462719577500, 1.486293639869522343 ) ;
#46651=ORIENTED_EDGE ( 'NONE', *, *, #58797, .F. ) ;
#46652=CARTESIAN_POINT ( 'NONE',  ( 0.5997462898726536595, -45.31995669577361951, 18.91172004968117903 ) ) ;
#46654=EDGE_CURVE ( 'NONE', #23810, #18917, #35252, .T. ) ;
#46656=CARTESIAN_POINT ( 'NONE',  ( 3.240649175237395596, 6.040174043042799035, -43.57500676910334647 ) ) ;
#46662=DIRECTION ( 'NONE',  ( -0.1011922191286467460, -0.4487230644346533737, -0.8879232772217393599 ) ) ;
#46668=ORIENTED_EDGE ( 'NONE', *, *, #59210, .F. ) ;
#46669=CARTESIAN_POINT ( 'NONE',  ( 1.834102595619085285, 5.524616319571569178, 43.69984392854519228 ) ) ;
#46671=CARTESIAN_POINT ( 'NONE',  ( 0.6008122571543327295, 46.46679251165622304, -15.88684185557360351 ) ) ;
#46672=VERTEX_POINT ( 'NONE', #58023 ) ;
#46673=ORIENTED_EDGE ( 'NONE', *, *, #52133, .T. ) ;
#46674=CARTESIAN_POINT ( 'NONE',  ( 0.5997462898726536595, 11.43624519451647714, 47.75734421002918140 ) ) ;
#46677=CARTESIAN_POINT ( 'NONE',  ( 2.299652685299200972, 5.989079187508338009, -48.66634006522278355 ) ) ;
#46679=ORIENTED_EDGE ( 'NONE', *, *, #57624, .F. ) ;
#46685=CARTESIAN_POINT ( 'NONE',  ( 1.479689385636123067, -43.53577155721767866, 6.798561626215384734 ) ) ;
#46693=EDGE_CURVE ( 'NONE', #5101, #13508, #33040, .T. ) ;
#46699=ADVANCED_FACE ( 'NONE', ( #43052 ), #49760, .F. ) ;
#46712=DIRECTION ( 'NONE',  ( 0.000000000000000000, 0.000000000000000000, 1.000000000000000000 ) ) ;
#46715=CARTESIAN_POINT ( 'NONE',  ( 0.8753041380234530822, -13.11588273819849704, 47.31925557181565267 ) ) ;
#46716=CARTESIAN_POINT ( 'NONE',  ( 0.6029443449137436017, 44.26313014289048198, -21.26769493708410508 ) ) ;
#46717=B_SPLINE_CURVE_WITH_KNOTS ( 'NONE', 3,
 ( #24941, #39361, #49043, #39990 ),
 .UNSPECIFIED., .F., .F.,
 ( 4, 4 ),
 ( 0.000000000000000000, 0.005013413432710147645 ),
 .UNSPECIFIED. ) ;
#46723=B_SPLINE_CURVE_WITH_KNOTS ( 'NONE', 3,
 ( #17750, #22444, #55320, #22752, #41886, #27143 ),
 .UNSPECIFIED., .F., .F.,
 ( 4, 2, 4 ),
 ( 1.843143693225357538E-18, 0.0002447193893791662386, 0.0004894387787583306341 ),
 .UNSPECIFIED. ) ;
#46725=ORIENTED_EDGE ( 'NONE', *, *, #35882, .T. ) ;
#46739=CARTESIAN_POINT ( 'NONE',  ( -6.079354080745853928, -14.66163526140110385, -12.48316493161096830 ) ) ;
#46741=CIRCLE ( 'NONE', #54700, 48.91267123290010943 ) ;
#46745=CARTESIAN_POINT ( 'NONE',  ( 0.1152339509894530906, -31.85158600912513904, -30.53553928062425271 ) ) ;
#46752=ORIENTED_EDGE ( 'NONE', *, *, #14095, .T. ) ;
#46754=FACE_OUTER_BOUND ( 'NONE', #44277, .T. ) ;
#46755=DIRECTION ( 'NONE',  ( 0.000000000000000000, 0.000000000000000000, 1.000000000000000000 ) ) ;
#46756=CARTESIAN_POINT ( 'NONE',  ( 0.6000166863083106206, 46.77044519531232680, -14.97828220927686793 ) ) ;
#46769=CARTESIAN_POINT ( 'NONE',  ( 0.5997462898726536595, 28.52220283460682282, -39.97543715340528081 ) ) ;
#46771=CONICAL_SURFACE ( 'NONE', #27884, 43.92652462719577500, 1.486293639869522343 ) ;
#46777=CARTESIAN_POINT ( 'NONE',  ( 0.8753041380234465318, -20.68664920503345073, 44.53314352862224013 ) ) ;
#46779=CARTESIAN_POINT ( 'NONE',  ( 4.694002226626921015, 32.98704702821333967, -31.46648216443294999 ) ) ;
#46781=CARTESIAN_POINT ( 'NONE',  ( 3.559346040607745287, -21.01279064855753020, 38.62502958836252986 ) ) ;
#46791=CARTESIAN_POINT ( 'NONE',  ( 0.1129192098497455998, 33.28205046155587610, 28.96993104685618547 ) ) ;
#46792=CARTESIAN_POINT ( 'NONE',  ( 5.901764892641288895, 45.37424261077635634, -18.41655708698249683 ) ) ;
#46795=ADVANCED_FACE ( 'NONE', ( #24220 ), #58535, .F. ) ;
#46797=CARTESIAN_POINT ( 'NONE',  ( 0.3676999524040366896, -23.56959980820299094, -37.28839696479317212 ) ) ;
#46804=LINE ( 'NONE', #33008, #55955 ) ;
#46806=ORIENTED_EDGE ( 'NONE', *, *, #37937, .F. ) ;
#46812=VERTEX_POINT ( 'NONE', #49885 ) ;
#46819=EDGE_LOOP ( 'NONE', ( #11213, #60964, #53394, #29820 ) ) ;
#46820=CARTESIAN_POINT ( 'NONE',  ( 0.5997462898726536595, 46.43852004798843325, 15.96920429754989890 ) ) ;
#46822=CARTESIAN_POINT ( 'NONE',  ( 0.1129192098497455998, -23.28677643606931014, 37.47903188453085477 ) ) ;
#46833=CARTESIAN_POINT ( 'NONE',  ( 0.5987334363312692975, -24.93754700689008885, -42.30462924729660301 ) ) ;
#46837=CARTESIAN_POINT ( 'NONE',  ( 0.8753041380234465318, -2.462982411634898838, 49.04153388213869391 ) ) ;
#46842=CARTESIAN_POINT ( 'NONE',  ( 3.678748215320119197, 20.99750299042923984, -44.24610358513390196 ) ) ;
#46845=B_SPLINE_CURVE_WITH_KNOTS ( 'NONE', 3,
 ( #43386, #113, #44015, #21334, #15479, #10783, #34588, #40463, #48367, #9851, #423, #29870, #49836, #45169, #5428, #35761, #2196, #24564, #19263 ),
 .UNSPECIFIED., .F., .F.,
 ( 4, 3, 3, 3, 3, 3, 4 ),
 ( 1.355252715606880543E-20, 0.0002612768053151711127, 0.0003919133833142926602, 0.0005225499612322640061, 0.0006531865391693361753, 0.0008112755173415186647, 0.0009693688056799727899 ),
 .UNSPECIFIED. ) ;
#46848=CARTESIAN_POINT ( 'NONE',  ( 0.1365634738349424393, 36.62793384158531040, 24.60197313468367142 ) ) ;
#46853=CARTESIAN_POINT ( 'NONE',  ( 0.6253024248130497620, -13.31237246887635628, -47.26758896609333505 ) ) ;
#46856=CARTESIAN_POINT ( 'NONE',  ( 2.359973842542476330, -24.09890286121120795, -36.84262172428024940 ) ) ;
#46863=FACE_OUTER_BOUND ( 'NONE', #56870, .T. ) ;
#46865=ORIENTED_EDGE ( 'NONE', *, *, #11036, .F. ) ;
#46872=CARTESIAN_POINT ( 'NONE',  ( 0.6024113833632039894, 11.13957392438117822, -47.82731188227197805 ) ) ;
#46881=CARTESIAN_POINT ( 'NONE',  ( 1.479689385636123067, 37.55715799008815736, 23.04438606201625817 ) ) ;
#46884=B_SPLINE_CURVE_WITH_KNOTS ( 'NONE', 3,
 ( #8416, #17846, #22235, #56034 ),
 .UNSPECIFIED., .F., .F.,
 ( 4, 4 ),
 ( 2.199414408396618760E-17, 0.004559932413162189405 ),
 .UNSPECIFIED. ) ;
#46885=CARTESIAN_POINT ( 'NONE',  ( 0.6024113833632039894, 48.99212586890816112, 3.363550497008568119 ) ) ;
#46893=CARTESIAN_POINT ( 'NONE',  ( -6.077587904424778920, -17.34643006009186195, -8.360465630828942452 ) ) ;
#46894=CARTESIAN_POINT ( 'NONE',  ( 1.112077966505211402, 39.24773055670718236, -20.06604024905431416 ) ) ;
#46895=CARTESIAN_POINT ( 'NONE',  ( 3.240649175237396484, 37.83429905813157035, -22.44617411002408147 ) ) ;
#46898=ORIENTED_EDGE ( 'NONE', *, *, #7555, .T. ) ;
#46900=CARTESIAN_POINT ( 'NONE',  ( 0.1158516988532803521, -44.12414005494260039, 0.04922646246316730867 ) ) ;
#46908=CARTESIAN_POINT ( 'NONE',  ( 1.834102595619085507, 43.46554130548571493, 7.137539063206623347 ) ) ;
#46909=CARTESIAN_POINT ( 'NONE',  ( 0.6029442701453591180, -25.38242846679687048, 42.03900034832199140 ) ) ;
#46910=CARTESIAN_POINT ( 'NONE',  ( 0.6029443449137436017, -13.93069009245118473, -47.09007763352503417 ) ) ;
#46911=ORIENTED_EDGE ( 'NONE', *, *, #52001, .T. ) ;
#46914=CARTESIAN_POINT ( 'NONE',  ( 0.1149546198390367230, -27.72460785286477858, 34.32626814012978400 ) ) ;
#46915=CARTESIAN_POINT ( 'NONE',  ( 3.678834586032786014, 44.89638856848508652, -19.56851203172985265 ) ) ;
#46934=CARTESIAN_POINT ( 'NONE',  ( 0.3676999524040366896, 3.413584541509296688, -43.98065510995495941 ) ) ;
#46937=CARTESIAN_POINT ( 'NONE',  ( -6.077587904424778920, 3.067159685105322442, 19.01022232536997691 ) ) ;
#46938=DIRECTION ( 'NONE',  ( 0.000000000000000000, 0.000000000000000000, 1.000000000000000000 ) ) ;
#46940=VERTEX_POINT ( 'NONE', #3180 ) ;
#46942=CARTESIAN_POINT ( 'NONE',  ( 0.1365634738349397193, 40.02584797782402859, -18.56863250967517587 ) ) ;
#46943=CARTESIAN_POINT ( 'NONE',  ( 0.6008123274975392114, -1.138712662034059075, -49.09437732196816029 ) ) ;
#46945=EDGE_CURVE ( 'NONE', #46672, #31513, #5252, .T. ) ;
#46951=CARTESIAN_POINT ( 'NONE',  ( 3.559346040607745287, -32.98083365439821080, -29.08083377420432214 ) ) ;
#46953=CARTESIAN_POINT ( 'NONE',  ( 0.6021447746440204973, -45.61591350405682732, -18.18597190910877615 ) ) ;
#46955=FACE_OUTER_BOUND ( 'NONE', #31540, .T. ) ;
#46958=VERTEX_POINT ( 'NONE', #36121 ) ;
#46960=CARTESIAN_POINT ( 'NONE',  ( -6.078075953587585900, -6.645381366291293723, -18.07302079741193879 ) ) ;
#46966=CARTESIAN_POINT ( 'NONE',  ( 5.901764892641307547, 39.21882766674595189, 29.32362569474928549 ) ) ;
#46969=CARTESIAN_POINT ( 'NONE',  ( 0.7044674535452954967, -48.80743866909971018, 5.443955673311092980 ) ) ;
#46971=ORIENTED_EDGE ( 'NONE', *, *, #51146, .T. ) ;
#46973=CARTESIAN_POINT ( 'NONE',  ( 0.6016117650947688800, -8.181245532462590120, -48.42125851092740874 ) ) ;
#46983=CARTESIAN_POINT ( 'NONE',  ( 0.3676999524040366896, -28.14442808720893296, -33.96824621564622504 ) ) ;
#46987=CARTESIAN_POINT ( 'NONE',  ( 2.706805983486680223, 0.2451503928605884286, 44.00813577742911065 ) ) ;
#46993=CARTESIAN_POINT ( 'NONE',  ( -6.077587904424778920, -11.01164173315279271, -15.79682777441781738 ) ) ;
#46994=CARTESIAN_POINT ( 'NONE',  ( 4.335381028904201628, 43.17230378757372478, 23.14970914153764170 ) ) ;
#46999=EDGE_CURVE ( 'NONE', #3847, #23682, #60808, .T. ) ;
#47001=CARTESIAN_POINT ( 'NONE',  ( 4.226256110419178924, 42.60700927045893138, -10.74569732563750968 ) ) ;
#47003=CARTESIAN_POINT ( 'NONE',  ( 4.060580049360325461, -41.54832425072979163, -14.32495885911816380 ) ) ;
#47008=CARTESIAN_POINT ( 'NONE',  ( 4.694002226626920127, 39.55162978021545683, -22.67053932254166781 ) ) ;
#47020=CARTESIAN_POINT ( 'NONE',  ( 0.1129192098497455998, 44.06201484046248140, -2.343210614524073421 ) ) ;
#47024=CARTESIAN_POINT ( 'NONE',  ( 0.1152809850208375841, 4.016710468846341975, 43.94099816229958577 ) ) ;
#47026=CARTESIAN_POINT ( 'NONE',  ( 0.1156867017252034696, 4.361299308302413635, -43.90810717417215159 ) ) ;
#47034=ORIENTED_EDGE ( 'NONE', *, *, #33316, .F. ) ;
#47036=FACE_OUTER_BOUND ( 'NONE', #17136, .T. ) ;
#47038=ORIENTED_EDGE ( 'NONE', *, *, #51915, .F. ) ;
#47045=ADVANCED_FACE ( 'NONE', ( #28531 ), #20744, .F. ) ;
#47051=CARTESIAN_POINT ( 'NONE',  ( 0.1158516988532803382, -22.91572194069864921, -37.70692040951341539 ) ) ;
#47055=FACE_OUTER_BOUND ( 'NONE', #25802, .T. ) ;
#47069=VERTEX_POINT ( 'NONE', #28230 ) ;
#47083=CARTESIAN_POINT ( 'NONE',  ( -6.077587904424778920, -17.34643006009186195, -8.360465630828942452 ) ) ;
#47087=CARTESIAN_POINT ( 'NONE',  ( 4.553261556744875094, 0.000000000000000000, 0.000000000000000000 ) ) ;
#47089=EDGE_LOOP ( 'NONE', ( #51773, #48034, #29432, #34540 ) ) ;
#47090=CARTESIAN_POINT ( 'NONE',  ( 0.6021447746440204973, -39.19855282349202241, 29.58064562568560163 ) ) ;
#47092=LINE ( 'NONE', #4740, #23711 ) ;
#47093=ORIENTED_EDGE ( 'NONE', *, *, #30895, .F. ) ;
#47094=ORIENTED_EDGE ( 'NONE', *, *, #41719, .F. ) ;
#47095=CARTESIAN_POINT ( 'NONE',  ( 3.390910168358336918, -30.18958311396259830, 31.97946541045958924 ) ) ;
#47096=CARTESIAN_POINT ( 'NONE',  ( 0.5997462898726536595, 5.235280152387000285, 48.82769165002921596 ) ) ;
#47098=ORIENTED_EDGE ( 'NONE', *, *, #23530, .F. ) ;
#47102=CARTESIAN_POINT ( 'NONE',  ( 0.8744876279028263033, 48.92939099258497038, 4.032957658374010101 ) ) ;
#47103=ORIENTED_EDGE ( 'NONE', *, *, #32694, .T. ) ;
#47107=LINE ( 'NONE', #3849, #3023 ) ;
#47108=CARTESIAN_POINT ( 'NONE',  ( 0.2285344041767099210, 9.075216059588225193, -43.17570640727545594 ) ) ;
#47112=EDGE_CURVE ( 'NONE', #1293, #40747, #24774, .T. ) ;
#47119=CARTESIAN_POINT ( 'NONE',  ( 0.6024113833632039894, 46.53665168057906953, 15.68062241944890722 ) ) ;
#47125=EDGE_LOOP ( 'NONE', ( #34981, #39967, #3152, #41433 ) ) ;
#47130=ORIENTED_EDGE ( 'NONE', *, *, #846, .T. ) ;
#47133=CARTESIAN_POINT ( 'NONE',  ( 3.221118495291109163, -5.149125434531551804, 43.68349719197414061 ) ) ;
#47135=ORIENTED_EDGE ( 'NONE', *, *, #12201, .T. ) ;
#47139=DIRECTION ( 'NONE',  ( -1.000000000000000000, -0.000000000000000000, -0.000000000000000000 ) ) ;
#47155=CARTESIAN_POINT ( 'NONE',  ( 0.6026777506516367566, -39.45935355539368317, -29.23193130170600540 ) ) ;
#47156=CARTESIAN_POINT ( 'NONE',  ( 2.879087469061463178, -24.27289634831959475, -36.70052015499387466 ) ) ;
#47165=VERTEX_POINT ( 'NONE', #1875 ) ;
#47166=CARTESIAN_POINT ( 'NONE',  ( 0.1145239942831223490, -7.364426063610032713, 43.50529518872725987 ) ) ;
#47167=FACE_OUTER_BOUND ( 'NONE', #19104, .T. ) ;
#47170=CARTESIAN_POINT ( 'NONE',  ( 0.6008122571543326185, 10.50252207146543704, -47.97136208826780290 ) ) ;
#47171=CARTESIAN_POINT ( 'NONE',  ( 0.1129192098497455998, 9.345467776858411568, 43.12324222292260600 ) ) ;
#47174=VERTEX_POINT ( 'NONE', #35424 ) ;
#47176=CARTESIAN_POINT ( 'NONE',  ( 0.5997462898726536595, -20.35457962188166192, -44.69052157405179315 ) ) ;
#47184=CARTESIAN_POINT ( 'NONE',  ( 0.1147471544378676350, 33.79869711786884778, 28.36547657995207317 ) ) ;
#47190=CARTESIAN_POINT ( 'NONE',  ( 0.1129192098497455998, 42.02659449688937343, -13.44310763101974260 ) ) ;
#47200=CARTESIAN_POINT ( 'NONE',  ( 0.6021447746440204973, 4.455320864211258503, -48.90492056107863306 ) ) ;
#47211=CARTESIAN_POINT ( 'NONE',  ( 1.830465331921978800, -42.90550687857155054, 9.974644623806854682 ) ) ;
#47219=ORIENTED_EDGE ( 'NONE', *, *, #17289, .F. ) ;
#47224=CARTESIAN_POINT ( 'NONE',  ( -6.057079549204054558, 5.487289185789351542, 18.45862639773766389 ) ) ;
#47226=( GEOMETRIC_REPRESENTATION_CONTEXT ( 3 ) GLOBAL_UNCERTAINTY_ASSIGNED_CONTEXT ( ( #21735 ) ) GLOBAL_UNIT_ASSIGNED_CONTEXT ( ( #11246, #7441, #6502 ) ) REPRESENTATION_CONTEXT ( 'NONE', 'WORKASPACE' ) );
#47232=CARTESIAN_POINT ( 'NONE',  ( 4.553261556744875094, 38.38432632180499837, -21.35844232721162683 ) ) ;
#47234=CARTESIAN_POINT ( 'NONE',  ( 4.834790513006553603, 43.96797211434409292, -17.30337449969347219 ) ) ;
#47235=ORIENTED_EDGE ( 'NONE', *, *, #9954, .T. ) ;
#47238=CARTESIAN_POINT ( 'NONE',  ( 2.648799415243708655, -6.455064903436325885, 48.60915140569751713 ) ) ;
#47246=CARTESIAN_POINT ( 'NONE',  ( -6.078726893082806448, -12.94836301907752585, 14.25250631976375004 ) ) ;
#47248=ORIENTED_EDGE ( 'NONE', *, *, #51071, .F. ) ;
#47249=CARTESIAN_POINT ( 'NONE',  ( 1.657374760986086049, -26.48956948988313087, 35.20217543693708251 ) ) ;
#47254=CARTESIAN_POINT ( 'NONE',  ( 0.5987334308729320709, 17.52678517438131678, 45.87346409440667117 ) ) ;
#47259=CARTESIAN_POINT ( 'NONE',  ( 0.5987334308729317378, -43.08218175136362049, -23.56880400258363650 ) ) ;
#47262=VECTOR ( 'NONE', #5660, 1000.000000000000114 ) ;
#47266=ORIENTED_EDGE ( 'NONE', *, *, #39779, .F. ) ;
#47267=CARTESIAN_POINT ( 'NONE',  ( 2.648799415243696664, -45.95403142182595246, 17.10977671892392493 ) ) ;
#47269=ORIENTED_EDGE ( 'NONE', *, *, #21371, .T. ) ;
#47271=CARTESIAN_POINT ( 'NONE',  ( 0.6029442701453591180, -42.83094826596455107, -24.02197110556389603 ) ) ;
#47274=CARTESIAN_POINT ( 'NONE',  ( 1.112077966505211180, -28.29638438491135943, -33.79859399250062069 ) ) ;
#47277=EDGE_CURVE ( 'NONE', #54460, #59959, #42869, .T. ) ;
#47283=CARTESIAN_POINT ( 'NONE',  ( 2.648799415243708655, 29.17954675436460121, 39.40902833741842670 ) ) ;
#47289=CARTESIAN_POINT ( 'NONE',  ( 0.7413678028165011646, -38.87127836507679746, -20.82089839644190121 ) ) ;
#47290=CARTESIAN_POINT ( 'NONE',  ( 0.3676999524040366896, -43.63756228305280160, 6.458617600967457406 ) ) ;
#47295=CARTESIAN_POINT ( 'NONE',  ( 4.553261556744873317, 38.16266689001211887, -21.75202109381124771 ) ) ;
#47301=DIRECTION ( 'NONE',  ( 0.000000000000000000, 0.000000000000000000, 1.000000000000000000 ) ) ;
#47303=VECTOR ( 'NONE', #14590, 1000.000000000000000 ) ;
#47305=ADVANCED_FACE ( 'NONE', ( #14354 ), #22162, .F. ) ;
#47309=ORIENTED_EDGE ( 'NONE', *, *, #21420, .F. ) ;
#47310=DIRECTION ( 'NONE',  ( 0.000000000000000000, 0.000000000000000000, 1.000000000000000000 ) ) ;
#47311=CARTESIAN_POINT ( 'NONE',  ( 3.390910168358337362, 23.51971099678612021, -37.16073641844702280 ) ) ;
#47313=DIRECTION ( 'NONE',  ( 0.000000000000000000, 0.000000000000000000, -1.000000000000000000 ) ) ;
#47315=CARTESIAN_POINT ( 'NONE',  ( 0.5980271706414734822, -13.30134363210459369, 47.27709276618364953 ) ) ;
#47316=CARTESIAN_POINT ( 'NONE',  ( 4.975610109902397937, 0.000000000000000000, 0.000000000000000000 ) ) ;
#47319=CARTESIAN_POINT ( 'NONE',  ( 0.1147471544378677322, 3.927779167740302668, -43.94911534129795427 ) ) ;
#47323=EDGE_CURVE ( 'NONE', #35039, #47174, #52540, .T. ) ;
#47326=EDGE_CURVE ( 'NONE', #23299, #28349, #61756, .T. ) ;
#47329=CARTESIAN_POINT ( 'NONE',  ( -6.078726893082806448, 19.09835798914753369, -2.459016752095146252 ) ) ;
#47334=EDGE_CURVE ( 'NONE', #4156, #55418, #53457, .T. ) ;
#47351=CARTESIAN_POINT ( 'NONE',  ( 0.6016118706126976079, 46.71438999114540991, -15.14321044359830992 ) ) ;
#47352=ORIENTED_EDGE ( 'NONE', *, *, #37861, .T. ) ;
#47354=CARTESIAN_POINT ( 'NONE',  ( 0.6000166863083106206, 49.04012132094737808, -2.624877622902994201 ) ) ;
#47356=CARTESIAN_POINT ( 'NONE',  ( 0.6000166863083106206, 46.44114019838995944, -15.97009639238106438 ) ) ;
#47358=CARTESIAN_POINT ( 'NONE',  ( 4.975610109902397937, -48.77192499014908833, -3.707929326867496655 ) ) ;
#47372=DIRECTION ( 'NONE',  ( 0.1011922191286468153, 0.9935638751191105955, 0.05090148176739390379 ) ) ;
#47373=CARTESIAN_POINT ( 'NONE',  ( 3.390910168358336474, -21.09049067108720621, 38.59129875744557125 ) ) ;
#47379=DIRECTION ( 'NONE',  ( 0.000000000000000000, 0.000000000000000000, 1.000000000000000000 ) ) ;
#47380=EDGE_CURVE ( 'NONE', #15373, #46397, #59071, .T. ) ;
#47383=CARTESIAN_POINT ( 'NONE',  ( 0.6016117650947689910, -39.14611488887053525, 29.65017273730201453 ) ) ;
#47385=EDGE_CURVE ( 'NONE', #56877, #1638, #8252, .T. ) ;
#47387=VERTEX_POINT ( 'NONE', #54808 ) ;
#47388=CARTESIAN_POINT ( 'NONE',  ( 4.553261556744875094, -36.93702150832111641, 23.77385134801386712 ) ) ;
#47394=ADVANCED_FACE ( 'NONE', ( #30698 ), #11361, .F. ) ;
#47404=CARTESIAN_POINT ( 'NONE',  ( 0.3676999524040323597, -23.56959980820351674, 37.28839696479283106 ) ) ;
#47406=B_SPLINE_CURVE_WITH_KNOTS ( 'NONE', 3,
 ( #891, #25022, #24709, #40376, #11232, #35670 ),
 .UNSPECIFIED., .F., .F.,
 ( 4, 2, 4 ),
 ( 1.951563910473907981E-18, 0.0002447193893791709007, 0.0004894387787583398498 ),
 .UNSPECIFIED. ) ;
#47410=CARTESIAN_POINT ( 'NONE',  ( 0.1119898979215349921, -7.595749101251602298, -43.46568651065648226 ) ) ;
#47415=B_SPLINE_CURVE_WITH_KNOTS ( 'NONE', 3,
 ( #938, #48258, #5001, #15369, #34474, #20070 ),
 .UNSPECIFIED., .F., .F.,
 ( 4, 2, 4 ),
 ( 4.878909776184769953E-19, 0.0002293801035737106731, 0.0004587602071474208582 ),
 .UNSPECIFIED. ) ;
#47417=CARTESIAN_POINT ( 'NONE',  ( 0.6016117650947689910, 46.71439353012161178, 15.14319950860553732 ) ) ;
#47427=ORIENTED_EDGE ( 'NONE', *, *, #52351, .T. ) ;
#47432=ORIENTED_EDGE ( 'NONE', *, *, #61415, .T. ) ;
#47440=CARTESIAN_POINT ( 'NONE',  ( 0.6027444965799114707, -42.85215455639489335, 23.98398144100112361 ) ) ;
#47441=CARTESIAN_POINT ( 'NONE',  ( -6.077587904424778920, -14.65844225831517633, 12.48703695652296553 ) ) ;
#47446=CARTESIAN_POINT ( 'NONE',  ( 0.1129192098497447394, 39.96249028893947752, 18.70698152272492365 ) ) ;
#47449=CARTESIAN_POINT ( 'NONE',  ( 0.5997462898726536595, 40.86908001809322855, 27.22627276398666041 ) ) ;
#47457=ADVANCED_FACE ( 'NONE', ( #12241 ), #34982, .F. ) ;
#47458=CARTESIAN_POINT ( 'NONE',  ( 0.6027444965799114707, 48.22663320652137742, -9.259069362041273621 ) ) ;
#47465=ORIENTED_EDGE ( 'NONE', *, *, #52128, .F. ) ;
#47466=CARTESIAN_POINT ( 'NONE',  ( 0.1129192098497455998, -7.520259262076605999, 43.47870154933683295 ) ) ;
#47471=CARTESIAN_POINT ( 'NONE',  ( 0.6029443449137436017, 10.96985678109974671, -47.86649956060598043 ) ) ;
#47474=EDGE_LOOP ( 'NONE', ( #61893, #42910, #20142, #5379 ) ) ;
#47480=CARTESIAN_POINT ( 'NONE',  ( 0.6253024248130478746, -7.158632958273170033, -48.58187112068006996 ) ) ;
#47484=( BOUNDED_SURFACE ( )  B_SPLINE_SURFACE ( 3, 1, ( 
 ( #33282, #32043 ),
 ( #52352, #9443 ),
 ( #32348, #8208 ),
 ( #23547, #18250 ) ),
 .UNSPECIFIED., .F., .F., .F. ) 
 B_SPLINE_SURFACE_WITH_KNOTS ( ( 4, 4 ),
 ( 2, 2 ),
 ( 0.000000000000000000, 1.000000000000000000 ),
 ( 0.000000000000000000, 1.000000000000000000 ),
 .UNSPECIFIED. ) 
 GEOMETRIC_REPRESENTATION_ITEM ( )  RATIONAL_B_SPLINE_SURFACE ( (
 ( 1.000000000000000000, 1.000000000000000000),
 ( 0.9953485035131437453, 0.8621029689291515030),
 ( 0.9953485035131437453, 0.8621029689291515030),
 ( 1.000000000000000000, 1.000000000000000000) ) ) 
 REPRESENTATION_ITEM ( '' )  SURFACE ( )  );
#47485=VECTOR ( 'NONE', #54873, 1000.000000000000000 ) ;
#47486=CARTESIAN_POINT ( 'NONE',  ( 0.1145239942831223490, 33.38557459180370302, 28.85045735997584515 ) ) ;
#47489=FACE_OUTER_BOUND ( 'NONE', #40194, .T. ) ;
#47497=ORIENTED_EDGE ( 'NONE', *, *, #25746, .F. ) ;
#47504=ORIENTED_EDGE ( 'NONE', *, *, #47112, .F. ) ;
#47505=CARTESIAN_POINT ( 'NONE',  ( 4.694002226626920127, -21.39119943673025048, -40.25793534328562373 ) ) ;
#47507=CARTESIAN_POINT ( 'NONE',  ( 0.6028777368367060907, -25.53134248582511745, 41.94866362808920002 ) ) ;
#47514=CARTESIAN_POINT ( 'NONE',  ( 0.1129192098497447394, 24.84520063729181416, -36.46461014569973713 ) ) ;
#47516=CARTESIAN_POINT ( 'NONE',  ( 0.6000166863083090663, 22.25084548767497239, 43.78039923061538730 ) ) ;
#47518=CARTESIAN_POINT ( 'NONE',  ( -6.077587904424778920, 13.82827771187084664, -13.40055061993000685 ) ) ;
#47526=CARTESIAN_POINT ( 'NONE',  ( 0.8744876279028306332, 40.65405044375329879, -27.52450240960324024 ) ) ;
#47531=CARTESIAN_POINT ( 'NONE',  ( 0.1368894036331293473, 3.601832553117911395, -43.97599490838877756 ) ) ;
#47533=EDGE_CURVE ( 'NONE', #4551, #36259, #5898, .T. ) ;
#47544=ADVANCED_FACE ( 'NONE', ( #41989 ), #28544, .F. ) ;
#47547=DIRECTION ( 'NONE',  ( -1.000000000000000000, -0.000000000000000000, -0.000000000000000000 ) ) ;
#47549=CARTESIAN_POINT ( 'NONE',  ( -2.739355103387247858, 4.908046929417170468, 14.09817868696718257 ) ) ;
#47553=CARTESIAN_POINT ( 'NONE',  ( 0.6029443199889047422, -45.51848969954281188, -18.42836773366042280 ) ) ;
#47563=DIRECTION ( 'NONE',  ( 0.09722883295013595717, -0.9860961158916726754, 0.1347627703281270295 ) ) ;
#47565=CARTESIAN_POINT ( 'NONE',  ( 0.1119898979215347423, 42.04997231376550815, 13.37015843823037287 ) ) ;
#47568=DIRECTION ( 'NONE',  ( 0.09722883295013594329, 0.3508110149947656353, -0.9313850899609124045 ) ) ;
#47569=CARTESIAN_POINT ( 'NONE',  ( 4.553261556744875094, -43.15908619232990873, 8.175135770534621926 ) ) ;
#47583=CARTESIAN_POINT ( 'NONE',  ( 0.1129192098497455998, -41.07894348801367812, 16.10814047907867064 ) ) ;
#47584=CARTESIAN_POINT ( 'NONE',  ( 0.1129192098497455998, -43.69739906996312584, -6.122834499277253428 ) ) ;
#47585=ORIENTED_EDGE ( 'NONE', *, *, #16816, .T. ) ;
#47588=CARTESIAN_POINT ( 'NONE',  ( 0.1145239942831223490, -38.60545397981544369, 21.36736773018673929 ) ) ;
#47590=ORIENTED_EDGE ( 'NONE', *, *, #21788, .T. ) ;
#47593=CARTESIAN_POINT ( 'NONE',  ( -6.072942160501519027, -11.00492040199063304, -15.80176854769334582 ) ) ;
#47595=CARTESIAN_POINT ( 'NONE',  ( 0.1368894036331284314, -42.51402964546802110, 11.80756576215436660 ) ) ;
#47596=EDGE_LOOP ( 'NONE', ( #23906, #5765, #19876, #60302 ) ) ;
#47597=EDGE_LOOP ( 'NONE', ( #55486, #60635, #29660, #41436 ) ) ;
#47599=CARTESIAN_POINT ( 'NONE',  ( 2.706805983486680223, 42.85020883812403270, -10.03173543555213243 ) ) ;
#47600=CARTESIAN_POINT ( 'NONE',  ( 2.185380717157383135, -39.05135512724729097, -20.34235644641046292 ) ) ;
#47605=CARTESIAN_POINT ( 'NONE',  ( -6.072942160501519915, -19.21763696748626060, -1.219258657925263112 ) ) ;
#47610=CARTESIAN_POINT ( 'NONE',  ( -6.079354080745853928, -8.905595498587343783, 17.07288271100410526 ) ) ;
#47611=CARTESIAN_POINT ( 'NONE',  ( 0.8753041380234465318, -0.6841799139044266731, -49.09857661601188994 ) ) ;
#47625=CARTESIAN_POINT ( 'NONE',  ( 2.114184763561894886, 5.677447754278171364E-15, -44.03514965515262247 ) ) ;
#47627=B_SPLINE_CURVE_WITH_KNOTS ( 'NONE', 3,
 ( #45648, #45347, #20597, #35639, #40344, #35949 ),
 .UNSPECIFIED., .F., .F.,
 ( 4, 2, 4 ),
 ( 8.131516293641283255E-19, 0.0002293801035737088028, 0.0004587602071474167925 ),
 .UNSPECIFIED. ) ;
#47628=CARTESIAN_POINT ( 'NONE',  ( -6.057079549204054558, -6.642710526269484994, -18.07500008198967834 ) ) ;
#47629=VERTEX_POINT ( 'NONE', #19705 ) ;
#47634=CONICAL_SURFACE ( 'NONE', #41657, 43.92652462719577500, 1.486293639869522343 ) ;
#47645=CARTESIAN_POINT ( 'NONE',  ( 0.1129192098497455998, -43.82135468580280957, 5.161459220629533107 ) ) ;
#47648=ORIENTED_EDGE ( 'NONE', *, *, #19519, .F. ) ;
#47649=CARTESIAN_POINT ( 'NONE',  ( 0.1158403557922069033, -22.84124094437145658, -37.75205980214838775 ) ) ;
#47652=CARTESIAN_POINT ( 'NONE',  ( 0.1158516988532803799, -17.81570362517812001, 40.36759669800286332 ) ) ;
#47656=ORIENTED_EDGE ( 'NONE', *, *, #25088, .T. ) ;
#47661=DIRECTION ( 'NONE',  ( -0.1011922191286467460, -0.5585841627631753514, -0.8232520075274534221 ) ) ;
#47662=EDGE_CURVE ( 'NONE', #34106, #1986, #11963, .T. ) ;
#47670=B_SPLINE_CURVE_WITH_KNOTS ( 'NONE', 3,
 ( #25634, #22178, #20943, #31575, #50665, #30632 ),
 .UNSPECIFIED., .F., .F.,
 ( 4, 2, 4 ),
 ( 2.224174099750402954E-17, 0.0002293755540694314540, 0.0004587511081388406277 ),
 .UNSPECIFIED. ) ;
#47677=B_SPLINE_CURVE_WITH_KNOTS ( 'NONE', 3,
 ( #50532, #45254, #59932, #30803, #31749, #41474, #3217, #45869, #7605, #54595, #17042, #36155, #6979, #55221, #12345, #40252, #50231, #60228, #51143, #36775, #45551, #1984, #40553, #26732, #2604 ),
 .UNSPECIFIED., .F., .F.,
 ( 4, 3, 3, 3, 3, 3, 3, 3, 4 ),
 ( 5.057544569639795705E-18, 0.0005656085177311397484, 0.001131215744874499189, 0.001696821861372765699, 0.002262427090022497284, 0.002828031679238745058, 0.003393635864401604429, 0.003977030878808130755, 0.004561030005651157265 ),
 .UNSPECIFIED. ) ;
#47679=DIRECTION ( 'NONE',  ( 0.000000000000000000, 0.000000000000000000, -1.000000000000000000 ) ) ;
#47681=ADVANCED_FACE ( 'NONE', ( #10300 ), #47780, .F. ) ;
#47688=EDGE_CURVE ( 'NONE', #5258, #1848, #57886, .T. ) ;
#47691=CARTESIAN_POINT ( 'NONE',  ( 0.1368894036331291253, 20.97178701940289258, 38.82068359954699588 ) ) ;
#47693=CARTESIAN_POINT ( 'NONE',  ( 0.5997462898726536595, -39.04071682475809268, 29.78882441375220580 ) ) ;
#47697=ADVANCED_FACE ( 'NONE', ( #25315 ), #2752, .F. ) ;
#47699=CARTESIAN_POINT ( 'NONE',  ( 0.3676999524040366896, 25.91024933382758277, 35.70167450949220722 ) ) ;
#47713=CARTESIAN_POINT ( 'NONE',  ( 4.553261556744875094, -41.75933753256810377, 13.62707946203756393 ) ) ;
#47717=DIRECTION ( 'NONE',  ( 0.09722883295013598492, 0.4536333312076149538, 0.8858687006891241555 ) ) ;
#47719=VERTEX_POINT ( 'NONE', #5261 ) ;
#47722=ADVANCED_FACE ( 'NONE', ( #250 ), #41391, .F. ) ;
#47725=CARTESIAN_POINT ( 'NONE',  ( 2.359973842542476330, 34.48061513594045380, 27.37193954544789420 ) ) ;
#47726=CARTESIAN_POINT ( 'NONE',  ( 0.8753041380234465318, -24.68967207985765455, -42.44476905888495111 ) ) ;
#47731=VERTEX_POINT ( 'NONE', #59124 ) ;
#47732=CARTESIAN_POINT ( 'NONE',  ( -6.057079549204054558, 11.99988366729722244, -15.06101002825082169 ) ) ;
#47735=EDGE_CURVE ( 'NONE', #2365, #22119, #13829, .T. ) ;
#47739=EDGE_CURVE ( 'NONE', #46120, #41724, #14952, .T. ) ;
#47741=CARTESIAN_POINT ( 'NONE',  ( 2.533389852662419894, -5.458459604331522996, 43.67671863225876194 ) ) ;
#47746=CARTESIAN_POINT ( 'NONE',  ( 4.975610109902397937, -43.81605102859442979, -21.73943604138302987 ) ) ;
#47747=CARTESIAN_POINT ( 'NONE',  ( 4.694002226626920127, -45.47116547585236646, 3.264641130933999325 ) ) ;
#47750=CARTESIAN_POINT ( 'NONE',  ( 0.1158516988532803660, -17.90573022250301349, -40.32774459391125532 ) ) ;
#47752=CARTESIAN_POINT ( 'NONE',  ( 4.694002226626920127, 1.805541223687672447, 45.55244002614677612 ) ) ;
#47756=LINE ( 'NONE', #23946, #16887 ) ;
#47764=LINE ( 'NONE', #14875, #26033 ) ;
#47765=B_SPLINE_CURVE_WITH_KNOTS ( 'NONE', 3,
 ( #29503, #10721, #29812, #48924, #1289, #52995 ),
 .UNSPECIFIED., .F., .F.,
 ( 4, 2, 4 ),
 ( 3.127317220692750759E-18, 0.0002447193893791708465, 0.0004894387787583385488 ),
 .UNSPECIFIED. ) ;
#47769=EDGE_CURVE ( 'NONE', #1942, #15748, #60503, .T. ) ;
#47780=( BOUNDED_SURFACE ( )  B_SPLINE_SURFACE ( 3, 1, ( 
 ( #5566, #38829 ),
 ( #571, #11228 ),
 ( #6178, #29394 ),
 ( #19396, #49425 ) ),
 .UNSPECIFIED., .F., .F., .F. ) 
 B_SPLINE_SURFACE_WITH_KNOTS ( ( 4, 4 ),
 ( 2, 2 ),
 ( 0.000000000000000000, 1.000000000000000000 ),
 ( 0.000000000000000000, 1.000000000000000000 ),
 .UNSPECIFIED. ) 
 GEOMETRIC_REPRESENTATION_ITEM ( )  RATIONAL_B_SPLINE_SURFACE ( (
 ( 1.000000000000000000, 1.000000000000000000),
 ( 0.9953485035131437453, 0.8621029689291515030),
 ( 0.9953485035131437453, 0.8621029689291515030),
 ( 1.000000000000000000, 1.000000000000000000) ) ) 
 REPRESENTATION_ITEM ( '' )  SURFACE ( )  );
#47784=FACE_OUTER_BOUND ( 'NONE', #4673, .T. ) ;
#47787=VERTEX_POINT ( 'NONE', #45376 ) ;
#47792=CARTESIAN_POINT ( 'NONE',  ( 0.5987334363312691865, -7.239498697625133872, -48.57110833694409280 ) ) ;
#47793=CARTESIAN_POINT ( 'NONE',  ( 4.335381028904216727, 42.17650767838677694, 24.91784596868934898 ) ) ;
#47802=CARTESIAN_POINT ( 'NONE',  ( -6.063463321072276813, -6.635954031850941348, 18.07718359055500557 ) ) ;
#47803=AXIS2_PLACEMENT_3D ( 'NONE', #43845, #43525, #9998 ) ;
#47809=CARTESIAN_POINT ( 'NONE',  ( 3.240649175237396484, -43.82655554202737136, 3.807616934414570053 ) ) ;
#47823=CARTESIAN_POINT ( 'NONE',  ( -2.601141883200665639, 14.55883463511893794, 3.291771792917906225 ) ) ;
#47824=ADVANCED_FACE ( 'NONE', ( #38067 ), #17773, .F. ) ;
#47827=EDGE_CURVE ( 'NONE', #22696, #3215, #35136, .T. ) ;
#47830=VECTOR ( 'NONE', #14398, 1000.000000000000000 ) ;
#47833=CARTESIAN_POINT ( 'NONE',  ( 3.240649175237395596, -42.97983288049779560, 9.380771981139487181 ) ) ;
#47838=VERTEX_POINT ( 'NONE', #42750 ) ;
#47840=CARTESIAN_POINT ( 'NONE',  ( 1.834102595619085729, -16.63057890322184207, 40.78751757831550862 ) ) ;
#47850=CARTESIAN_POINT ( 'NONE',  ( 0.5987334363312691865, -30.14260600494100828, -38.76836609534854716 ) ) ;
#47859=EDGE_CURVE ( 'NONE', #27767, #52998, #42567, .T. ) ;
#47864=EDGE_CURVE ( 'NONE', #27102, #17686, #9701, .T. ) ;
#47869=DIRECTION ( 'NONE',  ( -1.000000000000000000, -0.000000000000000000, -0.000000000000000000 ) ) ;
#47873=ORIENTED_EDGE ( 'NONE', *, *, #53523, .T. ) ;
#47874=DIRECTION ( 'NONE',  ( -1.000000000000000000, 0.000000000000000000, 0.000000000000000000 ) ) ;
#47875=ORIENTED_EDGE ( 'NONE', *, *, #54267, .F. ) ;
#47877=CARTESIAN_POINT ( 'NONE',  ( -6.077587904424778920, -1.855182226445892812, -19.16648951426968850 ) ) ;
#47882=CARTESIAN_POINT ( 'NONE',  ( 3.678834586032787346, 18.63781918815739047, -45.29066201258165592 ) ) ;
#47892=CARTESIAN_POINT ( 'NONE',  ( -4.915099999999998914, 12.80000000000000071, -3.000000000000000000 ) ) ;
#47893=EDGE_CURVE ( 'NONE', #14204, #1298, #24806, .T. ) ;
#47898=DIRECTION ( 'NONE',  ( -1.000000000000000000, -0.000000000000000000, -0.000000000000000000 ) ) ;
#47899=EDGE_CURVE ( 'NONE', #54294, #51708, #61507, .T. ) ;
#47901=CARTESIAN_POINT ( 'NONE',  ( 0.1147471544378676628, -38.29299291615923551, 21.92256558882251127 ) ) ;
#47908=CARTESIAN_POINT ( 'NONE',  ( 0.2285344041767114198, -42.47718627262295144, 11.92433715794502191 ) ) ;
#47914=CARTESIAN_POINT ( 'NONE',  ( 0.5987334308729321819, -34.85272393231409893, 34.59552776107961591 ) ) ;
#47915=CARTESIAN_POINT ( 'NONE',  ( 4.553261556744875094, 42.54662847375985280, -10.92355122382294752 ) ) ;
#47917=CARTESIAN_POINT ( 'NONE',  ( 0.2279481005628796741, -32.21654163078297728, 30.14295825603286971 ) ) ;
#47922=CARTESIAN_POINT ( 'NONE',  ( -6.063463321072276813, -19.21812676738393222, -1.218218384457852688 ) ) ;
#47934=CARTESIAN_POINT ( 'NONE',  ( 0.3676999524040323597, -40.57213187173838520, -17.31625533148287843 ) ) ;
#47936=CARTESIAN_POINT ( 'NONE',  ( 2.533389852662419894, 40.31838374093042177, 17.66008109417097316 ) ) ;
#47950=VERTEX_POINT ( 'NONE', #54258 ) ;
#47952=CARTESIAN_POINT ( 'NONE',  ( -6.078075953587585900, 19.09862890096253096, -2.457142313838282632 ) ) ;
#47959=EDGE_CURVE ( 'NONE', #31634, #41223, #10455, .T. ) ;
#47962=B_SPLINE_CURVE_WITH_KNOTS ( 'NONE', 3,
 ( #46021, #22190, #40391, #31583, #7758, #14572, #58062, #48075, #752, #28644, #43705, #9534, #19575, #9859, #33990, #19891 ),
 .UNSPECIFIED., .F., .F.,
 ( 4, 3, 3, 3, 3, 4 ),
 ( 2.501947744657918636E-17, 0.0002612764279487718617, 0.0003919131003184756130, 0.0005225497727000653642, 0.0007837925190632448122, 0.001045051706266714999 ),
 .UNSPECIFIED. ) ;
#47965=ADVANCED_FACE ( 'NONE', ( #11699 ), #30553, .F. ) ;
#47978=CARTESIAN_POINT ( 'NONE',  ( 0.1154773475650540254, 25.09645238721858007, -36.29203366611179149 ) ) ;
#47979=CARTESIAN_POINT ( 'NONE',  ( 0.2940135542859015350, -0.6094639541808186678, 44.11200632911605624 ) ) ;
#47980=CARTESIAN_POINT ( 'NONE',  ( 4.335381028904216727, -37.95090345676174337, 30.97556737946691285 ) ) ;
#47981=ADVANCED_FACE ( 'NONE', ( #35198 ), #2930, .F. ) ;
#47982=AXIS2_PLACEMENT_3D ( 'NONE', #44127, #53165, #28754 ) ;
#47983=VERTEX_POINT ( 'NONE', #5713 ) ;
#47985=CARTESIAN_POINT ( 'NONE',  ( 0.3676999524040366896, 5.056646555325087000, 43.82215089355334925 ) ) ;
#47992=CARTESIAN_POINT ( 'NONE',  ( 0.8744876279028263033, -35.88078294188978390, 33.50999053799454686 ) ) ;
#47993=CARTESIAN_POINT ( 'NONE',  ( 0.3676999524040323597, -41.19158123804999860, 15.78620342045440239 ) ) ;
#47998=CARTESIAN_POINT ( 'NONE',  ( 0.8744876279028306332, 32.34273794994798834, -36.93639603806098393 ) ) ;
#48000=CARTESIAN_POINT ( 'NONE',  ( 4.553261556744873317, -29.36425772793689859, 32.66925058691941075 ) ) ;
#48015=CARTESIAN_POINT ( 'NONE',  ( 0.6253024248130509832, -31.15133493648745855, 37.96101367314130925 ) ) ;
#48017=VECTOR ( 'NONE', #46582, 1000.000000000000000 ) ;
#48020=ORIENTED_EDGE ( 'NONE', *, *, #61644, .T. ) ;
#48024=CARTESIAN_POINT ( 'NONE',  ( 0.6039202388192952409, -45.45307514328631981, -18.58982713388583008 ) ) ;
#48025=ORIENTED_EDGE ( 'NONE', *, *, #60446, .T. ) ;
#48034=ORIENTED_EDGE ( 'NONE', *, *, #41898, .T. ) ;
#48035=CARTESIAN_POINT ( 'NONE',  ( 0.6008123274975392114, 46.46679437735655682, 15.88683642047475786 ) ) ;
#48036=CARTESIAN_POINT ( 'NONE',  ( 0.5980271706414711508, 36.93900200886698570, 32.36602189689958209 ) ) ;
#48039=EDGE_CURVE ( 'NONE', #29160, #26818, #6677, .T. ) ;
#48044=( BOUNDED_SURFACE ( )  B_SPLINE_SURFACE ( 3, 1, ( 
 ( #3799, #12312 ),
 ( #8825, #27939 ),
 ( #31402, #17311 ),
 ( #50501, #7573 ) ),
 .UNSPECIFIED., .F., .F., .F. ) 
 B_SPLINE_SURFACE_WITH_KNOTS ( ( 4, 4 ),
 ( 2, 2 ),
 ( 0.000000000000000000, 1.000000000000000000 ),
 ( 0.000000000000000000, 1.000000000000000000 ),
 .UNSPECIFIED. ) 
 GEOMETRIC_REPRESENTATION_ITEM ( )  RATIONAL_B_SPLINE_SURFACE ( (
 ( 1.000000000000000000, 1.000000000000000000),
 ( 0.9754377213608244057, 0.9999580625633939235),
 ( 0.9754377213608244057, 0.9999580625633939235),
 ( 1.000000000000000000, 1.000000000000000000) ) ) 
 REPRESENTATION_ITEM ( '' )  SURFACE ( )  );
#48047=CARTESIAN_POINT ( 'NONE',  ( 0.1129192098497455998, -35.64954734424960492, 26.00118385641814456 ) ) ;
#48058=CARTESIAN_POINT ( 'NONE',  ( 0.1147471544378676767, -31.47985608552908587, 30.91877826350230762 ) ) ;
#48061=CARTESIAN_POINT ( 'NONE',  ( 0.6000166863083106206, 44.01764848084250303, 21.77774331572114264 ) ) ;
#48062=CARTESIAN_POINT ( 'NONE',  ( -6.072942160501519027, 19.10003410082485331, -2.448031788263385522 ) ) ;
#48065=ORIENTED_EDGE ( 'NONE', *, *, #15513, .T. ) ;
#48066=CARTESIAN_POINT ( 'NONE',  ( 4.975610109902397937, -37.61482235126130291, -31.26618855282533360 ) ) ;
#48070=CARTESIAN_POINT ( 'NONE',  ( 0.8744876279028306332, -48.57046782678520458, 7.159588358747709158 ) ) ;
#48075=CARTESIAN_POINT ( 'NONE',  ( 0.6028777368367060907, 22.79122549791117436, -43.49827432915513015 ) ) ;
#48076=CARTESIAN_POINT ( 'NONE',  ( 0.6029443449137436017, -30.65199525294410421, 38.36658344180290214 ) ) ;
#48078=CARTESIAN_POINT ( 'NONE',  ( -6.078726893082806448, 3.069885851706565916, -19.00973019603939917 ) ) ;
#48083=CARTESIAN_POINT ( 'NONE',  ( 0.1368894036331282649, 14.63874681665168964, -41.62413263434208943 ) ) ;
#48087=CARTESIAN_POINT ( 'NONE',  ( 0.8753041380234530822, -2.462982411634171864, -49.04153388213872944 ) ) ;
#48092=ORIENTED_EDGE ( 'NONE', *, *, #55697, .T. ) ;
#48093=ORIENTED_EDGE ( 'NONE', *, *, #48494, .T. ) ;
#48095=EDGE_CURVE ( 'NONE', #53301, #52962, #58166, .T. ) ;
#48096=CARTESIAN_POINT ( 'NONE',  ( 0.8744876279028263033, -6.955970791787605911, -48.60004650947661275 ) ) ;
#48097=FACE_OUTER_BOUND ( 'NONE', #15279, .T. ) ;
#48098=CARTESIAN_POINT ( 'NONE',  ( 0.5997462898726536595, -47.63132954987522538, -11.95023328037962251 ) ) ;
#48106=CARTESIAN_POINT ( 'NONE',  ( 2.185380717157383135, 44.01027289648202867, 1.384081877772499691 ) ) ;
#48120=ORIENTED_EDGE ( 'NONE', *, *, #56283, .F. ) ;
#48124=CARTESIAN_POINT ( 'NONE',  ( 0.1149546198390367369, 9.551346850799093957, 43.07804937968931114 ) ) ;
#48125=( BOUNDED_SURFACE ( )  B_SPLINE_SURFACE ( 3, 1, ( 
 ( #38853, #52916 ),
 ( #39162, #43867 ),
 ( #9382, #33524 ),
 ( #57908, #15035 ) ),
 .UNSPECIFIED., .F., .F., .F. ) 
 B_SPLINE_SURFACE_WITH_KNOTS ( ( 4, 4 ),
 ( 2, 2 ),
 ( 0.000000000000000000, 1.000000000000000000 ),
 ( 0.000000000000000000, 1.000000000000000000 ),
 .UNSPECIFIED. ) 
 GEOMETRIC_REPRESENTATION_ITEM ( )  RATIONAL_B_SPLINE_SURFACE ( (
 ( 1.000000000000000000, 1.000000000000000000),
 ( 0.7211978278499970862, 0.9934217856018976445),
 ( 0.7211978278499970862, 0.9934217856018976445),
 ( 1.000000000000000000, 1.000000000000000000) ) ) 
 REPRESENTATION_ITEM ( '' )  SURFACE ( )  );
#48127=B_SPLINE_CURVE_WITH_KNOTS ( 'NONE', 3,
 ( #11268, #35398, #26279, #26587 ),
 .UNSPECIFIED., .F., .F.,
 ( 4, 4 ),
 ( 7.757919228897728493E-18, 0.005013413432710142441 ),
 .UNSPECIFIED. ) ;
#48134=CARTESIAN_POINT ( 'NONE',  ( -6.077587904424778920, -8.912150607695132010, -17.06955163264957420 ) ) ;
#48138=DIRECTION ( 'NONE',  ( 0.000000000000000000, 0.000000000000000000, 1.000000000000000000 ) ) ;
#48146=CARTESIAN_POINT ( 'NONE',  ( 0.5997462898726536595, 22.24958391914503153, 43.77793560195857481 ) ) ;
#48152=CARTESIAN_POINT ( 'NONE',  ( 0.6253024248130502061, -30.07742766060853867, -38.81742614778193001 ) ) ;
#48160=DIRECTION ( 'NONE',  ( 0.09722883295013595717, 0.5631913828983637904, -0.8205863880617221273 ) ) ;
#48165=ADVANCED_FACE ( 'NONE', ( #3497 ), #60547, .F. ) ;
#48169=CARTESIAN_POINT ( 'NONE',  ( 0.1119899015040011769, -22.39194001793237021, -38.02055142190635451 ) ) ;
#48185=ORIENTED_EDGE ( 'NONE', *, *, #60803, .T. ) ;
#48189=FACE_OUTER_BOUND ( 'NONE', #51164, .T. ) ;
#48204=CARTESIAN_POINT ( 'NONE',  ( -6.077587904424778920, 19.25606354205735116, 0.006185319731012296589 ) ) ;
#48205=EDGE_CURVE ( 'NONE', #26015, #47983, #32803, .T. ) ;
#48215=ORIENTED_EDGE ( 'NONE', *, *, #1761, .F. ) ;
#48217=CARTESIAN_POINT ( 'NONE',  ( 0.5997462898726536595, -19.39900779840410294, -45.11352487427429736 ) ) ;
#48227=FACE_OUTER_BOUND ( 'NONE', #40218, .T. ) ;
#48228=CARTESIAN_POINT ( 'NONE',  ( 0.1158403557922069033, 29.63666118841771535, 32.68957969730956847 ) ) ;
#48231=LINE ( 'NONE', #43545, #31202 ) ;
#48239=CARTESIAN_POINT ( 'NONE',  ( 0.6029443199889047422, -47.50135088858169752, -12.45629582236396082 ) ) ;
#48240=CARTESIAN_POINT ( 'NONE',  ( 0.7413678028165007206, 40.12541269520018261, 18.28762827187034645 ) ) ;
#48246=COLOUR_RGB ( '', 0.72549020, 0.75294118, 0.79215686) ;
#48247=ADVANCED_BREP_SHAPE_REPRESENTATION ( '', ( #30206, #14677 ), #61711 ) ;
#48248=CARTESIAN_POINT ( 'NONE',  ( -6.077587904424778920, -6.644566705894775716, -18.07334376049006508 ) ) ;
#48251=DIRECTION ( 'NONE',  ( 0.000000000000000000, 0.000000000000000000, 1.000000000000000000 ) ) ;
#48255=ORIENTED_EDGE ( 'NONE', *, *, #13045, .T. ) ;
#48256=DIRECTION ( 'NONE',  ( 0.000000000000000000, 0.000000000000000000, 1.000000000000000000 ) ) ;
#48258=CARTESIAN_POINT ( 'NONE',  ( 0.2940135542859009798, -13.32164043950363030, -42.05680021937001101 ) ) ;
#48269=CARTESIAN_POINT ( 'NONE',  ( 0.8753041380234471980, -34.64850320773107484, -34.79395857525886271 ) ) ;
#48270=CARTESIAN_POINT ( 'NONE',  ( 0.5980271706414711508, -38.93680501037938058, -29.93283244909104823 ) ) ;
#48271=EDGE_LOOP ( 'NONE', ( #6219, #4603, #36571, #19394 ) ) ;
#48274=VERTEX_POINT ( 'NONE', #6253 ) ;
#48279=CARTESIAN_POINT ( 'NONE',  ( 0.1158516988532803521, 25.28452981770051977, 36.16123215172029859 ) ) ;
#48280=ORIENTED_EDGE ( 'NONE', *, *, #47662, .F. ) ;
#48294=CARTESIAN_POINT ( 'NONE',  ( 4.553261556744873317, 12.71466023209499419, 42.04612920360230532 ) ) ;
#48298=CARTESIAN_POINT ( 'NONE',  ( 0.1158403557922069033, 39.73803855110582361, 19.17885813323219324 ) ) ;
#48307=CARTESIAN_POINT ( 'NONE',  ( 3.727782113643637096, 18.41520185780067465, -39.92064774577724506 ) ) ;
#48309=EDGE_CURVE ( 'NONE', #57398, #1942, #6567, .T. ) ;
#48311=CARTESIAN_POINT ( 'NONE',  ( 2.533389852662419894, 26.46405011077438729, 35.17249754379179194 ) ) ;
#48314=FACE_OUTER_BOUND ( 'NONE', #47125, .T. ) ;
#48317=CARTESIAN_POINT ( 'NONE',  ( 4.975610109902397937, 47.16372689271670993, -12.96272628450527264 ) ) ;
#48319=ORIENTED_EDGE ( 'NONE', *, *, #42443, .F. ) ;
#48326=CARTESIAN_POINT ( 'NONE',  ( 0.3676999524040366896, 9.009680404096547690, -43.18305503711933113 ) ) ;
#48331=VERTEX_POINT ( 'NONE', #35441 ) ;
#48332=ORIENTED_EDGE ( 'NONE', *, *, #7129, .T. ) ;
#48336=DIRECTION ( 'NONE',  ( 0.09722883295013591554, 0.3366266327598319563, -0.9366050737423600170 ) ) ;
#48347=CARTESIAN_POINT ( 'NONE',  ( 0.5980271706414711508, -30.07077130958509414, -38.83037413788716918 ) ) ;
#48349=CARTESIAN_POINT ( 'NONE',  ( 0.6000166863083090663, -25.01014854877471549, 42.26483113981026207 ) ) ;
#48355=CARTESIAN_POINT ( 'NONE',  ( -2.601141883200665639, -2.823446916239304105, 14.65686102071543395 ) ) ;
#48357=CARTESIAN_POINT ( 'NONE',  ( 0.3676999524040323597, 43.44964275340426951, -7.620966337964178550 ) ) ;
#48358=CARTESIAN_POINT ( 'NONE',  ( -2.601141883200662974, 5.573165628699144669, 13.84684990690933581 ) ) ;
#48359=CARTESIAN_POINT ( 'NONE',  ( 0.1139756605157203340, -31.41879322388790996, 30.98087558558663446 ) ) ;
#48360=CARTESIAN_POINT ( 'NONE',  ( 0.5997462898726536595, 33.39998138387895921, -35.99990102348682797 ) ) ;
#48366=CARTESIAN_POINT ( 'NONE',  ( 0.1129192098497455998, -35.64954734424960492, 26.00118385641814456 ) ) ;
#48367=CARTESIAN_POINT ( 'NONE',  ( 0.1158816050234199313, -35.35831000359211629, 26.39568061246079367 ) ) ;
#48374=EDGE_CURVE ( 'NONE', #24079, #873, #29786, .T. ) ;
#48382=CARTESIAN_POINT ( 'NONE',  ( 4.226256110419178924, 43.63133558763896502, -5.209011885762705241 ) ) ;
#48389=CARTESIAN_POINT ( 'NONE',  ( 0.5997462898726536595, -47.36625756029543055, 12.96106765957438789 ) ) ;
#48390=( BOUNDED_SURFACE ( )  B_SPLINE_SURFACE ( 3, 1, ( 
 ( #34854, #53921 ),
 ( #49543, #38635 ),
 ( #14819, #11048 ),
 ( #58002, #15432 ) ),
 .UNSPECIFIED., .F., .F., .F. ) 
 B_SPLINE_SURFACE_WITH_KNOTS ( ( 4, 4 ),
 ( 2, 2 ),
 ( 0.000000000000000000, 1.000000000000000000 ),
 ( 0.000000000000000000, 1.000000000000000000 ),
 .UNSPECIFIED. ) 
 GEOMETRIC_REPRESENTATION_ITEM ( )  RATIONAL_B_SPLINE_SURFACE ( (
 ( 1.000000000000000000, 1.000000000000000000),
 ( 0.9754377213608244057, 0.9999580625633939235),
 ( 0.9754377213608244057, 0.9999580625633939235),
 ( 1.000000000000000000, 1.000000000000000000) ) ) 
 REPRESENTATION_ITEM ( '' )  SURFACE ( )  );
#48400=( BOUNDED_SURFACE ( )  B_SPLINE_SURFACE ( 3, 1, ( 
 ( #11069, #58964 ),
 ( #59269, #34878 ),
 ( #25147, #25451 ),
 ( #2570, #49890 ) ),
 .UNSPECIFIED., .F., .F., .F. ) 
 B_SPLINE_SURFACE_WITH_KNOTS ( ( 4, 4 ),
 ( 2, 2 ),
 ( 0.000000000000000000, 1.000000000000000000 ),
 ( 0.000000000000000000, 1.000000000000000000 ),
 .UNSPECIFIED. ) 
 GEOMETRIC_REPRESENTATION_ITEM ( )  RATIONAL_B_SPLINE_SURFACE ( (
 ( 1.000000000000000000, 1.000000000000000000),
 ( 0.9754377213608244057, 0.9999580625633939235),
 ( 0.9754377213608244057, 0.9999580625633939235),
 ( 1.000000000000000000, 1.000000000000000000) ) ) 
 REPRESENTATION_ITEM ( '' )  SURFACE ( )  );
#48401=CARTESIAN_POINT ( 'NONE',  ( 0.1129192098497455998, 33.28205046155587610, 28.96993104685618547 ) ) ;
#48402=ORIENTED_EDGE ( 'NONE', *, *, #32284, .T. ) ;
#48404=CARTESIAN_POINT ( 'NONE',  ( 0.8753041380234530822, -19.05925361776951377, 45.25354328012912219 ) ) ;
#48405=CARTESIAN_POINT ( 'NONE',  ( 3.390910168358336918, 43.97017820572943236, 0.8488610546097931087 ) ) ;
#48412=ORIENTED_EDGE ( 'NONE', *, *, #3609, .F. ) ;
#48418=CARTESIAN_POINT ( 'NONE',  ( 0.6028777368367059797, 4.802101709542340835, -48.87207432145972774 ) ) ;
#48421=CARTESIAN_POINT ( 'NONE',  ( 0.1158816050234199174, 9.824088614716016465, 43.01661683809371794 ) ) ;
#48427=VECTOR ( 'NONE', #6784, 999.9999999999998863 ) ;
#48430=CARTESIAN_POINT ( 'NONE',  ( 0.7044674535452954967, 21.96536420255956656, 43.92408790470009450 ) ) ;
#48431=CARTESIAN_POINT ( 'NONE',  ( 0.2940133293163008088, -7.834165653650041250, 43.41504806042732412 ) ) ;
#48433=ORIENTED_EDGE ( 'NONE', *, *, #7201, .T. ) ;
#48436=DIRECTION ( 'NONE',  ( 0.000000000000000000, 0.000000000000000000, 1.000000000000000000 ) ) ;
#48440=CARTESIAN_POINT ( 'NONE',  ( 0.8753041380234524160, 46.31375555491767670, -16.31485134079719757 ) ) ;
#48453=EDGE_CURVE ( 'NONE', #19013, #3215, #21867, .T. ) ;
#48454=DIRECTION ( 'NONE',  ( 0.09722883295013597105, -0.5223840607312808526, 0.8471490111763407826 ) ) ;
#48466=CARTESIAN_POINT ( 'NONE',  ( 0.8744876279028306332, 23.49358985382604459, 43.10917867646859492 ) ) ;
#48470=ORIENTED_EDGE ( 'NONE', *, *, #4656, .T. ) ;
#48472=CARTESIAN_POINT ( 'NONE',  ( 0.8744876279028306332, 36.80052600666260787, -32.49725120702428427 ) ) ;
#48474=VERTEX_POINT ( 'NONE', #60433 ) ;
#48481=DIRECTION ( 'NONE',  ( 1.000000000000000000, 0.000000000000000000, 0.000000000000000000 ) ) ;
#48488=CARTESIAN_POINT ( 'NONE',  ( 2.299652685299202748, 12.16322236728107242, -47.50092363841177701 ) ) ;
#48494=EDGE_CURVE ( 'NONE', #24124, #5027, #36462, .T. ) ;
#48500=EDGE_LOOP ( 'NONE', ( #24186, #53006, #10893, #26011 ) ) ;
#48503=CARTESIAN_POINT ( 'NONE',  ( -6.078075953587585900, -12.94978436788747977, 14.25125464905995720 ) ) ;
#48504=CARTESIAN_POINT ( 'NONE',  ( 0.5997462898726536595, -13.47075269803155351, 47.22383351542719510 ) ) ;
#48513=CARTESIAN_POINT ( 'NONE',  ( -6.072942160501519027, 18.63017572808498556, -4.870391630012254502 ) ) ;
#48514=CARTESIAN_POINT ( 'NONE',  ( 0.6027444965799114707, -19.75836062456551190, -44.95715406158468852 ) ) ;
#48516=CARTESIAN_POINT ( 'NONE',  ( 0.1158516988532802966, -42.66856749330737841, 11.23990689026689616 ) ) ;
#48518=CARTESIAN_POINT ( 'NONE',  ( 1.657374760986086271, 11.00619257538987128, 42.65857677238747669 ) ) ;
#48521=EDGE_CURVE ( 'NONE', #24982, #37659, #12609, .T. ) ;
#48526=B_SPLINE_CURVE_WITH_KNOTS ( 'NONE', 3,
 ( #16417, #26119, #2293, #21422, #40558, #31125, #3525, #47095, #28270, #13894, #52071, #42699, #8539, #57070, #61158, #17971, #32070, #23275, #22661, #27663, #32372, #37091, #41791, #42401, #13575 ),
 .UNSPECIFIED., .F., .F.,
 ( 4, 3, 3, 3, 3, 3, 3, 3, 4 ),
 ( 2.602085213965210642E-18, 0.0005656085177311379053, 0.001131215744874499406, 0.001696821861372765916, 0.002262427090022497284, 0.002828031679238745925, 0.003393635864401605730, 0.003977030878808131623, 0.004561030005651159000 ),
 .UNSPECIFIED. ) ;
#48532=CARTESIAN_POINT ( 'NONE',  ( 4.335381028904216727, 34.47659336712059286, 34.80116890942834118 ) ) ;
#48533=CARTESIAN_POINT ( 'NONE',  ( 3.559346040607745287, 40.46425943014002513, 17.20680069949995072 ) ) ;
#48542=EDGE_CURVE ( 'NONE', #28462, #7712, #53804, .T. ) ;
#48547=AXIS2_PLACEMENT_3D ( 'NONE', #9395, #33231, #15357 ) ;
#48548=ORIENTED_EDGE ( 'NONE', *, *, #36184, .F. ) ;
#48557=VERTEX_POINT ( 'NONE', #10623 ) ;
#48560=DIRECTION ( 'NONE',  ( 1.000000000000000000, 0.000000000000000000, 0.000000000000000000 ) ) ;
#48562=ORIENTED_EDGE ( 'NONE', *, *, #52104, .F. ) ;
#48569=CARTESIAN_POINT ( 'NONE',  ( 0.7044674535453004927, 46.86672925371311749, 14.67352758780444510 ) ) ;
#48570=CARTESIAN_POINT ( 'NONE',  ( 0.1129192098497447394, -17.41650932123218354, 40.54154647825593827 ) ) ;
#48571=VERTEX_POINT ( 'NONE', #44168 ) ;
#48574=( BOUNDED_SURFACE ( )  B_SPLINE_SURFACE ( 3, 1, ( 
 ( #33568, #5327 ),
 ( #39203, #57950 ),
 ( #53262, #33878 ),
 ( #58564, #5019 ) ),
 .UNSPECIFIED., .F., .F., .F. ) 
 B_SPLINE_SURFACE_WITH_KNOTS ( ( 4, 4 ),
 ( 2, 2 ),
 ( 0.000000000000000000, 1.000000000000000000 ),
 ( 0.000000000000000000, 1.000000000000000000 ),
 .UNSPECIFIED. ) 
 GEOMETRIC_REPRESENTATION_ITEM ( )  RATIONAL_B_SPLINE_SURFACE ( (
 ( 1.000000000000000000, 1.000000000000000000),
 ( 0.9953485035131437453, 0.8621029689291523912),
 ( 0.9953485035131437453, 0.8621029689291523912),
 ( 1.000000000000000000, 1.000000000000000000) ) ) 
 REPRESENTATION_ITEM ( '' )  SURFACE ( )  );
#48580=CARTESIAN_POINT ( 'NONE',  ( 0.6039202388192953519, 48.99530948556961363, -3.320144765254160912 ) ) ;
#48581=CARTESIAN_POINT ( 'NONE',  ( 0.8744876279028306332, -48.79802643035336018, -5.394688766001929814 ) ) ;
#48591=EDGE_CURVE ( 'NONE', #31957, #28574, #45455, .T. ) ;
#48592=CARTESIAN_POINT ( 'NONE',  ( 0.7242486021783849370, -35.83732651437340166, 33.56631482120374699 ) ) ;
#48593=CARTESIAN_POINT ( 'NONE',  ( -6.078075953587585900, 18.62492360731175012, 4.889518879085924752 ) ) ;
#48598=CARTESIAN_POINT ( 'NONE',  ( 0.1157991065609915715, -43.75142591887181709, -5.723206758729824983 ) ) ;
#48603=LINE ( 'NONE', #43947, #53193 ) ;
#48604=AXIS2_PLACEMENT_3D ( 'NONE', #26882, #41018, #46938 ) ;
#48611=CARTESIAN_POINT ( 'NONE',  ( 2.185380717157383135, 26.35783754162028814, 35.27157783820779002 ) ) ;
#48619=ORIENTED_EDGE ( 'NONE', *, *, #13452, .F. ) ;
#48621=CARTESIAN_POINT ( 'NONE',  ( 0.6000166863083090663, -20.35571918921390377, -44.69304395538888031 ) ) ;
#48622=ORIENTED_EDGE ( 'NONE', *, *, #38809, .F. ) ;
#48630=ORIENTED_EDGE ( 'NONE', *, *, #26293, .T. ) ;
#48631=VERTEX_POINT ( 'NONE', #25949 ) ;
#48632=CARTESIAN_POINT ( 'NONE',  ( 0.3676999524040323597, 30.26295534861902681, -32.09523511193413725 ) ) ;
#48637=CARTESIAN_POINT ( 'NONE',  ( 0.3676999524040366896, -43.63756228305280160, 6.458617600967457406 ) ) ;
#48640=CARTESIAN_POINT ( 'NONE',  ( 0.1152809850208375009, -1.193148287966932397, -44.10806819225567921 ) ) ;
#48643=CARTESIAN_POINT ( 'NONE',  ( -6.078726893082806448, 9.979253153318763836, 16.46841060244423360 ) ) ;
#48646=CARTESIAN_POINT ( 'NONE',  ( 0.6029443199889047422, -13.97243605900292707, -47.07768762833914877 ) ) ;
#48648=CARTESIAN_POINT ( 'NONE',  ( 0.8753041380234530822, -24.68967207985825496, 42.44476905888459584 ) ) ;
#48649=CARTESIAN_POINT ( 'NONE',  ( 1.112077966505211846, -5.996671051578201350, 43.67001558767432812 ) ) ;
#48659=CARTESIAN_POINT ( 'NONE',  ( 0.6000166863083090663, 49.04012132094738519, -2.624877622902973329 ) ) ;
#48667=EDGE_CURVE ( 'NONE', #20580, #60741, #44672, .T. ) ;
#48670=CARTESIAN_POINT ( 'NONE',  ( 0.1158516988532803521, -7.090803588212395425, -43.55069073282524528 ) ) ;
#48671=CARTESIAN_POINT ( 'NONE',  ( 0.6026777506516367566, 41.25117635047293163, 26.64370170114134950 ) ) ;
#48672=EDGE_CURVE ( 'NONE', #25125, #40399, #27443, .T. ) ;
#48689=CONICAL_SURFACE ( 'NONE', #56677, 43.92652462719577500, 1.486293639869522343 ) ;
#48701=CARTESIAN_POINT ( 'NONE',  ( 0.5980271706414711508, 43.94069670602949884, 21.93773953328807735 ) ) ;
#48716=CARTESIAN_POINT ( 'NONE',  ( 0.1129192098497455998, -40.71518461128082578, -17.00663193740825463 ) ) ;
#48717=B_SPLINE_CURVE_WITH_KNOTS ( 'NONE', 3,
 ( #7306, #12671, #45883, #36170 ),
 .UNSPECIFIED., .F., .F.,
 ( 4, 4 ),
 ( 0.000000000000000000, 0.005013413432710150247 ),
 .UNSPECIFIED. ) ;
#48718=ORIENTED_EDGE ( 'NONE', *, *, #44180, .T. ) ;
#48722=CARTESIAN_POINT ( 'NONE',  ( 0.3676999524040323597, 42.11837424242189343, -13.11461530118710428 ) ) ;
#48725=ORIENTED_EDGE ( 'NONE', *, *, #61497, .F. ) ;
#48726=DIRECTION ( 'NONE',  ( -1.000000000000000000, -0.000000000000000000, -0.000000000000000000 ) ) ;
#48727=CARTESIAN_POINT ( 'NONE',  ( 0.1139756605157203201, 10.20580263603494409, 42.92780931109022902 ) ) ;
#48731=CARTESIAN_POINT ( 'NONE',  ( 0.8744876279028263033, 43.84003649649913115, 22.09980204357308153 ) ) ;
#48748=CARTESIAN_POINT ( 'NONE',  ( 0.7242003506639976829, 48.94187641115512832, -3.962878686162724318 ) ) ;
#48755=( BOUNDED_SURFACE ( )  B_SPLINE_SURFACE ( 3, 1, ( 
 ( #19322, #47516 ),
 ( #4564, #19025 ),
 ( #38142, #48430 ),
 ( #48134, #53119 ) ),
 .UNSPECIFIED., .F., .F., .F. ) 
 B_SPLINE_SURFACE_WITH_KNOTS ( ( 4, 4 ),
 ( 2, 2 ),
 ( 0.000000000000000000, 1.000000000000000000 ),
 ( 0.000000000000000000, 1.000000000000000000 ),
 .UNSPECIFIED. ) 
 GEOMETRIC_REPRESENTATION_ITEM ( )  RATIONAL_B_SPLINE_SURFACE ( (
 ( 1.000000000000000000, 1.000000000000000000),
 ( 0.9953485035131437453, 0.8621029689291523912),
 ( 0.9953485035131437453, 0.8621029689291523912),
 ( 1.000000000000000000, 1.000000000000000000) ) ) 
 REPRESENTATION_ITEM ( '' )  SURFACE ( )  );
#48763=CARTESIAN_POINT ( 'NONE',  ( 0.1129192098497447394, -42.80154921430116843, -10.72283417016740259 ) ) ;
#48774=CARTESIAN_POINT ( 'NONE',  ( 0.7044674535452954967, 28.78324386660444389, -39.79104918604790697 ) ) ;
#48784=CARTESIAN_POINT ( 'NONE',  ( -2.739355103387248747, -14.76959508014216738, 2.169476462111838977 ) ) ;
#48787=CARTESIAN_POINT ( 'NONE',  ( 5.901764892641288895, 1.612679500413170652, 48.94272910523713449 ) ) ;
#48791=CARTESIAN_POINT ( 'NONE',  ( 0.7948884756798498818, 21.93744097139700600, 43.92547470690128364 ) ) ;
#48792=FACE_OUTER_BOUND ( 'NONE', #12302, .T. ) ;
#48794=ORIENTED_EDGE ( 'NONE', *, *, #16258, .F. ) ;
#48798=ORIENTED_EDGE ( 'NONE', *, *, #32980, .F. ) ;
#48800=VERTEX_POINT ( 'NONE', #42233 ) ;
#48804=ORIENTED_EDGE ( 'NONE', *, *, #4893, .T. ) ;
#48807=CARTESIAN_POINT ( 'NONE',  ( -2.601141883200665639, -10.40580972892344036, -10.70114719807324732 ) ) ;
#48813=EDGE_CURVE ( 'NONE', #29981, #44808, #4235, .T. ) ;
#48817=CARTESIAN_POINT ( 'NONE',  ( -6.078457390727109555, 7.798524762019232170, 17.60617853407379130 ) ) ;
#48822=CARTESIAN_POINT ( 'NONE',  ( 4.975610109902397937, 42.33317580307156192, -24.50207406657668230 ) ) ;
#48825=CARTESIAN_POINT ( 'NONE',  ( -6.063463321072278589, 18.63085535290914052, -4.869464169541319443 ) ) ;
#48828=CARTESIAN_POINT ( 'NONE',  ( 0.1139756605157203201, -42.57864162325638802, 11.57646307009704856 ) ) ;
#48833=FACE_OUTER_BOUND ( 'NONE', #39549, .T. ) ;
#48835=CARTESIAN_POINT ( 'NONE',  ( 4.975610109902397937, 0.000000000000000000, 0.000000000000000000 ) ) ;
#48836=VECTOR ( 'NONE', #61206, 1000.000000000000000 ) ;
#48837=DIRECTION ( 'NONE',  ( 0.000000000000000000, 0.000000000000000000, 1.000000000000000000 ) ) ;
#48838=CARTESIAN_POINT ( 'NONE',  ( 3.221118495291109163, -19.51545154787827840, -39.41964701191737674 ) ) ;
#48842=AXIS2_PLACEMENT_3D ( 'NONE', #37363, #32349, #51422 ) ;
#48845=CARTESIAN_POINT ( 'NONE',  ( 0.6021447746440204973, -47.56697795495951908, -12.20343178457942912 ) ) ;
#48848=ORIENTED_EDGE ( 'NONE', *, *, #40723, .F. ) ;
#48852=EDGE_CURVE ( 'NONE', #27996, #17526, #55064, .T. ) ;
#48863=CARTESIAN_POINT ( 'NONE',  ( 4.834790513006555379, 43.96797211434383001, 17.30337449969409036 ) ) ;
#48867=ORIENTED_EDGE ( 'NONE', *, *, #30649, .F. ) ;
#48871=CARTESIAN_POINT ( 'NONE',  ( 0.1139756605157202923, -1.016815145924514940, 44.11259804924259242 ) ) ;
#48875=CARTESIAN_POINT ( 'NONE',  ( 0.6000166863083090663, 44.01764848084281567, -21.77774331572052802 ) ) ;
#48879=CARTESIAN_POINT ( 'NONE',  ( 0.1119899015040012186, -6.487605976147421849, -43.64484250046918845 ) ) ;
#48880=ORIENTED_EDGE ( 'NONE', *, *, #8319, .T. ) ;
#48881=EDGE_CURVE ( 'NONE', #4904, #11211, #15476, .T. ) ;
#48887=VERTEX_POINT ( 'NONE', #53432 ) ;
#48888=PRODUCT_DEFINITION_FORMATION_WITH_SPECIFIED_SOURCE ( 'ANY', '', #3260, .NOT_KNOWN. ) ;
#48890=CARTESIAN_POINT ( 'NONE',  ( 0.1129192098497455998, 24.84520063729130612, 36.46461014570008530 ) ) ;
#48893=CARTESIAN_POINT ( 'NONE',  ( -6.077587904424778920, 5.472951620448459842, 18.46192898789725945 ) ) ;
#48901=ADVANCED_FACE ( 'NONE', ( #29637 ), #43397, .F. ) ;
#48904=DIRECTION ( 'NONE',  ( -1.000000000000000000, -0.000000000000000000, -0.000000000000000000 ) ) ;
#48907=VECTOR ( 'NONE', #41198, 1000.000000000000000 ) ;
#48924=CARTESIAN_POINT ( 'NONE',  ( 0.6253024248130482077, -14.62917846302403291, 46.87676785908598731 ) ) ;
#48926=EDGE_CURVE ( 'NONE', #19080, #34420, #58833, .T. ) ;
#48927=AXIS2_PLACEMENT_3D ( 'NONE', #57024, #48481, #17146 ) ;
#48929=ORIENTED_EDGE ( 'NONE', *, *, #49050, .T. ) ;
#48940=CARTESIAN_POINT ( 'NONE',  ( 0.1365634738349425226, -11.94249462058610511, -42.47633978888153905 ) ) ;
#48942=CARTESIAN_POINT ( 'NONE',  ( 0.7242486021783812733, 46.85219368132524664, -14.69297143608327261 ) ) ;
#48949=ORIENTED_EDGE ( 'NONE', *, *, #58617, .F. ) ;
#48952=CARTESIAN_POINT ( 'NONE',  ( 0.1368894036331260167, 43.42692794240723941, 7.807896990118506686 ) ) ;
#48959=CARTESIAN_POINT ( 'NONE',  ( -6.077587904424778920, 17.84644683124317055, -7.231898567702747194 ) ) ;
#48960=CARTESIAN_POINT ( 'NONE',  ( 0.8753041380234465318, 48.01981714478390728, 10.25843502950123209 ) ) ;
#48963=CARTESIAN_POINT ( 'NONE',  ( 1.657374760986086271, -42.91185007314042821, -9.973142461258767355 ) ) ;
#48965=CARTESIAN_POINT ( 'NONE',  ( 3.559346040607745287, 7.771245481046687331, -43.27860932626300894 ) ) ;
#48966=CARTESIAN_POINT ( 'NONE',  ( 0.5549461598389365813, -6.171197268387964563, 43.67074558261452211 ) ) ;
#48973=CARTESIAN_POINT ( 'NONE',  ( 0.5980271706414711508, 49.05158475245164595, -2.447708339389331744 ) ) ;
#48976=CARTESIAN_POINT ( 'NONE',  ( 4.834790513006553603, 13.00147983508858474, 45.42632345922534398 ) ) ;
#48983=CARTESIAN_POINT ( 'NONE',  ( 0.1152809850208375980, -6.823767124828218122, -43.59336514557998754 ) ) ;
#48988=CARTESIAN_POINT ( 'NONE',  ( 0.6008123274975391004, 33.33610813491660707, -36.05909657181671690 ) ) ;
#48993=CARTESIAN_POINT ( 'NONE',  ( 0.6016118706126977189, 48.13416090936247116, 9.729008599828327775 ) ) ;
#49000=CARTESIAN_POINT ( 'NONE',  ( -2.601141883200665639, -4.674544242619546708, 14.17547401652520023 ) ) ;
#49002=ORIENTED_EDGE ( 'NONE', *, *, #61076, .T. ) ;
#49005=CARTESIAN_POINT ( 'NONE',  ( 1.830465331921977912, -43.51298832088521351, -6.855355808774353576 ) ) ;
#49014=CARTESIAN_POINT ( 'NONE',  ( 0.5987334308729317378, -0.9689265936116925326, 49.09810676417087905 ) ) ;
#49018=CARTESIAN_POINT ( 'NONE',  ( -6.078726893082806448, 5.482141236671949969, 18.45914864585853721 ) ) ;
#49019=CARTESIAN_POINT ( 'NONE',  ( 0.1119898979215348395, 43.99420329544292940, -3.386943260680373324 ) ) ;
#49022=FACE_OUTER_BOUND ( 'NONE', #37796, .T. ) ;
#49028=CARTESIAN_POINT ( 'NONE',  ( 0.1152339509894530906, -40.98274918812253986, -16.35105377150610195 ) ) ;
#49034=B_SPLINE_CURVE_WITH_KNOTS ( 'NONE', 3,
 ( #3894, #14260, #56522, #46853, #36839, #60913 ),
 .UNSPECIFIED., .F., .F.,
 ( 4, 2, 4 ),
 ( 3.218090308046738493E-18, 0.0002447193893791694912, 0.0004894387787583358383 ),
 .UNSPECIFIED. ) ;
#49035=ORIENTED_EDGE ( 'NONE', *, *, #29878, .F. ) ;
#49043=CARTESIAN_POINT ( 'NONE',  ( 4.834790513006555379, 13.00147983508924376, -45.42632345922514503 ) ) ;
#49044=B_SPLINE_CURVE_WITH_KNOTS ( 'NONE', 3,
 ( #3747, #52289, #32913, #51990 ),
 .UNSPECIFIED., .F., .F.,
 ( 4, 4 ),
 ( 0.000000000000000000, 0.004442905043737215703 ),
 .UNSPECIFIED. ) ;
#49045=CARTESIAN_POINT ( 'NONE',  ( -6.057079549204054558, -19.21686681020089082, -1.242280603864441613 ) ) ;
#49047=CARTESIAN_POINT ( 'NONE',  ( 0.1368894036331287922, -31.24908945182261633, 31.15053345217901537 ) ) ;
#49050=EDGE_CURVE ( 'NONE', #43021, #55001, #7186, .T. ) ;
#49052=ORIENTED_EDGE ( 'NONE', *, *, #39106, .F. ) ;
#49057=EDGE_LOOP ( 'NONE', ( #43773, #11225, #11428, #61958 ) ) ;
#49059=CARTESIAN_POINT ( 'NONE',  ( 4.975610109902397937, 8.374023221151757568, 48.19050883970187016 ) ) ;
#49063=CARTESIAN_POINT ( 'NONE',  ( 0.6016117650947688800, -19.55888191429318468, 45.04443575523212218 ) ) ;
#49068=B_SPLINE_CURVE_WITH_KNOTS ( 'NONE', 3,
 ( #11263, #30355, #44807, #59472 ),
 .UNSPECIFIED., .F., .F.,
 ( 4, 4 ),
 ( 0.000000000000000000, 0.005013413432710142441 ),
 .UNSPECIFIED. ) ;
#49071=CARTESIAN_POINT ( 'NONE',  ( 0.8744876279028306332, 48.35212675551500183, 8.510105087371359289 ) ) ;
#49072=ORIENTED_EDGE ( 'NONE', *, *, #60749, .T. ) ;
#49077=EDGE_CURVE ( 'NONE', #22282, #15568, #49034, .T. ) ;
#49080=CARTESIAN_POINT ( 'NONE',  ( 0.1154773475650540809, 9.643119492786247804, -43.05756468373434842 ) ) ;
#49082=VERTEX_POINT ( 'NONE', #57128 ) ;
#49091=CARTESIAN_POINT ( 'NONE',  ( 4.553261556744873317, 17.98701270972406618, 40.07501640179154379 ) ) ;
#49098=CARTESIAN_POINT ( 'NONE',  ( 4.975610109902397937, 20.32389311291169065, 44.49032227207074186 ) ) ;
#49100=CARTESIAN_POINT ( 'NONE',  ( -6.072942160501519027, -11.02874586101359000, 15.78514893886643122 ) ) ;
#49101=CARTESIAN_POINT ( 'NONE',  ( 0.6000166863083106206, 46.44114019838972496, 15.97009639238170919 ) ) ;
#49102=CARTESIAN_POINT ( 'NONE',  ( 0.7242486021783836048, -48.58740928524382952, -7.090495139422609228 ) ) ;
#49103=CARTESIAN_POINT ( 'NONE',  ( 0.6000166863083106206, 5.235566842224463890, 48.83044461756470866 ) ) ;
#49104=ADVANCED_FACE ( 'NONE', ( #15176 ), #18496, .F. ) ;
#49108=ORIENTED_EDGE ( 'NONE', *, *, #52542, .T. ) ;
#49113=CARTESIAN_POINT ( 'NONE',  ( 0.8744876279028263033, 11.79038800009220722, -47.65854384249244191 ) ) ;
#49117=CARTESIAN_POINT ( 'NONE',  ( 0.3676999524040366896, 41.59822836379080968, -14.68121181363270367 ) ) ;
#49124=CARTESIAN_POINT ( 'NONE',  ( 3.221118495291108275, 30.94270617206736063, 31.26196338061407332 ) ) ;
#49129=CARTESIAN_POINT ( 'NONE',  ( 4.834790513006553603, 45.58586227964563875, 12.43054709759641341 ) ) ;
#49134=CARTESIAN_POINT ( 'NONE',  ( 0.6029443449137436017, -19.83806479063774475, -44.92205163776239374 ) ) ;
#49137=CARTESIAN_POINT ( 'NONE',  ( 1.834102595619085507, 11.06747130359428510, 42.63459655962281403 ) ) ;
#49139=CONICAL_SURFACE ( 'NONE', #35155, 43.92652462719577500, 1.486293639869522343 ) ;
#49140=CARTESIAN_POINT ( 'NONE',  ( 0.6008122571543322854, 37.10904107904137561, -32.16323398943794842 ) ) ;
#49143=CARTESIAN_POINT ( 'NONE',  ( 4.975610109902397937, -28.45381238669816426, 39.78479568629648355 ) ) ;
#49146=CARTESIAN_POINT ( 'NONE',  ( 4.390527457369402420, -20.03612350786727703, -39.09909322997283709 ) ) ;
#49150=ADVANCED_FACE ( 'NONE', ( #54828 ), #4929, .F. ) ;
#49156=VERTEX_POINT ( 'NONE', #5727 ) ;
#49160=EDGE_CURVE ( 'NONE', #60741, #17733, #46845, .T. ) ;
#49162=B_SPLINE_CURVE_WITH_KNOTS ( 'NONE', 3,
 ( #25646, #44789, #20957, #8936, #125, #18041, #52146, #37158, #23350, #56535, #13972, #3594, #37465, #13651, #32442, #47166, #4207, #22729, #47466 ),
 .UNSPECIFIED., .F., .F.,
 ( 4, 3, 3, 3, 3, 3, 4 ),
 ( 0.000000000000000000, 0.0002612768053151720343, 0.0003919133833142926602, 0.0005225499612322615124, 0.0006531865391693370427, 0.0008112755173415195321, 0.0009693688056799733320 ),
 .UNSPECIFIED. ) ;
#49169=CARTESIAN_POINT ( 'NONE',  ( 1.830465331921977024, -28.41911767823002322, 33.65605155494778700 ) ) ;
#49173=ORIENTED_EDGE ( 'NONE', *, *, #48453, .F. ) ;
#49181=B_SPLINE_CURVE_WITH_KNOTS ( 'NONE', 3,
 ( #42623, #33224, #57000, #51995, #28190, #3445, #4053, #47311, #13189, #61684, #18817, #51067, #42940, #8161, #32290, #8454, #22892, #15348, #25351, #10959, #19738, #597, #34456, #29733, #53830 ),
 .UNSPECIFIED., .F., .F.,
 ( 4, 3, 3, 3, 3, 3, 3, 3, 4 ),
 ( 6.254634441385501517E-18, 0.0005656085177311410495, 0.001131215744874500924, 0.001696821861372766133, 0.002262427090022499018, 0.002828031679238747226, 0.003393635864401604862, 0.003977030878808132490, 0.004561030005651159867 ),
 .UNSPECIFIED. ) ;
#49184=CARTESIAN_POINT ( 'NONE',  ( 4.975610109902397937, -37.61482235126175766, 31.26618855282478648 ) ) ;
#49185=CARTESIAN_POINT ( 'NONE',  ( 0.8744876279028263033, -14.81965677138014037, 46.80521149998127584 ) ) ;
#49186=CARTESIAN_POINT ( 'NONE',  ( 0.2940133293163009753, -6.245378493101266137, -43.67191084731638995 ) ) ;
#49187=ORIENTED_EDGE ( 'NONE', *, *, #55692, .T. ) ;
#49189=CARTESIAN_POINT ( 'NONE',  ( -6.063463321072276813, 15.44190279602993243, 11.50513322467118549 ) ) ;
#49191=EDGE_LOOP ( 'NONE', ( #54954, #29375, #46679, #21439 ) ) ;
#49195=CARTESIAN_POINT ( 'NONE',  ( 0.1157991065609915715, 25.17735855925881694, 36.23593494745534116 ) ) ;
#49197=CARTESIAN_POINT ( 'NONE',  ( -2.601141883200662974, -0.9259886695526062805, -14.89758277215632098 ) ) ;
#49198=CARTESIAN_POINT ( 'NONE',  ( 0.8753041380234530822, -14.82204010568715447, -46.81287702094778780 ) ) ;
#49199=DIRECTION ( 'NONE',  ( -1.000000000000000000, -0.000000000000000000, -0.000000000000000000 ) ) ;
#49207=ADVANCED_FACE ( 'NONE', ( #55752 ), #24517, .F. ) ;
#49211=CARTESIAN_POINT ( 'NONE',  ( -6.078726893082806448, 18.62537590944114640, 4.887679766589625885 ) ) ;
#49216=CARTESIAN_POINT ( 'NONE',  ( 4.694002226626921015, -9.808094470216756733, 44.52062504401121146 ) ) ;
#49221=DIRECTION ( 'NONE',  ( 0.09722883295013598492, -0.2759265041300023591, -0.9562484605800682935 ) ) ;
#49224=CARTESIAN_POINT ( 'NONE',  ( 2.879087469061463178, -3.139839183809346235, -43.88898593819631344 ) ) ;
#49225=CARTESIAN_POINT ( 'NONE',  ( 1.834102595619085729, 19.20967481895078066, -39.63819040026742613 ) ) ;
#49226=ORIENTED_EDGE ( 'NONE', *, *, #46191, .T. ) ;
#49230=EDGE_CURVE ( 'NONE', #3214, #31693, #18183, .T. ) ;
#49232=ORIENTED_EDGE ( 'NONE', *, *, #45647, .F. ) ;
#49234=DIRECTION ( 'NONE',  ( -1.000000000000000000, 0.000000000000000000, 0.000000000000000000 ) ) ;
#49239=CARTESIAN_POINT ( 'NONE',  ( -6.078075953587585900, 7.789670135765644154, 17.61011679186417922 ) ) ;
#49242=EDGE_CURVE ( 'NONE', #15459, #25014, #16883, .T. ) ;
#49244=CARTESIAN_POINT ( 'NONE',  ( 0.6253024248130479856, 46.81662110580109726, -14.82053358194312764 ) ) ;
#49261=CARTESIAN_POINT ( 'NONE',  ( 1.834102595619085729, 8.527011080115599384, -43.21444002757956326 ) ) ;
#49262=CARTESIAN_POINT ( 'NONE',  ( 0.3676999524040366896, -6.224421213753956295, 43.67158302462379282 ) ) ;
#49267=CARTESIAN_POINT ( 'NONE',  ( 1.834102595619085507, 42.19596157538738623, 12.63719001938783926 ) ) ;
#49273=EDGE_CURVE ( 'NONE', #9094, #20821, #34085, .T. ) ;
#49274=B_SPLINE_CURVE_WITH_KNOTS ( 'NONE', 3,
 ( #34533, #30735, #44876, #54844 ),
 .UNSPECIFIED., .F., .F.,
 ( 4, 4 ),
 ( 0.000000000000000000, 0.004444103432399267896 ),
 .UNSPECIFIED. ) ;
#49276=CARTESIAN_POINT ( 'NONE',  ( 3.559346040607745287, -14.46634168074828608, -41.52294835290280162 ) ) ;
#49279=CARTESIAN_POINT ( 'NONE',  ( 2.648799415243696664, 33.97949776740117755, -35.35408314133994168 ) ) ;
#49284=CARTESIAN_POINT ( 'NONE',  ( 0.3676999524040323597, 33.04872056100222011, 29.21870381457103605 ) ) ;
#49292=CARTESIAN_POINT ( 'NONE',  ( 0.5997462898726536595, 49.03735788587803768, -2.624721264558313560 ) ) ;
#49293=DIRECTION ( 'NONE',  ( 0.09722883295013594329, -0.6264263058867762801, -0.7733929385093980535 ) ) ;
#49294=ORIENTED_EDGE ( 'NONE', *, *, #60368, .F. ) ;
#49297=CARTESIAN_POINT ( 'NONE',  ( 0.7242003506639999033, 49.04682596084168011, 2.328204736043216538 ) ) ;
#49298=CARTESIAN_POINT ( 'NONE',  ( 0.1156867017252034557, 41.83675885982486875, 14.02242544569421234 ) ) ;
#49305=AXIS2_PLACEMENT_3D ( 'NONE', #34970, #25239, #7031 ) ;
#49310=CARTESIAN_POINT ( 'NONE',  ( 0.1129192098497455998, 33.91039995638899995, -28.23183597612607798 ) ) ;
#49313=B_SPLINE_CURVE_WITH_KNOTS ( 'NONE', 3,
 ( #10279, #54085, #5241, #34401, #24373, #29372 ),
 .UNSPECIFIED., .F., .F.,
 ( 4, 2, 4 ),
 ( 0.000000000000000000, 0.0002447195606305749629, 0.0004894391212611499259 ),
 .UNSPECIFIED. ) ;
#49316=LINE ( 'NONE', #6370, #45620 ) ;
#49331=CARTESIAN_POINT ( 'NONE',  ( 0.6021447746440204973, -35.09404424325450833, 34.35038861120762732 ) ) ;
#49333=CARTESIAN_POINT ( 'NONE',  ( -2.601141883200662974, -14.54530301301453932, -3.351057703021369960 ) ) ;
#49334=B_SPLINE_CURVE_WITH_KNOTS ( 'NONE', 3,
 ( #12330, #41457, #55829, #12951, #59601, #35519 ),
 .UNSPECIFIED., .F., .F.,
 ( 4, 2, 4 ),
 ( 1.843143693225357538E-18, 0.0002447193893791695996, 0.0004894387787583373561 ),
 .UNSPECIFIED. ) ;
#49340=CARTESIAN_POINT ( 'NONE',  ( 0.1156495703730067298, 9.951406056163939695, 42.98735245088273160 ) ) ;
#49348=ADVANCED_FACE ( 'NONE', ( #57584 ), #33330, .F. ) ;
#49349=CARTESIAN_POINT ( 'NONE',  ( -6.077587904424778920, -19.21610359950803115, -1.239912838430589970 ) ) ;
#49350=CARTESIAN_POINT ( 'NONE',  ( 0.3676999524040323597, -35.84016207189440451, 25.71834687500696859 ) ) ;
#49360=EDGE_CURVE ( 'NONE', #51862, #29310, #8631, .T. ) ;
#49362=CARTESIAN_POINT ( 'NONE',  ( 0.5997462898726536595, -13.47075269803155351, 47.22383351542719510 ) ) ;
#49363=CARTESIAN_POINT ( 'NONE',  ( 0.6027444965799114707, 22.59817970401703846, 43.59886225525149683 ) ) ;
#49364=CARTESIAN_POINT ( 'NONE',  ( 0.1152809850208375841, 44.04716389649329500, -2.606268436906177488 ) ) ;
#49374=ORIENTED_EDGE ( 'NONE', *, *, #7690, .F. ) ;
#49378=CARTESIAN_POINT ( 'NONE',  ( 0.2285344041767065348, -42.86264843728616825, -10.45440286372519623 ) ) ;
#49390=VECTOR ( 'NONE', #24483, 1000.000000000000114 ) ;
#49391=CARTESIAN_POINT ( 'NONE',  ( 0.7044674535452954967, -26.17468433047410770, 41.55344297421019206 ) ) ;
#49396=ORIENTED_EDGE ( 'NONE', *, *, #26903, .T. ) ;
#49403=LINE ( 'NONE', #29074, #22360 ) ;
#49404=VECTOR ( 'NONE', #55717, 1000.000000000000000 ) ;
#49417=CARTESIAN_POINT ( 'NONE',  ( 0.1147471544378677460, 43.36887420253955128, 8.129756384882995235 ) ) ;
#49419=CARTESIAN_POINT ( 'NONE',  ( 4.553261556744873317, 40.63093864075514006, -16.69330377710856084 ) ) ;
#49421=EDGE_CURVE ( 'NONE', #12972, #4753, #23826, .T. ) ;
#49424=CARTESIAN_POINT ( 'NONE',  ( -6.072942160501519027, -18.90394509709863513, 3.666745430882924150 ) ) ;
#49425=CARTESIAN_POINT ( 'NONE',  ( 0.6000166863083090663, 48.10206967781414278, -9.900220927795849946 ) ) ;
#49428=CARTESIAN_POINT ( 'NONE',  ( -6.078726893082806448, -16.14009859332552921, 10.50196451462540992 ) ) ;
#49429=ORIENTED_EDGE ( 'NONE', *, *, #3675, .T. ) ;
#49432=EDGE_CURVE ( 'NONE', #1848, #44276, #12432, .T. ) ;
#49433=CARTESIAN_POINT ( 'NONE',  ( 4.975610109902397937, 42.33317580307119954, 24.50207406657730047 ) ) ;
#49440=CARTESIAN_POINT ( 'NONE',  ( -6.063463321072278589, -4.269814012169691253, -18.77735712982391902 ) ) ;
#49441=CARTESIAN_POINT ( 'NONE',  ( 0.5549461598389365813, 10.66800373468012175, 42.79499260174787878 ) ) ;
#49447=CARTESIAN_POINT ( 'NONE',  ( 0.5997462898726536595, -47.63132954987539591, 11.95023328037892441 ) ) ;
#49453=CARTESIAN_POINT ( 'NONE',  ( 1.296416391601052265, -18.84992721815818228, -39.83701316547587368 ) ) ;
#49456=CARTESIAN_POINT ( 'NONE',  ( 2.299746137290199055, -9.094862155372984702, -48.18261948110441750 ) ) ;
#49462=CARTESIAN_POINT ( 'NONE',  ( 2.299746137290199943, -21.01915573909004920, -44.29984683610109641 ) ) ;
#49467=CARTESIAN_POINT ( 'NONE',  ( 0.1129192098497455998, 43.21532672376827833, 8.909956450124401073 ) ) ;
#49469=CARTESIAN_POINT ( 'NONE',  ( 4.226256110419178924, -43.87543286663103004, 2.402840143026613973 ) ) ;
#49471=EDGE_CURVE ( 'NONE', #46958, #2310, #15649, .T. ) ;
#49479=VERTEX_POINT ( 'NONE', #30033 ) ;
#49482=( BOUNDED_SURFACE ( )  B_SPLINE_SURFACE ( 3, 1, ( 
 ( #27796, #22479 ),
 ( #60988, #26872 ),
 ( #56288, #17175 ),
 ( #17475, #46012 ) ),
 .UNSPECIFIED., .F., .F., .F. ) 
 B_SPLINE_SURFACE_WITH_KNOTS ( ( 4, 4 ),
 ( 2, 2 ),
 ( 0.000000000000000000, 1.000000000000000000 ),
 ( 0.000000000000000000, 1.000000000000000000 ),
 .UNSPECIFIED. ) 
 GEOMETRIC_REPRESENTATION_ITEM ( )  RATIONAL_B_SPLINE_SURFACE ( (
 ( 1.000000000000000000, 1.000000000000000000),
 ( 0.7211978278499968642, 0.9934217856018975334),
 ( 0.7211978278499968642, 0.9934217856018975334),
 ( 1.000000000000000000, 1.000000000000000000) ) ) 
 REPRESENTATION_ITEM ( '' )  SURFACE ( )  );
#49484=VECTOR ( 'NONE', #61886, 1000.000000000000000 ) ;
#49485=ORIENTED_EDGE ( 'NONE', *, *, #33721, .F. ) ;
#49493=DIRECTION ( 'NONE',  ( -1.000000000000000000, -0.000000000000000000, -0.000000000000000000 ) ) ;
#49494=CARTESIAN_POINT ( 'NONE',  ( 5.901764892641307547, -41.06410928599490262, 26.67827573115522810 ) ) ;
#49499=ORIENTED_EDGE ( 'NONE', *, *, #38356, .F. ) ;
#49502=CARTESIAN_POINT ( 'NONE',  ( -2.601141883200665639, -7.351091256667533713, -12.99064605035233733 ) ) ;
#49505=FACE_OUTER_BOUND ( 'NONE', #29069, .T. ) ;
#49509=EDGE_LOOP ( 'NONE', ( #5741, #672, #3630, #23389, #5611, #16984 ) ) ;
#49516=VECTOR ( 'NONE', #31198, 1000.000000000000227 ) ;
#49520=LINE ( 'NONE', #34208, #61400 ) ;
#49523=CARTESIAN_POINT ( 'NONE',  ( 5.901764892641307547, 7.772884649736512053, 48.34846152321259893 ) ) ;
#49527=VERTEX_POINT ( 'NONE', #51289 ) ;
#49528=CARTESIAN_POINT ( 'NONE',  ( 3.727782113643637096, -3.544252717309863243, -43.82026983693523903 ) ) ;
#49529=AXIS2_PLACEMENT_3D ( 'NONE', #60780, #61692, #22903 ) ;
#49530=CARTESIAN_POINT ( 'NONE',  ( 2.299652685299200972, -44.95079749811529979, -19.58845397527800003 ) ) ;
#49538=ORIENTED_EDGE ( 'NONE', *, *, #27506, .F. ) ;
#49539=CARTESIAN_POINT ( 'NONE',  ( 0.6028777368367060907, 10.84253002538188859, 47.89550471557602407 ) ) ;
#49541=ORIENTED_EDGE ( 'NONE', *, *, #58986, .T. ) ;
#49543=CARTESIAN_POINT ( 'NONE',  ( -6.079354080745853928, 19.09774425860443259, 2.463558296672413217 ) ) ;
#49544=ORIENTED_EDGE ( 'NONE', *, *, #31486, .F. ) ;
#49546=ADVANCED_FACE ( 'NONE', ( #7440 ), #35344, .F. ) ;
#49549=CARTESIAN_POINT ( 'NONE',  ( 0.5997462898726536595, 46.43852004798865352, -15.96920429754923632 ) ) ;
#49552=EDGE_CURVE ( 'NONE', #52623, #47838, #2640, .T. ) ;
#49555=B_SPLINE_CURVE_WITH_KNOTS ( 'NONE', 3,
 ( #2669, #59372, #40619, #26802, #21481, #59687, #36220, #54352, #8001, #45939, #16801, #40317, #17406, #45013, #49676, #46237, #35912, #3278, #22411, #2982, #36530, #6730, #26488, #31499, #60601 ),
 .UNSPECIFIED., .F., .F.,
 ( 4, 3, 3, 3, 3, 3, 3, 3, 4 ),
 ( 5.553824967135426632E-18, 0.0005656085177311387727, 0.001131215744874499406, 0.001696821861372765482, 0.002262427090022497284, 0.002828031679238746793, 0.003393635864401605730, 0.003977030878808133357, 0.004561030005651160735 ),
 .UNSPECIFIED. ) ;
#49561=CARTESIAN_POINT ( 'NONE',  ( 0.6000166863083090663, -45.71468846346261472, 17.94410043432136703 ) ) ;
#49571=ORIENTED_EDGE ( 'NONE', *, *, #56895, .F. ) ;
#49574=CARTESIAN_POINT ( 'NONE',  ( 3.390910168358336918, 42.31681000770872458, 11.97433619475916800 ) ) ;
#49575=EDGE_CURVE ( 'NONE', #24938, #46940, #43891, .T. ) ;
#49578=CARTESIAN_POINT ( 'NONE',  ( 0.6000166863083106206, 33.40185771989251862, 36.00193581696004230 ) ) ;
#49581=CARTESIAN_POINT ( 'NONE',  ( 1.296416391601052931, -41.25474789393634012, -15.50332707143577338 ) ) ;
#49582=CARTESIAN_POINT ( 'NONE',  ( 2.009741617377216460, -13.83851655386614077, -41.80908438618833145 ) ) ;
#49584=CARTESIAN_POINT ( 'NONE',  ( -2.601141883200665639, -8.117336596316299335, 12.52614362249981284 ) ) ;
#49597=CARTESIAN_POINT ( 'NONE',  ( 0.6027444965799114707, 48.17669769696837534, 9.515477649722281939 ) ) ;
#49602=CARTESIAN_POINT ( 'NONE',  ( 0.3676999524040366896, 43.96170928169366476, -3.649479463524768263 ) ) ;
#49609=CARTESIAN_POINT ( 'NONE',  ( -6.072942160501519027, -18.89839206595246424, -3.695259072185007376 ) ) ;
#49613=CARTESIAN_POINT ( 'NONE',  ( 0.8753041380234471980, 48.01981714478390728, 10.25843502950123742 ) ) ;
#49622=B_SPLINE_CURVE_WITH_KNOTS ( 'NONE', 3,
 ( #40315, #2359, #21479, #40617 ),
 .UNSPECIFIED., .F., .F.,
 ( 4, 4 ),
 ( 0.000000000000000000, 0.004442905043737217438 ),
 .UNSPECIFIED. ) ;
#49625=CARTESIAN_POINT ( 'NONE',  ( 0.1158516988532803382, 15.19273855081792846, -41.42611319155211191 ) ) ;
#49626=ORIENTED_EDGE ( 'NONE', *, *, #59662, .T. ) ;
#49627=EDGE_CURVE ( 'NONE', #51246, #37964, #60082, .T. ) ;
#49628=VECTOR ( 'NONE', #340, 1000.000000000000114 ) ;
#49654=CARTESIAN_POINT ( 'NONE',  ( 3.050102900204245682, 21.93629751651464943, 38.13429034930390316 ) ) ;
#49656=DIRECTION ( 'NONE',  ( 0.000000000000000000, 0.000000000000000000, 1.000000000000000000 ) ) ;
#49658=FACE_OUTER_BOUND ( 'NONE', #22757, .T. ) ;
#49668=CARTESIAN_POINT ( 'NONE',  ( 0.1129192098497455998, 44.06201484046248140, -2.343210614524073421 ) ) ;
#49671=CARTESIAN_POINT ( 'NONE',  ( 0.1129192098497447394, 19.97823103613683315, -39.34236993944178806 ) ) ;
#49676=CARTESIAN_POINT ( 'NONE',  ( 2.185380717157384023, 36.09826614752458340, -25.21378559855064339 ) ) ;
#49679=CARTESIAN_POINT ( 'NONE',  ( 0.5987334308729319599, -45.28813393713827651, 18.98809708900693849 ) ) ;
#49691=CARTESIAN_POINT ( 'NONE',  ( 4.553261556744875094, 0.000000000000000000, 0.000000000000000000 ) ) ;
#49693=CARTESIAN_POINT ( 'NONE',  ( 4.553261556744875094, -43.85016385001095784, 2.588956575693979190 ) ) ;
#49697=ORIENTED_EDGE ( 'NONE', *, *, #424, .T. ) ;
#49700=LINE ( 'NONE', #6758, #9694 ) ;
#49706=EDGE_CURVE ( 'NONE', #37795, #40320, #36301, .T. ) ;
#49709=CARTESIAN_POINT ( 'NONE',  ( -6.078726893082806448, 15.43407385306378998, -11.51448676958260187 ) ) ;
#49718=DIRECTION ( 'NONE',  ( -1.000000000000000000, -0.000000000000000000, -0.000000000000000000 ) ) ;
#49720=CARTESIAN_POINT ( 'NONE',  ( 0.6000166863083106206, -31.02657807334512086, -38.06803035050636197 ) ) ;
#49721=B_SPLINE_CURVE_WITH_KNOTS ( 'NONE', 3,
 ( #21821, #32153, #18057, #37173, #40959, #32457, #31523, #8315, #27753, #27436, #50615, #55619, #60019, #7702, #26828, #45961, #22128, #41257, #60316 ),
 .UNSPECIFIED., .F., .F.,
 ( 4, 3, 3, 3, 3, 3, 4 ),
 ( 0.000000000000000000, 0.0002612768053151694864, 0.0003919133833142915218, 0.0005225499612322621629, 0.0006531865391693355248, 0.0008112755173415210500, 0.0009693688056799720310 ),
 .UNSPECIFIED. ) ;
#49733=B_SPLINE_CURVE_WITH_KNOTS ( 'NONE', 3,
 ( #3419, #17547, #56047, #36665, #8430, #37284, #55734, #16944, #56352, #59829, #13469, #40764, #32578, #51657, #8748, #27864, #36058, #55123, #12245, #50434, #7501, #45756, #60135, #17244, #7822 ),
 .UNSPECIFIED., .F., .F.,
 ( 4, 3, 3, 3, 3, 3, 3, 3, 4 ),
 ( 4.336808689942017736E-18, 0.0005656085177311415916, 0.001131215744874502008, 0.001696821861372767868, 0.002262427090022499886, 0.002828031679238747660, 0.003393635864401606597, 0.003977030878808131623, 0.004561030005651158133 ),
 .UNSPECIFIED. ) ;
#49736=ORIENTED_EDGE ( 'NONE', *, *, #19888, .F. ) ;
#49738=CARTESIAN_POINT ( 'NONE',  ( 2.185380717157383135, 30.65186932183861046, 31.61143321876008017 ) ) ;
#49745=ORIENTED_EDGE ( 'NONE', *, *, #52603, .F. ) ;
#49749=EDGE_CURVE ( 'NONE', #57605, #31520, #54302, .T. ) ;
#49750=CARTESIAN_POINT ( 'NONE',  ( 0.6039202388192952409, -47.54548494440610540, 12.28782219314079960 ) ) ;
#49754=CARTESIAN_POINT ( 'NONE',  ( 0.1158403557922069033, 20.44267117180008242, -39.10290913148882908 ) ) ;
#49759=DIRECTION ( 'NONE',  ( 0.000000000000000000, 0.000000000000000000, 1.000000000000000000 ) ) ;
#49760=CONICAL_SURFACE ( 'NONE', #25743, 43.92652462719577500, 1.486293639869522343 ) ;
#49773=CARTESIAN_POINT ( 'NONE',  ( 0.6016118706126977189, -45.38674246209918550, -18.75085767273094817 ) ) ;
#49775=ORIENTED_EDGE ( 'NONE', *, *, #2613, .F. ) ;
#49780=CARTESIAN_POINT ( 'NONE',  ( 0.6016118706126976079, -14.30603973001664286, 46.97752954367775402 ) ) ;
#49783=CARTESIAN_POINT ( 'NONE',  ( 0.1129192098497455998, -0.9297496242496093855, -44.11448008785053787 ) ) ;
#49786=EDGE_CURVE ( 'NONE', #27427, #56473, #15264, .T. ) ;
#49794=CARTESIAN_POINT ( 'NONE',  ( 0.1129192098497455998, 19.97823103613628248, 39.34236993944205807 ) ) ;
#49803=CARTESIAN_POINT ( 'NONE',  ( 0.6016117650947689910, -25.75423423388752653, -41.81232441841228109 ) ) ;
#49810=CARTESIAN_POINT ( 'NONE',  ( -6.077587904424778920, 16.78120357693994791, -9.443898977817823948 ) ) ;
#49813=ORIENTED_EDGE ( 'NONE', *, *, #42189, .F. ) ;
#49817=FACE_OUTER_BOUND ( 'NONE', #3958, .T. ) ;
#49818=CARTESIAN_POINT ( 'NONE',  ( 0.5980271706414734822, 36.93900200886744756, -32.36602189689906339 ) ) ;
#49824=ORIENTED_EDGE ( 'NONE', *, *, #39071, .T. ) ;
#49831=EDGE_CURVE ( 'NONE', #3927, #52762, #60888, .T. ) ;
#49836=CARTESIAN_POINT ( 'NONE',  ( 0.1155031312995260795, -35.46222914138566296, 26.25589337378687205 ) ) ;
#49839=CARTESIAN_POINT ( 'NONE',  ( 0.6000166863083090663, 32.62822748873705336, 36.70452632376117919 ) ) ;
#49844=CARTESIAN_POINT ( 'NONE',  ( 0.6008122571543325074, -45.35344805040789851, 18.83133825314251197 ) ) ;
#49846=VERTEX_POINT ( 'NONE', #20874 ) ;
#49848=CARTESIAN_POINT ( 'NONE',  ( 0.7242486021783874905, -19.12396628233026163, -45.22483140937365675 ) ) ;
#49854=( BOUNDED_SURFACE ( )  B_SPLINE_SURFACE ( 3, 1, ( 
 ( #51428, #31419 ),
 ( #41458, #60520 ),
 ( #8215, #27642 ),
 ( #27334, #50517 ) ),
 .UNSPECIFIED., .F., .F., .F. ) 
 B_SPLINE_SURFACE_WITH_KNOTS ( ( 4, 4 ),
 ( 2, 2 ),
 ( 0.000000000000000000, 1.000000000000000000 ),
 ( 0.000000000000000000, 1.000000000000000000 ),
 .UNSPECIFIED. ) 
 GEOMETRIC_REPRESENTATION_ITEM ( )  RATIONAL_B_SPLINE_SURFACE ( (
 ( 1.000000000000000000, 1.000000000000000000),
 ( 0.7211978278499968642, 0.9934217856018975334),
 ( 0.7211978278499968642, 0.9934217856018975334),
 ( 1.000000000000000000, 1.000000000000000000) ) ) 
 REPRESENTATION_ITEM ( '' )  SURFACE ( )  );
#49857=CARTESIAN_POINT ( 'NONE',  ( 0.8744876279028263033, -45.16590161814997373, -19.24555484778471026 ) ) ;
#49865=CARTESIAN_POINT ( 'NONE',  ( 0.1135584504625007929, 44.00383457693749989, 3.258004705455698868 ) ) ;
#49868=CARTESIAN_POINT ( 'NONE',  ( 4.975610109902397937, 45.11887670192763267, -18.88746601040027784 ) ) ;
#49876=CARTESIAN_POINT ( 'NONE',  ( 0.1158403557922069033, 43.31768241345346837, -8.397541158637027436 ) ) ;
#49877=EDGE_CURVE ( 'NONE', #6486, #33035, #1134, .T. ) ;
#49878=CARTESIAN_POINT ( 'NONE',  ( 4.553261556744873317, -29.69864478935373242, -32.36556910513746743 ) ) ;
#49882=ORIENTED_EDGE ( 'NONE', *, *, #27029, .F. ) ;
#49885=CARTESIAN_POINT ( 'NONE',  ( 0.1129192098497455998, -6.563350895508677674, -43.63340707310831590 ) ) ;
#49887=CARTESIAN_POINT ( 'NONE',  ( 2.009741617377216460, 13.91607796886164294, -41.78333222216257070 ) ) ;
#49889=CARTESIAN_POINT ( 'NONE',  ( 0.5549461598389366923, -42.87637096466922770, -10.33607799732926580 ) ) ;
#49890=CARTESIAN_POINT ( 'NONE',  ( 0.6000166863083106206, -25.90381862410915659, 41.72308308835420831 ) ) ;
#49894=ORIENTED_EDGE ( 'NONE', *, *, #47893, .F. ) ;
#49901=CARTESIAN_POINT ( 'NONE',  ( 1.479689385636123067, -41.26970557461135058, -15.44005333710297379 ) ) ;
#49902=EDGE_CURVE ( 'NONE', #8195, #759, #33384, .T. ) ;
#49909=CARTESIAN_POINT ( 'NONE',  ( 0.6029443199889047422, 41.15634887181838764, 26.78978516889554129 ) ) ;
#49912=CARTESIAN_POINT ( 'NONE',  ( 0.3676999524040366896, 41.59822836379080968, -14.68121181363270367 ) ) ;
#49913=CARTESIAN_POINT ( 'NONE',  ( 3.240649175237396484, -24.34849563854561083, 36.63899121888286459 ) ) ;
#49919=CARTESIAN_POINT ( 'NONE',  ( 0.6026777506516366456, 48.23490875577608250, 9.216288187723721492 ) ) ;
#49921=VERTEX_POINT ( 'NONE', #6734 ) ;
#49930=CARTESIAN_POINT ( 'NONE',  ( -6.077587904424778920, -18.89978312007031391, -3.687033958107209131 ) ) ;
#49932=ORIENTED_EDGE ( 'NONE', *, *, #20584, .F. ) ;
#49944=FACE_OUTER_BOUND ( 'NONE', #37828, .T. ) ;
#49946=CARTESIAN_POINT ( 'NONE',  ( 0.2940135542859015905, 43.96669230334707379, -3.629120636493694985 ) ) ;
#49947=ORIENTED_EDGE ( 'NONE', *, *, #17507, .F. ) ;
#49955=CARTESIAN_POINT ( 'NONE',  ( 3.894904216938897878, -43.82365964150300641, -3.407519347252721875 ) ) ;
#49959=CARTESIAN_POINT ( 'NONE',  ( 0.6021448801613057400, -35.45754748828524328, 33.97504179162910276 ) ) ;
#49960=CARTESIAN_POINT ( 'NONE',  ( -6.078726893082806448, -8.903615017412541022, 17.07394743140630666 ) ) ;
#49964=CARTESIAN_POINT ( 'NONE',  ( 2.648799415243696664, -47.06172439114146044, -13.77358198225285157 ) ) ;
#49971=CARTESIAN_POINT ( 'NONE',  ( 3.221118495291108719, 22.00098041526288029, 38.08829584569215143 ) ) ;
#49975=( BOUNDED_SURFACE ( )  B_SPLINE_SURFACE ( 3, 1, ( 
 ( #53223, #10332 ),
 ( #58221, #48532 ),
 ( #9702, #28812 ),
 ( #280, #19427 ) ),
 .UNSPECIFIED., .F., .F., .F. ) 
 B_SPLINE_SURFACE_WITH_KNOTS ( ( 4, 4 ),
 ( 2, 2 ),
 ( 0.000000000000000000, 1.000000000000000000 ),
 ( 0.000000000000000000, 1.000000000000000000 ),
 .UNSPECIFIED. ) 
 GEOMETRIC_REPRESENTATION_ITEM ( )  RATIONAL_B_SPLINE_SURFACE ( (
 ( 1.000000000000000000, 1.000000000000000000),
 ( 0.7211978278499968642, 0.9934217856018975334),
 ( 0.7211978278499968642, 0.9934217856018975334),
 ( 1.000000000000000000, 1.000000000000000000) ) ) 
 REPRESENTATION_ITEM ( '' )  SURFACE ( )  );
#49976=CARTESIAN_POINT ( 'NONE',  ( 0.8744876279028263033, -47.70753782033983725, 11.59055156152357213 ) ) ;
#49977=CARTESIAN_POINT ( 'NONE',  ( -6.078726893082806448, -19.21666810860935470, 1.230328440814298041 ) ) ;
#49980=EDGE_LOOP ( 'NONE', ( #33460, #21814, #49226, #31512 ) ) ;
#49983=CARTESIAN_POINT ( 'NONE',  ( 0.8753041380234524160, -39.87785955339003863, -28.65125905284232388 ) ) ;
#49984=CARTESIAN_POINT ( 'NONE',  ( -6.078726893082806448, -14.66019907464911043, 12.48489504803213812 ) ) ;
#49988=CARTESIAN_POINT ( 'NONE',  ( 3.678748215320120973, 45.86478482322198857, -17.17656331805143921 ) ) ;
#49991=CARTESIAN_POINT ( 'NONE',  ( 0.3676999524040323597, 14.45783756353398175, 41.67639039443440652 ) ) ;
#49993=EDGE_CURVE ( 'NONE', #38699, #53425, #33296, .T. ) ;
#50000=DIRECTION ( 'NONE',  ( 0.09722883295013594329, -0.9952333609815530169, 0.007557197398263628546 ) ) ;
#50010=EDGE_CURVE ( 'NONE', #36259, #10386, #37746, .T. ) ;
#50011=B_SPLINE_CURVE_WITH_KNOTS ( 'NONE', 3,
 ( #5047, #49216, #15726, #53898 ),
 .UNSPECIFIED., .F., .F.,
 ( 4, 4 ),
 ( 0.000000000000000000, 0.005013413432710148512 ),
 .UNSPECIFIED. ) ;
#50012=CARTESIAN_POINT ( 'NONE',  ( -6.079354080745853928, -18.90111140843031379, 3.679802002046783205 ) ) ;
#50017=EDGE_CURVE ( 'NONE', #57409, #56877, #2674, .T. ) ;
#50028=CARTESIAN_POINT ( 'NONE',  ( 4.975610109902397937, 48.43414999183889336, 6.825138951393308950 ) ) ;
#50032=ORIENTED_EDGE ( 'NONE', *, *, #8314, .F. ) ;
#50034=CARTESIAN_POINT ( 'NONE',  ( 0.1158403557922069033, 39.77089686883259390, -19.11062713341717156 ) ) ;
#50036=CARTESIAN_POINT ( 'NONE',  ( -6.079354080745853928, 12.00682274379669146, 15.05420747987779606 ) ) ;
#50043=AXIS2_PLACEMENT_3D ( 'NONE', #59579, #11684, #17308 ) ;
#50052=CARTESIAN_POINT ( 'NONE',  ( 0.7242486021783802741, -38.85568807781807266, -30.02077557914319428 ) ) ;
#50065=CARTESIAN_POINT ( 'NONE',  ( 0.1157991065609915576, -42.70166050063943430, 11.11353031335356789 ) ) ;
#50066=CARTESIAN_POINT ( 'NONE',  ( 0.8753041380234524160, -24.68967207985825141, 42.44476905888459584 ) ) ;
#50078=PRESENTATION_STYLE_ASSIGNMENT (( #44786 ) ) ;
#50079=CARTESIAN_POINT ( 'NONE',  ( 0.3676999524040366896, -22.15802448780013378, 38.14410221935873579 ) ) ;
#50082=B_SPLINE_CURVE_WITH_KNOTS ( 'NONE', 3,
 ( #3093, #40741, #16599, #59489 ),
 .UNSPECIFIED., .F., .F.,
 ( 4, 4 ),
 ( 0.000000000000000000, 0.005013413432710144176 ),
 .UNSPECIFIED. ) ;
#50087=EDGE_CURVE ( 'NONE', #25604, #43021, #28731, .T. ) ;
#50090=FACE_OUTER_BOUND ( 'NONE', #25231, .T. ) ;
#50093=CARTESIAN_POINT ( 'NONE',  ( 0.6026777506516367566, 27.95217787757266237, -40.37600949249141991 ) ) ;
#50094=CARTESIAN_POINT ( 'NONE',  ( 0.6008123274975391004, -14.38933995680775091, 46.95211866109849552 ) ) ;
#50095=ORIENTED_EDGE ( 'NONE', *, *, #3340, .F. ) ;
#50102=EDGE_LOOP ( 'NONE', ( #56089, #53628, #1442, #61860 ) ) ;
#50105=ORIENTED_EDGE ( 'NONE', *, *, #25917, .T. ) ;
#50114=ORIENTED_EDGE ( 'NONE', *, *, #11696, .F. ) ;
#50116=CARTESIAN_POINT ( 'NONE',  ( 0.7044674535452954967, 41.61193891978883386, -26.08158856639429146 ) ) ;
#50121=LINE ( 'NONE', #43051, #28869 ) ;
#50123=CARTESIAN_POINT ( 'NONE',  ( 0.8753041380234524160, -48.80600061351578489, -5.395612290229641950 ) ) ;
#50130=CARTESIAN_POINT ( 'NONE',  ( 0.8744876279028306332, -43.20725972823464645, -23.31271664041680580 ) ) ;
#50138=CARTESIAN_POINT ( 'NONE',  ( 0.5980271706414734822, -47.32398142236193195, 13.13354579607525352 ) ) ;
#50139=CARTESIAN_POINT ( 'NONE',  ( 4.553261556744875094, 0.000000000000000000, 0.000000000000000000 ) ) ;
#50154=( BOUNDED_SURFACE ( )  B_SPLINE_SURFACE ( 3, 1, ( 
 ( #24281, #28668 ),
 ( #57451, #47793 ),
 ( #4528, #140 ),
 ( #52466, #23364 ) ),
 .UNSPECIFIED., .F., .F., .F. ) 
 B_SPLINE_SURFACE_WITH_KNOTS ( ( 4, 4 ),
 ( 2, 2 ),
 ( 0.000000000000000000, 1.000000000000000000 ),
 ( 0.000000000000000000, 1.000000000000000000 ),
 .UNSPECIFIED. ) 
 GEOMETRIC_REPRESENTATION_ITEM ( )  RATIONAL_B_SPLINE_SURFACE ( (
 ( 1.000000000000000000, 1.000000000000000000),
 ( 0.7211978278499968642, 0.9934217856018975334),
 ( 0.7211978278499968642, 0.9934217856018975334),
 ( 1.000000000000000000, 1.000000000000000000) ) ) 
 REPRESENTATION_ITEM ( '' )  SURFACE ( )  );
#50157=CARTESIAN_POINT ( 'NONE',  ( 4.975610109902397937, -32.45573888811652807, 36.59336579715199633 ) ) ;
#50159=FACE_OUTER_BOUND ( 'NONE', #41354, .T. ) ;
#50160=ORIENTED_EDGE ( 'NONE', *, *, #21077, .F. ) ;
#50163=CARTESIAN_POINT ( 'NONE',  ( 1.657374760986086271, -42.28389365164147051, 12.36781245446895738 ) ) ;
#50166=CARTESIAN_POINT ( 'NONE',  ( 0.5997462898726536595, 10.41743419021343087, -47.98988117339822423 ) ) ;
#50178=CARTESIAN_POINT ( 'NONE',  ( -6.063463321072278589, -8.920783457832412111, 17.06575738072979576 ) ) ;
#50182=EDGE_CURVE ( 'NONE', #31310, #39191, #6022, .T. ) ;
#50183=CARTESIAN_POINT ( 'NONE',  ( 0.6000166863083090663, 37.73145429715492583, 31.43502566135683551 ) ) ;
#50184=EDGE_LOOP ( 'NONE', ( #4755, #31005, #61926, #21540 ) ) ;
#50185=CARTESIAN_POINT ( 'NONE',  ( 0.1155031312995260795, 43.34236963370094031, -8.269257951439607623 ) ) ;
#50189=VERTEX_POINT ( 'NONE', #58673 ) ;
#50200=CARTESIAN_POINT ( 'NONE',  ( 3.050102900204245682, 42.28728544019637781, 12.13304328177459546 ) ) ;
#50210=CARTESIAN_POINT ( 'NONE',  ( -6.078726893082806448, -19.21666810860932983, -1.230328440814576041 ) ) ;
#50213=CARTESIAN_POINT ( 'NONE',  ( 0.5980271706414734822, -48.79397779905842469, -5.585425085582683913 ) ) ;
#50219=CARTESIAN_POINT ( 'NONE',  ( 4.335381028904216727, 45.01666255113116222, 19.31985870605503308 ) ) ;
#50224=( BOUNDED_SURFACE ( )  B_SPLINE_SURFACE ( 3, 1, ( 
 ( #17243, #11946 ),
 ( #59510, #31023 ),
 ( #35744, #55426 ),
 ( #21317, #26624 ) ),
 .UNSPECIFIED., .F., .F., .F. ) 
 B_SPLINE_SURFACE_WITH_KNOTS ( ( 4, 4 ),
 ( 2, 2 ),
 ( 0.000000000000000000, 1.000000000000000000 ),
 ( 0.000000000000000000, 1.000000000000000000 ),
 .UNSPECIFIED. ) 
 GEOMETRIC_REPRESENTATION_ITEM ( )  RATIONAL_B_SPLINE_SURFACE ( (
 ( 1.000000000000000000, 1.000000000000000000),
 ( 0.9953485035131437453, 0.8621029689291523912),
 ( 0.9953485035131437453, 0.8621029689291523912),
 ( 1.000000000000000000, 1.000000000000000000) ) ) 
 REPRESENTATION_ITEM ( '' )  SURFACE ( )  );
#50231=CARTESIAN_POINT ( 'NONE',  ( 1.834102595619085507, 2.930864502506626224, -43.95006004689448531 ) ) ;
#50233=ORIENTED_EDGE ( 'NONE', *, *, #51323, .F. ) ;
#50238=EDGE_LOOP ( 'NONE', ( #18598, #57715, #14773, #2259 ) ) ;
#50244=CARTESIAN_POINT ( 'NONE',  ( 0.1365634738349416899, -17.27620067578395435, -40.60043731086266661 ) ) ;
#50246=CARTESIAN_POINT ( 'NONE',  ( 0.6000166863083090663, -42.53190469623939407, 24.55321902762372588 ) ) ;
#50248=EDGE_CURVE ( 'NONE', #47719, #42350, #44325, .T. ) ;
#50249=CARTESIAN_POINT ( 'NONE',  ( 0.3676999524040366896, 37.41430475689384139, 23.36921870497834774 ) ) ;
#50250=VERTEX_POINT ( 'NONE', #44623 ) ;
#50267=CARTESIAN_POINT ( 'NONE',  ( 0.8753041380234471980, -47.26389509135280775, -13.31399822241900566 ) ) ;
#50268=CARTESIAN_POINT ( 'NONE',  ( 0.6252788684277225117, -48.61071527006939874, 6.960078455442126000 ) ) ;
#50272=CARTESIAN_POINT ( 'NONE',  ( 2.299652685299201860, 46.92539516736430727, -14.22283421983313367 ) ) ;
#50276=CARTESIAN_POINT ( 'NONE',  ( 4.975610109902397937, -48.84566763821283786, 2.559328059280373768 ) ) ;
#50280=CARTESIAN_POINT ( 'NONE',  ( 0.6027444965799114707, 41.22745124204113409, -26.68025074793268203 ) ) ;
#50283=EDGE_CURVE ( 'NONE', #52990, #43207, #39939, .T. ) ;
#50287=CARTESIAN_POINT ( 'NONE',  ( 0.7044674535453004927, 5.553212498070795533, 48.79512838144990639 ) ) ;
#50307=ORIENTED_EDGE ( 'NONE', *, *, #22831, .F. ) ;
#50320=CARTESIAN_POINT ( 'NONE',  ( 0.7044674535453004927, 10.10543771684659298, -48.05915991111207575 ) ) ;
#50323=CARTESIAN_POINT ( 'NONE',  ( -6.072942160501519027, 17.85441038494896304, -7.212779775845567620 ) ) ;
#50338=CARTESIAN_POINT ( 'NONE',  ( 0.7948884756798507700, 10.07807595004759271, 48.05341850217551070 ) ) ;
#50340=CARTESIAN_POINT ( 'NONE',  ( 0.1156495703730067853, -43.74427687214311078, 5.777646074687804223 ) ) ;
#50342=CARTESIAN_POINT ( 'NONE',  ( 0.1152809850208375703, 43.26768730443608035, 8.651734959838789152 ) ) ;
#50351=CARTESIAN_POINT ( 'NONE',  ( 0.6008122571543325074, 33.33611234963518655, 36.05909266575930161 ) ) ;
#50358=CARTESIAN_POINT ( 'NONE',  ( 4.834790513006553603, 40.94190515849751222, 23.58706728096937866 ) ) ;
#50363=CARTESIAN_POINT ( 'NONE',  ( 0.6021448801613057400, 44.13030167720265240, 21.54199648375312037 ) ) ;
#50368=EDGE_CURVE ( 'NONE', #45974, #53665, #8303, .T. ) ;
#50370=FACE_OUTER_BOUND ( 'NONE', #40222, .T. ) ;
#50375=CARTESIAN_POINT ( 'NONE',  ( 0.1129192098497455998, -18.30288010335110016, 40.14917642626692640 ) ) ;
#50385=CARTESIAN_POINT ( 'NONE',  ( 0.1152339509894530906, -38.55535503695174526, -21.45756949027179772 ) ) ;
#50392=( BOUNDED_SURFACE ( )  B_SPLINE_SURFACE ( 3, 1, ( 
 ( #27296, #2553 ),
 ( #16992, #7553 ),
 ( #56098, #26677 ),
 ( #21990, #37035 ) ),
 .UNSPECIFIED., .F., .F., .F. ) 
 B_SPLINE_SURFACE_WITH_KNOTS ( ( 4, 4 ),
 ( 2, 2 ),
 ( 0.000000000000000000, 1.000000000000000000 ),
 ( 0.000000000000000000, 1.000000000000000000 ),
 .UNSPECIFIED. ) 
 GEOMETRIC_REPRESENTATION_ITEM ( )  RATIONAL_B_SPLINE_SURFACE ( (
 ( 1.000000000000000000, 1.000000000000000000),
 ( 0.9754377213608244057, 0.9999580625633939235),
 ( 0.9754377213608244057, 0.9999580625633939235),
 ( 1.000000000000000000, 1.000000000000000000) ) ) 
 REPRESENTATION_ITEM ( '' )  SURFACE ( )  );
#50393=CARTESIAN_POINT ( 'NONE',  ( 0.1119899015040013712, 43.99420331743984747, 3.386942966197092897 ) ) ;
#50398=CARTESIAN_POINT ( 'NONE',  ( 0.8744876279028306332, 48.01195819035234535, -10.25679877482985169 ) ) ;
#50408=LINE ( 'NONE', #3700, #33776 ) ;
#50410=DIRECTION ( 'NONE',  ( 0.000000000000000000, 0.000000000000000000, -1.000000000000000000 ) ) ;
#50416=CARTESIAN_POINT ( 'NONE',  ( 0.5997462898726536595, 11.43624519451716992, -47.75734421002901797 ) ) ;
#50424=CARTESIAN_POINT ( 'NONE',  ( -6.072942160501519027, 19.09631935424740234, 2.476842629158438225 ) ) ;
#50428=DIRECTION ( 'NONE',  ( 1.000000000000000000, 0.000000000000000000, 0.000000000000000000 ) ) ;
#50429=CARTESIAN_POINT ( 'NONE',  ( 0.3676999524040323597, 33.04872056100222011, 29.21870381457103605 ) ) ;
#50434=CARTESIAN_POINT ( 'NONE',  ( 1.296416391601053153, -34.64371266338438460, 27.24188956318961274 ) ) ;
#50438=VERTEX_POINT ( 'NONE', #27344 ) ;
#50448=CARTESIAN_POINT ( 'NONE',  ( -6.072942160501519915, 0.6317110510321461980, 19.24591134337431342 ) ) ;
#50453=EDGE_CURVE ( 'NONE', #26555, #34535, #9834, .T. ) ;
#50462=CARTESIAN_POINT ( 'NONE',  ( 3.221118495291109163, -42.02902145736321415, 12.97392673781741657 ) ) ;
#50467=ORIENTED_EDGE ( 'NONE', *, *, #52740, .F. ) ;
#50471=CARTESIAN_POINT ( 'NONE',  ( 4.390527457369401532, -10.08871719600491978, 42.75983070555417953 ) ) ;
#50472=ORIENTED_EDGE ( 'NONE', *, *, #43299, .T. ) ;
#50481=CARTESIAN_POINT ( 'NONE',  ( -6.078457390727109555, -14.65958194562084316, -12.48563847855348286 ) ) ;
#50484=ORIENTED_EDGE ( 'NONE', *, *, #33698, .T. ) ;
#50486=CARTESIAN_POINT ( 'NONE',  ( 0.1158403557922069033, 15.20339722355584477, 41.42218029083685593 ) ) ;
#50489=CARTESIAN_POINT ( 'NONE',  ( -6.078457390727109555, 3.077585051286873430, 19.00849760737558825 ) ) ;
#50501=CARTESIAN_POINT ( 'NONE',  ( -6.078726893082806448, 0.6137717894420866571, -19.24622886331774652 ) ) ;
#50512=CARTESIAN_POINT ( 'NONE',  ( 0.1119898979215350893, 25.70258805518049172, 35.86555834665789178 ) ) ;
#50514=CARTESIAN_POINT ( 'NONE',  ( 4.975610109902397937, -23.13264022976521161, -43.09675583078175265 ) ) ;
#50516=CARTESIAN_POINT ( 'NONE',  ( 0.6252788684277179598, -42.44619877470422153, 24.69341087723536887 ) ) ;
#50517=CARTESIAN_POINT ( 'NONE',  ( 0.8753041380234524160, -35.88662119133316963, -33.51550010581278372 ) ) ;
#50518=CARTESIAN_POINT ( 'NONE',  ( -6.077587904424778920, 7.788877841491995468, -17.61049128685073129 ) ) ;
#50521=CARTESIAN_POINT ( 'NONE',  ( 0.7242486021783832717, 17.72443731528298372, -45.79143789214940341 ) ) ;
#50525=CARTESIAN_POINT ( 'NONE',  ( 0.8744876279028306332, -38.80702141274064587, 30.07266432244707843 ) ) ;
#50531=CARTESIAN_POINT ( 'NONE',  ( 0.6021447746440204973, 16.71456626119010025, -46.17536587606831944 ) ) ;
#50532=CARTESIAN_POINT ( 'NONE',  ( 4.553261556744875094, 1.633632119647590697, -43.89613664004262716 ) ) ;
#50534=VERTEX_POINT ( 'NONE', #39496 ) ;
#50549=ADVANCED_FACE ( 'NONE', ( #29441 ), #46349, .F. ) ;
#50552=EDGE_CURVE ( 'NONE', #26818, #10962, #12075, .T. ) ;
#50557=CARTESIAN_POINT ( 'NONE',  ( 0.8744876279028263033, 41.62483489565955352, -26.03311679934954626 ) ) ;
#50564=CARTESIAN_POINT ( 'NONE',  ( -6.063463321072276813, 19.09660126457258045, -2.477957348582642272 ) ) ;
#50565=FACE_OUTER_BOUND ( 'NONE', #8743, .T. ) ;
#50577=CARTESIAN_POINT ( 'NONE',  ( 0.6008123274975392114, -43.00034267269872146, 23.71761120325872341 ) ) ;
#50582=CARTESIAN_POINT ( 'NONE',  ( 0.2279481005628795909, 36.55606629206238267, 24.70136644647927682 ) ) ;
#50589=CARTESIAN_POINT ( 'NONE',  ( 0.3676999524040366896, -11.75791688508890331, 42.51707861373098041 ) ) ;
#50592=CARTESIAN_POINT ( 'NONE',  ( 0.7242003506639999033, -2.392178275000814036, -49.04374738156375457 ) ) ;
#50593=EDGE_CURVE ( 'NONE', #14207, #473, #22480, .T. ) ;
#50603=ORIENTED_EDGE ( 'NONE', *, *, #10609, .T. ) ;
#50608=ORIENTED_EDGE ( 'NONE', *, *, #23382, .F. ) ;
#50614=CARTESIAN_POINT ( 'NONE',  ( 3.050102900204245682, -43.95621292022238435, 1.810136704819465203 ) ) ;
#50615=CARTESIAN_POINT ( 'NONE',  ( 0.1157991065609915438, -42.66035988082465025, -11.27102747650922154 ) ) ;
#50619=EDGE_CURVE ( 'NONE', #15688, #26015, #56081, .T. ) ;
#50633=CARTESIAN_POINT ( 'NONE',  ( -6.078726893082806448, 12.00325722817128771, 15.05708661006749338 ) ) ;
#50642=CARTESIAN_POINT ( 'NONE',  ( 0.1158816050234198758, -43.76118062594752445, 5.648106897745077681 ) ) ;
#50644=CARTESIAN_POINT ( 'NONE',  ( 0.1147471544378676489, -27.75311504492739090, -34.30330587241221707 ) ) ;
#50645=VECTOR ( 'NONE', #46512, 1000.000000000000000 ) ;
#50648=CARTESIAN_POINT ( 'NONE',  ( 2.299652685299202304, 44.72136265055998905, -20.10675129242044434 ) ) ;
#50658=CONICAL_SURFACE ( 'NONE', #14693, 48.91267123290010943, 0.04450589592585339760 ) ;
#50665=CARTESIAN_POINT ( 'NONE',  ( 0.2940133293163011974, -38.03800459916556775, -22.34615751515019255 ) ) ;
#50671=CARTESIAN_POINT ( 'NONE',  ( 0.2940135542859017570, -28.13058121184755578, -33.98398077587541621 ) ) ;
#50672=DIRECTION ( 'NONE',  ( -1.000000000000000000, -0.000000000000000000, -0.000000000000000000 ) ) ;
#50675=CARTESIAN_POINT ( 'NONE',  ( 2.879087469061463178, 16.80966257193206914, 40.66370520502483998 ) ) ;
#50678=ORIENTED_EDGE ( 'NONE', *, *, #13745, .T. ) ;
#50681=CARTESIAN_POINT ( 'NONE',  ( 2.533389852662419894, -32.69955711577486568, -29.46505550929431649 ) ) ;
#50683=CARTESIAN_POINT ( 'NONE',  ( 0.1129192098497455998, -38.20615368646939203, -22.07354996984027196 ) ) ;
#50687=CARTESIAN_POINT ( 'NONE',  ( 2.185380717157383579, -40.25241636799283640, 17.84832708140854152 ) ) ;
#50691=( BOUNDED_SURFACE ( )  B_SPLINE_SURFACE ( 3, 1, ( 
 ( #30059, #30995 ),
 ( #59482, #40418 ),
 ( #40734, #21595 ),
 ( #44815, #2470 ) ),
 .UNSPECIFIED., .F., .F., .F. ) 
 B_SPLINE_SURFACE_WITH_KNOTS ( ( 4, 4 ),
 ( 2, 2 ),
 ( 0.000000000000000000, 1.000000000000000000 ),
 ( 0.000000000000000000, 1.000000000000000000 ),
 .UNSPECIFIED. ) 
 GEOMETRIC_REPRESENTATION_ITEM ( )  RATIONAL_B_SPLINE_SURFACE ( (
 ( 1.000000000000000000, 1.000000000000000000),
 ( 0.7211978278499968642, 0.9934217856018975334),
 ( 0.7211978278499968642, 0.9934217856018975334),
 ( 1.000000000000000000, 1.000000000000000000) ) ) 
 REPRESENTATION_ITEM ( '' )  SURFACE ( )  );
#50698=ORIENTED_EDGE ( 'NONE', *, *, #45527, .T. ) ;
#50699=CARTESIAN_POINT ( 'NONE',  ( -6.077587904424778920, -16.13490349385135758, 10.51003856501172606 ) ) ;
#50701=ORIENTED_EDGE ( 'NONE', *, *, #656, .F. ) ;
#50711=ORIENTED_EDGE ( 'NONE', *, *, #12906, .T. ) ;
#50716=CARTESIAN_POINT ( 'NONE',  ( 4.975610109902397937, -46.23629923292363486, -15.95788333023269878 ) ) ;
#50717=ORIENTED_EDGE ( 'NONE', *, *, #11664, .F. ) ;
#50720=EDGE_CURVE ( 'NONE', #35039, #40264, #41145, .T. ) ;
#50724=EDGE_LOOP ( 'NONE', ( #34336, #56594, #55380, #25382 ) ) ;
#50726=CARTESIAN_POINT ( 'NONE',  ( 2.648799415243708655, 23.90046839033397319, 42.81687837771741556 ) ) ;
#50732=MECHANICAL_DESIGN_GEOMETRIC_PRESENTATION_REPRESENTATION('',(#34752),#45759);
#50747=CARTESIAN_POINT ( 'NONE',  ( 0.1129192098497455998, 9.345467776858411568, 43.12324222292260600 ) ) ;
#50749=CARTESIAN_POINT ( 'NONE',  ( 4.553261556744873317, -3.993093339917161977, 43.74465420371208069 ) ) ;
#50755=( BOUNDED_SURFACE ( )  B_SPLINE_SURFACE ( 3, 1, ( 
 ( #41563, #28906 ),
 ( #60625, #22438 ),
 ( #29519, #377 ),
 ( #28595, #10430 ) ),
 .UNSPECIFIED., .F., .F., .F. ) 
 B_SPLINE_SURFACE_WITH_KNOTS ( ( 4, 4 ),
 ( 2, 2 ),
 ( 0.000000000000000000, 1.000000000000000000 ),
 ( 0.000000000000000000, 1.000000000000000000 ),
 .UNSPECIFIED. ) 
 GEOMETRIC_REPRESENTATION_ITEM ( )  RATIONAL_B_SPLINE_SURFACE ( (
 ( 1.000000000000000000, 1.000000000000000000),
 ( 0.9953485035131437453, 0.8621029689291523912),
 ( 0.9953485035131437453, 0.8621029689291523912),
 ( 1.000000000000000000, 1.000000000000000000) ) ) 
 REPRESENTATION_ITEM ( '' )  SURFACE ( )  );
#50758=CARTESIAN_POINT ( 'NONE',  ( 0.5980271706414711508, 10.24496086146881169, 48.03217692119142868 ) ) ;
#50759=CARTESIAN_POINT ( 'NONE',  ( -6.063463321072278589, -16.14731216720877782, 10.49212858547689109 ) ) ;
#50764=VERTEX_POINT ( 'NONE', #19373 ) ;
#50770=B_SPLINE_CURVE_WITH_KNOTS ( 'NONE', 3,
 ( #10168, #8083, #19578, #434 ),
 .UNSPECIFIED., .F., .F.,
 ( 4, 4 ),
 ( 0.000000000000000000, 0.005013413432710152849 ),
 .UNSPECIFIED. ) ;
#50772=CARTESIAN_POINT ( 'NONE',  ( 2.533389852662419894, -10.99890053681963664, 42.62012105467048428 ) ) ;
#50778=EDGE_LOOP ( 'NONE', ( #46078, #39357, #28232, #30996 ) ) ;
#50786=EDGE_CURVE ( 'NONE', #53183, #61378, #60508, .T. ) ;
#50793=CARTESIAN_POINT ( 'NONE',  ( 3.559346040607745287, -37.26281748359819801, 23.34336553982817364 ) ) ;
#50795=ORIENTED_EDGE ( 'NONE', *, *, #38228, .T. ) ;
#50797=ADVANCED_FACE ( 'NONE', ( #27839 ), #37001, .F. ) ;
#50799=VECTOR ( 'NONE', #45681, 1000.000000000000114 ) ;
#50803=CARTESIAN_POINT ( 'NONE',  ( 3.390910168358336918, 13.32450449336170095, -41.91127195087285173 ) ) ;
#50807=CARTESIAN_POINT ( 'NONE',  ( 0.6021448801613057400, 27.88052149016963810, 40.42545806868656655 ) ) ;
#50810=VERTEX_POINT ( 'NONE', #28443 ) ;
#50815=CARTESIAN_POINT ( 'NONE',  ( 0.2285344041767092271, -18.55084289203973924, -40.02958154028485893 ) ) ;
#50817=CARTESIAN_POINT ( 'NONE',  ( 4.060580049360325461, 12.02155469950848676, 42.27233039431271067 ) ) ;
#50821=AXIS2_PLACEMENT_3D ( 'NONE', #48835, #58213, #49759 ) ;
#50833=CARTESIAN_POINT ( 'NONE',  ( 0.6028777368367060907, 16.87825420422721834, 46.11577131880761726 ) ) ;
#50835=EDGE_CURVE ( 'NONE', #14950, #10066, #49313, .T. ) ;
#50837=ORIENTED_EDGE ( 'NONE', *, *, #41923, .T. ) ;
#50845=CARTESIAN_POINT ( 'NONE',  ( 0.6252788684277241771, 36.94309652552172452, -32.35200071525177634 ) ) ;
#50849=ORIENTED_EDGE ( 'NONE', *, *, #53036, .F. ) ;
#50855=CARTESIAN_POINT ( 'NONE',  ( 3.678748215320120529, 48.95863509520004442, 1.290296056930659629 ) ) ;
#50861=VECTOR ( 'NONE', #10406, 1000.000000000000000 ) ;
#50863=CARTESIAN_POINT ( 'NONE',  ( -2.601141883200665639, 3.756714151560036630, -14.44584806277766376 ) ) ;
#50865=ORIENTED_EDGE ( 'NONE', *, *, #4570, .F. ) ;
#50870=CARTESIAN_POINT ( 'NONE',  ( 0.7413678028165010536, -43.84383547618206478, -4.712131418766086099 ) ) ;
#50871=( BOUNDED_SURFACE ( )  B_SPLINE_SURFACE ( 3, 1, ( 
 ( #41826, #56194 ),
 ( #8267, #13307 ),
 ( #13011, #28011 ),
 ( #61498, #42437 ) ),
 .UNSPECIFIED., .F., .F., .F. ) 
 B_SPLINE_SURFACE_WITH_KNOTS ( ( 4, 4 ),
 ( 2, 2 ),
 ( 0.000000000000000000, 1.000000000000000000 ),
 ( 0.000000000000000000, 1.000000000000000000 ),
 .UNSPECIFIED. ) 
 GEOMETRIC_REPRESENTATION_ITEM ( )  RATIONAL_B_SPLINE_SURFACE ( (
 ( 1.000000000000000000, 1.000000000000000000),
 ( 0.7211978278499968642, 0.9934217856018975334),
 ( 0.7211978278499968642, 0.9934217856018975334),
 ( 1.000000000000000000, 1.000000000000000000) ) ) 
 REPRESENTATION_ITEM ( '' )  SURFACE ( )  );
#50873=ORIENTED_EDGE ( 'NONE', *, *, #3730, .T. ) ;
#50875=CARTESIAN_POINT ( 'NONE',  ( 5.901764892641288895, 7.772884649737204832, -48.34846152321248525 ) ) ;
#50876=EDGE_CURVE ( 'NONE', #43165, #16494, #49403, .T. ) ;
#50877=CARTESIAN_POINT ( 'NONE',  ( 2.648799415243696664, -9.190926635157635971, 48.16683849783737514 ) ) ;
#50881=CARTESIAN_POINT ( 'NONE',  ( 4.975610109902397937, 39.54077024310177535, -28.79195887257430897 ) ) ;
#50884=ORIENTED_EDGE ( 'NONE', *, *, #58852, .F. ) ;
#50887=FACE_OUTER_BOUND ( 'NONE', #42024, .T. ) ;
#50891=CARTESIAN_POINT ( 'NONE',  ( 0.8744876279028263033, 10.05549467470504865, 48.05452192277508061 ) ) ;
#50894=CARTESIAN_POINT ( 'NONE',  ( 0.6029443199889047422, 41.15632221336601759, -26.78982612343718728 ) ) ;
#50895=CARTESIAN_POINT ( 'NONE',  ( 0.3676999524040323597, 36.51379593394458567, 24.75264207750540635 ) ) ;
#50897=CARTESIAN_POINT ( 'NONE',  ( 5.901764892641307547, -41.01701952799340489, -26.75061824481604944 ) ) ;
#50903=CARTESIAN_POINT ( 'NONE',  ( 3.240649175237394708, -14.25852668140352364, 41.61681552297525144 ) ) ;
#50911=CARTESIAN_POINT ( 'NONE',  ( 0.5549461598389363592, -18.65190885362596518, -39.96653589670781059 ) ) ;
#50913=ADVANCED_FACE ( 'NONE', ( #48792 ), #26538, .F. ) ;
#50917=CARTESIAN_POINT ( 'NONE',  ( -6.078457390727109555, 3.068934028528322866, 19.00989623764550629 ) ) ;
#50925=ORIENTED_EDGE ( 'NONE', *, *, #30885, .F. ) ;
#50926=CARTESIAN_POINT ( 'NONE',  ( 2.225808406068902734, -0.2642358560988280480, -49.03513448940339714 ) ) ;
#50929=CARTESIAN_POINT ( 'NONE',  ( 0.3676999524040366896, 29.04098611012985742, -33.20499524279568249 ) ) ;
#50930=CARTESIAN_POINT ( 'NONE',  ( 0.1154773475650540671, 33.71449497992789901, 28.46535540432504874 ) ) ;
#50931=VERTEX_POINT ( 'NONE', #44437 ) ;
#50932=CARTESIAN_POINT ( 'NONE',  ( 0.7044674535452954967, -31.27352687970100931, 37.86514544162644569 ) ) ;
#50937=CARTESIAN_POINT ( 'NONE',  ( 0.8744876279028263033, -6.955970791787605911, -48.60004650947661275 ) ) ;
#50938=CARTESIAN_POINT ( 'NONE',  ( 0.5997462898726536595, 10.41743419021273631, 47.98988117339838055 ) ) ;
#50950=ORIENTED_EDGE ( 'NONE', *, *, #23382, .T. ) ;
#50956=CARTESIAN_POINT ( 'NONE',  ( 0.1157506346131639274, -43.74993170343814342, 5.734469090276133940 ) ) ;
#50957=ORIENTED_EDGE ( 'NONE', *, *, #60515, .T. ) ;
#50958=CARTESIAN_POINT ( 'NONE',  ( 0.1158403557922069033, 43.30320583737607620, 8.471875317169066832 ) ) ;
#50960=CARTESIAN_POINT ( 'NONE',  ( 5.901764892641307547, 1.526405342807678478, 48.94549574954908167 ) ) ;
#50963=CARTESIAN_POINT ( 'NONE',  ( 4.694002226626920127, 45.25670317367036688, 5.487767241458856304 ) ) ;
#50966=CARTESIAN_POINT ( 'NONE',  ( 0.2940133293162998096, 33.06489090063801939, 29.20536833027361112 ) ) ;
#50976=CARTESIAN_POINT ( 'NONE',  ( -2.739355103387248747, -14.37091041638174005, 4.040358988425137632 ) ) ;
#50979=ADVANCED_FACE ( 'NONE', ( #48189 ), #37730, .F. ) ;
#50981=CARTESIAN_POINT ( 'NONE',  ( 0.1129192098497447394, -38.68182264534125636, -21.22895156665819627 ) ) ;
#50983=CARTESIAN_POINT ( 'NONE',  ( 3.678834586032788678, -36.44297663525289721, 32.71882980167178800 ) ) ;
#50984=CARTESIAN_POINT ( 'NONE',  ( 2.648799415243696664, 46.08255460350029153, 16.76053771527072911 ) ) ;
#50987=CARTESIAN_POINT ( 'NONE',  ( 4.553261556744875094, 31.39705178283641018, 30.72075365562384519 ) ) ;
#50992=CARTESIAN_POINT ( 'NONE',  ( 2.879087469061463622, 32.35613322949701143, -29.81916027017557269 ) ) ;
#50999=B_SPLINE_CURVE_WITH_KNOTS ( 'NONE', 3,
 ( #3665, #27488, #42540, #61603 ),
 .UNSPECIFIED., .F., .F.,
 ( 4, 4 ),
 ( 1.734723475976807094E-18, 0.005013413432710139839 ),
 .UNSPECIFIED. ) ;
#51000=CARTESIAN_POINT ( 'NONE',  ( 0.6029442701453591180, -45.55116825581043116, -18.34765095834136162 ) ) ;
#51002=EDGE_CURVE ( 'NONE', #26826, #57221, #53727, .T. ) ;
#51003=CARTESIAN_POINT ( 'NONE',  ( 0.7044674535453004927, -35.85885898216606904, -33.55510326773016772 ) ) ;
#51006=CARTESIAN_POINT ( 'NONE',  ( 0.8753041380234530822, 17.79089796329305884, 45.76704357430872960 ) ) ;
#51010=AXIS2_PLACEMENT_3D ( 'NONE', #33513, #61062, #27259 ) ;
#51013=CARTESIAN_POINT ( 'NONE',  ( 4.834790513006553603, -10.06429236341580236, -46.16599787882930883 ) ) ;
#51019=ORIENTED_EDGE ( 'NONE', *, *, #60442, .T. ) ;
#51021=EDGE_LOOP ( 'NONE', ( #27760, #28514, #7064, #13061 ) ) ;
#51028=DIRECTION ( 'NONE',  ( 0.1011922191286467876, -0.8730847945189473824, -0.4769518595913295189 ) ) ;
#51031=CARTESIAN_POINT ( 'NONE',  ( 4.060580049360325461, 6.517192272988030943, 43.46255744012442079 ) ) ;
#51039=CARTESIAN_POINT ( 'NONE',  ( 4.975610109902397937, 19.27143522741721426, -44.95621415792522413 ) ) ;
#51042=CARTESIAN_POINT ( 'NONE',  ( 4.553261556744875094, 35.33793455049291765, -26.09156851415253087 ) ) ;
#51046=CARTESIAN_POINT ( 'NONE',  ( 2.009741617377216460, -43.48179227669744051, 6.988405971978110642 ) ) ;
#51052=EDGE_CURVE ( 'NONE', #61727, #34766, #57501, .T. ) ;
#51056=B_SPLINE_CURVE_WITH_KNOTS ( 'NONE', 3,
 ( #39495, #6224, #5919, #44203 ),
 .UNSPECIFIED., .F., .F.,
 ( 4, 4 ),
 ( 7.046480070129584215E-18, 0.005013413432710146778 ),
 .UNSPECIFIED. ) ;
#51059=CARTESIAN_POINT ( 'NONE',  ( 3.678748215320119641, 34.27176725038954430, 34.98655147102398644 ) ) ;
#51064=FACE_OUTER_BOUND ( 'NONE', #38033, .T. ) ;
#51067=CARTESIAN_POINT ( 'NONE',  ( 2.706805983486680223, 23.80251637563394596, -37.01643320887944100 ) ) ;
#51068=CARTESIAN_POINT ( 'NONE',  ( 2.648799415243708655, 9.556201303927180035, -48.09570126246647703 ) ) ;
#51070=VERTEX_POINT ( 'NONE', #38120 ) ;
#51071=EDGE_CURVE ( 'NONE', #11856, #27102, #26129, .T. ) ;
#51072=CARTESIAN_POINT ( 'NONE',  ( 4.975610109902397937, -28.45381238669758872, -39.78479568629688856 ) ) ;
#51073=CARTESIAN_POINT ( 'NONE',  ( 0.6008122571543327295, 44.05373654283606299, -21.69845264252053951 ) ) ;
#51076=CARTESIAN_POINT ( 'NONE',  ( 0.6039202388192952409, -49.10736577297868166, -0.1741829149863120263 ) ) ;
#51090=ORIENTED_EDGE ( 'NONE', *, *, #61415, .F. ) ;
#51091=CARTESIAN_POINT ( 'NONE',  ( 0.1145239942831223490, 43.37176113481423556, -8.113927333251773177 ) ) ;
#51092=CARTESIAN_POINT ( 'NONE',  ( 1.830465331921977246, -30.77164106904660912, -31.51955205576617658 ) ) ;
#51093=CARTESIAN_POINT ( 'NONE',  ( 4.060580049360325461, -37.10466027576811854, 23.55232218230391084 ) ) ;
#51095=ORIENTED_EDGE ( 'NONE', *, *, #30468, .F. ) ;
#51102=CARTESIAN_POINT ( 'NONE',  ( 0.1152339509894530906, -12.34020981180770526, 42.36345019301198533 ) ) ;
#51110=CARTESIAN_POINT ( 'NONE',  ( 4.975610109902397937, 30.04451009524474969, 38.59762713269442713 ) ) ;
#51115=DIRECTION ( 'NONE',  ( 0.000000000000000000, 0.000000000000000000, -1.000000000000000000 ) ) ;
#51116=CARTESIAN_POINT ( 'NONE',  ( 0.5980271706414734822, 46.38528005876716520, -16.13861941776310260 ) ) ;
#51118=CARTESIAN_POINT ( 'NONE',  ( -6.077587904424778920, 5.472951620448459842, 18.46192898789725945 ) ) ;
#51120=B_SPLINE_CURVE_WITH_KNOTS ( 'NONE', 3,
 ( #43117, #19300, #58398, #19612, #44062, #33714 ),
 .UNSPECIFIED., .F., .F.,
 ( 4, 2, 4 ),
 ( 3.252606517456513302E-18, 0.0002447193893791695454, 0.0004894387787583358383 ),
 .UNSPECIFIED. ) ;
#51124=B_SPLINE_CURVE_WITH_KNOTS ( 'NONE', 3,
 ( #57476, #10834, #25531, #58409, #29928, #48722 ),
 .UNSPECIFIED., .F., .F.,
 ( 4, 2, 4 ),
 ( 1.870429930157025393E-17, 0.0002293755540694321859, 0.0004587511081388456692 ),
 .UNSPECIFIED. ) ;
#51125=CARTESIAN_POINT ( 'NONE',  ( -2.739355103387247858, -2.122549901523845151, -14.77641190771826274 ) ) ;
#51126=EDGE_CURVE ( 'NONE', #2175, #45275, #32140, .T. ) ;
#51132=CARTESIAN_POINT ( 'NONE',  ( 1.830465331921978134, -16.69450186282941928, -40.76358256373419664 ) ) ;
#51133=EDGE_CURVE ( 'NONE', #9776, #4961, #18715, .T. ) ;
#51141=EDGE_LOOP ( 'NONE', ( #24705, #25046, #49187, #40136 ) ) ;
#51142=CARTESIAN_POINT ( 'NONE',  ( 0.6024113833632039894, -39.48520517600478286, 29.19692520300162641 ) ) ;
#51143=CARTESIAN_POINT ( 'NONE',  ( 1.479689385636123067, 3.059513055334726950, -43.95706115212809095 ) ) ;
#51145=ORIENTED_EDGE ( 'NONE', *, *, #31486, .T. ) ;
#51146=EDGE_CURVE ( 'NONE', #55001, #9995, #55296, .T. ) ;
#51155=CARTESIAN_POINT ( 'NONE',  ( 4.834790513006555379, -27.40943972694820019, -38.48781566650898611 ) ) ;
#51157=CARTESIAN_POINT ( 'NONE',  ( 4.975610109902397937, 0.000000000000000000, 0.000000000000000000 ) ) ;
#51161=CARTESIAN_POINT ( 'NONE',  ( 0.8744876279028263033, -48.79802643035343834, 5.394688766001209501 ) ) ;
#51163=ORIENTED_EDGE ( 'NONE', *, *, #48494, .F. ) ;
#51164=EDGE_LOOP ( 'NONE', ( #42095, #3183, #1063, #45805 ) ) ;
#51166=CARTESIAN_POINT ( 'NONE',  ( 0.5997462898726536595, 44.46857747280041195, -20.83500054451300088 ) ) ;
#51168=ORIENTED_EDGE ( 'NONE', *, *, #40273, .F. ) ;
#51171=CARTESIAN_POINT ( 'NONE',  ( 4.553261556744875094, 0.000000000000000000, 0.000000000000000000 ) ) ;
#51173=ADVANCED_FACE ( 'NONE', ( #61257 ), #57345, .F. ) ;
#51177=FACE_OUTER_BOUND ( 'NONE', #21982, .T. ) ;
#51182=CARTESIAN_POINT ( 'NONE',  ( 0.1119899015040013296, 15.76451783742778900, -41.21214973215941058 ) ) ;
#51185=FACE_OUTER_BOUND ( 'NONE', #18858, .T. ) ;
#51192=B_SPLINE_CURVE_WITH_KNOTS ( 'NONE', 3,
 ( #15766, #5702, #35187, #58961 ),
 .UNSPECIFIED., .F., .F.,
 ( 4, 4 ),
 ( 0.000000000000000000, 0.004442905043737213969 ),
 .UNSPECIFIED. ) ;
#51198=CARTESIAN_POINT ( 'NONE',  ( 4.975610109902397937, 13.36434394399761949, -47.05150069959838532 ) ) ;
#51203=CARTESIAN_POINT ( 'NONE',  ( 0.1157506346131639274, -35.41710508906525234, -26.31671193202034686 ) ) ;
#51205=CARTESIAN_POINT ( 'NONE',  ( 3.727782113643637540, -24.59154922726513703, -36.44219371153403131 ) ) ;
#51209=EDGE_CURVE ( 'NONE', #52291, #51706, #2932, .T. ) ;
#51211=CARTESIAN_POINT ( 'NONE',  ( 0.6021448801613057400, -1.835062463808373678, 49.07314626535442414 ) ) ;
#51213=ORIENTED_EDGE ( 'NONE', *, *, #60795, .T. ) ;
#51221=CARTESIAN_POINT ( 'NONE',  ( -6.072942160501519027, -6.664073831083622501, 18.06638542329059760 ) ) ;
#51226=EDGE_CURVE ( 'NONE', #27210, #37845, #15402, .T. ) ;
#51228=CARTESIAN_POINT ( 'NONE',  ( 4.553261556744875094, -43.07273893850278768, -8.618510669438375515 ) ) ;
#51229=CARTESIAN_POINT ( 'NONE',  ( 1.296416391601052487, 37.53038082136637854, 23.10363368562124720 ) ) ;
#51231=CARTESIAN_POINT ( 'NONE',  ( 1.657374760986086271, -44.03814544053055613, 1.237818003957595669 ) ) ;
#51236=ORIENTED_EDGE ( 'NONE', *, *, #52003, .T. ) ;
#51237=B_SPLINE_CURVE_WITH_KNOTS ( 'NONE', 3,
 ( #28830, #23831, #37325, #14142 ),
 .UNSPECIFIED., .F., .F.,
 ( 4, 4 ),
 ( 0.000000000000000000, 0.004444103432399267029 ),
 .UNSPECIFIED. ) ;
#51240=ORIENTED_EDGE ( 'NONE', *, *, #33254, .F. ) ;
#51241=DIRECTION ( 'NONE',  ( 0.000000000000000000, 0.000000000000000000, 1.000000000000000000 ) ) ;
#51243=CARTESIAN_POINT ( 'NONE',  ( 3.240649175237396040, -5.210370887173916721, -43.68199803827362615 ) ) ;
#51246=VERTEX_POINT ( 'NONE', #793 ) ;
#51247=CARTESIAN_POINT ( 'NONE',  ( 0.1158403557922069033, -44.12413028490447431, -0.03786534820748153896 ) ) ;
#51248=CARTESIAN_POINT ( 'NONE',  ( 0.6000166863083090663, 37.73145429715535215, -31.43502566135631682 ) ) ;
#51249=EDGE_CURVE ( 'NONE', #21737, #32638, #43430, .T. ) ;
#51252=ORIENTED_EDGE ( 'NONE', *, *, #43584, .F. ) ;
#51254=ORIENTED_EDGE ( 'NONE', *, *, #33078, .T. ) ;
#51264=AXIS2_PLACEMENT_3D ( 'NONE', #6273, #25409, #30411 ) ;
#51265=VERTEX_POINT ( 'NONE', #17071 ) ;
#51278=CARTESIAN_POINT ( 'NONE',  ( -6.072942160501519027, -18.27985097084440014, 6.054024345238414817 ) ) ;
#51281=CARTESIAN_POINT ( 'NONE',  ( 4.553261556744875094, 27.21079963941838997, 34.48350256002230196 ) ) ;
#51283=CARTESIAN_POINT ( 'NONE',  ( 0.6029442701453591180, 4.802144870275323107, 48.87212528428824498 ) ) ;
#51287=DIRECTION ( 'NONE',  ( 0.000000000000000000, 0.000000000000000000, -1.000000000000000000 ) ) ;
#51288=CARTESIAN_POINT ( 'NONE',  ( 0.5997462898726536595, 48.29911994996575686, -8.873930482211887849 ) ) ;
#51289=CARTESIAN_POINT ( 'NONE',  ( 4.553261556744873317, -41.61700166486752295, 14.05577241741092998 ) ) ;
#51292=CARTESIAN_POINT ( 'NONE',  ( 0.6016118706126976079, -1.225776398925409572, -49.09224508009149446 ) ) ;
#51296=CARTESIAN_POINT ( 'NONE',  ( 3.221118495291109607, 32.23766403744527764, -29.92481306659339779 ) ) ;
#51297=EDGE_CURVE ( 'NONE', #13208, #57613, #8815, .T. ) ;
#51301=CARTESIAN_POINT ( 'NONE',  ( 3.678748215320119641, 31.53400377379299258, -37.47291582321680892 ) ) ;
#51304=CARTESIAN_POINT ( 'NONE',  ( -6.077587904424778920, 13.82827771187065302, 13.40055061993020935 ) ) ;
#51306=CONICAL_SURFACE ( 'NONE', #37342, 43.92652462719577500, 1.486293639869522343 ) ;
#51314=ORIENTED_EDGE ( 'NONE', *, *, #45446, .T. ) ;
#51315=CARTESIAN_POINT ( 'NONE',  ( 4.335381028904201628, 42.17650767838711090, -24.91784596868873791 ) ) ;
#51323=EDGE_CURVE ( 'NONE', #22556, #55806, #12375, .T. ) ;
#51326=ORIENTED_EDGE ( 'NONE', *, *, #16007, .T. ) ;
#51329=CARTESIAN_POINT ( 'NONE',  ( 0.6028777368367060907, -42.74543088850748518, -24.17370404937778616 ) ) ;
#51333=CARTESIAN_POINT ( 'NONE',  ( 4.694002226626921015, 1.116723307532544451, 45.57452907601513203 ) ) ;
#51335=CARTESIAN_POINT ( 'NONE',  ( 1.657374760986086493, 5.460774167333708462, 43.71579111426014208 ) ) ;
#51338=CARTESIAN_POINT ( 'NONE',  ( 3.390910168358336918, 0.5608886540481926586, 43.97479437645385048 ) ) ;
#51339=B_SPLINE_CURVE_WITH_KNOTS ( 'NONE', 3,
 ( #60899, #18012, #13312, #32415 ),
 .UNSPECIFIED., .F., .F.,
 ( 4, 4 ),
 ( 7.152448122690996019E-18, 0.005013413432710146778 ),
 .UNSPECIFIED. ) ;
#51341=ORIENTED_EDGE ( 'NONE', *, *, #23256, .F. ) ;
#51343=CARTESIAN_POINT ( 'NONE',  ( 4.335381028904201628, 14.90794766671141858, 46.66379693114287619 ) ) ;
#51349=CARTESIAN_POINT ( 'NONE',  ( 4.975610109902397937, 13.36434394399692316, 47.05150069959858428 ) ) ;
#51350=EDGE_CURVE ( 'NONE', #47069, #1293, #7350, .T. ) ;
#51353=CARTESIAN_POINT ( 'NONE',  ( 2.533389852662419894, -39.10406001682097354, -20.20700427907317831 ) ) ;
#51361=CARTESIAN_POINT ( 'NONE',  ( 0.6000166863083090663, -1.051715750663601012, -49.09905676984293876 ) ) ;
#51364=CARTESIAN_POINT ( 'NONE',  ( 0.6021447746440204973, -49.10674983770864088, 0.2612651243270994184 ) ) ;
#51372=LINE ( 'NONE', #32921, #21143 ) ;
#51376=CARTESIAN_POINT ( 'NONE',  ( 0.1145239942831223490, 3.911746048396175901, 43.95046897994981805 ) ) ;
#51380=CARTESIAN_POINT ( 'NONE',  ( -6.078457390727109555, 17.84708778612949587, 7.230212209312759875 ) ) ;
#51381=( BOUNDED_SURFACE ( )  B_SPLINE_SURFACE ( 3, 1, ( 
 ( #30501, #16739 ),
 ( #1680, #45564 ),
 ( #20819, #17055 ),
 ( #54298, #35855 ) ),
 .UNSPECIFIED., .F., .F., .F. ) 
 B_SPLINE_SURFACE_WITH_KNOTS ( ( 4, 4 ),
 ( 2, 2 ),
 ( 0.000000000000000000, 1.000000000000000000 ),
 ( 0.000000000000000000, 1.000000000000000000 ),
 .UNSPECIFIED. ) 
 GEOMETRIC_REPRESENTATION_ITEM ( )  RATIONAL_B_SPLINE_SURFACE ( (
 ( 1.000000000000000000, 1.000000000000000000),
 ( 0.9953485035131437453, 0.8621029689291523912),
 ( 0.9953485035131437453, 0.8621029689291523912),
 ( 1.000000000000000000, 1.000000000000000000) ) ) 
 REPRESENTATION_ITEM ( '' )  SURFACE ( )  );
#51386=DIRECTION ( 'NONE',  ( -1.000000000000000000, -0.000000000000000000, -0.000000000000000000 ) ) ;
#51387=VERTEX_POINT ( 'NONE', #32403 ) ;
#51392=CARTESIAN_POINT ( 'NONE',  ( 0.6000166863083106206, 5.235566842225154005, -48.83044461756462340 ) ) ;
#51397=CARTESIAN_POINT ( 'NONE',  ( 0.5549461598389366923, -37.99084232143810169, 22.40342820138097579 ) ) ;
#51399=VERTEX_POINT ( 'NONE', #17677 ) ;
#51402=CARTESIAN_POINT ( 'NONE',  ( 0.1129192098497447394, -32.03190746134960420, -30.34647742609823595 ) ) ;
#51406=ORIENTED_EDGE ( 'NONE', *, *, #16060, .F. ) ;
#51410=DIRECTION ( 'NONE',  ( 0.000000000000000000, 0.000000000000000000, 1.000000000000000000 ) ) ;
#51411=CARTESIAN_POINT ( 'NONE',  ( -6.077587904424778920, 7.800189710370847074, -17.60548385805273242 ) ) ;
#51412=CARTESIAN_POINT ( 'NONE',  ( 0.5997462898726536595, 27.66511329191589397, 40.57330571557817223 ) ) ;
#51415=CARTESIAN_POINT ( 'NONE',  ( 4.553261556744875094, -20.11719049292643646, -39.04917684785361587 ) ) ;
#51418=EDGE_CURVE ( 'NONE', #61199, #56898, #61487, .T. ) ;
#51421=CARTESIAN_POINT ( 'NONE',  ( 0.5997462898726536595, 44.01516392039482639, 21.77652348757905898 ) ) ;
#51422=DIRECTION ( 'NONE',  ( 0.000000000000000000, 0.000000000000000000, -1.000000000000000000 ) ) ;
#51426=CARTESIAN_POINT ( 'NONE',  ( -6.078075953587585900, -19.21681836813549182, -1.228440496412561478 ) ) ;
#51428=CARTESIAN_POINT ( 'NONE',  ( -6.057079549204054558, 13.82732400278046470, 13.40284828019289698 ) ) ;
#51441=CARTESIAN_POINT ( 'NONE',  ( 0.6027444965799114707, -39.43333548727365923, 29.26688518164454322 ) ) ;
#51442=CARTESIAN_POINT ( 'NONE',  ( 4.335381028904201628, 45.01666255113143933, -19.31985870605438294 ) ) ;
#51450=EDGE_CURVE ( 'NONE', #55332, #29824, #38890, .T. ) ;
#51454=EDGE_CURVE ( 'NONE', #19355, #35035, #43241, .T. ) ;
#51457=ORIENTED_EDGE ( 'NONE', *, *, #20886, .T. ) ;
#51461=DIRECTION ( 'NONE',  ( -1.000000000000000000, -0.000000000000000000, -0.000000000000000000 ) ) ;
#51462=ORIENTED_EDGE ( 'NONE', *, *, #50248, .F. ) ;
#51463=CIRCLE ( 'NONE', #27474, 43.92652462719577500 ) ;
#51470=CARTESIAN_POINT ( 'NONE',  ( 0.6016118706126978299, -48.74769260159513351, 5.934098145827796600 ) ) ;
#51474=DIRECTION ( 'NONE',  ( 0.1011922191286468292, -0.9849719771322142936, 0.1399654923617842661 ) ) ;
#51476=ORIENTED_EDGE ( 'NONE', *, *, #41415, .F. ) ;
#51496=CARTESIAN_POINT ( 'NONE',  ( 0.1147471544378676350, -18.14425483850216025, -40.22111640455466386 ) ) ;
#51497=CARTESIAN_POINT ( 'NONE',  ( 0.2940135542859022566, 10.59968125873896305, 42.82391044620469955 ) ) ;
#51503=CARTESIAN_POINT ( 'NONE',  ( 0.1129192098497447394, -17.41650932123218354, 40.54154647825593827 ) ) ;
#51509=CARTESIAN_POINT ( 'NONE',  ( 1.296416391601052265, -23.78941374985365442, -37.09947664744655782 ) ) ;
#51517=ORIENTED_EDGE ( 'NONE', *, *, #17610, .T. ) ;
#51523=ADVANCED_FACE ( 'NONE', ( #44827 ), #56531, .F. ) ;
#51534=CARTESIAN_POINT ( 'NONE',  ( 3.221118495291108719, 37.86046104227076370, 22.39077732747234251 ) ) ;
#51538=CARTESIAN_POINT ( 'NONE',  ( 3.678748215320120973, 26.48317992319705283, -41.19774260144669853 ) ) ;
#51539=CARTESIAN_POINT ( 'NONE',  ( -6.078457390727109555, -6.646245994447285810, 18.07268450504245294 ) ) ;
#51544=VERTEX_POINT ( 'NONE', #34791 ) ;
#51545=CARTESIAN_POINT ( 'NONE',  ( 0.8753041380234524160, -45.17330286263802464, 19.24866323549142422 ) ) ;
#51547=CARTESIAN_POINT ( 'NONE',  ( -2.739355103387248747, 14.08251715046648833, -4.952805029257079994 ) ) ;
#51555=DIRECTION ( 'NONE',  ( 0.09722883295013595717, 0.08804304236304483222, 0.9913601649928313053 ) ) ;
#51560=CARTESIAN_POINT ( 'NONE',  ( 0.6016117650947689910, -25.15845835820325149, 42.17348725541975085 ) ) ;
#51561=CARTESIAN_POINT ( 'NONE',  ( 0.1129192098497447394, 36.71339784380064231, -24.47607416535520741 ) ) ;
#51567=EDGE_LOOP ( 'NONE', ( #7512, #7144, #55715, #12116 ) ) ;
#51573=CARTESIAN_POINT ( 'NONE',  ( 0.1119899015040012602, -38.71871408100971479, 21.16181674869922702 ) ) ;
#51574=ORIENTED_EDGE ( 'NONE', *, *, #47326, .F. ) ;
#51579=CARTESIAN_POINT ( 'NONE',  ( 4.553261556744875094, 0.000000000000000000, 0.000000000000000000 ) ) ;
#51582=AXIS2_PLACEMENT_3D ( 'NONE', #15794, #11094, #53969 ) ;
#51588=LINE ( 'NONE', #27802, #3704 ) ;
#51596=CARTESIAN_POINT ( 'NONE',  ( 1.296416391601052265, 16.25883182415322281, 40.96288273290907966 ) ) ;
#51601=CARTESIAN_POINT ( 'NONE',  ( 2.009741617377216460, 32.62915352493547516, -29.57773517139599306 ) ) ;
#51609=CARTESIAN_POINT ( 'NONE',  ( 0.1129192098497455998, -42.55567333040708888, -11.66046547873770756 ) ) ;
#51620=CARTESIAN_POINT ( 'NONE',  ( 0.5980271706414734822, 17.61704905854934822, 45.84417984117861522 ) ) ;
#51622=CARTESIAN_POINT ( 'NONE',  ( 0.8753041380234471980, -29.91468680897799004, -38.93905290314260270 ) ) ;
#51627=CARTESIAN_POINT ( 'NONE',  ( 5.901764892641288895, 42.64666365787720537, -24.06768676652523808 ) ) ;
#51629=ORIENTED_EDGE ( 'NONE', *, *, #36793, .T. ) ;
#51634=ORIENTED_EDGE ( 'NONE', *, *, #17354, .T. ) ;
#51635=DIRECTION ( 'NONE',  ( -0.1011922191286467460, -0.8906890386588581787, -0.4432078194264840176 ) ) ;
#51636=ORIENTED_EDGE ( 'NONE', *, *, #10329, .T. ) ;
#51638=CARTESIAN_POINT ( 'NONE',  ( 0.1129192098497455998, 25.64022107388826655, -35.91003830501005467 ) ) ;
#51648=CARTESIAN_POINT ( 'NONE',  ( 2.394385881922565851, 0.1126610846915976627, 44.02256615367562631 ) ) ;
#51652=CARTESIAN_POINT ( 'NONE',  ( 0.5987334363312686314, -49.10393658271619444, -0.6052425568828397884 ) ) ;
#51657=CARTESIAN_POINT ( 'NONE',  ( 2.359973842542475886, -34.35832655684843218, 27.52528457337841772 ) ) ;
#51662=CARTESIAN_POINT ( 'NONE',  ( 3.894904216938897434, 42.66483338720180996, -10.57526947734715783 ) ) ;
#51663=CARTESIAN_POINT ( 'NONE',  ( -2.739355103387248747, -0.2155581815329185580, 14.92652342715446956 ) ) ;
#51673=AXIS2_PLACEMENT_3D ( 'NONE', #30087, #49199, #34501 ) ;
#51676=CARTESIAN_POINT ( 'NONE',  ( 4.553261556744873317, 1.633632119646958980, 43.89613664004264848 ) ) ;
#51678=EDGE_CURVE ( 'NONE', #30264, #22007, #11929, .T. ) ;
#51679=( BOUNDED_SURFACE ( )  B_SPLINE_SURFACE ( 3, 1, ( 
 ( #27050, #21732 ),
 ( #46175, #35538 ),
 ( #59936, #36159 ),
 ( #22047, #16731 ) ),
 .UNSPECIFIED., .F., .F., .F. ) 
 B_SPLINE_SURFACE_WITH_KNOTS ( ( 4, 4 ),
 ( 2, 2 ),
 ( 0.000000000000000000, 1.000000000000000000 ),
 ( 0.000000000000000000, 1.000000000000000000 ),
 .UNSPECIFIED. ) 
 GEOMETRIC_REPRESENTATION_ITEM ( )  RATIONAL_B_SPLINE_SURFACE ( (
 ( 1.000000000000000000, 1.000000000000000000),
 ( 0.9754377213608244057, 0.9999580625633939235),
 ( 0.9754377213608244057, 0.9999580625633939235),
 ( 1.000000000000000000, 1.000000000000000000) ) ) 
 REPRESENTATION_ITEM ( '' )  SURFACE ( )  );
#51683=ORIENTED_EDGE ( 'NONE', *, *, #52028, .T. ) ;
#51684=EDGE_CURVE ( 'NONE', #52291, #52483, #21608, .T. ) ;
#51686=CARTESIAN_POINT ( 'NONE',  ( 0.3676999524040323597, 44.06746933160595603, -2.002181318164867552 ) ) ;
#51691=FACE_OUTER_BOUND ( 'NONE', #19703, .T. ) ;
#51696=ORIENTED_EDGE ( 'NONE', *, *, #24546, .F. ) ;
#51703=ORIENTED_EDGE ( 'NONE', *, *, #22474, .T. ) ;
#51704=CARTESIAN_POINT ( 'NONE',  ( 4.335381028904201628, 24.52155563981625974, -42.40813785899753441 ) ) ;
#51706=VERTEX_POINT ( 'NONE', #31313 ) ;
#51708=VERTEX_POINT ( 'NONE', #50416 ) ;
#51710=CARTESIAN_POINT ( 'NONE',  ( -6.078726893082806448, -1.845620846545631188, 19.16736092839899186 ) ) ;
#51712=AXIS2_PLACEMENT_3D ( 'NONE', #40133, #29447, #59180 ) ;
#51714=CARTESIAN_POINT ( 'NONE',  ( 4.975610109902397937, -46.23629923292386934, 15.95788333023201488 ) ) ;
#51715=FACE_OUTER_BOUND ( 'NONE', #27945, .T. ) ;
#51718=CARTESIAN_POINT ( 'NONE',  ( 0.8744876279028263033, 17.78802839418742110, -45.75954650373051891 ) ) ;
#51722=ORIENTED_EDGE ( 'NONE', *, *, #53900, .F. ) ;
#51730=CARTESIAN_POINT ( 'NONE',  ( -6.072942160501519027, 7.807899065004683337, -17.60229742049939006 ) ) ;
#51732=CARTESIAN_POINT ( 'NONE',  ( 0.8744876279028263033, -2.462621419133342204, 49.03351451941333750 ) ) ;
#51733=ORIENTED_EDGE ( 'NONE', *, *, #49421, .F. ) ;
#51734=CARTESIAN_POINT ( 'NONE',  ( 0.1139756605157203201, -40.74870632435499118, 16.92625630747966525 ) ) ;
#51741=CARTESIAN_POINT ( 'NONE',  ( 0.7242003506639982380, 46.85218299671425513, 14.69301271245709195 ) ) ;
#51748=CARTESIAN_POINT ( 'NONE',  ( 0.2940133293162997541, -31.12576116254606973, -31.26383760241506593 ) ) ;
#51754=( BOUNDED_SURFACE ( )  B_SPLINE_SURFACE ( 3, 1, ( 
 ( #33710, #4851 ),
 ( #57160, #61557 ),
 ( #10504, #9889 ),
 ( #37809, #52787 ) ),
 .UNSPECIFIED., .F., .F., .F. ) 
 B_SPLINE_SURFACE_WITH_KNOTS ( ( 4, 4 ),
 ( 2, 2 ),
 ( 0.000000000000000000, 1.000000000000000000 ),
 ( 0.000000000000000000, 1.000000000000000000 ),
 .UNSPECIFIED. ) 
 GEOMETRIC_REPRESENTATION_ITEM ( )  RATIONAL_B_SPLINE_SURFACE ( (
 ( 1.000000000000000000, 1.000000000000000000),
 ( 0.7211978278499970862, 0.9934217856018976445),
 ( 0.7211978278499970862, 0.9934217856018976445),
 ( 1.000000000000000000, 1.000000000000000000) ) ) 
 REPRESENTATION_ITEM ( '' )  SURFACE ( )  );
#51756=CARTESIAN_POINT ( 'NONE',  ( 4.553261556744875094, -36.69060082144763868, -24.15241969627107110 ) ) ;
#51761=CARTESIAN_POINT ( 'NONE',  ( 50.15577769773999961, 9.539392014169456147, -3.000000000000000000 ) ) ;
#51762=ADVANCED_FACE ( 'NONE', ( #22841 ), #56896, .F. ) ;
#51766=CARTESIAN_POINT ( 'NONE',  ( 0.1129192098497455998, 43.21532672376827833, 8.909956450124401073 ) ) ;
#51771=CARTESIAN_POINT ( 'NONE',  ( 50.15577769773999961, 0.000000000000000000, 0.000000000000000000 ) ) ;
#51773=ORIENTED_EDGE ( 'NONE', *, *, #41099, .F. ) ;
#51774=VERTEX_POINT ( 'NONE', #47892 ) ;
#51779=CARTESIAN_POINT ( 'NONE',  ( 4.553261556744875094, 17.57396821678876364, 40.25785894628445760 ) ) ;
#51780=CIRCLE ( 'NONE', #26796, 48.91267123290010943 ) ;
#51785=VECTOR ( 'NONE', #45622, 1000.000000000000000 ) ;
#51788=CARTESIAN_POINT ( 'NONE',  ( -6.078726893082806448, -16.14009859332537999, -10.50196451462564262 ) ) ;
#51794=CARTESIAN_POINT ( 'NONE',  ( 1.657374760986086271, -43.83488152824200057, -4.403817509528764162 ) ) ;
#51797=CARTESIAN_POINT ( 'NONE',  ( -6.063463321072276813, -1.833563764454537504, 19.16920698414906354 ) ) ;
#51801=CARTESIAN_POINT ( 'NONE',  ( 0.5997462898726536595, 41.43917033312096265, 26.35046094941977302 ) ) ;
#51803=CARTESIAN_POINT ( 'NONE',  ( 4.390527457369401532, -4.537883182548267058, 43.69888960660402688 ) ) ;
#51806=ORIENTED_EDGE ( 'NONE', *, *, #6537, .T. ) ;
#51810=CARTESIAN_POINT ( 'NONE',  ( 0.6008123274975392114, 32.69143758430389113, 36.64456930883510921 ) ) ;
#51812=CARTESIAN_POINT ( 'NONE',  ( 0.1158403557922069033, -17.82608841671577693, -40.36298897434691213 ) ) ;
#51822=CARTESIAN_POINT ( 'NONE',  ( 1.834102595619085285, -23.93815899361085187, -36.97515772588796779 ) ) ;
#51828=EDGE_CURVE ( 'NONE', #20580, #3844, #4620, .T. ) ;
#51831=CARTESIAN_POINT ( 'NONE',  ( 0.1119898979215348117, -35.69472108585459580, -25.93931754797872813 ) ) ;
#51839=CARTESIAN_POINT ( 'NONE',  ( 2.648799415243696664, 48.37728179772450687, -8.009748382636628250 ) ) ;
#51845=ORIENTED_EDGE ( 'NONE', *, *, #37704, .T. ) ;
#51849=CARTESIAN_POINT ( 'NONE',  ( 0.7948878604505670298, -20.66454813869003360, -44.53846761533425536 ) ) ;
#51852=EDGE_CURVE ( 'NONE', #46940, #31990, #9587, .T. ) ;
#51858=CARTESIAN_POINT ( 'NONE',  ( 0.5980271706414711508, 17.61704905855000547, -45.84417984117837364 ) ) ;
#51862=VERTEX_POINT ( 'NONE', #58796 ) ;
#51864=CARTESIAN_POINT ( 'NONE',  ( 0.6000166863083090663, 44.47108027094602534, 20.83618250168510144 ) ) ;
#51866=CARTESIAN_POINT ( 'NONE',  ( 0.1365634738349414679, -34.97642399247558842, -26.89818552099423954 ) ) ;
#51869=CARTESIAN_POINT ( 'NONE',  ( 0.1140933569871964842, -44.12262566372946537, -0.3792817189201296291 ) ) ;
#51870=CARTESIAN_POINT ( 'NONE',  ( -6.078457390727109555, -14.65958194562101546, 12.48563847855327680 ) ) ;
#51879=CARTESIAN_POINT ( 'NONE',  ( 0.1154773475650540532, 36.88152504251267771, -24.22182364283563416 ) ) ;
#51885=CARTESIAN_POINT ( 'NONE',  ( -6.078726893082806448, -4.281536037414130469, 18.77398440472997265 ) ) ;
#51887=B_SPLINE_CURVE_WITH_KNOTS ( 'NONE', 3,
 ( #8121, #27237, #56960, #37273 ),
 .UNSPECIFIED., .F., .F.,
 ( 4, 4 ),
 ( 0.000000000000000000, 0.004442905043737215703 ),
 .UNSPECIFIED. ) ;
#51890=CARTESIAN_POINT ( 'NONE',  ( 0.1154773475650540115, 33.48131017346754845, -28.73926754658474891 ) ) ;
#51901=VECTOR ( 'NONE', #57723, 1000.000000000000000 ) ;
#51908=CARTESIAN_POINT ( 'NONE',  ( 0.2285344041767106704, 3.479521872102009361, -43.98174732587396818 ) ) ;
#51909=B_SPLINE_CURVE_WITH_KNOTS ( 'NONE', 3,
 ( #34575, #725, #1034, #39287 ),
 .UNSPECIFIED., .F., .F.,
 ( 4, 4 ),
 ( 2.266397508114618048E-17, 0.004559932413162186803 ),
 .UNSPECIFIED. ) ;
#51911=DIRECTION ( 'NONE',  ( 1.000000000000000000, 0.000000000000000000, 0.000000000000000000 ) ) ;
#51912=CARTESIAN_POINT ( 'NONE',  ( -6.063463321072278589, 3.057971819381483325, 19.01234495877188024 ) ) ;
#51913=DIRECTION ( 'NONE',  ( 1.000000000000000000, 0.000000000000000000, 0.000000000000000000 ) ) ;
#51915=EDGE_CURVE ( 'NONE', #43985, #42350, #35026, .T. ) ;
#51921=CARTESIAN_POINT ( 'NONE',  ( 0.2279481005628775647, 40.07358784552179287, -18.45565074063110700 ) ) ;
#51927=CARTESIAN_POINT ( 'NONE',  ( 2.299746137290199943, 32.00013501491892498, -37.15202143508611954 ) ) ;
#51930=EDGE_CURVE ( 'NONE', #51399, #11906, #58127, .T. ) ;
#51934=CARTESIAN_POINT ( 'NONE',  ( 2.359973842542476330, -26.25271817560583898, 35.34021339812076690 ) ) ;
#51938=CARTESIAN_POINT ( 'NONE',  ( 0.7948878604505664747, 17.76850119055459132, 45.77094070193091113 ) ) ;
#51939=ORIENTED_EDGE ( 'NONE', *, *, #8550, .T. ) ;
#51942=CARTESIAN_POINT ( 'NONE',  ( 0.5997462898726536595, -43.04230894295718457, -23.64130434225950950 ) ) ;
#51948=CARTESIAN_POINT ( 'NONE',  ( -2.601141883200662974, 7.298105880293700665, 13.02048685838633091 ) ) ;
#51950=ORIENTED_EDGE ( 'NONE', *, *, #6632, .T. ) ;
#51951=CARTESIAN_POINT ( 'NONE',  ( -2.601141883200665639, 6.503674101140891395, 13.43494140871250231 ) ) ;
#51955=CARTESIAN_POINT ( 'NONE',  ( 2.879087469061463622, -28.76677455459574162, -33.29526030095637168 ) ) ;
#51956=ORIENTED_EDGE ( 'NONE', *, *, #51930, .T. ) ;
#51958=EDGE_CURVE ( 'NONE', #49082, #27245, #45364, .T. ) ;
#51960=CARTESIAN_POINT ( 'NONE',  ( 0.7044674535452954967, 48.35836311421829237, -8.559873814742601894 ) ) ;
#51967=CARTESIAN_POINT ( 'NONE',  ( 4.975610109902397937, 7.237810502494805398, -48.37420290059309025 ) ) ;
#51973=CARTESIAN_POINT ( 'NONE',  ( 3.221118495291108719, 42.77391066528618779, -10.25446176353823802 ) ) ;
#51974=CARTESIAN_POINT ( 'NONE',  ( 3.390910168358336474, -39.24745467111843311, -19.84274271294525960 ) ) ;
#51976=DIRECTION ( 'NONE',  ( -0.1011922191286467460, 0.9172554449906634710, 0.3852305587862932534 ) ) ;
#51979=B_SPLINE_CURVE_WITH_KNOTS ( 'NONE', 3,
 ( #61356, #37600, #56665, #18794 ),
 .UNSPECIFIED., .F., .F.,
 ( 4, 4 ),
 ( 0.000000000000000000, 0.005013413432710140706 ),
 .UNSPECIFIED. ) ;
#51982=FACE_OUTER_BOUND ( 'NONE', #382, .T. ) ;
#51990=CARTESIAN_POINT ( 'NONE',  ( 4.975610109902397937, -48.77192499014908833, -3.707929326867496655 ) ) ;
#51994=CARTESIAN_POINT ( 'NONE',  ( 0.5997462898726536595, 48.29911994996563607, 8.873930482212578852 ) ) ;
#51995=CARTESIAN_POINT ( 'NONE',  ( 4.060580049360325461, 23.21117414920292177, -37.31901779220056881 ) ) ;
#52001=EDGE_CURVE ( 'NONE', #49846, #60982, #24519, .T. ) ;
#52003=EDGE_CURVE ( 'NONE', #4753, #22282, #21533, .T. ) ;
#52010=CARTESIAN_POINT ( 'NONE',  ( -6.078457390727109555, 5.474669697364079823, -18.46137867934762866 ) ) ;
#52012=ORIENTED_EDGE ( 'NONE', *, *, #14095, .F. ) ;
#52013=LINE ( 'NONE', #57021, #13744 ) ;
#52021=CARTESIAN_POINT ( 'NONE',  ( -6.078457390727109555, 15.43466132010174618, 11.51371968441402238 ) ) ;
#52022=ORIENTED_EDGE ( 'NONE', *, *, #38452, .T. ) ;
#52025=CARTESIAN_POINT ( 'NONE',  ( 0.1154773475650540254, -31.82144335153932246, -30.56696538864947499 ) ) ;
#52028=EDGE_CURVE ( 'NONE', #61623, #22696, #43132, .T. ) ;
#52032=CARTESIAN_POINT ( 'NONE',  ( 0.6029442701453591180, 46.57822130577238084, -15.55681603506220512 ) ) ;
#52035=CARTESIAN_POINT ( 'NONE',  ( 0.1129192098497455998, 25.64022107388826655, -35.91003830501005467 ) ) ;
#52037=CARTESIAN_POINT ( 'NONE',  ( -6.079354080745853928, -18.27463532918897826, 6.068826808644322668 ) ) ;
#52047=B_SPLINE_CURVE_WITH_KNOTS ( 'NONE', 3,
 ( #20542, #55891, #36198, #26463 ),
 .UNSPECIFIED., .F., .F.,
 ( 4, 4 ),
 ( 0.000000000000000000, 0.005013413432710143308 ),
 .UNSPECIFIED. ) ;
#52053=CARTESIAN_POINT ( 'NONE',  ( 4.975610109902397937, 5.990074626311793528E-15, -48.91267123290010943 ) ) ;
#52064=CARTESIAN_POINT ( 'NONE',  ( 0.6252788684277214015, -39.76148085432274115, -28.81785855064513768 ) ) ;
#52071=CARTESIAN_POINT ( 'NONE',  ( 2.879087469061463622, -30.37913392544255586, 31.83095818104449748 ) ) ;
#52072=CARTESIAN_POINT ( 'NONE',  ( 0.6000166863083090663, -39.66797998683874482, 28.95297645272786724 ) ) ;
#52074=ORIENTED_EDGE ( 'NONE', *, *, #5624, .F. ) ;
#52075=VERTEX_POINT ( 'NONE', #37505 ) ;
#52079=CARTESIAN_POINT ( 'NONE',  ( 4.553261556744873317, 12.71466023209499419, 42.04612920360230532 ) ) ;
#52080=CARTESIAN_POINT ( 'NONE',  ( 0.1129192098497447394, 29.30421273086510681, -32.98810246148386227 ) ) ;
#52081=ORIENTED_EDGE ( 'NONE', *, *, #44649, .F. ) ;
#52090=CARTESIAN_POINT ( 'NONE',  ( 0.1129192098497447394, 30.02178898772887550, 32.33641869102754640 ) ) ;
#52094=VERTEX_POINT ( 'NONE', #38131 ) ;
#52095=CARTESIAN_POINT ( 'NONE',  ( 3.727782113643637985, 34.82198584334466318, 26.83667412016397691 ) ) ;
#52099=CARTESIAN_POINT ( 'NONE',  ( 0.5549461598389365813, -43.84610486898805704, -4.768310317555460642 ) ) ;
#52102=CARTESIAN_POINT ( 'NONE',  ( 4.335381028904201628, -32.17603896083255677, 36.93858909670658619 ) ) ;
#52104=EDGE_CURVE ( 'NONE', #26869, #45900, #4553, .T. ) ;
#52110=CARTESIAN_POINT ( 'NONE',  ( 0.8753041380234465318, -34.64850320773107484, -34.79395857525885560 ) ) ;
#52117=CARTESIAN_POINT ( 'NONE',  ( 4.553261556744873317, -33.30082861731504096, 28.64601855797499042 ) ) ;
#52119=DIRECTION ( 'NONE',  ( 0.000000000000000000, 0.000000000000000000, 1.000000000000000000 ) ) ;
#52120=CARTESIAN_POINT ( 'NONE',  ( 0.1157991065609915438, -17.78625520842043883, -40.38058309631790621 ) ) ;
#52121=CARTESIAN_POINT ( 'NONE',  ( 0.6028777368367060907, -42.83088177469218039, 24.02197734811634433 ) ) ;
#52122=FACE_OUTER_BOUND ( 'NONE', #57110, .T. ) ;
#52123=CARTESIAN_POINT ( 'NONE',  ( -6.078726893082806448, -8.909671472910670076, -17.07078778245227824 ) ) ;
#52128=EDGE_CURVE ( 'NONE', #21853, #20883, #44749, .T. ) ;
#52129=VERTEX_POINT ( 'NONE', #39667 ) ;
#52130=CARTESIAN_POINT ( 'NONE',  ( 0.8744876279028263033, -38.80702141274021955, -30.07266432244763621 ) ) ;
#52131=DIRECTION ( 'NONE',  ( -0.1011922191286467460, -0.8267003359790447981, -0.5534678755627595592 ) ) ;
#52133=EDGE_CURVE ( 'NONE', #53370, #15459, #41682, .T. ) ;
#52134=CARTESIAN_POINT ( 'NONE',  ( 0.6021447746440204973, -39.51108366771187264, -29.16188276657664602 ) ) ;
#52141=CARTESIAN_POINT ( 'NONE',  ( 0.7044674535452954967, -8.668117436800997666, 48.33907801057787879 ) ) ;
#52143=CARTESIAN_POINT ( 'NONE',  ( 0.2940135542859013684, -35.83075920381577362, -25.73707915769758969 ) ) ;
#52146=CARTESIAN_POINT ( 'NONE',  ( 0.1157506346131639274, -6.950611311771472067, 43.57326774750212905 ) ) ;
#52147=CARTESIAN_POINT ( 'NONE',  ( 0.5997462898726536595, 49.03735788587799505, 2.624721264559015221 ) ) ;
#52149=( BOUNDED_SURFACE ( )  B_SPLINE_SURFACE ( 3, 1, ( 
 ( #41504, #17374 ),
 ( #54628, #59965 ),
 ( #50564, #31150 ),
 ( #21759, #16144 ) ),
 .UNSPECIFIED., .F., .F., .F. ) 
 B_SPLINE_SURFACE_WITH_KNOTS ( ( 4, 4 ),
 ( 2, 2 ),
 ( 0.000000000000000000, 1.000000000000000000 ),
 ( 0.000000000000000000, 1.000000000000000000 ),
 .UNSPECIFIED. ) 
 GEOMETRIC_REPRESENTATION_ITEM ( )  RATIONAL_B_SPLINE_SURFACE ( (
 ( 1.000000000000000000, 1.000000000000000000),
 ( 0.7211978278499970862, 0.9934217856018976445),
 ( 0.7211978278499970862, 0.9934217856018976445),
 ( 1.000000000000000000, 1.000000000000000000) ) ) 
 REPRESENTATION_ITEM ( '' )  SURFACE ( )  );
#52153=B_SPLINE_CURVE_WITH_KNOTS ( 'NONE', 3,
 ( #12415, #49146, #55918, #29726, #12732, #25342, #15958, #44181, #48838, #39787, #5890, #20343, #54127, #31827, #53823, #36227, #55292, #25037, #60004, #49453, #17725, #44483, #40943, #50911, #58520 ),
 .UNSPECIFIED., .F., .F.,
 ( 4, 3, 3, 3, 3, 3, 3, 3, 4 ),
 ( 4.906538933386797396E-18, 0.0005656085177311379053, 0.001131215744874498538, 0.001696821861372765482, 0.002262427090022498151, 0.002828031679238745925, 0.003393635864401604429, 0.003977030878808131623, 0.004561030005651157265 ),
 .UNSPECIFIED. ) ;
#52154=EDGE_LOOP ( 'NONE', ( #58544, #5303, #53265, #45521 ) ) ;
#52158=CARTESIAN_POINT ( 'NONE',  ( 3.221118495291109163, -40.02489484504095429, 18.24196295098654019 ) ) ;
#52160=CARTESIAN_POINT ( 'NONE',  ( 0.6252788684277210685, -47.66997436610286343, -11.79058417165001416 ) ) ;
#52165=DIRECTION ( 'NONE',  ( 0.000000000000000000, 0.000000000000000000, 1.000000000000000000 ) ) ;
#52168=CARTESIAN_POINT ( 'NONE',  ( 3.894904216938897878, 43.95193974686379335, 0.5927267197078011085 ) ) ;
#52172=CARTESIAN_POINT ( 'NONE',  ( 2.359973842542475886, 38.98642570442579114, -20.44980453270367704 ) ) ;
#52173=CARTESIAN_POINT ( 'NONE',  ( 4.553261556744873317, -43.82122302957819215, 3.039733214543990591 ) ) ;
#52175=ORIENTED_EDGE ( 'NONE', *, *, #22921, .T. ) ;
#52185=DIRECTION ( 'NONE',  ( -0.1011922191286467321, -0.9739806266819500680, -0.2027852894961952035 ) ) ;
#52186=ORIENTED_EDGE ( 'NONE', *, *, #57510, .F. ) ;
#52189=CARTESIAN_POINT ( 'NONE',  ( -6.078726893082806448, -4.288195875146701752, 18.77246434022701749 ) ) ;
#52190=CARTESIAN_POINT ( 'NONE',  ( -2.601141883200665639, 14.30071512379483245, -4.276093359300567442 ) ) ;
#52192=CARTESIAN_POINT ( 'NONE',  ( 0.2940135542859001472, 24.57542350531248232, -36.63726392931048537 ) ) ;
#52200=VERTEX_POINT ( 'NONE', #44986 ) ;
#52221=CARTESIAN_POINT ( 'NONE',  ( 0.6252788684277220677, -35.74989368885943009, -33.66584964632434662 ) ) ;
#52222=DIRECTION ( 'NONE',  ( 0.09722883295013598492, 0.3366266327598188557, 0.9366050737423649020 ) ) ;
#52238=CARTESIAN_POINT ( 'NONE',  ( 0.1368894036331251562, 42.07194175847984496, 13.29710654971273698 ) ) ;
#52244=CARTESIAN_POINT ( 'NONE',  ( -6.078075953587585900, 19.09727103821296623, -2.467673629183584350 ) ) ;
#52251=VECTOR ( 'NONE', #48336, 1000.000000000000227 ) ;
#52255=CARTESIAN_POINT ( 'NONE',  ( 0.6029443199889047422, -42.78821616806403938, -24.09784635624990656 ) ) ;
#52257=CARTESIAN_POINT ( 'NONE',  ( 4.975610109902397937, -32.45573888811600227, -36.59336579715246529 ) ) ;
#52258=CARTESIAN_POINT ( 'NONE',  ( 1.834102595619085729, -28.46990526199986604, -33.61044836401974578 ) ) ;
#52259=ORIENTED_EDGE ( 'NONE', *, *, #363, .T. ) ;
#52263=CARTESIAN_POINT ( 'NONE',  ( 0.1156495703730067298, -38.37914333307228532, 21.77118072706586105 ) ) ;
#52264=ORIENTED_EDGE ( 'NONE', *, *, #55793, .F. ) ;
#52266=VERTEX_POINT ( 'NONE', #9207 ) ;
#52269=CARTESIAN_POINT ( 'NONE',  ( 4.975610109902397937, -22.11219452748553138, -43.62912170003438916 ) ) ;
#52271=ORIENTED_EDGE ( 'NONE', *, *, #42797, .T. ) ;
#52274=CARTESIAN_POINT ( 'NONE',  ( 1.296416391601052487, 43.03271948257037138, -9.512750811966421693 ) ) ;
#52276=CARTESIAN_POINT ( 'NONE',  ( 2.359973842542475886, -39.07714595377191813, -20.27591079927379525 ) ) ;
#52283=PLANE ( 'NONE',  #13617 ) ;
#52289=CARTESIAN_POINT ( 'NONE',  ( 2.299746137290199943, -48.77886755144294284, -4.990332462364070132 ) ) ;
#52291=VERTEX_POINT ( 'NONE', #42742 ) ;
#52298=EDGE_CURVE ( 'NONE', #24004, #41667, #52858, .T. ) ;
#52300=CARTESIAN_POINT ( 'NONE',  ( -6.078457390727109555, 5.483070842476203133, -18.45888526357686388 ) ) ;
#52310=ORIENTED_EDGE ( 'NONE', *, *, #17195, .T. ) ;
#52328=CARTESIAN_POINT ( 'NONE',  ( 0.6000166863083106206, 37.73145429715492583, 31.43502566135684262 ) ) ;
#52330=CARTESIAN_POINT ( 'NONE',  ( 0.1156495703730067715, -22.99010713679044926, -37.66162406309594246 ) ) ;
#52332=ADVANCED_FACE ( 'NONE', ( #23017 ), #9700, .F. ) ;
#52333=DIRECTION ( 'NONE',  ( 0.09722883295013592941, 0.1030875952483757685, 0.9899088350697055061 ) ) ;
#52334=CARTESIAN_POINT ( 'NONE',  ( 0.1140933569871964287, -18.20692391496250906, 40.19275894534575855 ) ) ;
#52336=AXIS2_PLACEMENT_3D ( 'NONE', #43461, #42533, #29031 ) ;
#52345=FACE_OUTER_BOUND ( 'NONE', #45465, .T. ) ;
#52349=CARTESIAN_POINT ( 'NONE',  ( 0.1129192098497447394, -40.71518461128108157, 17.00663193740767909 ) ) ;
#52351=EDGE_CURVE ( 'NONE', #20821, #52454, #58053, .T. ) ;
#52352=CARTESIAN_POINT ( 'NONE',  ( -6.078075953587585900, 9.977648803905792008, 16.46941706901168345 ) ) ;
#52354=EDGE_CURVE ( 'NONE', #22119, #10972, #38761, .T. ) ;
#52361=CARTESIAN_POINT ( 'NONE',  ( 0.1129192098497447394, 39.96249028893947752, 18.70698152272492365 ) ) ;
#52376=EDGE_CURVE ( 'NONE', #61495, #17545, #5082, .T. ) ;
#52391=CARTESIAN_POINT ( 'NONE',  ( -6.063463321072276813, -8.920783457832165197, -17.06575738072992365 ) ) ;
#52393=CARTESIAN_POINT ( 'NONE',  ( 0.2940135542859012574, 9.030615564221935898, -43.18203945186763804 ) ) ;
#52404=CARTESIAN_POINT ( 'NONE',  ( 1.112077966505211180, 34.23546808238941708, 27.76622139053583993 ) ) ;
#52411=( BOUNDED_SURFACE ( )  B_SPLINE_SURFACE ( 3, 1, ( 
 ( #43291, #37987 ),
 ( #56734, #48580 ),
 ( #14166, #15085 ),
 ( #34193, #47354 ) ),
 .UNSPECIFIED., .F., .F., .F. ) 
 B_SPLINE_SURFACE_WITH_KNOTS ( ( 4, 4 ),
 ( 2, 2 ),
 ( 0.000000000000000000, 1.000000000000000000 ),
 ( 0.000000000000000000, 1.000000000000000000 ),
 .UNSPECIFIED. ) 
 GEOMETRIC_REPRESENTATION_ITEM ( )  RATIONAL_B_SPLINE_SURFACE ( (
 ( 1.000000000000000000, 1.000000000000000000),
 ( 0.9754377213608244057, 0.9999580625633939235),
 ( 0.9754377213608244057, 0.9999580625633939235),
 ( 1.000000000000000000, 1.000000000000000000) ) ) 
 REPRESENTATION_ITEM ( '' )  SURFACE ( )  );
#52416=CARTESIAN_POINT ( 'NONE',  ( 4.226256110419178924, -4.630474462406013458, 43.69652109997080203 ) ) ;
#52434=CARTESIAN_POINT ( 'NONE',  ( 0.6008123274975392114, 40.91732262123389319, 27.15377065286363845 ) ) ;
#52436=CARTESIAN_POINT ( 'NONE',  ( 0.1147471544378676905, -35.54663639407677067, -26.14170670672713825 ) ) ;
#52443=CARTESIAN_POINT ( 'NONE',  ( 0.6016117650947688800, 48.13415862694574088, -9.729019864329799816 ) ) ;
#52448=EDGE_LOOP ( 'NONE', ( #48025, #58269, #23075, #20069 ) ) ;
#52454=VERTEX_POINT ( 'NONE', #55192 ) ;
#52455=CARTESIAN_POINT ( 'NONE',  ( 4.335381028904201628, 48.44495715814558423, -7.269317272604295610 ) ) ;
#52466=CARTESIAN_POINT ( 'NONE',  ( -6.077587904424778920, -16.13490349385120481, -10.51003856501195877 ) ) ;
#52469=B_SPLINE_CURVE_WITH_KNOTS ( 'NONE', 3,
 ( #35049, #6177, #30013, #15931, #15626, #35357, #34734, #7107, #49124, #16539, #59123, #21240, #11536, #25314, #49738, #6480, #25937, #25623, #44760, #2102, #1800, #45075, #16863, #54105, #59432 ),
 .UNSPECIFIED., .F., .F.,
 ( 4, 3, 3, 3, 3, 3, 3, 3, 4 ),
 ( 3.469446951953614189E-18, 0.0005656085177311399653, 0.001131215744874499839, 0.001696821861372763748, 0.002262427090022497284, 0.002828031679238744624, 0.003393635864401604429, 0.003977030878808131623, 0.004561030005651159000 ),
 .UNSPECIFIED. ) ;
#52471=CONICAL_SURFACE ( 'NONE', #44515, 43.92652462719577500, 1.486293639869522343 ) ;
#52472=CARTESIAN_POINT ( 'NONE',  ( 2.299746137290198611, -34.31472549160143615, 35.02543293268731617 ) ) ;
#52476=CARTESIAN_POINT ( 'NONE',  ( 1.834102595619085507, 44.02141804901769007, 1.520689912935467847 ) ) ;
#52477=EDGE_LOOP ( 'NONE', ( #28598, #58504, #6321, #7495 ) ) ;
#52481=CARTESIAN_POINT ( 'NONE',  ( 0.3676999524040323597, -6.224421213753346116, -43.67158302462387098 ) ) ;
#52483=VERTEX_POINT ( 'NONE', #8199 ) ;
#52490=CARTESIAN_POINT ( 'NONE',  ( 0.6016118706126978299, 5.062064169927822377, -48.84594723335257527 ) ) ;
#52491=ORIENTED_EDGE ( 'NONE', *, *, #22502, .T. ) ;
#52493=CARTESIAN_POINT ( 'NONE',  ( 0.6029443199889047422, -25.45689510285765067, 41.99385828399795884 ) ) ;
#52497=CARTESIAN_POINT ( 'NONE',  ( 0.1158516988532803382, -27.47246454191935428, 34.52833402910977156 ) ) ;
#52503=CIRCLE ( 'NONE', #57491, 43.92652462719577500 ) ;
#52510=CARTESIAN_POINT ( 'NONE',  ( 4.390527457369402420, -15.47389475202081321, 41.11865656647844958 ) ) ;
#52516=LINE ( 'NONE', #9605, #5956 ) ;
#52536=EDGE_CURVE ( 'NONE', #39191, #8264, #41447, .T. ) ;
#52538=CARTESIAN_POINT ( 'NONE',  ( 0.8744876279028306332, -19.05609938969034545, 45.24616145519679122 ) ) ;
#52539=B_SPLINE_CURVE_WITH_KNOTS ( 'NONE', 3,
 ( #55792, #2861, #60184, #46123, #27608, #17295, #3169, #22298, #41427, #3471, #60794, #44139, #5547 ),
 .UNSPECIFIED., .F., .F.,
 ( 4, 3, 3, 3, 4 ),
 ( 0.002715792992282060631, 0.002828031679238745925, 0.003393635864401604862, 0.003977030878808131623, 0.004561030005651158133 ),
 .UNSPECIFIED. ) ;
#52540=LINE ( 'NONE', #44119, #37810 ) ;
#52542=EDGE_CURVE ( 'NONE', #39332, #19355, #37197, .T. ) ;
#52549=CARTESIAN_POINT ( 'NONE',  ( 2.299746137290199943, 43.60338919182262885, -22.42823641467567342 ) ) ;
#52552=DIRECTION ( 'NONE',  ( -1.000000000000000000, -0.000000000000000000, -0.000000000000000000 ) ) ;
#52561=CARTESIAN_POINT ( 'NONE',  ( -6.063463321072276813, 17.84349906452544943, -7.240855861964748286 ) ) ;
#52564=VERTEX_POINT ( 'NONE', #37989 ) ;
#52565=VERTEX_POINT ( 'NONE', #51110 ) ;
#52566=CARTESIAN_POINT ( 'NONE',  ( 0.6029443449137436017, -42.76684749053210055, -24.13578864891102072 ) ) ;
#52571=ORIENTED_EDGE ( 'NONE', *, *, #60880, .F. ) ;
#52578=CARTESIAN_POINT ( 'NONE',  ( 0.5997462898726536595, -49.10477184366966696, -0.5225058138009923692 ) ) ;
#52582=CARTESIAN_POINT ( 'NONE',  ( -6.057079549204054558, -17.35362438320621337, -8.347631512370986329 ) ) ;
#52585=ORIENTED_EDGE ( 'NONE', *, *, #19800, .T. ) ;
#52587=CARTESIAN_POINT ( 'NONE',  ( 4.060580049360325461, 42.63592134878009432, -10.66048334269353859 ) ) ;
#52588=CARTESIAN_POINT ( 'NONE',  ( -6.078726893082806448, -16.13637198556892827, -10.50768958487384808 ) ) ;
#52590=CARTESIAN_POINT ( 'NONE',  ( 0.5987334363312686314, 37.78232946234383860, -31.36970651553788159 ) ) ;
#52595=DIRECTION ( 'NONE',  ( 0.09722883295013592941, 0.9783250423059141054, 0.1828296082156442293 ) ) ;
#52596=CARTESIAN_POINT ( 'NONE',  ( 0.8753041380234471980, 27.35839019124358984, 40.77568900725831469 ) ) ;
#52603=EDGE_CURVE ( 'NONE', #450, #10386, #39467, .T. ) ;
#52607=FACE_OUTER_BOUND ( 'NONE', #55385, .T. ) ;
#52608=CARTESIAN_POINT ( 'NONE',  ( 0.3676999524040366896, 40.09552319080398775, 18.39292264373822405 ) ) ;
#52611=ADVANCED_FACE ( 'NONE', ( #42368 ), #9924, .F. ) ;
#52620=EDGE_LOOP ( 'NONE', ( #30379, #36834, #39800, #15903 ) ) ;
#52622=CARTESIAN_POINT ( 'NONE',  ( 0.5980271706414734822, 16.30306832862545008, -46.32773689609533818 ) ) ;
#52623=VERTEX_POINT ( 'NONE', #8827 ) ;
#52624=DIRECTION ( 'NONE',  ( -1.000000000000000000, -0.000000000000000000, -0.000000000000000000 ) ) ;
#52633=B_SPLINE_CURVE_WITH_KNOTS ( 'NONE', 3,
 ( #13088, #17777, #50052, #22166, #7736, #32184 ),
 .UNSPECIFIED., .F., .F.,
 ( 4, 2, 4 ),
 ( 1.734723475976807094E-18, 0.0002447193893791697081, 0.0004894387787583376814 ),
 .UNSPECIFIED. ) ;
#52635=B_SPLINE_CURVE_WITH_KNOTS ( 'NONE', 3,
 ( #48366, #422, #38684, #57426, #23334, #14873 ),
 .UNSPECIFIED., .F., .F.,
 ( 4, 2, 4 ),
 ( 1.553784678811103104E-17, 0.0002293755540694292585, 0.0004587511081388430129 ),
 .UNSPECIFIED. ) ;
#52636=ORIENTED_EDGE ( 'NONE', *, *, #22281, .T. ) ;
#52639=CARTESIAN_POINT ( 'NONE',  ( -6.077587904424778920, 15.43577113102525189, 11.51229738082446552 ) ) ;
#52641=CARTESIAN_POINT ( 'NONE',  ( -2.739355103387248747, 1.694972997839557793, 14.83154184458284419 ) ) ;
#52642=CARTESIAN_POINT ( 'NONE',  ( 0.1147471544378675934, -17.57640881104399355, 40.47248499635647789 ) ) ;
#52650=CARTESIAN_POINT ( 'NONE',  ( 0.1157991065609915854, 25.31090088263283278, -36.14278160362363934 ) ) ;
#52663=CARTESIAN_POINT ( 'NONE',  ( 2.706805983486679779, -8.653164499869760107, -43.14972604151675029 ) ) ;
#52679=ORIENTED_EDGE ( 'NONE', *, *, #61298, .T. ) ;
#52681=CARTESIAN_POINT ( 'NONE',  ( 0.1129192098497455998, -44.12161472487017733, -0.4846667466135657909 ) ) ;
#52685=EDGE_LOOP ( 'NONE', ( #21203, #9268, #15438, #55617 ) ) ;
#52688=ADVANCED_FACE ( 'NONE', ( #9751 ), #7389, .F. ) ;
#52693=ORIENTED_EDGE ( 'NONE', *, *, #58400, .T. ) ;
#52715=CARTESIAN_POINT ( 'NONE',  ( 0.6026112563231247332, 46.55052957697731131, 15.63934752498222913 ) ) ;
#52721=DIRECTION ( 'NONE',  ( 0.000000000000000000, 0.000000000000000000, -1.000000000000000000 ) ) ;
#52725=CARTESIAN_POINT ( 'NONE',  ( 0.6016118706126978299, -35.03315395170277924, -34.41263109644804530 ) ) ;
#52726=ORIENTED_EDGE ( 'NONE', *, *, #11036, .T. ) ;
#52738=CARTESIAN_POINT ( 'NONE',  ( 0.6039202388192953519, 22.86846745447336460, 43.45799016444136953 ) ) ;
#52739=VECTOR ( 'NONE', #59288, 1000.000000000000114 ) ;
#52740=EDGE_CURVE ( 'NONE', #16844, #34863, #3531, .T. ) ;
#52744=ORIENTED_EDGE ( 'NONE', *, *, #21194, .T. ) ;
#52746=EDGE_CURVE ( 'NONE', #21737, #4022, #26747, .T. ) ;
#52752=CARTESIAN_POINT ( 'NONE',  ( 0.6008122571543323964, 32.69143329158589495, -36.64457312900650976 ) ) ;
#52755=CARTESIAN_POINT ( 'NONE',  ( 0.3676999524040323597, -18.60775935196367925, 39.99627326667132365 ) ) ;
#52757=CARTESIAN_POINT ( 'NONE',  ( 0.6016117650947691020, -30.34493361141474566, 38.61005126082236671 ) ) ;
#52761=CARTESIAN_POINT ( 'NONE',  ( -2.739355103387248747, -2.641750642665895210, -14.69247155835230068 ) ) ;
#52762=VERTEX_POINT ( 'NONE', #1884 ) ;
#52763=ORIENTED_EDGE ( 'NONE', *, *, #59672, .T. ) ;
#52777=CARTESIAN_POINT ( 'NONE',  ( 0.1129192098497447394, -44.12161472487018443, 0.4846667466135898827 ) ) ;
#52783=CARTESIAN_POINT ( 'NONE',  ( 3.678748215320120973, -33.87011174114093137, 35.37553314004060212 ) ) ;
#52787=CARTESIAN_POINT ( 'NONE',  ( 5.901764892641288895, -48.07448765165364080, -9.318535532511509345 ) ) ;
#52789=ORIENTED_EDGE ( 'NONE', *, *, #33643, .T. ) ;
#52790=CARTESIAN_POINT ( 'NONE',  ( 0.1135584504625008623, 42.01051332454492382, -13.49328804789572978 ) ) ;
#52793=CARTESIAN_POINT ( 'NONE',  ( 0.1157506346131639274, -40.93413843134928243, -16.47230920927504627 ) ) ;
#52795=ORIENTED_EDGE ( 'NONE', *, *, #13420, .F. ) ;
#52797=CARTESIAN_POINT ( 'NONE',  ( 3.678748215320120529, 48.72168477532871833, -4.980988551782284723 ) ) ;
#52802=CARTESIAN_POINT ( 'NONE',  ( 0.5997462898726536595, 5.235280152387709940, -48.82769165002913070 ) ) ;
#52806=B_SPLINE_CURVE_WITH_KNOTS ( 'NONE', 3,
 ( #29860, #48976, #15466, #19558 ),
 .UNSPECIFIED., .F., .F.,
 ( 4, 4 ),
 ( 0.000000000000000000, 0.005013413432710148512 ),
 .UNSPECIFIED. ) ;
#52823=VECTOR ( 'NONE', #52906, 1000.000000000000114 ) ;
#52824=CARTESIAN_POINT ( 'NONE',  ( -6.078726893082806448, 5.475592473157615991, -18.46109228449443052 ) ) ;
#52825=EDGE_CURVE ( 'NONE', #17365, #15298, #22199, .T. ) ;
#52827=ORIENTED_EDGE ( 'NONE', *, *, #27029, .T. ) ;
#52831=CARTESIAN_POINT ( 'NONE',  ( -6.072942160501519915, -14.67202460315899515, -12.47140153845257871 ) ) ;
#52833=CARTESIAN_POINT ( 'NONE',  ( 4.335381028904201628, -11.88755795484448363, -47.52307664213838478 ) ) ;
#52836=B_SPLINE_CURVE_WITH_KNOTS ( 'NONE', 3,
 ( #48632, #30757, #20444, #21062 ),
 .UNSPECIFIED., .F., .F.,
 ( 4, 4 ),
 ( 2.100108283942812283E-17, 0.004559932413162185068 ),
 .UNSPECIFIED. ) ;
#52843=ORIENTED_EDGE ( 'NONE', *, *, #32032, .F. ) ;
#52850=CARTESIAN_POINT ( 'NONE',  ( 0.7948878604505680290, -35.86813329665885419, -33.52872889197455208 ) ) ;
#52855=AXIS2_PLACEMENT_3D ( 'NONE', #21091, #44010, #59600 ) ;
#52857=ORIENTED_EDGE ( 'NONE', *, *, #30179, .T. ) ;
#52858=B_SPLINE_CURVE_WITH_KNOTS ( 'NONE', 3,
 ( #13012, #61202, #4785, #46513, #46833, #33038 ),
 .UNSPECIFIED., .F., .F.,
 ( 4, 2, 4 ),
 ( 3.035766082959412415E-18, 0.0002447193893791692202, 0.0004894387787583354046 ),
 .UNSPECIFIED. ) ;
#52863=CARTESIAN_POINT ( 'NONE',  ( 3.678834586032787346, -46.87103877373264993, -14.20274951900528748 ) ) ;
#52867=FACE_OUTER_BOUND ( 'NONE', #54041, .T. ) ;
#52872=CARTESIAN_POINT ( 'NONE',  ( -6.079354080745853928, -1.847856142170251736, -19.16711723045502325 ) ) ;
#52889=CARTESIAN_POINT ( 'NONE',  ( 0.1152339509894530906, -38.33609478102006562, 21.84688827718698079 ) ) ;
#52893=CARTESIAN_POINT ( 'NONE',  ( 0.5980271706414734822, 32.49685829779753021, -36.82395203688124496 ) ) ;
#52902=CARTESIAN_POINT ( 'NONE',  ( 3.559346040607745287, 42.72017740054766932, -10.41233520434895610 ) ) ;
#52905=CARTESIAN_POINT ( 'NONE',  ( 0.7242486021783834937, 37.91429605804456315, -31.20124383413132563 ) ) ;
#52906=DIRECTION ( 'NONE',  ( -0.9990097760809876215, 5.448601141171670962E-18, -0.04449120468828399177 ) ) ;
#52908=ORIENTED_EDGE ( 'NONE', *, *, #26889, .T. ) ;
#52915=EDGE_CURVE ( 'NONE', #60938, #48571, #31176, .T. ) ;
#52916=CARTESIAN_POINT ( 'NONE',  ( 0.8753041380234471980, -19.05925361776887073, -45.25354328012939931 ) ) ;
#52922=CARTESIAN_POINT ( 'NONE',  ( 0.6024113833632039894, -47.44569806650977739, -12.66679138860581055 ) ) ;
#52923=CARTESIAN_POINT ( 'NONE',  ( 1.296416391601052709, 40.17668401393044775, 18.11467459605454522 ) ) ;
#52925=ORIENTED_EDGE ( 'NONE', *, *, #11259, .F. ) ;
#52927=CARTESIAN_POINT ( 'NONE',  ( 0.1129192098497455998, 36.71339784380029414, 24.47607416535571545 ) ) ;
#52928=B_SPLINE_CURVE_WITH_KNOTS ( 'NONE', 3,
 ( #26103, #54582, #21714, #45541 ),
 .UNSPECIFIED., .F., .F.,
 ( 4, 4 ),
 ( 0.000000000000000000, 0.004442905043737217438 ),
 .UNSPECIFIED. ) ;
#52939=CARTESIAN_POINT ( 'NONE',  ( 0.1158816050234199035, 29.66051085023697453, -32.66796806365733374 ) ) ;
#52941=ORIENTED_EDGE ( 'NONE', *, *, #48039, .T. ) ;
#52946=DIRECTION ( 'NONE',  ( 0.000000000000000000, 0.000000000000000000, -1.000000000000000000 ) ) ;
#52947=ORIENTED_EDGE ( 'NONE', *, *, #18369, .T. ) ;
#52950=CARTESIAN_POINT ( 'NONE',  ( 0.5997462898726536595, 27.66511329191646951, -40.57330571557777432 ) ) ;
#52957=( BOUNDED_SURFACE ( )  B_SPLINE_SURFACE ( 3, 1, ( 
 ( #24104, #23182 ),
 ( #53912, #38233 ),
 ( #42311, #13485 ),
 ( #19417, #28799 ) ),
 .UNSPECIFIED., .F., .F., .F. ) 
 B_SPLINE_SURFACE_WITH_KNOTS ( ( 4, 4 ),
 ( 2, 2 ),
 ( 0.000000000000000000, 1.000000000000000000 ),
 ( 0.000000000000000000, 1.000000000000000000 ),
 .UNSPECIFIED. ) 
 GEOMETRIC_REPRESENTATION_ITEM ( )  RATIONAL_B_SPLINE_SURFACE ( (
 ( 1.000000000000000000, 1.000000000000000000),
 ( 0.9754377213608244057, 0.9999580625633939235),
 ( 0.9754377213608244057, 0.9999580625633939235),
 ( 1.000000000000000000, 1.000000000000000000) ) ) 
 REPRESENTATION_ITEM ( '' )  SURFACE ( )  );
#52961=CARTESIAN_POINT ( 'NONE',  ( 0.1147471544378676905, 25.49827294024393609, 36.01097423755804527 ) ) ;
#52962=VERTEX_POINT ( 'NONE', #1108 ) ;
#52964=CARTESIAN_POINT ( 'NONE',  ( 0.1149546198390367230, 25.46835312172088450, -36.03206286476739706 ) ) ;
#52973=CARTESIAN_POINT ( 'NONE',  ( 3.598898625538307083, 0.2887647096731989493, -48.97398349821926189 ) ) ;
#52975=CARTESIAN_POINT ( 'NONE',  ( -6.079354080745853928, 15.43270669589052524, 11.51627193525655279 ) ) ;
#52976=CARTESIAN_POINT ( 'NONE',  ( 3.559346040607745287, -9.037736435379585487, -43.03196023499975098 ) ) ;
#52977=CARTESIAN_POINT ( 'NONE',  ( 0.1129192098497455998, -41.07894348801367812, 16.10814047907867064 ) ) ;
#52983=CARTESIAN_POINT ( 'NONE',  ( 0.1156495703730067576, -43.77914071683246533, -5.507248979922001020 ) ) ;
#52988=CARTESIAN_POINT ( 'NONE',  ( -2.739355103387247858, 11.19469682329918925, 9.875542009704176394 ) ) ;
#52989=CARTESIAN_POINT ( 'NONE',  ( -6.079354080745853928, 19.09804277166047370, -2.461243088357813136 ) ) ;
#52990=VERTEX_POINT ( 'NONE', #11153 ) ;
#52992=CARTESIAN_POINT ( 'NONE',  ( 0.3676999524040366896, 19.66859742988788184, -39.48540057367844724 ) ) ;
#52994=VERTEX_POINT ( 'NONE', #10223 ) ;
#52995=CARTESIAN_POINT ( 'NONE',  ( 0.5997462898726536595, -14.47257175146309649, 46.92649887902422279 ) ) ;
#52996=CARTESIAN_POINT ( 'NONE',  ( 2.009741617377216460, 26.30790974367969426, 35.31852152258708344 ) ) ;
#52998=VERTEX_POINT ( 'NONE', #43768 ) ;
#53000=ORIENTED_EDGE ( 'NONE', *, *, #29785, .T. ) ;
#53004=ADVANCED_FACE ( 'NONE', ( #16161 ), #22722, .F. ) ;
#53006=ORIENTED_EDGE ( 'NONE', *, *, #24698, .F. ) ;
#53007=CARTESIAN_POINT ( 'NONE',  ( -6.077587904424778920, -12.94128980615197477, 14.25899854643086329 ) ) ;
#53021=VERTEX_POINT ( 'NONE', #5794 ) ;
#53027=CARTESIAN_POINT ( 'NONE',  ( 0.6039202388192953519, -20.03711874569759743, -44.83388880322344505 ) ) ;
#53033=CARTESIAN_POINT ( 'NONE',  ( 0.5997462898726536595, 33.39998138387845472, 35.99990102348730403 ) ) ;
#53036=EDGE_CURVE ( 'NONE', #18280, #45974, #46077, .T. ) ;
#53045=EDGE_CURVE ( 'NONE', #27320, #23759, #14663, .T. ) ;
#53055=CARTESIAN_POINT ( 'NONE',  ( 0.8753041380234524160, -43.21430456406316978, -23.31656511833100964 ) ) ;
#53058=DIRECTION ( 'NONE',  ( 0.09722883295013594329, -0.8708738917981048155, 0.4817937511296480624 ) ) ;
#53071=CARTESIAN_POINT ( 'NONE',  ( 2.706805983486679779, 43.78123907016031779, -4.469811942489746670 ) ) ;
#53074=CARTESIAN_POINT ( 'NONE',  ( -6.078457390727109555, 0.6128065477896523783, 19.24627182527810731 ) ) ;
#53095=ORIENTED_EDGE ( 'NONE', *, *, #16481, .F. ) ;
#53096=CARTESIAN_POINT ( 'NONE',  ( 0.1129192098497447394, 41.72114954716796120, -14.36305915353690743 ) ) ;
#53097=CARTESIAN_POINT ( 'NONE',  ( 0.5997462898726536595, -34.91088276334750873, 34.53667463477217581 ) ) ;
#53098=CARTESIAN_POINT ( 'NONE',  ( 0.8744876279028306332, -39.87136468799875644, -28.64654129726831044 ) ) ;
#53099=CARTESIAN_POINT ( 'NONE',  ( 4.975610109902397937, 0.000000000000000000, 0.000000000000000000 ) ) ;
#53118=CARTESIAN_POINT ( 'NONE',  ( 0.1158816050234198758, 33.59448550014165136, -28.60686255579127035 ) ) ;
#53119=CARTESIAN_POINT ( 'NONE',  ( 0.8753041380234465318, 21.91949880997691835, 43.93943445007457171 ) ) ;
#53128=CARTESIAN_POINT ( 'NONE',  ( 0.5997462898726536595, 23.17609050332868037, 43.29457771044576475 ) ) ;
#53132=CARTESIAN_POINT ( 'NONE',  ( 0.6027444965799114707, -19.99722852491714775, 44.85141432786352311 ) ) ;
#53152=ORIENTED_EDGE ( 'NONE', *, *, #55793, .T. ) ;
#53154=B_SPLINE_CURVE_WITH_KNOTS ( 'NONE', 3,
 ( #16550, #59442, #57650, #29477 ),
 .UNSPECIFIED., .F., .F.,
 ( 4, 4 ),
 ( 0.000000000000000000, 0.004444103432399266161 ),
 .UNSPECIFIED. ) ;
#53158=EDGE_CURVE ( 'NONE', #47174, #19080, #56454, .T. ) ;
#53165=DIRECTION ( 'NONE',  ( 1.000000000000000000, 0.000000000000000000, 0.000000000000000000 ) ) ;
#53178=B_SPLINE_CURVE_WITH_KNOTS ( 'NONE', 3,
 ( #8469, #27599, #56699, #9099 ),
 .UNSPECIFIED., .F., .F.,
 ( 4, 4 ),
 ( 0.000000000000000000, 0.004442905043737214836 ),
 .UNSPECIFIED. ) ;
#53179=ORIENTED_EDGE ( 'NONE', *, *, #19339, .F. ) ;
#53181=EDGE_CURVE ( 'NONE', #52962, #47950, #37083, .T. ) ;
#53183=VERTEX_POINT ( 'NONE', #42753 ) ;
#53184=ORIENTED_EDGE ( 'NONE', *, *, #50087, .T. ) ;
#53186=CARTESIAN_POINT ( 'NONE',  ( 0.6027444965799114707, -30.51574894146176220, -38.47502543766692895 ) ) ;
#53189=CARTESIAN_POINT ( 'NONE',  ( 0.1158516988532803660, 43.31986377834537905, 8.386391420533449548 ) ) ;
#53191=CARTESIAN_POINT ( 'NONE',  ( 0.1158516988532803799, -38.42203224407807483, 21.69538192952180822 ) ) ;
#53193=VECTOR ( 'NONE', #983, 1000.000000000000000 ) ;
#53200=CARTESIAN_POINT ( 'NONE',  ( 0.3676999524040366896, -42.45338881270437525, 11.98584004733023534 ) ) ;
#53206=CARTESIAN_POINT ( 'NONE',  ( 4.553261556744875094, 42.54662847375985280, -10.92355122382294752 ) ) ;
#53207=CARTESIAN_POINT ( 'NONE',  ( 0.1365634738349420230, -32.13563235107024951, 30.23514102861263098 ) ) ;
#53212=CARTESIAN_POINT ( 'NONE',  ( 0.1149546198390368201, 20.65158036586270995, -38.99306083671213230 ) ) ;
#53214=CARTESIAN_POINT ( 'NONE',  ( 0.7242486021783854921, -47.69731273660525517, 11.66095279470975399 ) ) ;
#53216=B_SPLINE_CURVE_WITH_KNOTS ( 'NONE', 3,
 ( #57360, #24177, #9773, #28878, #40709, #41320 ),
 .UNSPECIFIED., .F., .F.,
 ( 4, 2, 4 ),
 ( 0.000000000000000000, 0.0002447195606305753966, 0.0004894391212611507933 ),
 .UNSPECIFIED. ) ;
#53223=CARTESIAN_POINT ( 'NONE',  ( -6.057079549204054558, -12.94019084496072125, -14.26123038155309786 ) ) ;
#53231=CARTESIAN_POINT ( 'NONE',  ( 0.8753041380234524160, 17.79089796329306239, 45.76704357430872960 ) ) ;
#53232=CIRCLE ( 'NONE', #26231, 48.91267123290010943 ) ;
#53233=ORIENTED_EDGE ( 'NONE', *, *, #38380, .T. ) ;
#53236=CARTESIAN_POINT ( 'NONE',  ( 0.3676999524040323597, 9.009680404095913531, 43.18305503711946614 ) ) ;
#53238=EDGE_CURVE ( 'NONE', #44212, #50189, #52806, .T. ) ;
#53243=VERTEX_POINT ( 'NONE', #20469 ) ;
#53255=CARTESIAN_POINT ( 'NONE',  ( 3.221118495291109163, -36.34809063562757103, -24.77050114159895244 ) ) ;
#53262=CARTESIAN_POINT ( 'NONE',  ( -6.078075953587585900, -1.843738688193722997, 19.16757162232069689 ) ) ;
#53265=ORIENTED_EDGE ( 'NONE', *, *, #57338, .F. ) ;
#53266=CARTESIAN_POINT ( 'NONE',  ( 4.553261556744873317, 6.787618719204111528, -43.39893775135914922 ) ) ;
#53270=CARTESIAN_POINT ( 'NONE',  ( -6.078726893082806448, -12.94330610022628214, -14.25709887966570832 ) ) ;
#53271=CARTESIAN_POINT ( 'NONE',  ( 4.975610109902397937, 0.000000000000000000, 0.000000000000000000 ) ) ;
#53277=CONICAL_SURFACE ( 'NONE', #56271, 43.92652462719577500, 1.486293639869522343 ) ;
#53281=EDGE_CURVE ( 'NONE', #4853, #11136, #34850, .T. ) ;
#53286=CARTESIAN_POINT ( 'NONE',  ( 0.1149546198390366536, 39.63494256384228720, 19.39118080427653013 ) ) ;
#53291=CARTESIAN_POINT ( 'NONE',  ( -6.078457390727109555, 17.85037638348237010, 7.222089310270451534 ) ) ;
#53292=CARTESIAN_POINT ( 'NONE',  ( 0.6016117650947689910, -45.38673806846551173, 18.75086829320185444 ) ) ;
#53299=CARTESIAN_POINT ( 'NONE',  ( 3.221118495291109607, 26.69097583632542481, 34.96216853352267862 ) ) ;
#53301=VERTEX_POINT ( 'NONE', #53640 ) ;
#53309=FACE_OUTER_BOUND ( 'NONE', #39832, .T. ) ;
#53315=FACE_OUTER_BOUND ( 'NONE', #41749, .T. ) ;
#53316=( BOUNDED_SURFACE ( )  B_SPLINE_SURFACE ( 3, 1, ( 
 ( #43217, #58498 ),
 ( #48503, #43846 ),
 ( #5567, #52893 ),
 ( #43526, #34736 ) ),
 .UNSPECIFIED., .F., .F., .F. ) 
 B_SPLINE_SURFACE_WITH_KNOTS ( ( 4, 4 ),
 ( 2, 2 ),
 ( 0.000000000000000000, 1.000000000000000000 ),
 ( 0.000000000000000000, 1.000000000000000000 ),
 .UNSPECIFIED. ) 
 GEOMETRIC_REPRESENTATION_ITEM ( )  RATIONAL_B_SPLINE_SURFACE ( (
 ( 1.000000000000000000, 1.000000000000000000),
 ( 0.9953485035131437453, 0.8621029689291515030),
 ( 0.9953485035131437453, 0.8621029689291515030),
 ( 1.000000000000000000, 1.000000000000000000) ) ) 
 REPRESENTATION_ITEM ( '' )  SURFACE ( )  );
#53321=CARTESIAN_POINT ( 'NONE',  ( 0.1119898979215349782, 43.41448053468967316, 7.883158513875082818 ) ) ;
#53327=VECTOR ( 'NONE', #21804, 1000.000000000000114 ) ;
#53328=ORIENTED_EDGE ( 'NONE', *, *, #30877, .F. ) ;
#53329=CARTESIAN_POINT ( 'NONE',  ( 0.1156867017252035112, -1.289351019103671669, -44.10533279802707796 ) ) ;
#53331=B_SPLINE_CURVE_WITH_KNOTS ( 'NONE', 3,
 ( #56813, #19248, #38670, #52117 ),
 .UNSPECIFIED., .F., .F.,
 ( 4, 4 ),
 ( 2.306275401152138554E-17, 0.004559932413162185935 ),
 .UNSPECIFIED. ) ;
#53336=CARTESIAN_POINT ( 'NONE',  ( 0.7242003506640013466, 33.61306414422924149, 35.79348534247477431 ) ) ;
#53344=CARTESIAN_POINT ( 'NONE',  ( 5.901764892641288895, -44.10106349911009715, 21.28585600080809925 ) ) ;
#53357=CARTESIAN_POINT ( 'NONE',  ( -6.063463321072278589, 16.77106408806596960, 9.463184550322056410 ) ) ;
#53361=EDGE_CURVE ( 'NONE', #30048, #61623, #51237, .T. ) ;
#53365=EDGE_CURVE ( 'NONE', #51774, #14204, #61397, .T. ) ;
#53370=VERTEX_POINT ( 'NONE', #8797 ) ;
#53373=CARTESIAN_POINT ( 'NONE',  ( 0.1147471544378676211, 41.97320617314998970, 13.60889973581589274 ) ) ;
#53374=B_SPLINE_CURVE_WITH_KNOTS ( 'NONE', 3,
 ( #11780, #55900, #31171, #7342 ),
 .UNSPECIFIED., .F., .F.,
 ( 4, 4 ),
 ( 3.469446951953614189E-18, 0.005013413432710145043 ),
 .UNSPECIFIED. ) ;
#53380=ORIENTED_EDGE ( 'NONE', *, *, #13780, .T. ) ;
#53384=ADVANCED_FACE ( 'NONE', ( #47036 ), #29480, .F. ) ;
#53387=CARTESIAN_POINT ( 'NONE',  ( 4.975610109902397937, 30.04451009524474969, 38.59762713269442713 ) ) ;
#53390=CARTESIAN_POINT ( 'NONE',  ( 0.6039202388192953519, 41.06127625758664834, -26.93576256479739683 ) ) ;
#53394=ORIENTED_EDGE ( 'NONE', *, *, #58450, .F. ) ;
#53395=CARTESIAN_POINT ( 'NONE',  ( 0.2940133293163013084, 43.44929869380207776, -7.641923357035950382 ) ) ;
#53402=ADVANCED_FACE ( 'NONE', ( #33553 ), #37446, .F. ) ;
#53403=VECTOR ( 'NONE', #18881, 1000.000000000000114 ) ;
#53404=ORIENTED_EDGE ( 'NONE', *, *, #59660, .T. ) ;
#53408=CARTESIAN_POINT ( 'NONE',  ( -2.739355103387247858, -5.801236230415786288, -13.75475282038642177 ) ) ;
#53410=ORIENTED_EDGE ( 'NONE', *, *, #17821, .T. ) ;
#53413=CARTESIAN_POINT ( 'NONE',  ( 4.975610109902397937, 0.000000000000000000, 0.000000000000000000 ) ) ;
#53414=CARTESIAN_POINT ( 'NONE',  ( 0.1155031312995260795, 9.654200663125585891, 43.05505826366879063 ) ) ;
#53420=CARTESIAN_POINT ( 'NONE',  ( -6.063463321072278589, -19.21612852159693929, -1.249342675545178638 ) ) ;
#53421=LINE ( 'NONE', #34048, #57814 ) ;
#53425=VERTEX_POINT ( 'NONE', #13832 ) ;
#53432=CARTESIAN_POINT ( 'NONE',  ( 0.3676999524040323597, -11.75791688508830646, -42.51707861373114383 ) ) ;
#53441=EDGE_CURVE ( 'NONE', #52994, #53665, #19875, .T. ) ;
#53457=LINE ( 'NONE', #4916, #21816 ) ;
#53458=ADVANCED_FACE ( 'NONE', ( #59803 ), #50691, .F. ) ;
#53464=EDGE_LOOP ( 'NONE', ( #6706, #52585 ) ) ;
#53466=EDGE_LOOP ( 'NONE', ( #33310, #2805, #9285, #3192, #38821, #13076, #48255, #55953, #33879, #34092, #11826, #48332, #3146, #55098, #5766, #11585, #17193, #1562, #12692, #9579, #50160, #26728, #25124, #38172, #21836, #35262, #31920, #12903, #46281, #2111, #10138, #32095, #547, #59197, #36591, #45761, #25765, #22737, #17517, #27985, #42593, #55169, #47656, #58842, #46192, #32021, #27766, #14985, #17552, #44115, #47309, #49824, #52726, #28296, #55570, #61694, #38636, #20461, #28509, #24020, #9501, #43523, #32259, #48093, #59568, #48880, #60161, #31706, #2511, #32816, #14343, #20054, #33407, #42968, #1073, #60497, #28988, #29368, #9525, #41483, #15325, #19285, #1559, #26128, #48470, #61304, #49173, #12171, #17314, #40996, #37019, #59700, #91, #38510, #46269, #27937, #48402, #61104, #59118, #13819, #48185, #2698, #35851, #42789, #36580, #46184, #12712, #50698, #35624, #53859, #6012, #25551, #303, #32952, #10439, #22762, #13066, #57104, #43284, #19552, #15941, #13014, #26201, #41049, #39335, #19991, #22908, #22932, #47219, #60157, #30756, #53592, #34732, #41140, #9783, #14708, #4866, #46673, #38877, #6748, #4607, #10538, #23513, #31924, #26280, #51019, #16431, #10736, #33481, #22785 ) ) ;
#53474=ADVANCED_FACE ( 'NONE', ( #35719 ), #46337, .F. ) ;
#53480=ORIENTED_EDGE ( 'NONE', *, *, #43067, .T. ) ;
#53489=CARTESIAN_POINT ( 'NONE',  ( 0.3676999524040323597, -28.14442808720941969, 33.96824621564581292 ) ) ;
#53491=( BOUNDED_SURFACE ( )  B_SPLINE_SURFACE ( 3, 1, ( 
 ( #28714, #13399 ),
 ( #32501, #24017 ),
 ( #9293, #61891 ),
 ( #52824, #14024 ) ),
 .UNSPECIFIED., .F., .F., .F. ) 
 B_SPLINE_SURFACE_WITH_KNOTS ( ( 4, 4 ),
 ( 2, 2 ),
 ( 0.000000000000000000, 1.000000000000000000 ),
 ( 0.000000000000000000, 1.000000000000000000 ),
 .UNSPECIFIED. ) 
 GEOMETRIC_REPRESENTATION_ITEM ( )  RATIONAL_B_SPLINE_SURFACE ( (
 ( 1.000000000000000000, 1.000000000000000000),
 ( 0.9754377213608244057, 0.9999580625633939235),
 ( 0.9754377213608244057, 0.9999580625633939235),
 ( 1.000000000000000000, 1.000000000000000000) ) ) 
 REPRESENTATION_ITEM ( '' )  SURFACE ( )  );
#53494=CARTESIAN_POINT ( 'NONE',  ( 0.2940133293162984773, 24.57542356339362399, 36.63726390245101783 ) ) ;
#53501=EDGE_LOOP ( 'NONE', ( #37279, #27969, #60394, #2996 ) ) ;
#53504=CARTESIAN_POINT ( 'NONE',  ( 0.3676999524040323597, -42.87209381266892194, 10.38913641457044434 ) ) ;
#53506=CARTESIAN_POINT ( 'NONE',  ( -6.078457390727109555, -16.13585499094657649, -10.50850582854918969 ) ) ;
#53507=CARTESIAN_POINT ( 'NONE',  ( 0.8753041380234524160, 11.79227530596866025, 47.66634631457734628 ) ) ;
#53519=CARTESIAN_POINT ( 'NONE',  ( -2.601141883200662974, 11.07005473184238653, -10.01245802505072113 ) ) ;
#53521=B_SPLINE_CURVE_WITH_KNOTS ( 'NONE', 3,
 ( #27106, #23036, #42463, #60914 ),
 .UNSPECIFIED., .F., .F.,
 ( 4, 4 ),
 ( 0.000000000000000000, 0.004442905043737215703 ),
 .UNSPECIFIED. ) ;
#53523=EDGE_CURVE ( 'NONE', #12972, #11409, #17645, .T. ) ;
#53528=CARTESIAN_POINT ( 'NONE',  ( 2.185380717157383135, 40.27445918234111133, 17.79853197983303659 ) ) ;
#53538=ORIENTED_EDGE ( 'NONE', *, *, #2826, .F. ) ;
#53539=CARTESIAN_POINT ( 'NONE',  ( 0.2279481005628808121, 41.62610996520416506, 14.62089108904256385 ) ) ;
#53541=ORIENTED_EDGE ( 'NONE', *, *, #52536, .F. ) ;
#53543=ORIENTED_EDGE ( 'NONE', *, *, #30877, .T. ) ;
#53544=CARTESIAN_POINT ( 'NONE',  ( 0.1156867017252034419, 29.75710594952617072, -32.58001615689993713 ) ) ;
#53547=AXIS2_PLACEMENT_3D ( 'NONE', #41371, #11616, #36664 ) ;
#53548=ADVANCED_FACE ( 'NONE', ( #32548 ), #56621, .F. ) ;
#53549=ORIENTED_EDGE ( 'NONE', *, *, #1761, .T. ) ;
#53551=CARTESIAN_POINT ( 'NONE',  ( 0.6000166863083106206, -45.32251430608278753, 18.91277818522109655 ) ) ;
#53552=ADVANCED_FACE ( 'NONE', ( #23140 ), #61476, .F. ) ;
#53555=CARTESIAN_POINT ( 'NONE',  ( 4.553261556744875094, -33.59363643963393997, 28.30206982864213217 ) ) ;
#53561=ORIENTED_EDGE ( 'NONE', *, *, #656, .T. ) ;
#53563=ORIENTED_EDGE ( 'NONE', *, *, #26289, .F. ) ;
#53565=LINE ( 'NONE', #58571, #26971 ) ;
#53566=ORIENTED_EDGE ( 'NONE', *, *, #53896, .T. ) ;
#53568=DIRECTION ( 'NONE',  ( 0.000000000000000000, 0.000000000000000000, -1.000000000000000000 ) ) ;
#53571=CARTESIAN_POINT ( 'NONE',  ( 0.1158403557922069033, -40.91360538020781235, 16.52323218914656877 ) ) ;
#53576=CARTESIAN_POINT ( 'NONE',  ( 3.727782113643636652, -9.118766182490292138, -43.00727704953018815 ) ) ;
#53592=ORIENTED_EDGE ( 'NONE', *, *, #8402, .T. ) ;
#53603=CARTESIAN_POINT ( 'NONE',  ( 4.834790513006555379, 45.58586227964580928, -12.43054709759575971 ) ) ;
#53610=CARTESIAN_POINT ( 'NONE',  ( 50.15577769773999961, 9.539392014169456147, 3.000000000000000000 ) ) ;
#53611=CARTESIAN_POINT ( 'NONE',  ( 0.5997462898726536595, 41.43917033312134635, -26.35046094941917971 ) ) ;
#53613=CARTESIAN_POINT ( 'NONE',  ( 4.553261556744875094, 0.000000000000000000, 0.000000000000000000 ) ) ;
#53628=ORIENTED_EDGE ( 'NONE', *, *, #20886, .F. ) ;
#53631=FACE_OUTER_BOUND ( 'NONE', #53749, .T. ) ;
#53632=CARTESIAN_POINT ( 'NONE',  ( 0.6026112563231247332, -35.15491935172932614, -34.28808306507691839 ) ) ;
#53634=ORIENTED_EDGE ( 'NONE', *, *, #19903, .T. ) ;
#53638=CARTESIAN_POINT ( 'NONE',  ( -6.078726893082806448, -19.21623043802547315, 1.237145513439503297 ) ) ;
#53640=CARTESIAN_POINT ( 'NONE',  ( 0.3676999524040366896, -18.60775935196311082, -39.99627326667158655 ) ) ;
#53643=DIRECTION ( 'NONE',  ( -0.1011922191286467598, -0.9788975924247133031, 0.1775377096081844075 ) ) ;
#53648=VERTEX_POINT ( 'NONE', #38805 ) ;
#53650=CARTESIAN_POINT ( 'NONE',  ( 0.1152339509894530906, -7.262667307842109565, -43.52236613548078026 ) ) ;
#53652=CARTESIAN_POINT ( 'NONE',  ( -6.078726893082806448, -8.903615017412541022, 17.07394743140630666 ) ) ;
#53656=CARTESIAN_POINT ( 'NONE',  ( 0.6026112563231247332, 33.14369577886151319, -36.23584447784382689 ) ) ;
#53662=CARTESIAN_POINT ( 'NONE',  ( 0.6028777368367060907, 48.18512964921514197, 9.472756198667941163 ) ) ;
#53664=ORIENTED_EDGE ( 'NONE', *, *, #21371, .F. ) ;
#53665=VERTEX_POINT ( 'NONE', #14990 ) ;
#53670=CARTESIAN_POINT ( 'NONE',  ( 0.1152339509894530906, 41.94616134658625128, 13.69168502199042514 ) ) ;
#53682=CARTESIAN_POINT ( 'NONE',  ( 2.706805983486679779, -10.92573265357083301, 42.63102719032760035 ) ) ;
#53685=CARTESIAN_POINT ( 'NONE',  ( 2.299652685299200972, 43.60340470841921956, 22.42821487974374151 ) ) ;
#53686=EDGE_CURVE ( 'NONE', #48274, #19623, #26467, .T. ) ;
#53687=CARTESIAN_POINT ( 'NONE',  ( 0.1156867017252034974, 15.35615507261531043, -41.36582295399159648 ) ) ;
#53688=ORIENTED_EDGE ( 'NONE', *, *, #34496, .T. ) ;
#53694=CARTESIAN_POINT ( 'NONE',  ( 0.6016117650947689910, -7.493478393550796923, 48.53245136823285577 ) ) ;
#53695=CARTESIAN_POINT ( 'NONE',  ( 3.678748215320119197, -40.32774817307750226, -27.79002593716545277 ) ) ;
#53705=CARTESIAN_POINT ( 'NONE',  ( 1.657374760986086049, -28.42509966000220345, -33.65864163288807731 ) ) ;
#53710=VECTOR ( 'NONE', #56111, 1000.000000000000114 ) ;
#53714=CARTESIAN_POINT ( 'NONE',  ( 4.975610109902397937, -33.30777373088901072, 35.81957029655259817 ) ) ;
#53715=CARTESIAN_POINT ( 'NONE',  ( 0.1156867017252034557, 33.67904051480007155, -28.50728042584282917 ) ) ;
#53724=EDGE_CURVE ( 'NONE', #7202, #57990, #38187, .T. ) ;
#53727=B_SPLINE_CURVE_WITH_KNOTS ( 'NONE', 3,
 ( #55018, #2398, #11841, #30919 ),
 .UNSPECIFIED., .F., .F.,
 ( 4, 4 ),
 ( 0.000000000000000000, 0.004442905043737216571 ),
 .UNSPECIFIED. ) ;
#53728=CARTESIAN_POINT ( 'NONE',  ( 0.6252788684277201803, 10.25662847928439803, -48.02338912875260490 ) ) ;
#53736=VECTOR ( 'NONE', #6054, 1000.000000000000114 ) ;
#53739=ORIENTED_EDGE ( 'NONE', *, *, #18558, .T. ) ;
#53741=CARTESIAN_POINT ( 'NONE',  ( 0.7044674535452954967, -47.71057267246434463, 11.64061759858144285 ) ) ;
#53745=CARTESIAN_POINT ( 'NONE',  ( 0.1135584504625008068, -23.24200312127439005, 37.50681728760683598 ) ) ;
#53749=EDGE_LOOP ( 'NONE', ( #51845, #54248, #30593, #1072 ) ) ;
#53757=ORIENTED_EDGE ( 'NONE', *, *, #51002, .T. ) ;
#53759=CARTESIAN_POINT ( 'NONE',  ( 4.553261556744873317, 27.56395660609696563, 34.20186927699770507 ) ) ;
#53762=ORIENTED_EDGE ( 'NONE', *, *, #25894, .T. ) ;
#53767=CARTESIAN_POINT ( 'NONE',  ( 0.6000166863083106206, 46.77044519531211364, 14.97828220927751808 ) ) ;
#53769=CARTESIAN_POINT ( 'NONE',  ( -6.078726893082806448, -1.852420388636412119, -19.16670498475114570 ) ) ;
#53771=B_SPLINE_CURVE_WITH_KNOTS ( 'NONE', 3,
 ( #15838, #5779, #29306, #24614, #1095, #43751 ),
 .UNSPECIFIED., .F., .F.,
 ( 4, 2, 4 ),
 ( 3.469446951953614189E-18, 0.0002447193893791685696, 0.0004894387787583336698 ),
 .UNSPECIFIED. ) ;
#53775=CARTESIAN_POINT ( 'NONE',  ( 3.678834586032786458, -46.05790299361684959, 16.65178493312157570 ) ) ;
#53781=CIRCLE ( 'NONE', #26804, 43.92652462719577500 ) ;
#53783=CARTESIAN_POINT ( 'NONE',  ( 0.3676999524040366896, 36.51379593394493384, -24.75264207750488055 ) ) ;
#53784=CARTESIAN_POINT ( 'NONE',  ( 0.6021448801613057400, -30.41330595987364660, -38.55608848441529091 ) ) ;
#53785=CARTESIAN_POINT ( 'NONE',  ( -6.078075953587585900, 16.78075473395859518, 9.444651650847811553 ) ) ;
#53787=CARTESIAN_POINT ( 'NONE',  ( 2.299652685299201416, -49.01654791059075222, -1.288315096129431403 ) ) ;
#53788=CARTESIAN_POINT ( 'NONE',  ( 0.2940135542859015905, -38.03800455849015805, 22.34615756455018243 ) ) ;
#53791=B_SPLINE_CURVE_WITH_KNOTS ( 'NONE', 3,
 ( #32350, #33515, #52905, #60946, #52590, #8513 ),
 .UNSPECIFIED., .F., .F.,
 ( 4, 2, 4 ),
 ( 1.843143693225357538E-18, 0.0002447193893791656423, 0.0004894387787583359467 ),
 .UNSPECIFIED. ) ;
#53794=CARTESIAN_POINT ( 'NONE',  ( 0.8744876279028306332, -35.88078294188929362, -33.50999053799506555 ) ) ;
#53800=ADVANCED_FACE ( 'NONE', ( #54081 ), #24623, .F. ) ;
#53804=CIRCLE ( 'NONE', #12851, 48.91267123290010943 ) ;
#53809=B_SPLINE_CURVE_WITH_KNOTS ( 'NONE', 3,
 ( #6208, #33848, #43250, #57292, #25045, #5901 ),
 .UNSPECIFIED., .F., .F.,
 ( 4, 2, 4 ),
 ( 1.823721537572523311E-17, 0.0002293755540694312914, 0.0004587511081388443140 ),
 .UNSPECIFIED. ) ;
#53823=CARTESIAN_POINT ( 'NONE',  ( 2.185380717157383135, -19.12931034577501421, -39.65966828860555182 ) ) ;
#53830=CARTESIAN_POINT ( 'NONE',  ( 0.3676999524040366896, 24.55639947021014180, -36.64606156713571750 ) ) ;
#53859=ORIENTED_EDGE ( 'NONE', *, *, #47385, .T. ) ;
#53861=ADVANCED_FACE ( 'NONE', ( #30594 ), #33054, .F. ) ;
#53862=CARTESIAN_POINT ( 'NONE',  ( 1.834102595619085063, -36.06423740592772731, -25.28969207377914685 ) ) ;
#53869=CARTESIAN_POINT ( 'NONE',  ( 4.335381028904201628, -37.95090345676129573, -30.97556737946744221 ) ) ;
#53877=ADVANCED_FACE ( 'NONE', ( #31532 ), #39463, .F. ) ;
#53878=CARTESIAN_POINT ( 'NONE',  ( 0.1139756605157202923, 25.56931991171277119, 35.96060481898923911 ) ) ;
#53883=CARTESIAN_POINT ( 'NONE',  ( 0.5987334363312694085, 49.04182530238752236, -2.542100997635586168 ) ) ;
#53886=CARTESIAN_POINT ( 'NONE',  ( 0.1157506346131639274, -40.86450982400815235, 16.64429321558520058 ) ) ;
#53889=CARTESIAN_POINT ( 'NONE',  ( 1.479689385636123067, -8.190458794601717329, -43.29549895776260371 ) ) ;
#53894=CARTESIAN_POINT ( 'NONE',  ( 4.975610109902397937, -10.32228546579766260, 47.81108480154320972 ) ) ;
#53896=EDGE_CURVE ( 'NONE', #43185, #9433, #16503, .T. ) ;
#53898=CARTESIAN_POINT ( 'NONE',  ( 4.975610109902397937, -10.32228546579766260, 47.81108480154320972 ) ) ;
#53900=EDGE_CURVE ( 'NONE', #22617, #22007, #46723, .T. ) ;
#53902=CARTESIAN_POINT ( 'NONE',  ( -6.078726893082806448, 17.85000270430350611, 7.222980321520863001 ) ) ;
#53903=CARTESIAN_POINT ( 'NONE',  ( 0.6016118706126976079, -45.64818144247053766, 18.10509833663487811 ) ) ;
#53906=CARTESIAN_POINT ( 'NONE',  ( 0.2279481005628803125, -44.11266182516073542, -0.7593113800818089842 ) ) ;
#53907=CARTESIAN_POINT ( 'NONE',  ( 0.9268187852002115479, 19.50810647315381274, -39.53717383350407744 ) ) ;
#53911=CARTESIAN_POINT ( 'NONE',  ( 0.1157991065609916131, 4.155894141114022666, 43.92801963924112130 ) ) ;
#53912=CARTESIAN_POINT ( 'NONE',  ( -6.079354080745853928, 3.074405391879413862, -19.00897121715283689 ) ) ;
#53914=ORIENTED_EDGE ( 'NONE', *, *, #24745, .T. ) ;
#53915=CARTESIAN_POINT ( 'NONE',  ( -6.078726893082806448, -8.909671472910916989, 17.07078778245215034 ) ) ;
#53921=CARTESIAN_POINT ( 'NONE',  ( 0.6000166863083106206, -48.77118664543507975, -5.761495891223789023 ) ) ;
#53922=ORIENTED_EDGE ( 'NONE', *, *, #5624, .T. ) ;
#53925=ORIENTED_EDGE ( 'NONE', *, *, #31397, .F. ) ;
#53934=VECTOR ( 'NONE', #47563, 1000.000000000000114 ) ;
#53940=CARTESIAN_POINT ( 'NONE',  ( 0.1156495703730067298, -1.550490393351041218, -44.09692656831308710 ) ) ;
#53941=CARTESIAN_POINT ( 'NONE',  ( -6.078726893082806448, 17.84743921491362073, -7.229312189875575889 ) ) ;
#53944=EDGE_CURVE ( 'NONE', #31779, #45251, #4849, .T. ) ;
#53949=CARTESIAN_POINT ( 'NONE',  ( 2.009741617377216460, 8.458693230811739738, -43.21984019463820914 ) ) ;
#53956=CARTESIAN_POINT ( 'NONE',  ( 0.8744876279028306332, -49.08725279547490317, 0.8897546699139438076 ) ) ;
#53957=CARTESIAN_POINT ( 'NONE',  ( 0.1368894036331277653, 15.83533010450942768, 41.18377892331582046 ) ) ;
#53958=CARTESIAN_POINT ( 'NONE',  ( 0.1158403557922069033, -31.72288257580944304, 30.66918695148641660 ) ) ;
#53961=CARTESIAN_POINT ( 'NONE',  ( 2.185380717157383135, -13.90069315816946904, -41.78026487218121332 ) ) ;
#53964=B_SPLINE_CURVE_WITH_KNOTS ( 'NONE', 3,
 ( #16520, #21838, #16215, #2710, #40975, #7088, #55326, #40354, #26530, #50034, #30297, #44741, #22146, #35336, #60039, #31539, #1781, #35958, #25920 ),
 .UNSPECIFIED., .F., .F.,
 ( 4, 3, 3, 3, 3, 3, 4 ),
 ( 3.469552829456483146E-18, 0.0002612768053151684564, 0.0003919133833142928770, 0.0005225499612322577177, 0.0006531865391693348743, 0.0008112755173415179058, 0.0009693688056799707299 ),
 .UNSPECIFIED. ) ;
#53969=DIRECTION ( 'NONE',  ( 0.000000000000000000, 0.000000000000000000, -1.000000000000000000 ) ) ;
#53975=CARTESIAN_POINT ( 'NONE',  ( 0.6021448801613057400, -30.82180960111880808, 38.23031770126069517 ) ) ;
#53977=CARTESIAN_POINT ( 'NONE',  ( 4.975610109902397937, -43.81605102859474954, 21.73943604138237973 ) ) ;
#53982=CARTESIAN_POINT ( 'NONE',  ( 3.727782113643637096, 43.68415680130915035, -4.946940515572275210 ) ) ;
#53990=ORIENTED_EDGE ( 'NONE', *, *, #14308, .T. ) ;
#53992=CARTESIAN_POINT ( 'NONE',  ( 4.335381028904201628, 47.63237751920336649, 11.44174197980512631 ) ) ;
#53996=CARTESIAN_POINT ( 'NONE',  ( 2.879087469061463178, -10.84989772776556016, 42.64248346520645327 ) ) ;
#53997=CARTESIAN_POINT ( 'NONE',  ( 0.1129192098497447394, 4.719118110134695954, 43.87119455916095490 ) ) ;
#53999=EDGE_CURVE ( 'NONE', #15275, #7236, #16885, .T. ) ;
#54000=CARTESIAN_POINT ( 'NONE',  ( 0.1139756605157204311, 14.86525642157594440, -41.54490788551370173 ) ) ;
#54005=CARTESIAN_POINT ( 'NONE',  ( -6.078457390727109555, 7.798524762019481749, -17.60617853407368116 ) ) ;
#54009=CARTESIAN_POINT ( 'NONE',  ( 0.5997462898726536595, -7.321308210775749004, 48.55872811583040516 ) ) ;
#54012=CARTESIAN_POINT ( 'NONE',  ( 0.1147471544378675934, -41.01504251968592030, -16.27017134456798786 ) ) ;
#54015=CARTESIAN_POINT ( 'NONE',  ( 0.6008123274975391004, -35.57792977512935551, 33.84915750907875065 ) ) ;
#54017=CARTESIAN_POINT ( 'NONE',  ( -2.739355103387248747, 3.577672767447565683, 14.49302675496326565 ) ) ;
#54019=CARTESIAN_POINT ( 'NONE',  ( 1.830465331921978800, -26.48837546677528110, -35.19576708937492526 ) ) ;
#54032=CARTESIAN_POINT ( 'NONE',  ( 4.060580049360325461, 22.35095848363190285, 37.84048558385809002 ) ) ;
#54039=CARTESIAN_POINT ( 'NONE',  ( 1.830465331921978134, 16.36602852630565863, -40.89656667930132272 ) ) ;
#54041=EDGE_LOOP ( 'NONE', ( #12973, #46113, #25362, #61098 ) ) ;
#54044=CARTESIAN_POINT ( 'NONE',  ( 0.6000166863083106206, 37.73145429715533794, -31.43502566135633458 ) ) ;
#54045=CARTESIAN_POINT ( 'NONE',  ( 0.7948878604505663636, 48.93475821598755005, -4.010995592275964583 ) ) ;
#54046=CARTESIAN_POINT ( 'NONE',  ( 0.1158403557922069033, 44.03589856812533299, -2.789255184022604972 ) ) ;
#54051=( BOUNDED_SURFACE ( )  B_SPLINE_SURFACE ( 3, 1, ( 
 ( #60278, #36205 ),
 ( #59666, #7035 ),
 ( #2968, #17094 ),
 ( #12096, #17391 ) ),
 .UNSPECIFIED., .F., .F., .F. ) 
 B_SPLINE_SURFACE_WITH_KNOTS ( ( 4, 4 ),
 ( 2, 2 ),
 ( 0.000000000000000000, 1.000000000000000000 ),
 ( 0.000000000000000000, 1.000000000000000000 ),
 .UNSPECIFIED. ) 
 GEOMETRIC_REPRESENTATION_ITEM ( )  RATIONAL_B_SPLINE_SURFACE ( (
 ( 1.000000000000000000, 1.000000000000000000),
 ( 0.7211978278499968642, 0.9934217856018975334),
 ( 0.7211978278499968642, 0.9934217856018975334),
 ( 1.000000000000000000, 1.000000000000000000) ) ) 
 REPRESENTATION_ITEM ( '' )  SURFACE ( )  );
#54061=DIRECTION ( 'NONE',  ( 1.000000000000000000, 0.000000000000000000, 0.000000000000000000 ) ) ;
#54064=B_SPLINE_CURVE_WITH_KNOTS ( 'NONE', 3,
 ( #61574, #23083, #3328, #41583, #9275, #22459, #4552, #13381, #17764, #61876, #18694, #42213, #22766, #32801, #37829, #23386, #46908, #60967, #8975, #56880, #37195, #8651, #28084, #32481, #33110 ),
 .UNSPECIFIED., .F., .F.,
 ( 4, 3, 3, 3, 3, 3, 3, 3, 4 ),
 ( 5.057544569639794935E-18, 0.0005656085177311397484, 0.001131215744874499406, 0.001696821861372765699, 0.002262427090022498151, 0.002828031679238745492, 0.003393635864401604862, 0.003977030878808131623, 0.004561030005651158133 ),
 .UNSPECIFIED. ) ;
#54066=VERTEX_POINT ( 'NONE', #44356 ) ;
#54069=CARTESIAN_POINT ( 'NONE',  ( 3.240649175237397372, -34.13167035129225013, -27.75417079338471282 ) ) ;
#54073=ORIENTED_EDGE ( 'NONE', *, *, #51454, .F. ) ;
#54081=FACE_OUTER_BOUND ( 'NONE', #24603, .T. ) ;
#54082=CARTESIAN_POINT ( 'NONE',  ( 0.6039202388192953519, 46.66051417535179979, 15.30882522405896928 ) ) ;
#54085=CARTESIAN_POINT ( 'NONE',  ( 0.5987334308729320709, 28.58958371212215610, 39.92741676764588021 ) ) ;
#54097=ORIENTED_EDGE ( 'NONE', *, *, #4404, .T. ) ;
#54098=CARTESIAN_POINT ( 'NONE',  ( 0.1129192098497447394, 41.72114954716796120, -14.36305915353690743 ) ) ;
#54105=CARTESIAN_POINT ( 'NONE',  ( 0.5549461598389366923, 30.29548519724135858, 32.05310081927385113 ) ) ;
#54114=CARTESIAN_POINT ( 'NONE',  ( 0.6028777368367060907, -19.79822363375413374, -44.93962806097678708 ) ) ;
#54115=CARTESIAN_POINT ( 'NONE',  ( 0.1140933569871964565, -42.77579569491688005, 10.82502899537159458 ) ) ;
#54117=CARTESIAN_POINT ( 'NONE',  ( 0.7413678028165009426, 10.71994208820953354, 42.77346061982449754 ) ) ;
#54121=CARTESIAN_POINT ( 'NONE',  ( 0.1157506346131639274, 20.32681236405533909, -39.16326542717449399 ) ) ;
#54127=CARTESIAN_POINT ( 'NONE',  ( 2.533389852662419894, -19.25250431882765056, -39.58271856741450279 ) ) ;
#54129=CARTESIAN_POINT ( 'NONE',  ( 0.8744876279028263033, -34.64280934553510605, -34.78829991575325664 ) ) ;
#54134=CARTESIAN_POINT ( 'NONE',  ( 4.553261556744873317, 22.96401893593727550, 37.44587293859699173 ) ) ;
#54144=CARTESIAN_POINT ( 'NONE',  ( 0.6026112563231247332, -14.13929437185411331, 47.02787842939825680 ) ) ;
#54150=CARTESIAN_POINT ( 'NONE',  ( 4.553261556744873317, 31.39705178283683296, -30.72075365562339755 ) ) ;
#54161=EDGE_CURVE ( 'NONE', #55501, #16844, #3468, .T. ) ;
#54167=CARTESIAN_POINT ( 'NONE',  ( 0.5549461598389363592, -35.86403770907894284, -25.67077121296841113 ) ) ;
#54170=ORIENTED_EDGE ( 'NONE', *, *, #56626, .T. ) ;
#54171=CARTESIAN_POINT ( 'NONE',  ( -6.078457390727109555, -11.02028633642675182, 15.79075046033827867 ) ) ;
#54178=CARTESIAN_POINT ( 'NONE',  ( 0.8744876279028306332, 37.95405449045402690, 31.14225101233274273 ) ) ;
#54182=DIRECTION ( 'NONE',  ( 0.1011922191286468153, -0.04473873795207425341, -0.9938604429769180015 ) ) ;
#54185=CARTESIAN_POINT ( 'NONE',  ( 0.8744876279028263033, 49.04340454744552602, -2.257104511335871422 ) ) ;
#54198=CARTESIAN_POINT ( 'NONE',  ( -6.078075953587585900, -12.94978436788727549, -14.25125464906014372 ) ) ;
#54205=CARTESIAN_POINT ( 'NONE',  ( 0.6008123274975392114, -45.68025125636955863, 18.02412817068846707 ) ) ;
#54222=EDGE_CURVE ( 'NONE', #47387, #17907, #38520, .T. ) ;
#54225=CARTESIAN_POINT ( 'NONE',  ( 0.6253024248130516494, -48.78635602192721166, 5.597829357832809549 ) ) ;
#54232=( BOUNDED_SURFACE ( )  B_SPLINE_SURFACE ( 3, 1, ( 
 ( #6620, #25143 ),
 ( #34560, #29844 ),
 ( #44289, #25768 ),
 ( #44908, #48960 ) ),
 .UNSPECIFIED., .F., .F., .F. ) 
 B_SPLINE_SURFACE_WITH_KNOTS ( ( 4, 4 ),
 ( 2, 2 ),
 ( 0.000000000000000000, 1.000000000000000000 ),
 ( 0.000000000000000000, 1.000000000000000000 ),
 .UNSPECIFIED. ) 
 GEOMETRIC_REPRESENTATION_ITEM ( )  RATIONAL_B_SPLINE_SURFACE ( (
 ( 1.000000000000000000, 1.000000000000000000),
 ( 0.9953485035131437453, 0.8621029689291523912),
 ( 0.9953485035131437453, 0.8621029689291523912),
 ( 1.000000000000000000, 1.000000000000000000) ) ) 
 REPRESENTATION_ITEM ( '' )  SURFACE ( )  );
#54245=EDGE_CURVE ( 'NONE', #1980, #36560, #7067, .T. ) ;
#54246=CARTESIAN_POINT ( 'NONE',  ( -6.079354080745853928, -6.651439635596617883, 18.07073064439223131 ) ) ;
#54247=CARTESIAN_POINT ( 'NONE',  ( 4.834790513006553603, -10.96306168285437899, 45.96085964668537116 ) ) ;
#54248=ORIENTED_EDGE ( 'NONE', *, *, #45490, .F. ) ;
#54251=CARTESIAN_POINT ( 'NONE',  ( 3.894904216938897878, 7.599853990351282285, -43.29395514158463243 ) ) ;
#54252=ORIENTED_EDGE ( 'NONE', *, *, #61784, .F. ) ;
#54253=ORIENTED_EDGE ( 'NONE', *, *, #20124, .F. ) ;
#54255=CARTESIAN_POINT ( 'NONE',  ( 2.706805983486679779, 42.25893709153612576, 12.28651086408780380 ) ) ;
#54257=B_SPLINE_CURVE_WITH_KNOTS ( 'NONE', 3,
 ( #45743, #11933, #51333, #17531 ),
 .UNSPECIFIED., .F., .F.,
 ( 4, 4 ),
 ( 0.000000000000000000, 0.005013413432710140706 ),
 .UNSPECIFIED. ) ;
#54258=CARTESIAN_POINT ( 'NONE',  ( 0.1129192098497455998, -17.41650932123162931, -40.54154647825617275 ) ) ;
#54260=CARTESIAN_POINT ( 'NONE',  ( -6.078726893082806448, -17.35055002122446410, -8.351793533709264139 ) ) ;
#54261=CARTESIAN_POINT ( 'NONE',  ( 3.390910168358337362, -14.38913369447737090, -41.55779070229905159 ) ) ;
#54267=EDGE_CURVE ( 'NONE', #27055, #40756, #16750, .T. ) ;
#54269=CARTESIAN_POINT ( 'NONE',  ( 2.879087469061463622, 41.18158905594808061, -15.49769013790108652 ) ) ;
#54277=CARTESIAN_POINT ( 'NONE',  ( 0.6021447746440204973, 48.98911543949576952, -3.407008591748049930 ) ) ;
#54281=ORIENTED_EDGE ( 'NONE', *, *, #17990, .F. ) ;
#54294=VERTEX_POINT ( 'NONE', #39894 ) ;
#54298=CARTESIAN_POINT ( 'NONE',  ( -6.077587904424778920, -18.27312872431383894, 6.073614082124997537 ) ) ;
#54302=CIRCLE ( 'NONE', #40368, 44.12552607296456131 ) ;
#54341=ORIENTED_EDGE ( 'NONE', *, *, #18089, .T. ) ;
#54344=CARTESIAN_POINT ( 'NONE',  ( 4.834790513006555379, -42.36901421273586266, 20.91544825160024601 ) ) ;
#54345=CARTESIAN_POINT ( 'NONE',  ( 0.1157506346131639274, 44.02745147267454229, -2.919619260130152050 ) ) ;
#54348=CARTESIAN_POINT ( 'NONE',  ( 3.678748215320119641, -36.44294827805337889, -32.71886818187038415 ) ) ;
#54352=CARTESIAN_POINT ( 'NONE',  ( 3.390910168358337362, 35.74601250571907229, -25.61873780018469660 ) ) ;
#54356=CARTESIAN_POINT ( 'NONE',  ( -2.739355103387248747, -5.801236230415970141, 13.75475282038634361 ) ) ;
#54359=CARTESIAN_POINT ( 'NONE',  ( 5.901764892641288895, -4.659217859064160194, 48.74713485305014160 ) ) ;
#54364=CARTESIAN_POINT ( 'NONE',  ( 0.1157506346131639274, -22.79424777909198951, 37.78045695843545104 ) ) ;
#54367=B_SPLINE_CURVE_WITH_KNOTS ( 'NONE', 3,
 ( #46631, #33148, #13419, #61612, #42250, #3982, #61310, #38169, #51296, #57215, #50992, #18734, #8088, #41622, #32527, #51601, #3674, #18425, #37547, #17808, #56924, #22501, #14048, #22809, #37237 ),
 .UNSPECIFIED., .F., .F.,
 ( 4, 3, 3, 3, 3, 3, 3, 3, 4 ),
 ( 6.254634441385500747E-18, 0.0005656085177311399653, 0.001131215744874498755, 0.001696821861372766783, 0.002262427090022496850, 0.002828031679238745925, 0.003393635864401603128, 0.003977030878808131623, 0.004561030005651158133 ),
 .UNSPECIFIED. ) ;
#54375=B_SPLINE_CURVE_WITH_KNOTS ( 'NONE', 3,
 ( #36418, #21999, #41128, #51093, #12611, #3475, #50793, #61107, #31703, #7882, #32321, #46128, #32017, #17299, #3174, #45509, #37336, #22303, #41431, #17604, #8186, #7561, #13217, #51397, #12921 ),
 .UNSPECIFIED., .F., .F.,
 ( 4, 3, 3, 3, 3, 3, 3, 3, 4 ),
 ( 2.602085213965210642E-18, 0.0005656085177311389895, 0.001131215744874498755, 0.001696821861372763965, 0.002262427090022495983, 0.002828031679238745925, 0.003393635864401605296, 0.003977030878808129888, 0.004561030005651158133 ),
 .UNSPECIFIED. ) ;
#54376=CIRCLE ( 'NONE', #1347, 43.92652462719577500 ) ;
#54377=EDGE_LOOP ( 'NONE', ( #27224, #56664, #10999, #29888 ) ) ;
#54390=CARTESIAN_POINT ( 'NONE',  ( 4.335381028904201628, -41.60039470203945200, -25.86820458205155759 ) ) ;
#54399=EDGE_CURVE ( 'NONE', #52564, #37381, #9986, .T. ) ;
#54405=EDGE_LOOP ( 'NONE', ( #11534, #180, #39586, #41712 ) ) ;
#54406=CARTESIAN_POINT ( 'NONE',  ( 0.1154773475650539977, 43.34451959701775792, 8.258102139708901390 ) ) ;
#54407=CARTESIAN_POINT ( 'NONE',  ( 0.1129192098497447394, -38.20615368646970467, 22.07354996983974260 ) ) ;
#54410=ORIENTED_EDGE ( 'NONE', *, *, #55143, .F. ) ;
#54413=CARTESIAN_POINT ( 'NONE',  ( 0.8744876279028263033, 46.30617036199606673, 16.31222353896886545 ) ) ;
#54414=CARTESIAN_POINT ( 'NONE',  ( 4.694002226626920127, -34.93533603653836650, -29.28834354244495941 ) ) ;
#54416=CARTESIAN_POINT ( 'NONE',  ( 0.5997462898726536595, -47.63132954987539591, 11.95023328037892441 ) ) ;
#54417=B_SPLINE_CURVE_WITH_KNOTS ( 'NONE', 3,
 ( #8375, #46943, #51292, #56303, #60372, #12811, #46627, #32522, #36931, #57752, #29262, #3670, #31904, #14886, #55677, #27194 ),
 .UNSPECIFIED., .F., .F.,
 ( 4, 3, 3, 3, 3, 4 ),
 ( 2.081781105835003463E-17, 0.0002612764279487749517, 0.0003919131003184794077, 0.0005225497727000653642, 0.0007837925190632465469, 0.001045051706266716084 ),
 .UNSPECIFIED. ) ;
#54424=CARTESIAN_POINT ( 'NONE',  ( 0.6016117650947689910, -20.19595095677608398, -44.76242418810664248 ) ) ;
#54428=CARTESIAN_POINT ( 'NONE',  ( -6.077587904424778920, 9.987489566522819828, -16.46347695818013435 ) ) ;
#54433=ADVANCED_FACE ( 'NONE', ( #41430 ), #11957, .F. ) ;
#54434=FACE_OUTER_BOUND ( 'NONE', #9599, .T. ) ;
#54438=CARTESIAN_POINT ( 'NONE',  ( 1.296416391601052043, -21.88885550073866781, 38.25160622698007273 ) ) ;
#54441=CARTESIAN_POINT ( 'NONE',  ( 4.975610109902397937, -10.32228546579698403, -47.81108480154335183 ) ) ;
#54446=CARTESIAN_POINT ( 'NONE',  ( 0.1147471544378676767, -38.59772625589639006, -21.38148068652244760 ) ) ;
#54447=CARTESIAN_POINT ( 'NONE',  ( 0.5997462898726536595, -45.31995669577334240, -18.91172004968183984 ) ) ;
#54452=CARTESIAN_POINT ( 'NONE',  ( 0.5997462898726536595, 27.66511329191646951, -40.57330571557777432 ) ) ;
#54454=CARTESIAN_POINT ( 'NONE',  ( 0.3676999524040323597, 43.96170928169360081, 3.649479463525401535 ) ) ;
#54460=VERTEX_POINT ( 'NONE', #41737 ) ;
#54467=CARTESIAN_POINT ( 'NONE',  ( 0.1157991065609915715, -1.495616162223984746, 44.09881515225770698 ) ) ;
#54476=CARTESIAN_POINT ( 'NONE',  ( -2.739355103387247858, 10.22927580983326656, -10.87241846864702843 ) ) ;
#54478=CARTESIAN_POINT ( 'NONE',  ( -6.078075953587585900, -11.02105682227026762, 15.79023371478161053 ) ) ;
#54479=CARTESIAN_POINT ( 'NONE',  ( -6.057079549204054558, 19.09779050476948115, 2.470957088999126139 ) ) ;
#54490=CARTESIAN_POINT ( 'NONE',  ( 4.553261556744873317, -33.30082861731504096, 28.64601855797499042 ) ) ;
#54502=ADVANCED_FACE ( 'NONE', ( #23224 ), #42319, .F. ) ;
#54506=ADVANCED_FACE ( 'NONE', ( #37335 ), #3852, .F. ) ;
#54513=FACE_OUTER_BOUND ( 'NONE', #47597, .T. ) ;
#54514=CARTESIAN_POINT ( 'NONE',  ( 0.1145239942831223490, 36.80079408639558380, 24.34434298385119888 ) ) ;
#54516=CARTESIAN_POINT ( 'NONE',  ( 1.296416391601052487, -2.522796799315330851, -43.99935079504609092 ) ) ;
#54519=CARTESIAN_POINT ( 'NONE',  ( 3.390910168358336474, -41.99763341749859791, 13.04974803829719221 ) ) ;
#54520=ORIENTED_EDGE ( 'NONE', *, *, #32032, .T. ) ;
#54521=ADVANCED_FACE ( 'NONE', ( #51715 ), #23097, .F. ) ;
#54522=CARTESIAN_POINT ( 'NONE',  ( 0.7044674535453004927, 48.35836311421820710, 8.559873814743298226 ) ) ;
#54530=B_SPLINE_CURVE_WITH_KNOTS ( 'NONE', 3,
 ( #34989, #14958, #34066, #10239 ),
 .UNSPECIFIED., .F., .F.,
 ( 4, 4 ),
 ( 0.000000000000000000, 0.004442905043737215703 ),
 .UNSPECIFIED. ) ;
#54531=CARTESIAN_POINT ( 'NONE',  ( -6.078457390727109555, -4.280596808180907153, -18.77421108870621325 ) ) ;
#54532=VERTEX_POINT ( 'NONE', #5552 ) ;
#54534=CARTESIAN_POINT ( 'NONE',  ( 0.1145239942831223490, 44.01141660824960411, 3.152885795547452741 ) ) ;
#54541=ORIENTED_EDGE ( 'NONE', *, *, #31649, .T. ) ;
#54542=CARTESIAN_POINT ( 'NONE',  ( 0.1152339509894530906, 43.26722510425824453, -8.653896361332732212 ) ) ;
#54546=VERTEX_POINT ( 'NONE', #37972 ) ;
#54552=CARTESIAN_POINT ( 'NONE',  ( -6.078726893082806448, -6.647148524917739998, 18.07233957617010134 ) ) ;
#54553=CARTESIAN_POINT ( 'NONE',  ( 3.221118495291109163, 13.40464864085779517, -41.89363692109937887 ) ) ;
#54562=VERTEX_POINT ( 'NONE', #20912 ) ;
#54568=CARTESIAN_POINT ( 'NONE',  ( 0.6039202388192952409, 32.88598194813054931, 36.47020570487947566 ) ) ;
#54570=CARTESIAN_POINT ( 'NONE',  ( 2.009741617377216460, -41.31583237047342294, -15.24814982737201774 ) ) ;
#54576=CARTESIAN_POINT ( 'NONE',  ( 0.5987334308729318488, -42.48817502201134744, 24.62352310025235269 ) ) ;
#54579=B_SPLINE_CURVE_WITH_KNOTS ( 'NONE', 3,
 ( #20105, #5953, #33898, #29176, #24793, #53576, #52976, #10079, #43932, #14481, #20406, #52663, #25096, #9759, #28866, #5040, #5348, #57971, #53889, #39225, #16022, #36073, #30096, #39852, #11313 ),
 .UNSPECIFIED., .F., .F.,
 ( 4, 3, 3, 3, 3, 3, 3, 3, 4 ),
 ( 4.670885906470169154E-18, 0.0005656085177311400737, 0.001131215744874498538, 0.001696821861372766133, 0.002262427090022497717, 0.002828031679238745925, 0.003393635864401603995, 0.003977030878808132490, 0.004561030005651159000 ),
 .UNSPECIFIED. ) ;
#54581=CARTESIAN_POINT ( 'NONE',  ( 0.3676999524040323597, -23.56959980820351674, 37.28839696479283106 ) ) ;
#54582=CARTESIAN_POINT ( 'NONE',  ( 2.299746137290199943, 46.92539900250360319, 14.22280795560328137 ) ) ;
#54585=( BOUNDED_SURFACE ( )  B_SPLINE_SURFACE ( 3, 1, ( 
 ( #43862, #906 ),
 ( #15647, #39462 ),
 ( #10948, #20042 ),
 ( #39157, #58212 ) ),
 .UNSPECIFIED., .F., .F., .F. ) 
 B_SPLINE_SURFACE_WITH_KNOTS ( ( 4, 4 ),
 ( 2, 2 ),
 ( 0.000000000000000000, 1.000000000000000000 ),
 ( 0.000000000000000000, 1.000000000000000000 ),
 .UNSPECIFIED. ) 
 GEOMETRIC_REPRESENTATION_ITEM ( )  RATIONAL_B_SPLINE_SURFACE ( (
 ( 1.000000000000000000, 1.000000000000000000),
 ( 0.7211978278499970862, 0.9934217856018976445),
 ( 0.7211978278499970862, 0.9934217856018976445),
 ( 1.000000000000000000, 1.000000000000000000) ) ) 
 REPRESENTATION_ITEM ( '' )  SURFACE ( )  );
#54586=B_SPLINE_CURVE_WITH_KNOTS ( 'NONE', 3,
 ( #24271, #49005, #61842, #10180 ),
 .UNSPECIFIED., .F., .F.,
 ( 4, 4 ),
 ( 2.147596245779529078E-17, 0.004559932413162187670 ),
 .UNSPECIFIED. ) ;
#54587=CARTESIAN_POINT ( 'NONE',  ( 4.553261556744875094, -36.93702150832111641, 23.77385134801386712 ) ) ;
#54595=CARTESIAN_POINT ( 'NONE',  ( 3.050102900204245682, 2.419036304482272026, -43.92691102884036525 ) ) ;
#54599=ORIENTED_EDGE ( 'NONE', *, *, #30191, .F. ) ;
#54605=ORIENTED_EDGE ( 'NONE', *, *, #43236, .F. ) ;
#54610=ORIENTED_EDGE ( 'NONE', *, *, #59880, .F. ) ;
#54615=AXIS2_PLACEMENT_3D ( 'NONE', #44238, #42998, #38300 ) ;
#54616=EDGE_LOOP ( 'NONE', ( #11662, #56483, #38734, #4955 ) ) ;
#54618=CARTESIAN_POINT ( 'NONE',  ( 0.5997462898726536595, -19.39900779840473888, 45.11352487427402025 ) ) ;
#54620=VERTEX_POINT ( 'NONE', #25299 ) ;
#54623=CARTESIAN_POINT ( 'NONE',  ( 0.7044674535453004927, -38.84805681606468397, 30.04382140185760619 ) ) ;
#54624=CARTESIAN_POINT ( 'NONE',  ( 4.226256110419178924, -43.82248454676872740, -3.227552963996462854 ) ) ;
#54628=CARTESIAN_POINT ( 'NONE',  ( -6.072942160501519915, 19.09631935424743077, -2.476842629158153564 ) ) ;
#54629=CARTESIAN_POINT ( 'NONE',  ( 0.6026777506516367566, -35.15493876059303346, 34.28814184781924013 ) ) ;
#54636=EDGE_LOOP ( 'NONE', ( #45261, #38338, #33153, #13155 ) ) ;
#54637=CARTESIAN_POINT ( 'NONE',  ( 0.5987334308729317378, -48.62339718036277958, 6.879546003219879857 ) ) ;
#54642=EDGE_CURVE ( 'NONE', #52094, #38290, #39180, .T. ) ;
#54644=CARTESIAN_POINT ( 'NONE',  ( 0.1365634738349413013, -42.51423502781833008, -11.80688102856425203 ) ) ;
#54651=CARTESIAN_POINT ( 'NONE',  ( -6.078457390727109555, -19.21674198601423456, 1.229365072086278987 ) ) ;
#54652=CARTESIAN_POINT ( 'NONE',  ( 0.8744876279028263033, -48.57046782678510510, -7.159588358748426806 ) ) ;
#54661=CARTESIAN_POINT ( 'NONE',  ( 4.694002226626921015, -4.034398983147053031, -45.40934261020431251 ) ) ;
#54663=CARTESIAN_POINT ( 'NONE',  ( 0.1156495703730067298, 44.02457461872624833, -2.963069839081658330 ) ) ;
#54681=ORIENTED_EDGE ( 'NONE', *, *, #17896, .F. ) ;
#54694=CIRCLE ( 'NONE', #33771, 10.00000000000000000 ) ;
#54700=AXIS2_PLACEMENT_3D ( 'NONE', #19174, #18866, #23540 ) ;
#54704=ORIENTED_EDGE ( 'NONE', *, *, #9656, .F. ) ;
#54713=ORIENTED_EDGE ( 'NONE', *, *, #35677, .T. ) ;
#54718=CARTESIAN_POINT ( 'NONE',  ( 0.1129192098497455998, -43.82135468580280957, 5.161459220629533107 ) ) ;
#54722=CARTESIAN_POINT ( 'NONE',  ( 0.5997462898726536595, 46.76781179977606229, 14.97743000668126001 ) ) ;
#54723=CARTESIAN_POINT ( 'NONE',  ( 4.975610109902397937, -40.67634447773618689, 27.16402781375239073 ) ) ;
#54730=CARTESIAN_POINT ( 'NONE',  ( 4.975610109902397937, 0.000000000000000000, 0.000000000000000000 ) ) ;
#54731=CARTESIAN_POINT ( 'NONE',  ( 4.975610109902397937, -16.35148546628888866, -46.09857188876371481 ) ) ;
#54733=CARTESIAN_POINT ( 'NONE',  ( -6.077587904424778920, -16.14165210942818618, 10.49967087922869702 ) ) ;
#54737=ORIENTED_EDGE ( 'NONE', *, *, #48095, .T. ) ;
#54745=CARTESIAN_POINT ( 'NONE',  ( 0.1157506346131639274, -12.64344793106056031, -42.27391493838008074 ) ) ;
#54747=CARTESIAN_POINT ( 'NONE',  ( 0.2279481005628848644, 30.21908332445557832, -32.14514722477598951 ) ) ;
#54749=CARTESIAN_POINT ( 'NONE',  ( 0.5997462898726536595, 4.195097405482933972, 48.92803682862026449 ) ) ;
#54755=CARTESIAN_POINT ( 'NONE',  ( 4.553261556744875094, 0.000000000000000000, 0.000000000000000000 ) ) ;
#54760=VERTEX_POINT ( 'NONE', #27459 ) ;
#54765=DIRECTION ( 'NONE',  ( 0.09722883295013594329, -0.8634569929835251845, -0.4949632060173795312 ) ) ;
#54769=CARTESIAN_POINT ( 'NONE',  ( 4.975610109902397937, 34.73360008816180056, -34.43873447229760387 ) ) ;
#54775=CARTESIAN_POINT ( 'NONE',  ( 0.1119899015040014406, -0.8531642396357116409, -44.11613558521091250 ) ) ;
#54787=CARTESIAN_POINT ( 'NONE',  ( 4.335381028904216727, -33.67825942593300681, 35.57431221687780010 ) ) ;
#54791=( BOUNDED_SURFACE ( )  B_SPLINE_SURFACE ( 3, 1, ( 
 ( #60499, #32335 ),
 ( #37350, #32028 ),
 ( #51730, #8197 ),
 ( #51411, #42366 ) ),
 .UNSPECIFIED., .F., .F., .F. ) 
 B_SPLINE_SURFACE_WITH_KNOTS ( ( 4, 4 ),
 ( 2, 2 ),
 ( 0.000000000000000000, 1.000000000000000000 ),
 ( 0.000000000000000000, 1.000000000000000000 ),
 .UNSPECIFIED. ) 
 GEOMETRIC_REPRESENTATION_ITEM ( )  RATIONAL_B_SPLINE_SURFACE ( (
 ( 1.000000000000000000, 1.000000000000000000),
 ( 0.7211978278499968642, 0.9934217856018975334),
 ( 0.7211978278499968642, 0.9934217856018975334),
 ( 1.000000000000000000, 1.000000000000000000) ) ) 
 REPRESENTATION_ITEM ( '' )  SURFACE ( )  );
#54794=VERTEX_POINT ( 'NONE', #19622 ) ;
#54795=CARTESIAN_POINT ( 'NONE',  ( -6.078075953587585900, -16.13536320617233244, 10.50929248103962443 ) ) ;
#54801=EDGE_CURVE ( 'NONE', #46201, #41166, #32396, .T. ) ;
#54803=FACE_OUTER_BOUND ( 'NONE', #31208, .T. ) ;
#54808=CARTESIAN_POINT ( 'NONE',  ( 0.5997462898726536595, -48.76843890605309184, 5.761162800240605897 ) ) ;
#54817=CARTESIAN_POINT ( 'NONE',  ( 4.553261556744873317, 27.21079963941887314, -34.48350256002191117 ) ) ;
#54818=ORIENTED_EDGE ( 'NONE', *, *, #46312, .T. ) ;
#54820=CARTESIAN_POINT ( 'NONE',  ( 0.8753041380234530822, -47.26389509135299249, 13.31399822241830577 ) ) ;
#54821=CARTESIAN_POINT ( 'NONE',  ( 0.7242003506640024568, -26.15097733078639308, -41.55885054679355761 ) ) ;
#54828=FACE_OUTER_BOUND ( 'NONE', #20681, .T. ) ;
#54833=CARTESIAN_POINT ( 'NONE',  ( -6.072942160501519027, -1.834587804586597759, -19.16868409349693891 ) ) ;
#54839=CARTESIAN_POINT ( 'NONE',  ( 0.5997462898726536595, -19.39900779840410294, -45.11352487427429736 ) ) ;
#54842=ORIENTED_EDGE ( 'NONE', *, *, #5639, .F. ) ;
#54843=CARTESIAN_POINT ( 'NONE',  ( -6.078457390727109555, -18.90008989325092870, -3.685256173530143897 ) ) ;
#54844=CARTESIAN_POINT ( 'NONE',  ( 0.8744876279028263033, 27.35388303025786882, 40.76904626731490566 ) ) ;
#54845=B_SPLINE_CURVE_WITH_KNOTS ( 'NONE', 3,
 ( #29689, #20014, #48488, #49113 ),
 .UNSPECIFIED., .F., .F.,
 ( 4, 4 ),
 ( 0.000000000000000000, 0.004444103432399265294 ),
 .UNSPECIFIED. ) ;
#54851=CARTESIAN_POINT ( 'NONE',  ( -6.077587904424778920, -4.278847002849007097, -18.77465018902190863 ) ) ;
#54854=VERTEX_POINT ( 'NONE', #37827 ) ;
#54860=DIRECTION ( 'NONE',  ( 0.09722883295013594329, -0.6146093961964115282, 0.7828166095262905078 ) ) ;
#54861=EDGE_CURVE ( 'NONE', #9797, #46207, #5513, .T. ) ;
#54862=( BOUNDED_SURFACE ( )  B_SPLINE_SURFACE ( 3, 1, ( 
 ( #20945, #24718 ),
 ( #43857, #900 ),
 ( #20038, #15332 ),
 ( #5883, #25030 ) ),
 .UNSPECIFIED., .F., .F., .F. ) 
 B_SPLINE_SURFACE_WITH_KNOTS ( ( 4, 4 ),
 ( 2, 2 ),
 ( 0.000000000000000000, 1.000000000000000000 ),
 ( 0.000000000000000000, 1.000000000000000000 ),
 .UNSPECIFIED. ) 
 GEOMETRIC_REPRESENTATION_ITEM ( )  RATIONAL_B_SPLINE_SURFACE ( (
 ( 1.000000000000000000, 1.000000000000000000),
 ( 0.9953485035131437453, 0.8621029689291523912),
 ( 0.9953485035131437453, 0.8621029689291523912),
 ( 1.000000000000000000, 1.000000000000000000) ) ) 
 REPRESENTATION_ITEM ( '' )  SURFACE ( )  );
#54869=ORIENTED_EDGE ( 'NONE', *, *, #40779, .T. ) ;
#54873=DIRECTION ( 'NONE',  ( 0.1011922191286468292, -0.9269080304894992128, -0.3613884859841242636 ) ) ;
#54874=B_SPLINE_CURVE_WITH_KNOTS ( 'NONE', 3,
 ( #61081, #14123, #33225, #18194 ),
 .UNSPECIFIED., .F., .F.,
 ( 4, 4 ),
 ( 0.000000000000000000, 0.005013413432710146778 ),
 .UNSPECIFIED. ) ;
#54875=CARTESIAN_POINT ( 'NONE',  ( 2.359973842542475886, 13.77930139075350269, -41.81227986866154822 ) ) ;
#54878=CARTESIAN_POINT ( 'NONE',  ( 0.5987334363312689645, 48.08272125986815837, 9.980722554900580690 ) ) ;
#54879=CARTESIAN_POINT ( 'NONE',  ( 2.879087469061463178, 8.095492153095989352, -43.25002524372141721 ) ) ;
#54894=CARTESIAN_POINT ( 'NONE',  ( 0.2285344041767079226, 25.86074962531460386, 35.74524862289040072 ) ) ;
#54896=CARTESIAN_POINT ( 'NONE',  ( 0.3676999524040366896, -38.02468164711607557, 22.36233818182511257 ) ) ;
#54901=CARTESIAN_POINT ( 'NONE',  ( 4.226256110419179812, 40.88307703899232592, -16.10593871250618392 ) ) ;
#54904=CARTESIAN_POINT ( 'NONE',  ( -6.063463321072278589, -17.34291445406321230, -8.369215657307158551 ) ) ;
#54905=CARTESIAN_POINT ( 'NONE',  ( 0.7948878604505663636, -38.82350069238938062, 30.05718618378071127 ) ) ;
#54911=CARTESIAN_POINT ( 'NONE',  ( 0.6016118706126976079, 17.28650708908693900, -45.96441805835117123 ) ) ;
#54913=ORIENTED_EDGE ( 'NONE', *, *, #24775, .F. ) ;
#54914=VERTEX_POINT ( 'NONE', #19309 ) ;
#54915=CARTESIAN_POINT ( 'NONE',  ( 4.834790513006555379, -16.75039937818070612, -44.18159641293900108 ) ) ;
#54916=B_SPLINE_CURVE_WITH_KNOTS ( 'NONE', 3,
 ( #7193, #40452, #35437, #26322 ),
 .UNSPECIFIED., .F., .F.,
 ( 4, 4 ),
 ( 0.000000000000000000, 0.005013413432710153717 ),
 .UNSPECIFIED. ) ;
#54918=EDGE_CURVE ( 'NONE', #9573, #16048, #33961, .T. ) ;
#54919=B_SPLINE_CURVE_WITH_KNOTS ( 'NONE', 3,
 ( #37804, #38721, #29288, #10191 ),
 .UNSPECIFIED., .F., .F.,
 ( 4, 4 ),
 ( 0.000000000000000000, 0.004444103432399269631 ),
 .UNSPECIFIED. ) ;
#54923=EDGE_CURVE ( 'NONE', #7236, #17964, #51124, .T. ) ;
#54928=CARTESIAN_POINT ( 'NONE',  ( 0.2940133293163010308, -17.11870290862044897, -40.65944613868263247 ) ) ;
#54932=ORIENTED_EDGE ( 'NONE', *, *, #55861, .F. ) ;
#54939=CARTESIAN_POINT ( 'NONE',  ( 0.6026112563231247332, -8.009419346916665461, 48.44987303006526247 ) ) ;
#54943=ORIENTED_EDGE ( 'NONE', *, *, #44725, .F. ) ;
#54947=DIRECTION ( 'NONE',  ( 1.000000000000000000, 0.000000000000000000, -0.000000000000000000 ) ) ;
#54948=CARTESIAN_POINT ( 'NONE',  ( 4.553261556744875094, 0.000000000000000000, 0.000000000000000000 ) ) ;
#54950=ORIENTED_EDGE ( 'NONE', *, *, #44418, .F. ) ;
#54952=CARTESIAN_POINT ( 'NONE',  ( 4.335381028904201628, -46.80143676542513731, -14.47005059964403628 ) ) ;
#54954=ORIENTED_EDGE ( 'NONE', *, *, #23420, .F. ) ;
#54966=CARTESIAN_POINT ( 'NONE',  ( 0.5997462898726536595, 40.86908001809362645, -27.22627276398607421 ) ) ;
#54974=CARTESIAN_POINT ( 'NONE',  ( 4.553261556744875094, 0.000000000000000000, 0.000000000000000000 ) ) ;
#54981=CARTESIAN_POINT ( 'NONE',  ( 0.7948878604505671408, -45.17791583987795434, 19.22640287894023103 ) ) ;
#54982=ORIENTED_EDGE ( 'NONE', *, *, #196, .T. ) ;
#55001=VERTEX_POINT ( 'NONE', #59341 ) ;
#55003=CARTESIAN_POINT ( 'NONE',  ( 0.6000166863083090663, -25.90381862410917435, 41.72308308835420121 ) ) ;
#55011=CARTESIAN_POINT ( 'NONE',  ( 0.5997462898726536595, 22.24958391914565681, -43.77793560195825506 ) ) ;
#55017=CARTESIAN_POINT ( 'NONE',  ( 3.678748215320120529, 48.39168598034271440, 7.540394040060985681 ) ) ;
#55018=CARTESIAN_POINT ( 'NONE',  ( 0.8744876279028306332, -42.33402326122651971, 24.86323641237049387 ) ) ;
#55027=ORIENTED_EDGE ( 'NONE', *, *, #6258, .T. ) ;
#55029=CARTESIAN_POINT ( 'NONE',  ( 0.6008123274975391004, -25.82835474539317389, 41.76662115020298671 ) ) ;
#55036=EDGE_CURVE ( 'NONE', #7202, #4827, #13646, .T. ) ;
#55038=B_SPLINE_CURVE_WITH_KNOTS ( 'NONE', 3,
 ( #33042, #42441, #56197, #13311 ),
 .UNSPECIFIED., .F., .F.,
 ( 4, 4 ),
 ( 0.000000000000000000, 0.004442905043737215703 ),
 .UNSPECIFIED. ) ;
#55042=CARTESIAN_POINT ( 'NONE',  ( 0.6029443199889047422, 33.01497303511078485, 36.35311812410746057 ) ) ;
#55056=CARTESIAN_POINT ( 'NONE',  ( 0.6016117650947689910, 5.062075601541858205, 48.84594604313416966 ) ) ;
#55063=CARTESIAN_POINT ( 'NONE',  ( -6.057079549204054558, -18.27862279149365676, -6.059965341982332276 ) ) ;
#55064=B_SPLINE_CURVE_WITH_KNOTS ( 'NONE', 3,
 ( #34985, #1421, #20558, #48748, #54045, #25554 ),
 .UNSPECIFIED., .F., .F.,
 ( 4, 2, 4 ),
 ( 0.000000000000000000, 0.0002447195606305752882, 0.0004894391212611505764 ),
 .UNSPECIFIED. ) ;
#55067=CARTESIAN_POINT ( 'NONE',  ( 4.390527457369402420, 17.48986963896179603, 40.30247879027717062 ) ) ;
#55069=CARTESIAN_POINT ( 'NONE',  ( 4.553261556744873317, 40.80044851610476542, 16.27461110774448372 ) ) ;
#55082=ORIENTED_EDGE ( 'NONE', *, *, #56626, .F. ) ;
#55083=LINE ( 'NONE', #11260, #32302 ) ;
#55086=EDGE_LOOP ( 'NONE', ( #51574, #31531, #11416, #46752 ) ) ;
#55093=ORIENTED_EDGE ( 'NONE', *, *, #33871, .T. ) ;
#55098=ORIENTED_EDGE ( 'NONE', *, *, #24589, .T. ) ;
#55099=CARTESIAN_POINT ( 'NONE',  ( -6.063463321072278589, 13.84388120595888161, -13.38534294049907736 ) ) ;
#55100=ORIENTED_EDGE ( 'NONE', *, *, #6587, .T. ) ;
#55103=ORIENTED_EDGE ( 'NONE', *, *, #11503, .F. ) ;
#55107=DIRECTION ( 'NONE',  ( 0.000000000000000000, 0.000000000000000000, 1.000000000000000000 ) ) ;
#55114=ORIENTED_EDGE ( 'NONE', *, *, #11767, .F. ) ;
#55116=CIRCLE ( 'NONE', #29147, 43.92652462719577500 ) ;
#55123=CARTESIAN_POINT ( 'NONE',  ( 1.657374760986086271, -34.55241765484513650, 27.33168274104962592 ) ) ;
#55127=CARTESIAN_POINT ( 'NONE',  ( 0.6000166863083090663, -47.36892948402883263, 12.96179004788911726 ) ) ;
#55129=CARTESIAN_POINT ( 'NONE',  ( 4.975610109902397937, -17.43163075979710541, 45.70106843599904778 ) ) ;
#55131=CARTESIAN_POINT ( 'NONE',  ( 0.3676999524040323597, 21.13209774130321250, -38.72189339862975288 ) ) ;
#55137=CARTESIAN_POINT ( 'NONE',  ( 0.1368894036331284314, 43.18319334776396090, -9.059422620287191918 ) ) ;
#55138=CARTESIAN_POINT ( 'NONE',  ( 4.975610109902397937, -44.31543648230415755, 20.70245146161774841 ) ) ;
#55143=EDGE_CURVE ( 'NONE', #23235, #57605, #43055, .T. ) ;
#55145=CARTESIAN_POINT ( 'NONE',  ( -6.079354080745853928, -11.01571246550386540, 15.79389230447975478 ) ) ;
#55148=CARTESIAN_POINT ( 'NONE',  ( 0.9268187852002115479, -2.403807104641838333, -44.02244932204816763 ) ) ;
#55150=CARTESIAN_POINT ( 'NONE',  ( 4.390527457369401532, -41.79567579338402794, 13.53908496180415888 ) ) ;
#55153=FACE_OUTER_BOUND ( 'NONE', #42778, .T. ) ;
#55160=B_SPLINE_CURVE_WITH_KNOTS ( 'NONE', 3,
 ( #452, #51927, #51301, #8703 ),
 .UNSPECIFIED., .F., .F.,
 ( 4, 4 ),
 ( 0.000000000000000000, 0.004442905043737215703 ),
 .UNSPECIFIED. ) ;
#55161=CARTESIAN_POINT ( 'NONE',  ( 0.3676999524040323597, 40.09552319080426486, -18.39292264373764851 ) ) ;
#55165=VERTEX_POINT ( 'NONE', #9823 ) ;
#55169=ORIENTED_EDGE ( 'NONE', *, *, #10057, .T. ) ;
#55173=CARTESIAN_POINT ( 'NONE',  ( 0.5997462898726536595, 40.86908001809362645, -27.22627276398607421 ) ) ;
#55174=ORIENTED_EDGE ( 'NONE', *, *, #18335, .F. ) ;
#55177=CARTESIAN_POINT ( 'NONE',  ( 5.901764892641307547, 35.20706988846512075, -34.03606465660227798 ) ) ;
#55186=ADVANCED_FACE ( 'NONE', ( #10134 ), #11832, .F. ) ;
#55192=CARTESIAN_POINT ( 'NONE',  ( 0.3676999524040366896, -6.224421213753956295, 43.67158302462379282 ) ) ;
#55194=ORIENTED_EDGE ( 'NONE', *, *, #15808, .F. ) ;
#55197=CARTESIAN_POINT ( 'NONE',  ( 0.8744876279028306332, -42.33402326122651971, 24.86323641237049387 ) ) ;
#55209=CARTESIAN_POINT ( 'NONE',  ( 0.9268187852002115479, 41.51895754277288120, -14.83005385931043918 ) ) ;
#55210=CARTESIAN_POINT ( 'NONE',  ( 2.299652685299201416, 9.651193673476788248, 48.07427779525340839 ) ) ;
#55211=DIRECTION ( 'NONE',  ( -1.000000000000000000, -0.000000000000000000, -0.000000000000000000 ) ) ;
#55214=EDGE_CURVE ( 'NONE', #26819, #51265, #5393, .T. ) ;
#55215=CARTESIAN_POINT ( 'NONE',  ( 0.6021448801613057400, 16.71458247052639123, 46.17536000360927062 ) ) ;
#55221=CARTESIAN_POINT ( 'NONE',  ( 2.359973842542475886, 2.722770999149179527, -43.93998648974180554 ) ) ;
#55227=CARTESIAN_POINT ( 'NONE',  ( 0.3676999524040323597, 21.13209774130321250, -38.72189339862975288 ) ) ;
#55245=CARTESIAN_POINT ( 'NONE',  ( 0.6000166863083090663, -25.01014854877412219, -42.26483113981062445 ) ) ;
#55247=CARTESIAN_POINT ( 'NONE',  ( -6.078726893082806448, 12.00325722817128771, 15.05708661006749338 ) ) ;
#55248=CARTESIAN_POINT ( 'NONE',  ( 0.8744876279028263033, -8.712669995482247742, 48.31603700562906312 ) ) ;
#55251=DIRECTION ( 'NONE',  ( 0.09722883295013592941, 0.9936727386027172093, 0.05622315004453748433 ) ) ;
#55256=EDGE_CURVE ( 'NONE', #31776, #36339, #42839, .T. ) ;
#55269=DIRECTION ( 'NONE',  ( 0.1011922191286468153, -0.2953728085273201187, -0.9500079151093968610 ) ) ;
#55270=CARTESIAN_POINT ( 'NONE',  ( 0.8744876279028306332, 21.91587810745098963, -43.93226988397984911 ) ) ;
#55274=CARTESIAN_POINT ( 'NONE',  ( 2.299746137290200831, -12.71146744108550131, 47.35715292519559227 ) ) ;
#55279=CARTESIAN_POINT ( 'NONE',  ( 0.1139756605157203478, 44.00639638324004466, -3.223708587354096267 ) ) ;
#55287=CARTESIAN_POINT ( 'NONE',  ( -6.078726893082806448, 16.77644806189623239, -9.452239506869167585 ) ) ;
#55289=VERTEX_POINT ( 'NONE', #10446 ) ;
#55290=ORIENTED_EDGE ( 'NONE', *, *, #11399, .F. ) ;
#55292=CARTESIAN_POINT ( 'NONE',  ( 1.834102595619085729, -19.01334881635286678, -39.73273602013052397 ) ) ;
#55294=CARTESIAN_POINT ( 'NONE',  ( 3.678834586032788234, 38.46440325416317307, -30.31669592698840532 ) ) ;
#55296=B_SPLINE_CURVE_WITH_KNOTS ( 'NONE', 3,
 ( #56254, #27449, #51866, #32470, #8640, #42201 ),
 .UNSPECIFIED., .F., .F.,
 ( 4, 2, 4 ),
 ( 1.553784678811103104E-17, 0.0002293755540694291772, 0.0004587511081388428503 ),
 .UNSPECIFIED. ) ;
#55302=VERTEX_POINT ( 'NONE', #59895 ) ;
#55310=CARTESIAN_POINT ( 'NONE',  ( 0.8744876279028306332, 27.35388303025845147, -40.76904626731451486 ) ) ;
#55313=CARTESIAN_POINT ( 'NONE',  ( 0.3676999524040366896, 33.04872056100262512, -29.21870381457057775 ) ) ;
#55318=FACE_OUTER_BOUND ( 'NONE', #29398, .T. ) ;
#55320=CARTESIAN_POINT ( 'NONE',  ( 0.7242486021783859362, -20.62188805686228577, 44.56174587405900667 ) ) ;
#55325=LINE ( 'NONE', #8037, #36776 ) ;
#55326=CARTESIAN_POINT ( 'NONE',  ( 0.1157506346131639274, 39.71414577812362268, -19.22829386390743878 ) ) ;
#55327=ORIENTED_EDGE ( 'NONE', *, *, #38018, .F. ) ;
#55328=DIRECTION ( 'NONE',  ( 0.000000000000000000, 0.000000000000000000, 1.000000000000000000 ) ) ;
#55332=VERTEX_POINT ( 'NONE', #17009 ) ;
#55335=LINE ( 'NONE', #2094, #10243 ) ;
#55336=ORIENTED_EDGE ( 'NONE', *, *, #49877, .F. ) ;
#55340=CARTESIAN_POINT ( 'NONE',  ( -6.077587904424778920, 0.6233693561571294062, -19.24597183931574662 ) ) ;
#55341=ORIENTED_EDGE ( 'NONE', *, *, #21428, .F. ) ;
#55347=CARTESIAN_POINT ( 'NONE',  ( 0.5997462898726536595, 33.39998138387845472, 35.99990102348730403 ) ) ;
#55354=ORIENTED_EDGE ( 'NONE', *, *, #2465, .F. ) ;
#55355=CARTESIAN_POINT ( 'NONE',  ( -6.077587904424778920, 16.77513308702627981, 9.454677747363296803 ) ) ;
#55358=LINE ( 'NONE', #21872, #40065 ) ;
#55359=B_SPLINE_CURVE_WITH_KNOTS ( 'NONE', 3,
 ( #34897, #26397, #44923, #6638, #30166, #2266, #49276, #54261, #21704, #58657, #30466, #45234, #6329, #11383, #53961, #49582, #44610, #59911, #21396, #36137, #11086, #16089, #2582, #25785, #35824 ),
 .UNSPECIFIED., .F., .F.,
 ( 4, 3, 3, 3, 3, 3, 3, 3, 4 ),
 ( 4.670885906470169154E-18, 0.0005656085177311403990, 0.001131215744874500707, 0.001696821861372765266, 0.002262427090022498151, 0.002828031679238745492, 0.003393635864401603995, 0.003977030878808131623, 0.004561030005651158133 ),
 .UNSPECIFIED. ) ;
#55366=CARTESIAN_POINT ( 'NONE',  ( 0.6039202388192952409, -35.15506827346133889, -34.28826165814277260 ) ) ;
#55370=B_SPLINE_CURVE_WITH_KNOTS ( 'NONE', 3,
 ( #30640, #41020, #41313, #7439, #45699, #54749 ),
 .UNSPECIFIED., .F., .F.,
 ( 4, 2, 4 ),
 ( 2.335442953235084577E-18, 0.0002447193893791698707, 0.0004894387787583364888 ),
 .UNSPECIFIED. ) ;
#55374=CARTESIAN_POINT ( 'NONE',  ( 3.221118495291109163, 16.94972950403165157, 40.58901439308313286 ) ) ;
#55376=DIRECTION ( 'NONE',  ( 0.000000000000000000, 0.000000000000000000, 1.000000000000000000 ) ) ;
#55380=ORIENTED_EDGE ( 'NONE', *, *, #38478, .F. ) ;
#55382=CARTESIAN_POINT ( 'NONE',  ( 3.894904216938898323, -33.08280459236107163, -28.94222473791284500 ) ) ;
#55384=CARTESIAN_POINT ( 'NONE',  ( -6.072942160501519027, -12.95676005301717382, 14.24522836663417280 ) ) ;
#55385=EDGE_LOOP ( 'NONE', ( #1226, #60544, #484, #30603 ) ) ;
#55388=EDGE_CURVE ( 'NONE', #54854, #52998, #25573, .T. ) ;
#55394=ORIENTED_EDGE ( 'NONE', *, *, #38228, .F. ) ;
#55409=CARTESIAN_POINT ( 'NONE',  ( 0.8753041380234465318, 41.63161868429074985, -26.03740873433439162 ) ) ;
#55411=DIRECTION ( 'NONE',  ( -1.000000000000000000, -0.000000000000000000, -0.000000000000000000 ) ) ;
#55416=DIRECTION ( 'NONE',  ( 0.09722883295013597105, -0.9253344465965372967, 0.3664733496245457522 ) ) ;
#55418=VERTEX_POINT ( 'NONE', #8501 ) ;
#55426=CARTESIAN_POINT ( 'NONE',  ( 0.7044674535452954967, 40.69315356317272148, 27.49308960257011947 ) ) ;
#55440=ORIENTED_EDGE ( 'NONE', *, *, #16816, .F. ) ;
#55445=CARTESIAN_POINT ( 'NONE',  ( -2.601141883200662974, 14.30071512379477028, 4.276093359300773500 ) ) ;
#55452=CARTESIAN_POINT ( 'NONE',  ( 0.6000166863083090663, 10.41802958826926506, 47.99258423138307705 ) ) ;
#55455=CARTESIAN_POINT ( 'NONE',  ( 3.559346040607745287, -3.460731807603660837, -43.83438851972076833 ) ) ;
#55458=CARTESIAN_POINT ( 'NONE',  ( 0.6000166863083090663, 48.30184070260993678, 8.874438937090557644 ) ) ;
#55464=CARTESIAN_POINT ( 'NONE',  ( 0.3676999524040323597, 3.413584541508654091, 43.98065510995502336 ) ) ;
#55474=CARTESIAN_POINT ( 'NONE',  ( 0.1158403557922069033, 44.03104648574668545, 2.864830283600325878 ) ) ;
#55476=CARTESIAN_POINT ( 'NONE',  ( -6.077587904424778920, -8.912150607695380700, 17.06955163264944630 ) ) ;
#55479=CARTESIAN_POINT ( 'NONE',  ( 4.975610109902397937, -37.61482235126175766, 31.26618855282478648 ) ) ;
#55486=ORIENTED_EDGE ( 'NONE', *, *, #24038, .F. ) ;
#55491=CARTESIAN_POINT ( 'NONE',  ( 0.1157506346131639274, -12.46557269385145439, 42.32670737509757686 ) ) ;
#55497=EDGE_CURVE ( 'NONE', #55302, #36560, #34811, .T. ) ;
#55498=CARTESIAN_POINT ( 'NONE',  ( 0.6008123274975391004, 27.73703781927353518, 40.52420615102345636 ) ) ;
#55501=VERTEX_POINT ( 'NONE', #15702 ) ;
#55506=CARTESIAN_POINT ( 'NONE',  ( 0.3676999524040366896, 3.413584541509296688, -43.98065510995495941 ) ) ;
#55514=VECTOR ( 'NONE', #50000, 1000.000000000000000 ) ;
#55522=( BOUNDED_SURFACE ( )  B_SPLINE_SURFACE ( 3, 1, ( 
 ( #61484, #28300 ),
 ( #56794, #48036 ),
 ( #19535, #83 ),
 ( #14225, #24214 ) ),
 .UNSPECIFIED., .F., .F., .F. ) 
 B_SPLINE_SURFACE_WITH_KNOTS ( ( 4, 4 ),
 ( 2, 2 ),
 ( 0.000000000000000000, 1.000000000000000000 ),
 ( 0.000000000000000000, 1.000000000000000000 ),
 .UNSPECIFIED. ) 
 GEOMETRIC_REPRESENTATION_ITEM ( )  RATIONAL_B_SPLINE_SURFACE ( (
 ( 1.000000000000000000, 1.000000000000000000),
 ( 0.9953485035131437453, 0.8621029689291523912),
 ( 0.9953485035131437453, 0.8621029689291523912),
 ( 1.000000000000000000, 1.000000000000000000) ) ) 
 REPRESENTATION_ITEM ( '' )  SURFACE ( )  );
#55524=CARTESIAN_POINT ( 'NONE',  ( 0.6016118706126977189, 16.63270000191639397, 46.20502511015637737 ) ) ;
#55534=CARTESIAN_POINT ( 'NONE',  ( 0.8744876279028306332, 5.599149760997630842, 48.77498920895230583 ) ) ;
#55535=UNCERTAINTY_MEASURE_WITH_UNIT (LENGTH_MEASURE( 1.000000000000000082E-05 ), #45164, 'distance_accuracy_value', 'NONE');
#55546=VECTOR ( 'NONE', #18757, 1000.000000000000227 ) ;
#55549=VERTEX_POINT ( 'NONE', #39213 ) ;
#55559=ORIENTED_EDGE ( 'NONE', *, *, #49471, .F. ) ;
#55563=CARTESIAN_POINT ( 'NONE',  ( -6.072942160501519915, 3.058960253794702489, -19.01175753197806273 ) ) ;
#55564=ORIENTED_EDGE ( 'NONE', *, *, #9870, .F. ) ;
#55566=EDGE_CURVE ( 'NONE', #51862, #27417, #16305, .T. ) ;
#55567=CARTESIAN_POINT ( 'NONE',  ( 0.8744876279028263033, -45.83369275826233036, 17.59609782084381280 ) ) ;
#55570=ORIENTED_EDGE ( 'NONE', *, *, #57510, .T. ) ;
#55571=CARTESIAN_POINT ( 'NONE',  ( 0.2940135542859018680, -11.77874396291204384, 42.51472379479353947 ) ) ;
#55584=ORIENTED_EDGE ( 'NONE', *, *, #3872, .F. ) ;
#55589=CARTESIAN_POINT ( 'NONE',  ( 3.240649175237396484, 11.56283248366031913, -42.44485625317231126 ) ) ;
#55601=CARTESIAN_POINT ( 'NONE',  ( 0.5997462898726536595, 27.66511329191589397, 40.57330571557817223 ) ) ;
#55602=CARTESIAN_POINT ( 'NONE',  ( -2.739355103387248747, -14.92576340101414800, 0.2629711922692996584 ) ) ;
#55604=AXIS2_PLACEMENT_3D ( 'NONE', #28875, #57661, #33908 ) ;
#55606=CARTESIAN_POINT ( 'NONE',  ( 0.5987334363312692975, -47.34446306252520742, -13.04088661837312380 ) ) ;
#55607=CARTESIAN_POINT ( 'NONE',  ( -6.078726893082806448, 3.069885851706299462, 19.00973019603943825 ) ) ;
#55614=CIRCLE ( 'NONE', #54615, 48.91267123290010943 ) ;
#55615=CARTESIAN_POINT ( 'NONE',  ( 3.727782113643637096, 37.96789553646228654, 22.16340868274241771 ) ) ;
#55617=ORIENTED_EDGE ( 'NONE', *, *, #38507, .F. ) ;
#55618=CARTESIAN_POINT ( 'NONE',  ( 3.390910168358336918, -43.93422347332083433, 1.970062011699514448 ) ) ;
#55619=CARTESIAN_POINT ( 'NONE',  ( 0.1156867017252034557, -42.64922063473789393, -11.31312452528629109 ) ) ;
#55621=DIRECTION ( 'NONE',  ( 0.1011922191286467876, -0.8604626000150176202, 0.4993638440688468183 ) ) ;
#55622=CARTESIAN_POINT ( 'NONE',  ( -6.078726893082806448, -6.647148524917739998, 18.07233957617010134 ) ) ;
#55634=VERTEX_POINT ( 'NONE', #50130 ) ;
#55636=VERTEX_POINT ( 'NONE', #30701 ) ;
#55644=CARTESIAN_POINT ( 'NONE',  ( 0.1147471544378677599, -43.72123235070954905, 5.950296648782622100 ) ) ;
#55646=CARTESIAN_POINT ( 'NONE',  ( 0.1152339509894530906, -27.68528683457054740, -34.35793333922745774 ) ) ;
#55648=ADVANCED_FACE ( 'NONE', ( #49817 ), #50224, .F. ) ;
#55664=ORIENTED_EDGE ( 'NONE', *, *, #16028, .T. ) ;
#55668=CARTESIAN_POINT ( 'NONE',  ( 0.3676999524040366896, 19.66859742988788184, -39.48540057367844724 ) ) ;
#55670=CARTESIAN_POINT ( 'NONE',  ( 0.6008123274975393224, 4.281860609577630150, 48.92055008765341029 ) ) ;
#55672=CARTESIAN_POINT ( 'NONE',  ( -6.079354080745853928, -11.01571246550363803, -15.79389230447991110 ) ) ;
#55673=CARTESIAN_POINT ( 'NONE',  ( -6.078726893082806448, 13.83016815118519638, 13.39852567182907350 ) ) ;
#55675=CARTESIAN_POINT ( 'NONE',  ( 4.553261556744873317, 43.59419396814051595, 5.393126930805304475 ) ) ;
#55677=CARTESIAN_POINT ( 'NONE',  ( 0.6008122571543325074, -2.009120241389370509, -49.06646498700467873 ) ) ;
#55678=CARTESIAN_POINT ( 'NONE',  ( 1.657374760986085827, 16.37088960564075180, 40.90090977927223292 ) ) ;
#55683=CARTESIAN_POINT ( 'NONE',  ( 4.060580049360325461, -33.13615358156597779, -28.86975961413743974 ) ) ;
#55686=CARTESIAN_POINT ( 'NONE',  ( 4.553261556744873317, -20.11719049292697648, 39.04917684785332455 ) ) ;
#55687=CIRCLE ( 'NONE', #31704, 48.91267123290010943 ) ;
#55688=VERTEX_POINT ( 'NONE', #22248 ) ;
#55691=B_SPLINE_CURVE_WITH_KNOTS ( 'NONE', 3,
 ( #45337, #6141, #2378, #26506, #1149, #1760, #25278, #39401, #45034, #59084, #2064, #30583, #6754, #16196, #44422, #1446 ),
 .UNSPECIFIED., .F., .F.,
 ( 4, 3, 3, 3, 3, 4 ),
 ( 1.962735358247463844E-17, 0.0002612764279487778249, 0.0003919131003184803835, 0.0005225497727000590759, 0.0007837925190632501248, 0.001045051706266716517 ),
 .UNSPECIFIED. ) ;
#55692=EDGE_CURVE ( 'NONE', #14390, #6519, #1543, .T. ) ;
#55697=EDGE_CURVE ( 'NONE', #14464, #53183, #6829, .T. ) ;
#55704=CARTESIAN_POINT ( 'NONE',  ( 0.8753041380234524160, 37.96023374381034898, 31.14737520222631417 ) ) ;
#55706=CARTESIAN_POINT ( 'NONE',  ( 0.7948878604505668077, -43.19977686076578038, -23.33405079446049868 ) ) ;
#55709=ORIENTED_EDGE ( 'NONE', *, *, #1048, .F. ) ;
#55715=ORIENTED_EDGE ( 'NONE', *, *, #3803, .F. ) ;
#55717=DIRECTION ( 'NONE',  ( 0.09722883295013594329, -0.9253344465965321897, -0.3664733496245589084 ) ) ;
#55718=CARTESIAN_POINT ( 'NONE',  ( 0.6027444965799114707, -25.34513801577104530, -42.06141337198453556 ) ) ;
#55719=LINE ( 'NONE', #12852, #38298 ) ;
#55722=CARTESIAN_POINT ( 'NONE',  ( 2.009741617377216460, 5.591155404095686343, 43.68344147237367991 ) ) ;
#55725=CARTESIAN_POINT ( 'NONE',  ( 0.8744876279028263033, 16.11801507201566253, 46.37412684372363714 ) ) ;
#55728=ORIENTED_EDGE ( 'NONE', *, *, #49242, .F. ) ;
#55729=CARTESIAN_POINT ( 'NONE',  ( 0.6252788684277224007, 11.59566469080381523, 47.71776285150123442 ) ) ;
#55730=CARTESIAN_POINT ( 'NONE',  ( 0.7044674535452954967, -35.85885898216653800, 33.55510326772964191 ) ) ;
#55733=CARTESIAN_POINT ( 'NONE',  ( 4.553261556744873317, 17.57396821678933563, -40.25785894628420181 ) ) ;
#55734=CARTESIAN_POINT ( 'NONE',  ( 3.559346040607745287, -33.97180693775380433, 27.91678016759760084 ) ) ;
#55740=CARTESIAN_POINT ( 'NONE',  ( 4.553261556744873317, -36.93702150832076825, -23.77385134801438937 ) ) ;
#55745=CARTESIAN_POINT ( 'NONE',  ( 2.359973842542475886, -43.44419283542142551, 7.123061386174991405 ) ) ;
#55752=FACE_OUTER_BOUND ( 'NONE', #18758, .T. ) ;
#55757=VECTOR ( 'NONE', #40154, 1000.000000000000114 ) ;
#55761=VERTEX_POINT ( 'NONE', #52269 ) ;
#55763=CARTESIAN_POINT ( 'NONE',  ( 0.8744876279028306332, -38.80702141274064587, 30.07266432244707843 ) ) ;
#55768=ADVANCED_FACE ( 'NONE', ( #61659 ), #37935, .F. ) ;
#55774=CARTESIAN_POINT ( 'NONE',  ( -6.079354080745853928, 19.25598488485689330, 0.001167186744194736829 ) ) ;
#55780=EDGE_CURVE ( 'NONE', #50250, #58000, #22508, .T. ) ;
#55784=ORIENTED_EDGE ( 'NONE', *, *, #17358, .F. ) ;
#55786=CARTESIAN_POINT ( 'NONE',  ( 0.1152339509894530906, 44.04726506203218150, 2.604060485150331505 ) ) ;
#55788=CARTESIAN_POINT ( 'NONE',  ( 2.648799415243708655, 21.44335952302255777, -44.09875049994042229 ) ) ;
#55789=ORIENTED_EDGE ( 'NONE', *, *, #57090, .T. ) ;
#55792=CARTESIAN_POINT ( 'NONE',  ( 2.114184763582917181, 7.651710973661706259E-12, 44.03514965515166324 ) ) ;
#55793=EDGE_CURVE ( 'NONE', #52998, #48557, #2283, .T. ) ;
#55795=CARTESIAN_POINT ( 'NONE',  ( 0.1145239942831223490, 14.93204977986375503, 41.52083055619605290 ) ) ;
#55804=CARTESIAN_POINT ( 'NONE',  ( 4.975610109902397937, -36.86873347511098586, -32.14258700041121131 ) ) ;
#55806=VERTEX_POINT ( 'NONE', #23780 ) ;
#55807=CARTESIAN_POINT ( 'NONE',  ( 0.1140933569871964842, -12.91770938709908734, 42.19102670325003146 ) ) ;
#55808=CARTESIAN_POINT ( 'NONE',  ( 4.553261556744875094, 6.787618719203488915, 43.39893775135925580 ) ) ;
#55812=CARTESIAN_POINT ( 'NONE',  ( 0.6029443449137434907, 28.05947194175915271, 40.30143387440406144 ) ) ;
#55826=CIRCLE ( 'NONE', #13870, 48.91267123290010943 ) ;
#55827=CARTESIAN_POINT ( 'NONE',  ( 0.8753041380234465318, 48.93739466471249955, 4.033575498629935474 ) ) ;
#55829=CARTESIAN_POINT ( 'NONE',  ( 0.7242486021783801631, 43.87788672623142361, 22.03956711947809310 ) ) ;
#55831=CARTESIAN_POINT ( 'NONE',  ( 4.975610109902397937, 38.85236532789244279, 29.71435874397685595 ) ) ;
#55833=CARTESIAN_POINT ( 'NONE',  ( 0.7948884756798502149, 16.14026985310537654, 46.37014485279392062 ) ) ;
#55843=VECTOR ( 'NONE', #57654, 1000.000000000000114 ) ;
#55860=CARTESIAN_POINT ( 'NONE',  ( 0.8744876279028306332, 49.04340454744548339, 2.257104511336577968 ) ) ;
#55861=EDGE_CURVE ( 'NONE', #17733, #34547, #10000, .T. ) ;
#55864=CARTESIAN_POINT ( 'NONE',  ( 4.975610109902397937, -48.77192499014914517, 3.707929326866768349 ) ) ;
#55870=ORIENTED_EDGE ( 'NONE', *, *, #2108, .F. ) ;
#55872=CIRCLE ( 'NONE', #37942, 48.91267123290010943 ) ;
#55873=EDGE_LOOP ( 'NONE', ( #38376, #32937, #55103, #38804 ) ) ;
#55874=CARTESIAN_POINT ( 'NONE',  ( 0.5997462898726536595, -48.63480578518805686, 6.797594896825438049 ) ) ;
#55877=CARTESIAN_POINT ( 'NONE',  ( 0.6252788684277210685, 16.31351639750482718, -46.31752922946136408 ) ) ;
#55880=FACE_OUTER_BOUND ( 'NONE', #33261, .T. ) ;
#55891=CARTESIAN_POINT ( 'NONE',  ( 4.694002226626920127, 36.74006825548320876, 26.98985283451114014 ) ) ;
#55896=CARTESIAN_POINT ( 'NONE',  ( 0.1119898979215351170, 10.36499891643169846, 42.88972028020465643 ) ) ;
#55897=( BOUNDED_SURFACE ( )  B_SPLINE_SURFACE ( 3, 1, ( 
 ( #26770, #41202 ),
 ( #55563, #50877 ),
 ( #3251, #17685 ),
 ( #13007, #10442 ) ),
 .UNSPECIFIED., .F., .F., .F. ) 
 B_SPLINE_SURFACE_WITH_KNOTS ( ( 4, 4 ),
 ( 2, 2 ),
 ( 0.000000000000000000, 1.000000000000000000 ),
 ( 0.000000000000000000, 1.000000000000000000 ),
 .UNSPECIFIED. ) 
 GEOMETRIC_REPRESENTATION_ITEM ( )  RATIONAL_B_SPLINE_SURFACE ( (
 ( 1.000000000000000000, 1.000000000000000000),
 ( 0.7211978278499970862, 0.9934217856018976445),
 ( 0.7211978278499970862, 0.9934217856018976445),
 ( 1.000000000000000000, 1.000000000000000000) ) ) 
 REPRESENTATION_ITEM ( '' )  SURFACE ( )  );
#55900=CARTESIAN_POINT ( 'NONE',  ( 4.834790513006553603, -27.40943972694875441, 38.48781566650860242 ) ) ;
#55905=CARTESIAN_POINT ( 'NONE',  ( -6.057079549204054558, 15.42772006041527355, 11.52461213391576678 ) ) ;
#55906=DIRECTION ( 'NONE',  ( 0.000000000000000000, 0.000000000000000000, -1.000000000000000000 ) ) ;
#55908=CARTESIAN_POINT ( 'NONE',  ( 0.6008123274975392114, -39.09350553450490651, -29.71956218018853590 ) ) ;
#55909=CARTESIAN_POINT ( 'NONE',  ( 1.657374760986086715, -23.88755842655104900, -37.01722571547405494 ) ) ;
#55911=CARTESIAN_POINT ( 'NONE',  ( 0.8744876279028306332, 10.05549467470575209, -48.05452192277493850 ) ) ;
#55913=CARTESIAN_POINT ( 'NONE',  ( 0.6024113833632039894, -1.791547436567632490, 49.07476160801390108 ) ) ;
#55918=CARTESIAN_POINT ( 'NONE',  ( 4.226256110419178924, -19.95723175456961229, -39.14761998744732097 ) ) ;
#55921=B_SPLINE_CURVE_WITH_KNOTS ( 'NONE', 3,
 ( #55989, #37227, #13109, #46622 ),
 .UNSPECIFIED., .F., .F.,
 ( 4, 4 ),
 ( 0.000000000000000000, 0.005013413432710150247 ),
 .UNSPECIFIED. ) ;
#55926=EDGE_CURVE ( 'NONE', #33035, #41260, #32279, .T. ) ;
#55927=ORIENTED_EDGE ( 'NONE', *, *, #61934, .T. ) ;
#55928=VERTEX_POINT ( 'NONE', #54416 ) ;
#55935=EDGE_CURVE ( 'NONE', #41374, #37381, #46564, .T. ) ;
#55936=CARTESIAN_POINT ( 'NONE',  ( 2.185380717157383135, -44.00852750110943390, 1.438509732776827477 ) ) ;
#55937=CARTESIAN_POINT ( 'NONE',  ( 0.6026777506516367566, 49.01745359636671395, 2.972479363301738342 ) ) ;
#55938=CARTESIAN_POINT ( 'NONE',  ( 0.6252788684277218456, -24.86667677503463736, 42.34492552053455228 ) ) ;
#55953=ORIENTED_EDGE ( 'NONE', *, *, #41997, .T. ) ;
#55955=VECTOR ( 'NONE', #61464, 999.9999999999998863 ) ;
#55960=CARTESIAN_POINT ( 'NONE',  ( 0.6021447746440204973, -48.73699394290184017, -6.020511647529366073 ) ) ;
#55962=CARTESIAN_POINT ( 'NONE',  ( 0.1155031312995260795, -43.78313126285997470, 5.475312717186315403 ) ) ;
#55964=CARTESIAN_POINT ( 'NONE',  ( 0.1145239942831223490, -27.25490258565300650, -34.70037126244096726 ) ) ;
#55965=CARTESIAN_POINT ( 'NONE',  ( 0.6039202388192952409, 11.09723268158311171, -47.83738224087722557 ) ) ;
#55968=CARTESIAN_POINT ( 'NONE',  ( 0.5997462898726536595, 49.03735788587803768, -2.624721264558313560 ) ) ;
#55974=ORIENTED_EDGE ( 'NONE', *, *, #11207, .T. ) ;
#55977=CIRCLE ( 'NONE', #51010, 48.91267123290010943 ) ;
#55978=ORIENTED_EDGE ( 'NONE', *, *, #33698, .F. ) ;
#55986=CARTESIAN_POINT ( 'NONE',  ( 0.6028777368367060907, 4.628771803277713204, 48.88879524905737384 ) ) ;
#55989=CARTESIAN_POINT ( 'NONE',  ( 4.553261556744873317, -4.442710778081946366, -43.70128015019640344 ) ) ;
#55991=CARTESIAN_POINT ( 'NONE',  ( 0.5997462898726536595, 44.46857747280011353, 20.83500054451363326 ) ) ;
#55996=CARTESIAN_POINT ( 'NONE',  ( 0.8744876279028263033, 28.81338721758142896, -39.75095932715596092 ) ) ;
#56000=ORIENTED_EDGE ( 'NONE', *, *, #30649, .T. ) ;
#56004=CARTESIAN_POINT ( 'NONE',  ( 3.050102900204245682, -32.83519750374883728, -29.27925979371518750 ) ) ;
#56005=CARTESIAN_POINT ( 'NONE',  ( 3.559346040607745287, 28.00880476468896774, -33.89597523594098050 ) ) ;
#56006=CARTESIAN_POINT ( 'NONE',  ( 3.240649175237396928, -19.46330462187410504, 39.45180212099042905 ) ) ;
#56013=CARTESIAN_POINT ( 'NONE',  ( 1.834102595619085729, -26.43261434248111286, 35.23513365774772410 ) ) ;
#56019=CARTESIAN_POINT ( 'NONE',  ( -6.072942160501519027, -1.863502906426436789, 19.16589468839794463 ) ) ;
#56029=ORIENTED_EDGE ( 'NONE', *, *, #26720, .T. ) ;
#56031=CARTESIAN_POINT ( 'NONE',  ( 0.6024113833632039894, -42.68099031389036213, -24.28734104274209926 ) ) ;
#56034=CARTESIAN_POINT ( 'NONE',  ( 4.553261556744873317, 42.43205150231990075, -11.36048287389704292 ) ) ;
#56037=CARTESIAN_POINT ( 'NONE',  ( 1.112077966505211402, 5.276550529686780067, 43.76286484722197656 ) ) ;
#56043=CARTESIAN_POINT ( 'NONE',  ( -6.057079549204054558, -6.658663215491944065, -18.06912934489077216 ) ) ;
#56047=CARTESIAN_POINT ( 'NONE',  ( 4.226256110419179812, -33.72520557204028790, 28.16802724918466083 ) ) ;
#56054=CARTESIAN_POINT ( 'NONE',  ( 2.879087469061463178, -41.40359735493927928, -14.89442187039979260 ) ) ;
#56056=B_SPLINE_CURVE_WITH_KNOTS ( 'NONE', 3,
 ( #34470, #42636, #28507, #53539, #614, #43568 ),
 .UNSPECIFIED., .F., .F.,
 ( 4, 2, 4 ),
 ( 2.197015137584158753E-17, 0.0002293755540694321316, 0.0004587511081388422540 ),
 .UNSPECIFIED. ) ;
#56058=CONICAL_SURFACE ( 'NONE', #24100, 43.92652462719577500, 1.486293639869522343 ) ;
#56064=CARTESIAN_POINT ( 'NONE',  ( 0.7044674535452954967, 3.876803250505699072, 48.95684956538539012 ) ) ;
#56066=CARTESIAN_POINT ( 'NONE',  ( 0.6026112563231248442, -49.10713455106970571, -0.1741582250239009644 ) ) ;
#56067=B_SPLINE_CURVE_WITH_KNOTS ( 'NONE', 3,
 ( #41550, #46246, #2993, #11807, #55606, #2371 ),
 .UNSPECIFIED., .F., .F.,
 ( 4, 2, 4 ),
 ( 2.611104600503255956E-18, 0.0002447193893791690575, 0.0004894387787583355130 ),
 .UNSPECIFIED. ) ;
#56069=( BOUNDED_SURFACE ( )  B_SPLINE_SURFACE ( 3, 1, ( 
 ( #60775, #46715 ),
 ( #32294, #27898 ),
 ( #52300, #47315 ),
 ( #27281, #22279 ) ),
 .UNSPECIFIED., .F., .F., .F. ) 
 B_SPLINE_SURFACE_WITH_KNOTS ( ( 4, 4 ),
 ( 2, 2 ),
 ( 0.000000000000000000, 1.000000000000000000 ),
 ( 0.000000000000000000, 1.000000000000000000 ),
 .UNSPECIFIED. ) 
 GEOMETRIC_REPRESENTATION_ITEM ( )  RATIONAL_B_SPLINE_SURFACE ( (
 ( 1.000000000000000000, 1.000000000000000000),
 ( 0.9953485035131437453, 0.8621029689291515030),
 ( 0.9953485035131437453, 0.8621029689291515030),
 ( 1.000000000000000000, 1.000000000000000000) ) ) 
 REPRESENTATION_ITEM ( '' )  SURFACE ( )  );
#56070=EDGE_CURVE ( 'NONE', #45566, #20883, #12586, .T. ) ;
#56072=CARTESIAN_POINT ( 'NONE',  ( -6.077587904424778920, -16.14165210942818618, 10.49967087922869702 ) ) ;
#56077=FACE_OUTER_BOUND ( 'NONE', #9084, .T. ) ;
#56080=EDGE_CURVE ( 'NONE', #45127, #43289, #8280, .T. ) ;
#56081=B_SPLINE_CURVE_WITH_KNOTS ( 'NONE', 3,
 ( #6852, #22222, #40737, #25990 ),
 .UNSPECIFIED., .F., .F.,
 ( 4, 4 ),
 ( 0.000000000000000000, 0.005013413432710145910 ),
 .UNSPECIFIED. ) ;
#56089=ORIENTED_EDGE ( 'NONE', *, *, #47277, .F. ) ;
#56091=ORIENTED_EDGE ( 'NONE', *, *, #10057, .F. ) ;
#56098=CARTESIAN_POINT ( 'NONE',  ( -6.079354080745853928, 16.77867255551491255, 9.448232772480407604 ) ) ;
#56105=CARTESIAN_POINT ( 'NONE',  ( -6.063463321072276813, -11.00428472829056759, 15.80272666656551372 ) ) ;
#56111=DIRECTION ( 'NONE',  ( 0.09722883295013590166, -0.1513788123411506925, 0.9836823721188344694 ) ) ;
#56118=CARTESIAN_POINT ( 'NONE',  ( 4.975610109902397937, 47.16372689271652519, 12.96272628450595832 ) ) ;
#56130=CARTESIAN_POINT ( 'NONE',  ( 0.1129192098497455998, -22.45785791439690371, -37.98152716363461678 ) ) ;
#56140=DIRECTION ( 'NONE',  ( 0.000000000000000000, 0.000000000000000000, -1.000000000000000000 ) ) ;
#56150=EDGE_LOOP ( 'NONE', ( #17888, #59657, #5249, #45494 ) ) ;
#56151=B_SPLINE_CURVE_WITH_KNOTS ( 'NONE', 3,
 ( #48570, #23846, #52642, #5936, #10371, #38897, #29460, #47652, #15075, #24144, #33263, #14767, #43283, #5626, #28846, #58256, #52334, #39513, #15387 ),
 .UNSPECIFIED., .F., .F.,
 ( 4, 3, 3, 3, 3, 3, 4 ),
 ( 3.469552829456483146E-18, 0.0002612768053151668301, 0.0003919133833142874560, 0.0005225499612322542483, 0.0006531865391693342238, 0.0008112755173415162795, 0.0009693688056799698626 ),
 .UNSPECIFIED. ) ;
#56153=CARTESIAN_POINT ( 'NONE',  ( -6.063463321072276813, -17.34291445406333310, 8.369215657306909861 ) ) ;
#56160=EDGE_CURVE ( 'NONE', #41822, #28421, #29241, .T. ) ;
#56161=B_SPLINE_CURVE_WITH_KNOTS ( 'NONE', 3,
 ( #51766, #8234, #18278, #12661, #22662, #61458 ),
 .UNSPECIFIED., .F., .F.,
 ( 4, 2, 4 ),
 ( 1.870366591887036261E-17, 0.0002293755540694321316, 0.0004587511081388455608 ),
 .UNSPECIFIED. ) ;
#56183=CARTESIAN_POINT ( 'NONE',  ( 0.8744876279028263033, 3.827863332834932297, 48.94586308039354350 ) ) ;
#56194=CARTESIAN_POINT ( 'NONE',  ( 5.901764892641307547, -28.05153439370029389, 40.13854613210009603 ) ) ;
#56196=ORIENTED_EDGE ( 'NONE', *, *, #34196, .F. ) ;
#56197=CARTESIAN_POINT ( 'NONE',  ( 3.678748215320120529, -46.87105689412023679, 14.20270537354160822 ) ) ;
#56202=CARTESIAN_POINT ( 'NONE',  ( 0.1152809850208375564, -17.65825178363827774, -40.43675835716051381 ) ) ;
#56203=CARTESIAN_POINT ( 'NONE',  ( 0.3676999524040366896, 10.61898383218289155, 42.81574203134493928 ) ) ;
#56207=EDGE_CURVE ( 'NONE', #41822, #27686, #25375, .T. ) ;
#56210=CARTESIAN_POINT ( 'NONE',  ( 4.975610109902397937, -11.44439439467595143, 47.55497076097179843 ) ) ;
#56217=CARTESIAN_POINT ( 'NONE',  ( 4.390527457369402420, -24.87150827751877813, -36.21592760968486857 ) ) ;
#56224=LINE ( 'NONE', #28042, #27435 ) ;
#56227=ORIENTED_EDGE ( 'NONE', *, *, #49273, .T. ) ;
#56233=CARTESIAN_POINT ( 'NONE',  ( 2.648799415243708655, 15.62808678998979239, -46.47881632070836844 ) ) ;
#56236=ORIENTED_EDGE ( 'NONE', *, *, #18952, .F. ) ;
#56241=CARTESIAN_POINT ( 'NONE',  ( 0.7948878604505671408, 43.85325310457696446, -22.08145917833165939 ) ) ;
#56243=CARTESIAN_POINT ( 'NONE',  ( 0.6008122571543327295, 49.03265619930817820, 2.711674114963254389 ) ) ;
#56248=CARTESIAN_POINT ( 'NONE',  ( 4.553261556744875094, 42.54662847375985280, -10.92355122382294752 ) ) ;
#56251=CARTESIAN_POINT ( 'NONE',  ( 5.901764892641307547, -44.13851569553294496, 21.20808571358740124 ) ) ;
#56253=CARTESIAN_POINT ( 'NONE',  ( 0.9268187852002115479, 39.28166228011650674, -20.01762576879431066 ) ) ;
#56254=CARTESIAN_POINT ( 'NONE',  ( 0.1129192098497455998, -35.06977877439224045, -26.77802092202373174 ) ) ;
#56263=ORIENTED_EDGE ( 'NONE', *, *, #39784, .F. ) ;
#56266=CARTESIAN_POINT ( 'NONE',  ( 0.6021447746440204973, -14.22269149442896463, -47.00272530122892789 ) ) ;
#56271=AXIS2_PLACEMENT_3D ( 'NONE', #7215, #36693, #40472 ) ;
#56276=CARTESIAN_POINT ( 'NONE',  ( 0.3676999524040323597, -34.85286720109652947, -27.04123205746306979 ) ) ;
#56283=EDGE_CURVE ( 'NONE', #31513, #46120, #24595, .T. ) ;
#56288=CARTESIAN_POINT ( 'NONE',  ( -6.072942160501519027, -17.35560219702265528, 8.341896347217623742 ) ) ;
#56289=CARTESIAN_POINT ( 'NONE',  ( 0.1368894036331302633, -34.97597666220990220, 26.89874313881377788 ) ) ;
#56293=B_SPLINE_CURVE_WITH_KNOTS ( 'NONE', 3,
 ( #26850, #50338, #2718, #31546, #6468, #16221 ),
 .UNSPECIFIED., .F., .F.,
 ( 4, 2, 4 ),
 ( 2.693102327163510278E-18, 0.0002447193893791694912, 0.0004894387787583362719 ),
 .UNSPECIFIED. ) ;
#56294=CARTESIAN_POINT ( 'NONE',  ( 0.2940135542859016460, 3.434477694418887950, -43.98232499150039132 ) ) ;
#56300=EDGE_CURVE ( 'NONE', #20883, #16844, #737, .T. ) ;
#56303=CARTESIAN_POINT ( 'NONE',  ( 0.6021448801613057400, -1.312835145200685227, -49.08989307900835541 ) ) ;
#56308=CARTESIAN_POINT ( 'NONE',  ( 1.830465331921977690, 39.13607268272329520, 20.21741503879734481 ) ) ;
#56310=CARTESIAN_POINT ( 'NONE',  ( 1.657374760986086271, 28.69055495241272880, -33.43265624766942778 ) ) ;
#56317=EDGE_CURVE ( 'NONE', #3844, #41582, #9733, .T. ) ;
#56318=CARTESIAN_POINT ( 'NONE',  ( 2.185380717157382691, -26.31419589484018928, 35.30414844568801414 ) ) ;
#56328=CARTESIAN_POINT ( 'NONE',  ( 2.299652685299203636, 18.13764577205347805, -45.55554335869198468 ) ) ;
#56341=CARTESIAN_POINT ( 'NONE',  ( 4.226256110419179812, -29.23450101563807024, -32.80504839737084666 ) ) ;
#56343=CARTESIAN_POINT ( 'NONE',  ( 2.185380717157383135, 5.657694518177669885, 43.66703900891589285 ) ) ;
#56345=CARTESIAN_POINT ( 'NONE',  ( 3.727782113643637096, 0.7293963419152633687, 43.95731744411134656 ) ) ;
#56346=ORIENTED_EDGE ( 'NONE', *, *, #15721, .F. ) ;
#56352=CARTESIAN_POINT ( 'NONE',  ( 3.221118495291108719, -34.08871765526027531, 27.79785510217824651 ) ) ;
#56358=CARTESIAN_POINT ( 'NONE',  ( 1.479689385636123067, 43.01073730641239479, -9.573939712912206801 ) ) ;
#56359=CARTESIAN_POINT ( 'NONE',  ( 4.553261556744875094, -39.47791437445886942, -19.26223877088359515 ) ) ;
#56361=CARTESIAN_POINT ( 'NONE',  ( 3.050102900204245682, -41.42303492486365002, -14.81747032362766880 ) ) ;
#56367=CARTESIAN_POINT ( 'NONE',  ( 0.6000166863083106206, 49.04012132094733545, 2.624877622903676766 ) ) ;
#56368=CARTESIAN_POINT ( 'NONE',  ( -6.077587904424778920, -18.27312872431383894, 6.073614082124997537 ) ) ;
#56370=CARTESIAN_POINT ( 'NONE',  ( 0.6000166863083090663, 4.195342255946697740, 48.93079383234981350 ) ) ;
#56381=CARTESIAN_POINT ( 'NONE',  ( 0.7242003506640011246, 46.33602329577892931, -16.24760349279418392 ) ) ;
#56390=EDGE_CURVE ( 'NONE', #14899, #35341, #8958, .T. ) ;
#56391=CARTESIAN_POINT ( 'NONE',  ( -2.739355103387248747, -10.90485690860409029, -10.19468796746063433 ) ) ;
#56395=EDGE_LOOP ( 'NONE', ( #34922, #19685, #26655, #13769, #49499, #49894 ) ) ;
#56397=CARTESIAN_POINT ( 'NONE',  ( 2.648799415243696664, 23.90046839033458426, -42.81687837771707450 ) ) ;
#56402=ORIENTED_EDGE ( 'NONE', *, *, #26805, .T. ) ;
#56404=B_SPLINE_CURVE_WITH_KNOTS ( 'NONE', 3,
 ( #54178, #29777, #35428, #21006 ),
 .UNSPECIFIED., .F., .F.,
 ( 4, 4 ),
 ( 0.000000000000000000, 0.004442905043737213101 ),
 .UNSPECIFIED. ) ;
#56407=CARTESIAN_POINT ( 'NONE',  ( -6.078726893082806448, -14.66019907464893635, -12.48489504803234418 ) ) ;
#56410=CARTESIAN_POINT ( 'NONE',  ( 4.335381028904201628, 29.74326630871473398, -38.92422069808487350 ) ) ;
#56415=CARTESIAN_POINT ( 'NONE',  ( 0.1158403557922069033, -31.67019805176805747, -30.72358804803900867 ) ) ;
#56417=ORIENTED_EDGE ( 'NONE', *, *, #10119, .F. ) ;
#56420=CARTESIAN_POINT ( 'NONE',  ( 0.1139756605157203617, -12.17292277066103701, 42.41196966558549519 ) ) ;
#56421=CARTESIAN_POINT ( 'NONE',  ( 0.6021448801613057400, 46.68736458834386838, -15.22600165578615083 ) ) ;
#56429=CARTESIAN_POINT ( 'NONE',  ( 50.15577769773999961, 0.000000000000000000, 3.000000000000000000 ) ) ;
#56434=EDGE_CURVE ( 'NONE', #59176, #18115, #3056, .T. ) ;
#56435=FACE_OUTER_BOUND ( 'NONE', #30325, .T. ) ;
#56437=( BOUNDED_SURFACE ( )  B_SPLINE_SURFACE ( 3, 1, ( 
 ( #20635, #39770 ),
 ( #11238, #21562 ),
 ( #59137, #49750 ),
 ( #15331, #58207 ) ),
 .UNSPECIFIED., .F., .F., .F. ) 
 B_SPLINE_SURFACE_WITH_KNOTS ( ( 4, 4 ),
 ( 2, 2 ),
 ( 0.000000000000000000, 1.000000000000000000 ),
 ( 0.000000000000000000, 1.000000000000000000 ),
 .UNSPECIFIED. ) 
 GEOMETRIC_REPRESENTATION_ITEM ( )  RATIONAL_B_SPLINE_SURFACE ( (
 ( 1.000000000000000000, 1.000000000000000000),
 ( 0.9754377213608244057, 0.9999580625633939235),
 ( 0.9754377213608244057, 0.9999580625633939235),
 ( 1.000000000000000000, 1.000000000000000000) ) ) 
 REPRESENTATION_ITEM ( '' )  SURFACE ( )  );
#56445=CARTESIAN_POINT ( 'NONE',  ( 4.834790513006553603, 34.26126461650199673, -32.53851698836949424 ) ) ;
#56447=CARTESIAN_POINT ( 'NONE',  ( 2.533389852662419894, -21.44996906063816056, 38.43630261915527768 ) ) ;
#56452=CARTESIAN_POINT ( 'NONE',  ( 4.834790513006553603, -39.34655703395242909, -26.16176199146973147 ) ) ;
#56454=B_SPLINE_CURVE_WITH_KNOTS ( 'NONE', 3,
 ( #23024, #33047, #28022, #27712 ),
 .UNSPECIFIED., .F., .F.,
 ( 4, 4 ),
 ( 2.189128766608093472E-17, 0.004559932413162188537 ),
 .UNSPECIFIED. ) ;
#56456=CARTESIAN_POINT ( 'NONE',  ( 0.6016118706126977189, -39.56281023115544571, 29.09183908585898592 ) ) ;
#56461=CARTESIAN_POINT ( 'NONE',  ( 0.1119898979215350199, -23.35186511842599089, -37.43863918123450674 ) ) ;
#56464=ORIENTED_EDGE ( 'NONE', *, *, #5501, .T. ) ;
#56470=EDGE_CURVE ( 'NONE', #18514, #28003, #60364, .T. ) ;
#56473=VERTEX_POINT ( 'NONE', #35685 ) ;
#56474=CARTESIAN_POINT ( 'NONE',  ( 0.2279481005628783696, -23.51699569010370894, 37.32900214022007646 ) ) ;
#56479=VECTOR ( 'NONE', #22807, 1000.000000000000114 ) ;
#56483=ORIENTED_EDGE ( 'NONE', *, *, #11958, .F. ) ;
#56486=CARTESIAN_POINT ( 'NONE',  ( 1.479689385636123067, 34.30196355977874845, 27.65789473570436385 ) ) ;
#56493=CARTESIAN_POINT ( 'NONE',  ( 4.975610109902397937, -47.89734868211986907, 9.914302615978730415 ) ) ;
#56497=CARTESIAN_POINT ( 'NONE',  ( -6.077587904424778920, 12.01079512011132522, 15.05114022181178335 ) ) ;
#56500=CARTESIAN_POINT ( 'NONE',  ( 0.7044674535452954967, -34.68719619958476130, -34.76494128604877432 ) ) ;
#56502=AXIS2_PLACEMENT_3D ( 'NONE', #21808, #8008, #46243 ) ;
#56507=CARTESIAN_POINT ( 'NONE',  ( 4.975610109902397937, 47.45567470742105343, -11.84940273605426242 ) ) ;
#56514=FACE_OUTER_BOUND ( 'NONE', #438, .T. ) ;
#56520=CARTESIAN_POINT ( 'NONE',  ( 4.553261556744875094, -43.07273893850278768, -8.618510669438375515 ) ) ;
#56522=CARTESIAN_POINT ( 'NONE',  ( 0.7242486021783856032, -13.18373570521661975, -47.29905469699126286 ) ) ;
#56523=CARTESIAN_POINT ( 'NONE',  ( 0.6028777368367060907, -39.30322683055775457, -29.44140265029500725 ) ) ;
#56524=EDGE_CURVE ( 'NONE', #26869, #8116, #28366, .T. ) ;
#56530=CARTESIAN_POINT ( 'NONE',  ( -6.079354080745853928, 16.77752703747136920, -9.450266755763003346 ) ) ;
#56531=( BOUNDED_SURFACE ( )  B_SPLINE_SURFACE ( 3, 1, ( 
 ( #40138, #25376 ),
 ( #2167, #11285 ),
 ( #16292, #29762 ),
 ( #15689, #48875 ) ),
 .UNSPECIFIED., .F., .F., .F. ) 
 B_SPLINE_SURFACE_WITH_KNOTS ( ( 4, 4 ),
 ( 2, 2 ),
 ( 0.000000000000000000, 1.000000000000000000 ),
 ( 0.000000000000000000, 1.000000000000000000 ),
 .UNSPECIFIED. ) 
 GEOMETRIC_REPRESENTATION_ITEM ( )  RATIONAL_B_SPLINE_SURFACE ( (
 ( 1.000000000000000000, 1.000000000000000000),
 ( 0.9953485035131437453, 0.8621029689291515030),
 ( 0.9953485035131437453, 0.8621029689291515030),
 ( 1.000000000000000000, 1.000000000000000000) ) ) 
 REPRESENTATION_ITEM ( '' )  SURFACE ( )  );
#56535=CARTESIAN_POINT ( 'NONE',  ( 0.1158403557922069033, -7.079586543883442218, 43.55249432066416659 ) ) ;
#56538=( BOUNDED_SURFACE ( )  B_SPLINE_SURFACE ( 3, 1, ( 
 ( #46042, #45723 ),
 ( #16586, #39807 ),
 ( #21589, #1847 ),
 ( #40412, #2773 ) ),
 .UNSPECIFIED., .F., .F., .F. ) 
 B_SPLINE_SURFACE_WITH_KNOTS ( ( 4, 4 ),
 ( 2, 2 ),
 ( 0.000000000000000000, 1.000000000000000000 ),
 ( 0.000000000000000000, 1.000000000000000000 ),
 .UNSPECIFIED. ) 
 GEOMETRIC_REPRESENTATION_ITEM ( )  RATIONAL_B_SPLINE_SURFACE ( (
 ( 1.000000000000000000, 1.000000000000000000),
 ( 0.7211978278499970862, 0.9934217856018976445),
 ( 0.7211978278499970862, 0.9934217856018976445),
 ( 1.000000000000000000, 1.000000000000000000) ) ) 
 REPRESENTATION_ITEM ( '' )  SURFACE ( )  );
#56545=AXIS2_PLACEMENT_3D ( 'NONE', #16136, #30214, #44354 ) ;
#56548=VECTOR ( 'NONE', #29508, 1000.000000000000000 ) ;
#56549=CARTESIAN_POINT ( 'NONE',  ( 0.3676999524040366896, 37.41430475689384139, 23.36921870497834774 ) ) ;
#56553=CARTESIAN_POINT ( 'NONE',  ( 0.5997462898726536595, -35.63787911784795170, 33.78599121123970406 ) ) ;
#56555=CARTESIAN_POINT ( 'NONE',  ( 0.6016118706126977189, 48.98309811941713576, 3.493873696555625852 ) ) ;
#56556=FACE_OUTER_BOUND ( 'NONE', #39426, .T. ) ;
#56560=DIRECTION ( 'NONE',  ( -0.1011922191286467460, 0.8049255303601348110, -0.5846836968500794818 ) ) ;
#56565=CARTESIAN_POINT ( 'NONE',  ( 0.5980271706414711508, -43.13192993667259856, 23.48799401353017302 ) ) ;
#56566=CARTESIAN_POINT ( 'NONE',  ( 3.727782113643637540, 38.63515341906938261, -20.97862474498617757 ) ) ;
#56568=ORIENTED_EDGE ( 'NONE', *, *, #11878, .F. ) ;
#56569=ORIENTED_EDGE ( 'NONE', *, *, #27906, .T. ) ;
#56572=CARTESIAN_POINT ( 'NONE',  ( -2.739355103387248747, -14.50431811309219832, -3.531617621606664592 ) ) ;
#56580=CARTESIAN_POINT ( 'NONE',  ( 0.6008123274975391004, -13.55448476036326610, -47.19989930115886523 ) ) ;
#56587=CARTESIAN_POINT ( 'NONE',  ( 0.1139756605157200980, 33.33919145751784896, -28.90421306062476958 ) ) ;
#56588=FACE_OUTER_BOUND ( 'NONE', #18300, .T. ) ;
#56594=ORIENTED_EDGE ( 'NONE', *, *, #8630, .F. ) ;
#56602=FACE_OUTER_BOUND ( 'NONE', #61783, .T. ) ;
#56611=ORIENTED_EDGE ( 'NONE', *, *, #4871, .F. ) ;
#56615=DIRECTION ( 'NONE',  ( 0.000000000000000000, 0.000000000000000000, 1.000000000000000000 ) ) ;
#56620=CARTESIAN_POINT ( 'NONE',  ( 3.240649175237396484, 38.80770280631830360, 20.71779718730070385 ) ) ;
#56621=( BOUNDED_SURFACE ( )  B_SPLINE_SURFACE ( 3, 1, ( 
 ( #50699, #4002 ),
 ( #27523, #46048 ),
 ( #27217, #51315 ),
 ( #26594, #51627 ) ),
 .UNSPECIFIED., .F., .F., .F. ) 
 B_SPLINE_SURFACE_WITH_KNOTS ( ( 4, 4 ),
 ( 2, 2 ),
 ( 0.000000000000000000, 1.000000000000000000 ),
 ( 0.000000000000000000, 1.000000000000000000 ),
 .UNSPECIFIED. ) 
 GEOMETRIC_REPRESENTATION_ITEM ( )  RATIONAL_B_SPLINE_SURFACE ( (
 ( 1.000000000000000000, 1.000000000000000000),
 ( 0.7211978278499970862, 0.9934217856018976445),
 ( 0.7211978278499970862, 0.9934217856018976445),
 ( 1.000000000000000000, 1.000000000000000000) ) ) 
 REPRESENTATION_ITEM ( '' )  SURFACE ( )  );
#56626=EDGE_CURVE ( 'NONE', #34842, #46672, #2957, .T. ) ;
#56629=CARTESIAN_POINT ( 'NONE',  ( 4.975610109902397937, -44.31543648230415755, 20.70245146161774841 ) ) ;
#56636=VERTEX_POINT ( 'NONE', #49671 ) ;
#56639=EDGE_CURVE ( 'NONE', #10029, #1548, #54530, .T. ) ;
#56642=CARTESIAN_POINT ( 'NONE',  ( 0.6000166863083090663, -48.77118664543516502, 5.761495891223071375 ) ) ;
#56643=ORIENTED_EDGE ( 'NONE', *, *, #14014, .F. ) ;
#56645=VERTEX_POINT ( 'NONE', #19649 ) ;
#56646=CARTESIAN_POINT ( 'NONE',  ( 2.114184763561894886, 5.677447754278171364E-15, -44.03514965515262247 ) ) ;
#56647=B_SPLINE_CURVE_WITH_KNOTS ( 'NONE', 3,
 ( #44185, #20350, #39471, #10956 ),
 .UNSPECIFIED., .F., .F.,
 ( 4, 4 ),
 ( 2.199414408396618760E-17, 0.004559932413162187670 ),
 .UNSPECIFIED. ) ;
#56648=ORIENTED_EDGE ( 'NONE', *, *, #35672, .F. ) ;
#56650=CARTESIAN_POINT ( 'NONE',  ( 0.5997462898726536595, -42.52950339524468859, -24.55184251941555118 ) ) ;
#56656=CARTESIAN_POINT ( 'NONE',  ( 3.050102900204245682, 0.4003407177367952485, 43.99164666715468996 ) ) ;
#56664=ORIENTED_EDGE ( 'NONE', *, *, #43988, .T. ) ;
#56665=CARTESIAN_POINT ( 'NONE',  ( 4.694002226626921015, -43.37309735483348305, 14.03777750551250136 ) ) ;
#56667=DIRECTION ( 'NONE',  ( 0.09722883295013592941, -0.8708738917980980432, -0.4817937511296604414 ) ) ;
#56668=CARTESIAN_POINT ( 'NONE',  ( 4.390527457369402420, -43.18387362959315823, 8.083216870278070232 ) ) ;
#56670=DIRECTION ( 'NONE',  ( 0.000000000000000000, 0.000000000000000000, 1.000000000000000000 ) ) ;
#56673=CARTESIAN_POINT ( 'NONE',  ( -6.079354080745853928, -19.21649618062450671, -1.232570398884354379 ) ) ;
#56677=AXIS2_PLACEMENT_3D ( 'NONE', #42414, #22987, #27676 ) ;
#56683=CARTESIAN_POINT ( 'NONE',  ( 0.8753041380234471980, 32.34805756193355819, 36.94240787824763572 ) ) ;
#56684=ORIENTED_EDGE ( 'NONE', *, *, #45527, .F. ) ;
#56692=EDGE_CURVE ( 'NONE', #51070, #37795, #14975, .T. ) ;
#56694=CARTESIAN_POINT ( 'NONE',  ( 0.1156495703730067715, 4.101228919911528159, -43.93316372147072713 ) ) ;
#56699=CARTESIAN_POINT ( 'NONE',  ( 3.678748215320121417, 12.69311693770709404, 47.30219441743878406 ) ) ;
#56703=DIRECTION ( 'NONE',  ( 0.000000000000000000, 0.000000000000000000, -1.000000000000000000 ) ) ;
#56704=CARTESIAN_POINT ( 'NONE',  ( 0.7044674535453004927, -48.59206901384838062, 7.114320189891886415 ) ) ;
#56707=B_SPLINE_CURVE_WITH_KNOTS ( 'NONE', 3,
 ( #37893, #37261, #56951, #41968, #43196, #57239, #4614, #19378, #38494, #19082, #33482, #227, #61034, #46973, #28764, #57548 ),
 .UNSPECIFIED., .F., .F.,
 ( 4, 3, 3, 3, 3, 4 ),
 ( 1.908319024389645146E-17, 0.0002612764279487757107, 0.0003919131003184790824, 0.0005225497727000649306, 0.0007837925190632454627, 0.001045051706266716951 ),
 .UNSPECIFIED. ) ;
#56711=LINE ( 'NONE', #59956, #30828 ) ;
#56718=CARTESIAN_POINT ( 'NONE',  ( 2.648799415243696664, 29.17954675436516609, -39.40902833741801459 ) ) ;
#56721=CARTESIAN_POINT ( 'NONE',  ( 0.6000166863083090663, -39.04292238714128160, -29.79049669240369624 ) ) ;
#56734=CARTESIAN_POINT ( 'NONE',  ( -6.079354080745853928, -19.21649618062452802, 1.232570398884076823 ) ) ;
#56735=CARTESIAN_POINT ( 'NONE',  ( -6.078726893082806448, -18.90156862012328887, -3.677600436084754509 ) ) ;
#56737=VERTEX_POINT ( 'NONE', #13032 ) ;
#56738=CARTESIAN_POINT ( 'NONE',  ( 4.834790513006553603, -47.12142688710416394, -3.487186408507438440 ) ) ;
#56749=LINE ( 'NONE', #42084, #53403 ) ;
#56758=CARTESIAN_POINT ( 'NONE',  ( -6.078726893082806448, 19.09835798914753369, -2.459016752095146252 ) ) ;
#56762=CARTESIAN_POINT ( 'NONE',  ( 0.6026112563231247332, -39.45929242848867347, 29.23192152334880944 ) ) ;
#56766=CARTESIAN_POINT ( 'NONE',  ( 4.834790513006553603, -39.84947630189473244, 25.38914294317774178 ) ) ;
#56775=ORIENTED_EDGE ( 'NONE', *, *, #32008, .T. ) ;
#56780=CARTESIAN_POINT ( 'NONE',  ( 0.1129192098497455998, 15.69290830752535726, -41.23935519181593889 ) ) ;
#56783=CARTESIAN_POINT ( 'NONE',  ( -6.079354080745853928, 17.84825706230192210, 7.227217658694907954 ) ) ;
#56788=VERTEX_POINT ( 'NONE', #8928 ) ;
#56793=CARTESIAN_POINT ( 'NONE',  ( 4.226256110419178924, 34.96636023808753890, 26.61166852505640534 ) ) ;
#56794=CARTESIAN_POINT ( 'NONE',  ( -6.078457390727109555, -14.66526260008060234, -12.47896565858665419 ) ) ;
#56799=ORIENTED_EDGE ( 'NONE', *, *, #9954, .F. ) ;
#56800=CARTESIAN_POINT ( 'NONE',  ( -6.063463321072276813, 11.99415941893250093, -15.06521132651987394 ) ) ;
#56801=CARTESIAN_POINT ( 'NONE',  ( 0.8753041380234471980, 5.600023814136011246, -48.78296896616778611 ) ) ;
#56813=CARTESIAN_POINT ( 'NONE',  ( 0.3676999524040323597, -32.25712563511804376, 30.09033780274075198 ) ) ;
#56819=CARTESIAN_POINT ( 'NONE',  ( -6.057079549204054558, -14.65763772032107148, 12.48939100034742644 ) ) ;
#56824=ORIENTED_EDGE ( 'NONE', *, *, #34684, .F. ) ;
#56827=CARTESIAN_POINT ( 'NONE',  ( 0.6039202388192952409, -1.399875120785617488, -49.08771804122897464 ) ) ;
#56842=CARTESIAN_POINT ( 'NONE',  ( 0.6000166863083090663, -7.321729200003415983, 48.56146376737702752 ) ) ;
#56849=ORIENTED_EDGE ( 'NONE', *, *, #49993, .F. ) ;
#56864=ORIENTED_EDGE ( 'NONE', *, *, #41681, .F. ) ;
#56870=EDGE_LOOP ( 'NONE', ( #16426, #7614, #55354, #25285 ) ) ;
#56872=EDGE_LOOP ( 'NONE', ( #28049, #34411, #17522, #61094 ) ) ;
#56873=CARTESIAN_POINT ( 'NONE',  ( 0.1158816050234198758, -44.12416581690439443, 0.005680447781237294401 ) ) ;
#56874=FACE_OUTER_BOUND ( 'NONE', #31229, .T. ) ;
#56877=VERTEX_POINT ( 'NONE', #49284 ) ;
#56880=CARTESIAN_POINT ( 'NONE',  ( 1.296416391601052487, 43.45757030793557618, 7.331231615969850068 ) ) ;
#56881=CARTESIAN_POINT ( 'NONE',  ( 0.6016118706126977189, -25.75422445077556333, 41.81233045075345700 ) ) ;
#56882=( BOUNDED_SURFACE ( )  B_SPLINE_SURFACE ( 3, 1, ( 
 ( #61900, #37851 ),
 ( #38155, #43155 ),
 ( #23409, #56908 ),
 ( #13407, #57200 ) ),
 .UNSPECIFIED., .F., .F., .F. ) 
 B_SPLINE_SURFACE_WITH_KNOTS ( ( 4, 4 ),
 ( 2, 2 ),
 ( 0.000000000000000000, 1.000000000000000000 ),
 ( 0.000000000000000000, 1.000000000000000000 ),
 .UNSPECIFIED. ) 
 GEOMETRIC_REPRESENTATION_ITEM ( )  RATIONAL_B_SPLINE_SURFACE ( (
 ( 1.000000000000000000, 1.000000000000000000),
 ( 0.9754377213608244057, 0.9999580625633939235),
 ( 0.9754377213608244057, 0.9999580625633939235),
 ( 1.000000000000000000, 1.000000000000000000) ) ) 
 REPRESENTATION_ITEM ( '' )  SURFACE ( )  );
#56895=EDGE_CURVE ( 'NONE', #19147, #12519, #41059, .T. ) ;
#56896=( BOUNDED_SURFACE ( )  B_SPLINE_SURFACE ( 3, 1, ( 
 ( #21923, #31007 ),
 ( #16606, #35731 ),
 ( #54795, #50116 ),
 ( #36349, #55409 ) ),
 .UNSPECIFIED., .F., .F., .F. ) 
 B_SPLINE_SURFACE_WITH_KNOTS ( ( 4, 4 ),
 ( 2, 2 ),
 ( 0.000000000000000000, 1.000000000000000000 ),
 ( 0.000000000000000000, 1.000000000000000000 ),
 .UNSPECIFIED. ) 
 GEOMETRIC_REPRESENTATION_ITEM ( )  RATIONAL_B_SPLINE_SURFACE ( (
 ( 1.000000000000000000, 1.000000000000000000),
 ( 0.9953485035131437453, 0.8621029689291523912),
 ( 0.9953485035131437453, 0.8621029689291523912),
 ( 1.000000000000000000, 1.000000000000000000) ) ) 
 REPRESENTATION_ITEM ( '' )  SURFACE ( )  );
#56898=VERTEX_POINT ( 'NONE', #48070 ) ;
#56906=B_SPLINE_CURVE_WITH_KNOTS ( 'NONE', 3,
 ( #28568, #5359, #43012, #47691, #38013, #4127 ),
 .UNSPECIFIED., .F., .F.,
 ( 4, 2, 4 ),
 ( 8.673617379884035472E-19, 0.0002293801035737091281, 0.0004587602071474173888 ),
 .UNSPECIFIED. ) ;
#56908=CARTESIAN_POINT ( 'NONE',  ( 0.6039202388192952409, 10.75760111029171107, 47.91490093072135181 ) ) ;
#56913=CARTESIAN_POINT ( 'NONE',  ( -6.072942160501519027, 3.058960253794435591, 19.01175753197810181 ) ) ;
#56914=AXIS2_PLACEMENT_3D ( 'NONE', #14013, #39058, #19631 ) ;
#56915=ADVANCED_FACE ( 'NONE', ( #24879 ), #5561, .F. ) ;
#56920=CARTESIAN_POINT ( 'NONE',  ( 0.3676999524040323597, 40.09552319080426486, -18.39292264373764851 ) ) ;
#56922=CARTESIAN_POINT ( 'NONE',  ( 5.901764892641307547, -4.745137497650260272, 48.73884628884923131 ) ) ;
#56924=CARTESIAN_POINT ( 'NONE',  ( 1.112077966505211846, 32.87428506335748324, -29.36514441819868537 ) ) ;
#56929=CARTESIAN_POINT ( 'NONE',  ( 0.6026777506516368677, -45.58364336417871954, -18.26685107741847958 ) ) ;
#56939=CARTESIAN_POINT ( 'NONE',  ( 1.112077966505211624, -26.65465479487276568, 35.10782965229723374 ) ) ;
#56941=CARTESIAN_POINT ( 'NONE',  ( 0.2940135542859015905, 42.11535309265164528, 13.13535620273383664 ) ) ;
#56947=CARTESIAN_POINT ( 'NONE',  ( 0.7242003506639985710, -43.17949308384103801, -23.37826022501576873 ) ) ;
#56951=CARTESIAN_POINT ( 'NONE',  ( 0.6016118706126978299, -7.493489753196714176, -48.53244961984368899 ) ) ;
#56960=CARTESIAN_POINT ( 'NONE',  ( 3.678748215320120529, 42.02540356438220215, 25.14912065163104771 ) ) ;
#56964=CARTESIAN_POINT ( 'NONE',  ( 0.1155031312995260795, -38.52861385246892212, 21.50552364252377657 ) ) ;
#56971=LINE ( 'NONE', #61353, #8773 ) ;
#56972=ORIENTED_EDGE ( 'NONE', *, *, #10260, .F. ) ;
#56975=EDGE_CURVE ( 'NONE', #8504, #23672, #33603, .T. ) ;
#56977=CARTESIAN_POINT ( 'NONE',  ( 2.009741617377216460, 42.94470556311812715, -9.759935538728488069 ) ) ;
#56978=CARTESIAN_POINT ( 'NONE',  ( 1.112077966505211846, -38.91188999537838100, -20.70978372934219891 ) ) ;
#56983=ORIENTED_EDGE ( 'NONE', *, *, #31204, .T. ) ;
#56985=CARTESIAN_POINT ( 'NONE',  ( 4.694002226626921015, 45.25670317367046636, -5.487767241458218592 ) ) ;
#56986=EDGE_CURVE ( 'NONE', #52075, #2327, #57407, .T. ) ;
#56988=EDGE_CURVE ( 'NONE', #37964, #55501, #4369, .T. ) ;
#56995=EDGE_CURVE ( 'NONE', #61378, #57990, #60410, .T. ) ;
#57000=CARTESIAN_POINT ( 'NONE',  ( 4.226256110419179812, 23.13112329552939528, -37.36011757307789338 ) ) ;
#57001=CARTESIAN_POINT ( 'NONE',  ( 0.5997462898726536595, -42.52950339524468859, -24.55184251941555118 ) ) ;
#57010=CARTESIAN_POINT ( 'NONE',  ( -6.077587904424778920, 17.84644683124306397, 7.231898567703008318 ) ) ;
#57019=CARTESIAN_POINT ( 'NONE',  ( 0.3676999524040366896, -43.84864779214676389, -4.821480075983068048 ) ) ;
#57021=CARTESIAN_POINT ( 'NONE',  ( -2.739355103387247858, 14.91194544146095069, -0.6938660547317456739 ) ) ;
#57024=CARTESIAN_POINT ( 'NONE',  ( 4.553261556744875094, 0.000000000000000000, 0.000000000000000000 ) ) ;
#57029=CARTESIAN_POINT ( 'NONE',  ( 0.1140933569871964703, -22.54850122134973489, -37.92776084551650229 ) ) ;
#57030=VERTEX_POINT ( 'NONE', #8524 ) ;
#57032=EDGE_LOOP ( 'NONE', ( #36158, #19140, #34234, #14687 ) ) ;
#57037=EDGE_LOOP ( 'NONE', ( #23074, #41365, #56417, #47875 ) ) ;
#57049=CARTESIAN_POINT ( 'NONE',  ( -2.739355103387248747, 13.56174707817303293, 6.239117176226312012 ) ) ;
#57052=CARTESIAN_POINT ( 'NONE',  ( 0.5997462898726536595, 48.97040376101519144, -3.667585803694250135 ) ) ;
#57053=EDGE_CURVE ( 'NONE', #26589, #885, #61596, .T. ) ;
#57064=ORIENTED_EDGE ( 'NONE', *, *, #31156, .F. ) ;
#57066=CARTESIAN_POINT ( 'NONE',  ( 0.6026777506516367566, -39.25098745825879831, 29.51112288932478478 ) ) ;
#57068=VERTEX_POINT ( 'NONE', #23560 ) ;
#57070=CARTESIAN_POINT ( 'NONE',  ( 2.359973842542475442, -30.55638990495834051, 31.69294764783894180 ) ) ;
#57085=CARTESIAN_POINT ( 'NONE',  ( 0.6000166863083106206, -45.71468846346234471, -17.94410043432203494 ) ) ;
#57086=ORIENTED_EDGE ( 'NONE', *, *, #28573, .T. ) ;
#57089=B_SPLINE_CURVE_WITH_KNOTS ( 'NONE', 3,
 ( #31415, #45235, #54894, #12028, #50512, #31103 ),
 .UNSPECIFIED., .F., .F.,
 ( 4, 2, 4 ),
 ( 1.463672932855430986E-18, 0.0002293801035737111881, 0.0004587602071474209124 ),
 .UNSPECIFIED. ) ;
#57090=EDGE_CURVE ( 'NONE', #45131, #8350, #26821, .T. ) ;
#57097=FACE_OUTER_BOUND ( 'NONE', #32377, .T. ) ;
#57104=ORIENTED_EDGE ( 'NONE', *, *, #4727, .T. ) ;
#57110=EDGE_LOOP ( 'NONE', ( #59827, #60040, #5222, #58791 ) ) ;
#57114=CARTESIAN_POINT ( 'NONE',  ( 0.8753041380234471980, -43.21430456406350373, 23.31656511833038081 ) ) ;
#57122=CARTESIAN_POINT ( 'NONE',  ( -6.057079549204054558, -4.293366707802237947, -18.77227299535338290 ) ) ;
#57126=CARTESIAN_POINT ( 'NONE',  ( 4.834790513006553603, -46.28862912354740189, -9.484310981144691510 ) ) ;
#57127=CARTESIAN_POINT ( 'NONE',  ( -2.601141883200665639, 12.25953444924667401, 8.514648704269756507 ) ) ;
#57128=CARTESIAN_POINT ( 'NONE',  ( 0.3676999524040366896, 10.61898383218289155, 42.81574203134493928 ) ) ;
#57131=FACE_OUTER_BOUND ( 'NONE', #29502, .T. ) ;
#57133=CARTESIAN_POINT ( 'NONE',  ( 0.6029442701453591180, 48.18517623212597556, -9.472804053565065274 ) ) ;
#57139=EDGE_CURVE ( 'NONE', #5538, #8036, #22384, .T. ) ;
#57140=CARTESIAN_POINT ( 'NONE',  ( 4.834790513006553603, -26.65333699373555021, -39.01524020203834908 ) ) ;
#57149=ORIENTED_EDGE ( 'NONE', *, *, #50593, .F. ) ;
#57155=( BOUNDED_SURFACE ( )  B_SPLINE_SURFACE ( 3, 1, ( 
 ( #31210, #6440 ),
 ( #50012, #16500 ),
 ( #45033, #11495 ),
 ( #30277, #26195 ) ),
 .UNSPECIFIED., .F., .F., .F. ) 
 B_SPLINE_SURFACE_WITH_KNOTS ( ( 4, 4 ),
 ( 2, 2 ),
 ( 0.000000000000000000, 1.000000000000000000 ),
 ( 0.000000000000000000, 1.000000000000000000 ),
 .UNSPECIFIED. ) 
 GEOMETRIC_REPRESENTATION_ITEM ( )  RATIONAL_B_SPLINE_SURFACE ( (
 ( 1.000000000000000000, 1.000000000000000000),
 ( 0.9754377213608244057, 0.9999580625633939235),
 ( 0.9754377213608244057, 0.9999580625633939235),
 ( 1.000000000000000000, 1.000000000000000000) ) ) 
 REPRESENTATION_ITEM ( '' )  SURFACE ( )  );
#57157=CARTESIAN_POINT ( 'NONE',  ( 0.1149546198390367369, 33.42001444042882241, 28.81057444454637562 ) ) ;
#57159=CARTESIAN_POINT ( 'NONE',  ( 4.975610109902397937, 0.000000000000000000, 0.000000000000000000 ) ) ;
#57160=CARTESIAN_POINT ( 'NONE',  ( -6.072942160501519915, 19.10003410082481778, 2.448031788263668851 ) ) ;
#57163=CARTESIAN_POINT ( 'NONE',  ( -2.739355103387247858, -0.2155581815327103357, -14.92652342715447134 ) ) ;
#57165=CARTESIAN_POINT ( 'NONE',  ( 0.3676999524040323597, -43.84864779214683495, 4.821480075982420566 ) ) ;
#57169=CARTESIAN_POINT ( 'NONE',  ( 0.1154773475650540393, -44.12381759653407443, 0.1798631532872248806 ) ) ;
#57182=DIRECTION ( 'NONE',  ( 0.000000000000000000, 0.000000000000000000, 1.000000000000000000 ) ) ;
#57184=CARTESIAN_POINT ( 'NONE',  ( 0.5987334363312691865, -0.9689270393919278135, -49.09810675437915251 ) ) ;
#57185=CARTESIAN_POINT ( 'NONE',  ( 0.1129192098497447394, 33.28205046155626690, -28.96993104685574139 ) ) ;
#57189=ORIENTED_EDGE ( 'NONE', *, *, #47688, .F. ) ;
#57190=EDGE_CURVE ( 'NONE', #52200, #33819, #50011, .T. ) ;
#57192=CARTESIAN_POINT ( 'NONE',  ( 2.706805983486679779, -16.28756729630821809, 40.88387536533181787 ) ) ;
#57194=EDGE_CURVE ( 'NONE', #44276, #40973, #42628, .T. ) ;
#57199=CARTESIAN_POINT ( 'NONE',  ( -6.063463321072276813, 5.494009911919050637, 18.45633516078436287 ) ) ;
#57200=CARTESIAN_POINT ( 'NONE',  ( 0.6000166863083106206, 10.41802958826928638, 47.99258423138307705 ) ) ;
#57204=CARTESIAN_POINT ( 'NONE',  ( 0.7948884756798517692, -29.92962957645406519, -38.92192079042860797 ) ) ;
#57205=FACE_OUTER_BOUND ( 'NONE', #11202, .T. ) ;
#57215=CARTESIAN_POINT ( 'NONE',  ( 3.050102900204245682, 32.29689866186377856, -29.87198664306346174 ) ) ;
#57221=VERTEX_POINT ( 'NONE', #33595 ) ;
#57229=CARTESIAN_POINT ( 'NONE',  ( -6.057079549204054558, -1.857573237466950022, -19.16717644221978745 ) ) ;
#57235=B_SPLINE_CURVE_WITH_KNOTS ( 'NONE', 3,
 ( #15774, #16083, #58972, #15158 ),
 .UNSPECIFIED., .F., .F.,
 ( 4, 4 ),
 ( 0.000000000000000000, 0.005013413432710150247 ),
 .UNSPECIFIED. ) ;
#57236=AXIS2_PLACEMENT_3D ( 'NONE', #20049, #44487, #1516 ) ;
#57238=EDGE_CURVE ( 'NONE', #9806, #38401, #58588, .T. ) ;
#57239=CARTESIAN_POINT ( 'NONE',  ( 0.6026112563231247332, -7.665567692565208091, -48.50546429893140044 ) ) ;
#57240=ORIENTED_EDGE ( 'NONE', *, *, #29725, .T. ) ;
#57254=( BOUNDED_SURFACE ( )  B_SPLINE_SURFACE ( 3, 1, ( 
 ( #27017, #36429 ),
 ( #8198, #13541 ),
 ( #41752, #22623 ),
 ( #56735, #17936 ) ),
 .UNSPECIFIED., .F., .F., .F. ) 
 B_SPLINE_SURFACE_WITH_KNOTS ( ( 4, 4 ),
 ( 2, 2 ),
 ( 0.000000000000000000, 1.000000000000000000 ),
 ( 0.000000000000000000, 1.000000000000000000 ),
 .UNSPECIFIED. ) 
 GEOMETRIC_REPRESENTATION_ITEM ( )  RATIONAL_B_SPLINE_SURFACE ( (
 ( 1.000000000000000000, 1.000000000000000000),
 ( 0.9754377213608244057, 0.9999580625633939235),
 ( 0.9754377213608244057, 0.9999580625633939235),
 ( 1.000000000000000000, 1.000000000000000000) ) ) 
 REPRESENTATION_ITEM ( '' )  SURFACE ( )  );
#57259=CARTESIAN_POINT ( 'NONE',  ( 0.8753041380234471980, 16.12068986424767303, 46.38169559399184294 ) ) ;
#57262=CARTESIAN_POINT ( 'NONE',  ( 0.1129192098497447394, -42.55567333040724520, 11.66046547873710537 ) ) ;
#57277=CARTESIAN_POINT ( 'NONE',  ( -6.078726893082806448, -19.21666810860932983, -1.230328440814576041 ) ) ;
#57287=CARTESIAN_POINT ( 'NONE',  ( 2.648799415243696664, 31.92790172190984066, 37.21728838759838709 ) ) ;
#57288=ORIENTED_EDGE ( 'NONE', *, *, #49552, .F. ) ;
#57292=CARTESIAN_POINT ( 'NONE',  ( 0.2279481005628798962, 4.991633957252439302, -43.83591082103482961 ) ) ;
#57294=CARTESIAN_POINT ( 'NONE',  ( 0.7242486021783792749, 32.40042614170994284, 36.89476721988594932 ) ) ;
#57295=DIRECTION ( 'NONE',  ( 0.000000000000000000, 0.000000000000000000, 1.000000000000000000 ) ) ;
#57299=CARTESIAN_POINT ( 'NONE',  ( 3.240649175237395596, 7.998380844884640517, 43.25841907950212573 ) ) ;
#57301=CARTESIAN_POINT ( 'NONE',  ( 0.7044674535453004927, 16.16814117525605354, -46.37234017976553702 ) ) ;
#57302=ORIENTED_EDGE ( 'NONE', *, *, #13452, .T. ) ;
#57303=CARTESIAN_POINT ( 'NONE',  ( 4.553261556744873317, 40.80044851610476542, 16.27461110774448372 ) ) ;
#57306=CARTESIAN_POINT ( 'NONE',  ( 0.8753041380234465318, -14.82204010568780994, 46.81287702094758174 ) ) ;
#57308=ORIENTED_EDGE ( 'NONE', *, *, #19519, .T. ) ;
#57319=FACE_OUTER_BOUND ( 'NONE', #23931, .T. ) ;
#57320=CARTESIAN_POINT ( 'NONE',  ( 0.1147471544378676211, -23.13865296268714289, -37.57066578523163258 ) ) ;
#57325=B_SPLINE_CURVE_WITH_KNOTS ( 'NONE', 3,
 ( #43885, #34773, #930, #14434 ),
 .UNSPECIFIED., .F., .F.,
 ( 4, 4 ),
 ( 0.000000000000000000, 0.005013413432710153717 ),
 .UNSPECIFIED. ) ;
#57338=EDGE_CURVE ( 'NONE', #49479, #39074, #31276, .T. ) ;
#57345=CONICAL_SURFACE ( 'NONE', #8348, 43.92652462719577500, 1.486293639869522343 ) ;
#57347=B_SPLINE_CURVE_WITH_KNOTS ( 'NONE', 3,
 ( #13043, #57140, #14273, #33379 ),
 .UNSPECIFIED., .F., .F.,
 ( 4, 4 ),
 ( 3.469446951953613804E-18, 0.005013413432710145910 ),
 .UNSPECIFIED. ) ;
#57349=CARTESIAN_POINT ( 'NONE',  ( 0.5987334363312691865, -35.69483761714066361, 33.72597624914712355 ) ) ;
#57350=CARTESIAN_POINT ( 'NONE',  ( 0.6252788684277206244, 46.81660596960011844, 14.82058489604466445 ) ) ;
#57352=DIRECTION ( 'NONE',  ( 0.000000000000000000, 0.000000000000000000, 1.000000000000000000 ) ) ;
#57360=CARTESIAN_POINT ( 'NONE',  ( 0.5997462898726536595, -45.71211507932765983, -17.94308126043611296 ) ) ;
#57368=CARTESIAN_POINT ( 'NONE',  ( 0.5549461598389362482, 25.94790012659789014, 35.66404596350370326 ) ) ;
#57370=VERTEX_POINT ( 'NONE', #42859 ) ;
#57372=CARTESIAN_POINT ( 'NONE',  ( 0.5987334363312686314, -31.08900137594245550, 38.01364097161339117 ) ) ;
#57380=FACE_OUTER_BOUND ( 'NONE', #58079, .T. ) ;
#57389=EDGE_CURVE ( 'NONE', #58614, #16223, #61608, .T. ) ;
#57392=CARTESIAN_POINT ( 'NONE',  ( 0.6026777506516367566, 46.66034804694161409, 15.30876581490131905 ) ) ;
#57397=B_SPLINE_CURVE_WITH_KNOTS ( 'NONE', 3,
 ( #580, #48828, #38841, #44169, #15025, #34133, #10312, #48516, #12481, #6810, #50065, #11555, #1814, #41011, #6494, #60071, #54115, #2431, #2740 ),
 .UNSPECIFIED., .F., .F.,
 ( 4, 3, 3, 3, 3, 3, 4 ),
 ( 1.734776414728241573E-18, 0.0002612768053151736064, 0.0003919133833142913049, 0.0005225499612322628135, 0.0006531865391693353080, 0.0008112755173415186647, 0.0009693688056799721394 ),
 .UNSPECIFIED. ) ;
#57398=VERTEX_POINT ( 'NONE', #38164 ) ;
#57407=B_SPLINE_CURVE_WITH_KNOTS ( 'NONE', 3,
 ( #54581, #30792, #49913, #6967 ),
 .UNSPECIFIED., .F., .F.,
 ( 4, 4 ),
 ( 2.186012127670277422E-17, 0.004559932413162186803 ),
 .UNSPECIFIED. ) ;
#57409=VERTEX_POINT ( 'NONE', #57518 ) ;
#57413=CARTESIAN_POINT ( 'NONE',  ( 4.553261556744873317, 42.54662847375970358, 10.92355122382355148 ) ) ;
#57414=CIRCLE ( 'NONE', #6380, 43.92652462719577500 ) ;
#57416=CARTESIAN_POINT ( 'NONE',  ( 0.1129192098497447394, -18.30288010335054949, -40.14917642626718930 ) ) ;
#57422=CARTESIAN_POINT ( 'NONE',  ( 5.901764892641288895, 7.858096707078647825, 48.33468509861089046 ) ) ;
#57426=CARTESIAN_POINT ( 'NONE',  ( 0.2279481005628827273, -35.80664021588747659, 25.77572508238910487 ) ) ;
#57443=CARTESIAN_POINT ( 'NONE',  ( -6.057079549204054558, -18.90023728169077444, 3.689479881436475761 ) ) ;
#57451=CARTESIAN_POINT ( 'NONE',  ( -6.063463321072278589, -16.13029782234875142, -10.51826718817319950 ) ) ;
#57461=CARTESIAN_POINT ( 'NONE',  ( 4.553261556744875094, 43.53643125131386427, 5.841123155974254466 ) ) ;
#57469=ORIENTED_EDGE ( 'NONE', *, *, #31649, .F. ) ;
#57476=CARTESIAN_POINT ( 'NONE',  ( 0.1129192098497455998, 42.02659449688937343, -13.44310763101974260 ) ) ;
#57491=AXIS2_PLACEMENT_3D ( 'NONE', #33383, #61840, #27742 ) ;
#57501=B_SPLINE_CURVE_WITH_KNOTS ( 'NONE', 3,
 ( #8964, #41572, #61562, #23375, #28073, #41889 ),
 .UNSPECIFIED., .F., .F.,
 ( 4, 2, 4 ),
 ( 3.361026734705063745E-18, 0.0002447193893791674854, 0.0004894387787583316099 ),
 .UNSPECIFIED. ) ;
#57503=CARTESIAN_POINT ( 'NONE',  ( 4.975610109902397937, 30.04451009524531102, -38.59762713269398660 ) ) ;
#57509=( BOUNDED_SURFACE ( )  B_SPLINE_SURFACE ( 3, 1, ( 
 ( #3145, #22272 ),
 ( #50759, #37012 ),
 ( #2834, #7849 ),
 ( #56072, #17268 ) ),
 .UNSPECIFIED., .F., .F., .F. ) 
 B_SPLINE_SURFACE_WITH_KNOTS ( ( 4, 4 ),
 ( 2, 2 ),
 ( 0.000000000000000000, 1.000000000000000000 ),
 ( 0.000000000000000000, 1.000000000000000000 ),
 .UNSPECIFIED. ) 
 GEOMETRIC_REPRESENTATION_ITEM ( )  RATIONAL_B_SPLINE_SURFACE ( (
 ( 1.000000000000000000, 1.000000000000000000),
 ( 0.7211978278499968642, 0.9934217856018975334),
 ( 0.7211978278499968642, 0.9934217856018975334),
 ( 1.000000000000000000, 1.000000000000000000) ) ) 
 REPRESENTATION_ITEM ( '' )  SURFACE ( )  );
#57510=EDGE_CURVE ( 'NONE', #50764, #14922, #41778, .T. ) ;
#57515=ORIENTED_EDGE ( 'NONE', *, *, #18124, .T. ) ;
#57518=CARTESIAN_POINT ( 'NONE',  ( 0.8744876279028263033, 36.80052600666216023, 32.49725120702480297 ) ) ;
#57523=CARTESIAN_POINT ( 'NONE',  ( 0.1155031312995260795, 9.982755425405617444, -42.98006778319857091 ) ) ;
#57543=CARTESIAN_POINT ( 'NONE',  ( 1.830465331921977246, 2.999073074481199086, 43.94748703364405884 ) ) ;
#57547=ORIENTED_EDGE ( 'NONE', *, *, #9504, .F. ) ;
#57548=CARTESIAN_POINT ( 'NONE',  ( 0.5997462898726536595, -8.352924653000044941, -48.39194436975655123 ) ) ;
#57550=CARTESIAN_POINT ( 'NONE',  ( 0.3676999524040366896, -42.45338881270437525, 11.98584004733023534 ) ) ;
#57560=CARTESIAN_POINT ( 'NONE',  ( 4.553261556744873317, 22.57774691820481294, -37.68003330573274923 ) ) ;
#57572=ORIENTED_EDGE ( 'NONE', *, *, #6258, .F. ) ;
#57574=CARTESIAN_POINT ( 'NONE',  ( 3.390910168358337362, 42.74744500291679827, -10.33213831964325813 ) ) ;
#57575=DIRECTION ( 'NONE',  ( -1.000000000000000000, -0.000000000000000000, -0.000000000000000000 ) ) ;
#57577=FACE_OUTER_BOUND ( 'NONE', #55086, .T. ) ;
#57578=CARTESIAN_POINT ( 'NONE',  ( 0.8744876279028306332, -0.6840263623749832655, 49.09055060105833235 ) ) ;
#57584=FACE_OUTER_BOUND ( 'NONE', #23568, .T. ) ;
#57585=DIRECTION ( 'NONE',  ( 0.1011922191286468292, 0.7491372366378290515, -0.6546400044837293875 ) ) ;
#57591=ORIENTED_EDGE ( 'NONE', *, *, #47959, .T. ) ;
#57594=( BOUNDED_SURFACE ( )  B_SPLINE_SURFACE ( 3, 1, ( 
 ( #26061, #31074 ),
 ( #50178, #6928 ),
 ( #2856, #55788 ),
 ( #55476, #26991 ) ),
 .UNSPECIFIED., .F., .F., .F. ) 
 B_SPLINE_SURFACE_WITH_KNOTS ( ( 4, 4 ),
 ( 2, 2 ),
 ( 0.000000000000000000, 1.000000000000000000 ),
 ( 0.000000000000000000, 1.000000000000000000 ),
 .UNSPECIFIED. ) 
 GEOMETRIC_REPRESENTATION_ITEM ( )  RATIONAL_B_SPLINE_SURFACE ( (
 ( 1.000000000000000000, 1.000000000000000000),
 ( 0.7211978278499968642, 0.9934217856018975334),
 ( 0.7211978278499968642, 0.9934217856018975334),
 ( 1.000000000000000000, 1.000000000000000000) ) ) 
 REPRESENTATION_ITEM ( '' )  SURFACE ( )  );
#57595=CARTESIAN_POINT ( 'NONE',  ( 3.240649175237395596, -40.05536204209594331, -18.18881219525537318 ) ) ;
#57596=VECTOR ( 'NONE', #20001, 1000.000000000000000 ) ;
#57597=CARTESIAN_POINT ( 'NONE',  ( 0.6008123274975391004, -47.38919646901772609, -12.87705747363489373 ) ) ;
#57603=CARTESIAN_POINT ( 'NONE',  ( 0.3676999524040366896, 43.13409918076302318, -9.241215893319285613 ) ) ;
#57605=VERTEX_POINT ( 'NONE', #2053 ) ;
#57611=CARTESIAN_POINT ( 'NONE',  ( 0.8753041380234530822, 16.12068986424834804, -46.38169559399161557 ) ) ;
#57613=VERTEX_POINT ( 'NONE', #1139 ) ;
#57623=LINE ( 'NONE', #19450, #35786 ) ;
#57624=EDGE_CURVE ( 'NONE', #23099, #39332, #11140, .T. ) ;
#57626=VERTEX_POINT ( 'NONE', #44409 ) ;
#57640=CARTESIAN_POINT ( 'NONE',  ( 0.1157506346131639274, 25.16801674065300531, -36.24240048817191706 ) ) ;
#57650=CARTESIAN_POINT ( 'NONE',  ( 2.299652685299199195, 41.78300659542229312, -25.66051606466733759 ) ) ;
#57653=VECTOR ( 'NONE', #20648, 999.9999999999998863 ) ;
#57654=DIRECTION ( 'NONE',  ( -0.9990097760809875105, 5.448601141172011466E-18, -0.04449120468828677427 ) ) ;
#57658=EDGE_CURVE ( 'NONE', #56645, #33616, #43533, .T. ) ;
#57659=CARTESIAN_POINT ( 'NONE',  ( 0.1365634738349373045, 34.00677838472008574, -28.11408265470851475 ) ) ;
#57661=DIRECTION ( 'NONE',  ( -1.000000000000000000, -0.000000000000000000, -0.000000000000000000 ) ) ;
#57667=CARTESIAN_POINT ( 'NONE',  ( 0.6000166863083106206, -48.63754814943186489, 6.797969676318823318 ) ) ;
#57671=CARTESIAN_POINT ( 'NONE',  ( 4.390527457369401532, 18.07658334720816384, -40.04275803588028992 ) ) ;
#57674=CARTESIAN_POINT ( 'NONE',  ( 1.830465331921977912, -21.77017147165016198, -38.29406860041564187 ) ) ;
#57675=CARTESIAN_POINT ( 'NONE',  ( 3.390910168358336474, 26.75129140044841947, 34.90652582171320972 ) ) ;
#57681=ORIENTED_EDGE ( 'NONE', *, *, #57190, .T. ) ;
#57688=FACE_OUTER_BOUND ( 'NONE', #41743, .T. ) ;
#57689=ORIENTED_EDGE ( 'NONE', *, *, #22325, .T. ) ;
#57690=FACE_OUTER_BOUND ( 'NONE', #16044, .T. ) ;
#57693=CARTESIAN_POINT ( 'NONE',  ( 0.1129192098497447394, 9.345467776859020859, -43.12324222292247811 ) ) ;
#57696=EDGE_CURVE ( 'NONE', #30901, #29160, #3286, .T. ) ;
#57700=ORIENTED_EDGE ( 'NONE', *, *, #11796, .F. ) ;
#57709=DIRECTION ( 'NONE',  ( 0.000000000000000000, 0.000000000000000000, -1.000000000000000000 ) ) ;
#57713=B_SPLINE_CURVE_WITH_KNOTS ( 'NONE', 3,
 ( #23638, #42765, #61822, #18959 ),
 .UNSPECIFIED., .F., .F.,
 ( 4, 4 ),
 ( 2.101926620404615003E-17, 0.004559932413162187670 ),
 .UNSPECIFIED. ) ;
#57714=CARTESIAN_POINT ( 'NONE',  ( 4.553261556744875094, -9.994631851593741345, 42.77437199977043036 ) ) ;
#57715=ORIENTED_EDGE ( 'NONE', *, *, #45294, .T. ) ;
#57717=CARTESIAN_POINT ( 'NONE',  ( 0.1155031312995260795, 37.07158905255104031, -23.92987500281993363 ) ) ;
#57719=CARTESIAN_POINT ( 'NONE',  ( 0.6021448801613057400, -35.09405629939740123, -34.35037628733741144 ) ) ;
#57722=ORIENTED_EDGE ( 'NONE', *, *, #32341, .T. ) ;
#57723=DIRECTION ( 'NONE',  ( 0.1011922191286468292, -0.1714634860903167801, -0.9799797996517967125 ) ) ;
#57734=CARTESIAN_POINT ( 'NONE',  ( -2.739355103387247858, 13.56174707817311642, -6.239117176226129047 ) ) ;
#57744=CARTESIAN_POINT ( 'NONE',  ( -2.739355103387247858, -13.13414140434199950, 7.095202359465602626 ) ) ;
#57750=CARTESIAN_POINT ( 'NONE',  ( 0.6008123274975392114, 48.28333653898867794, -8.959573863818473427 ) ) ;
#57752=CARTESIAN_POINT ( 'NONE',  ( 0.6029443199889047422, -1.573994357226665697, -49.08217786139712047 ) ) ;
#57755=ORIENTED_EDGE ( 'NONE', *, *, #39106, .T. ) ;
#57762=CARTESIAN_POINT ( 'NONE',  ( 0.8744876279028263033, 32.34273794994744833, 36.93639603806145288 ) ) ;
#57767=ORIENTED_EDGE ( 'NONE', *, *, #51678, .T. ) ;
#57768=EDGE_CURVE ( 'NONE', #4686, #26055, #16342, .T. ) ;
#57770=CARTESIAN_POINT ( 'NONE',  ( 0.3676999524040366896, 21.13209774130265473, 38.72189339863005841 ) ) ;
#57782=VECTOR ( 'NONE', #18628, 1000.000000000000114 ) ;
#57784=CARTESIAN_POINT ( 'NONE',  ( 0.1155031312995260795, 41.92908014207336720, -13.74386666740468854 ) ) ;
#57791=CARTESIAN_POINT ( 'NONE',  ( 4.975610109902397937, 7.237810502494091303, 48.37420290059321104 ) ) ;
#57793=B_SPLINE_CURVE_WITH_KNOTS ( 'NONE', 3,
 ( #58308, #11665, #48942, #49244, #11350, #25752 ),
 .UNSPECIFIED., .F., .F.,
 ( 4, 2, 4 ),
 ( 3.686287386450715076E-18, 0.0002447193893791697623, 0.0004894387787583358383 ),
 .UNSPECIFIED. ) ;
#57796=EDGE_LOOP ( 'NONE', ( #16625, #4549, #44631, #38948 ) ) ;
#57800=CARTESIAN_POINT ( 'NONE',  ( 0.1135584504625008206, 9.396960478524508886, 43.11205383532893620 ) ) ;
#57805=LINE ( 'NONE', #52190, #31936 ) ;
#57814=VECTOR ( 'NONE', #44382, 1000.000000000000114 ) ;
#57827=ADVANCED_FACE ( 'NONE', ( #47167 ), #9168, .F. ) ;
#57829=EDGE_CURVE ( 'NONE', #52266, #39018, #34263, .T. ) ;
#57837=AXIS2_PLACEMENT_3D ( 'NONE', #3358, #50672, #36928 ) ;
#57839=EDGE_CURVE ( 'NONE', #54854, #30625, #20065, .T. ) ;
#57850=CARTESIAN_POINT ( 'NONE',  ( 4.975610109902397937, 0.000000000000000000, 0.000000000000000000 ) ) ;
#57862=CARTESIAN_POINT ( 'NONE',  ( 4.834790513006553603, -46.46485498443001916, 8.579428430861252508 ) ) ;
#57877=DIRECTION ( 'NONE',  ( 0.09722883295013594329, 0.8933953294778640419, -0.4386243715416339728 ) ) ;
#57878=EDGE_LOOP ( 'NONE', ( #43057, #31568, #39662, #58957 ) ) ;
#57881=CARTESIAN_POINT ( 'NONE',  ( 2.299652685299201860, -26.51150749201314838, 41.24829324177042622 ) ) ;
#57882=ORIENTED_EDGE ( 'NONE', *, *, #56639, .F. ) ;
#57885=CARTESIAN_POINT ( 'NONE',  ( 0.5997462898726536595, 5.235280152387709940, -48.82769165002913070 ) ) ;
#57886=LINE ( 'NONE', #24393, #18792 ) ;
#57890=ORIENTED_EDGE ( 'NONE', *, *, #57696, .F. ) ;
#57893=EDGE_LOOP ( 'NONE', ( #43634, #21675, #35982, #29606 ) ) ;
#57894=CARTESIAN_POINT ( 'NONE',  ( 1.830465331921977468, -8.246493558563114945, 43.27090708393997431 ) ) ;
#57903=EDGE_CURVE ( 'NONE', #1293, #29313, #8131, .T. ) ;
#57904=CARTESIAN_POINT ( 'NONE',  ( 0.5987334363312689645, -47.65150816038625692, 11.86999058604166279 ) ) ;
#57905=CARTESIAN_POINT ( 'NONE',  ( 0.1129192098497447394, -1.898585089631814826, -44.08341142019957459 ) ) ;
#57908=CARTESIAN_POINT ( 'NONE',  ( -6.057079549204054558, 7.802675369763562685, 17.60538236374954479 ) ) ;
#57910=VECTOR ( 'NONE', #61239, 1000.000000000000114 ) ;
#57928=VECTOR ( 'NONE', #8057, 1000.000000000000114 ) ;
#57932=ORIENTED_EDGE ( 'NONE', *, *, #32694, .F. ) ;
#57933=CARTESIAN_POINT ( 'NONE',  ( 0.1154773475650539977, 29.53133311701487784, -32.78481347175886640 ) ) ;
#57939=LINE ( 'NONE', #33829, #41716 ) ;
#57942=EDGE_CURVE ( 'NONE', #11949, #26869, #47677, .T. ) ;
#57945=CARTESIAN_POINT ( 'NONE',  ( 4.226256110419179812, -36.59953355730235813, -24.31668960559979453 ) ) ;
#57950=CARTESIAN_POINT ( 'NONE',  ( 0.5980271706414711508, 5.412294693955235658, -48.81348490926914963 ) ) ;
#57954=EDGE_LOOP ( 'NONE', ( #12785, #35738, #39901, #2193 ) ) ;
#57955=CIRCLE ( 'NONE', #36862, 48.91267123290010943 ) ;
#57960=FACE_OUTER_BOUND ( 'NONE', #51021, .T. ) ;
#57970=CARTESIAN_POINT ( 'NONE',  ( 0.3676999524040323597, -13.34038000160386339, 42.04741186726771929 ) ) ;
#57971=CARTESIAN_POINT ( 'NONE',  ( 1.657374760986086049, -8.250434774462597431, -43.27609933074585058 ) ) ;
#57980=CARTESIAN_POINT ( 'NONE',  ( 0.1152339509894530906, -43.78992250378124851, -5.420828125671850017 ) ) ;
#57981=DIRECTION ( 'NONE',  ( -1.000000000000000000, -0.000000000000000000, -0.000000000000000000 ) ) ;
#57984=CARTESIAN_POINT ( 'NONE',  ( -6.077587904424778920, 17.85108912406241899, 7.220432014686572586 ) ) ;
#57985=CARTESIAN_POINT ( 'NONE',  ( 0.5987334308729317378, -39.71456587457169007, -28.88453156906020780 ) ) ;
#57987=CARTESIAN_POINT ( 'NONE',  ( 0.2940133293163009753, -44.10887658731336103, -0.8047085082206926199 ) ) ;
#57990=VERTEX_POINT ( 'NONE', #26417 ) ;
#57993=CARTESIAN_POINT ( 'NONE',  ( 1.834102595619085507, 26.25798196791792449, 35.36546518611314838 ) ) ;
#57996=( BOUNDED_SURFACE ( )  B_SPLINE_SURFACE ( 3, 1, ( 
 ( #17924, #12301 ),
 ( #50489, #7562 ),
 ( #2866, #22000 ),
 ( #9118, #37654 ) ),
 .UNSPECIFIED., .F., .F., .F. ) 
 B_SPLINE_SURFACE_WITH_KNOTS ( ( 4, 4 ),
 ( 2, 2 ),
 ( 0.000000000000000000, 1.000000000000000000 ),
 ( 0.000000000000000000, 1.000000000000000000 ),
 .UNSPECIFIED. ) 
 GEOMETRIC_REPRESENTATION_ITEM ( )  RATIONAL_B_SPLINE_SURFACE ( (
 ( 1.000000000000000000, 1.000000000000000000),
 ( 0.9953485035131437453, 0.8621029689291523912),
 ( 0.9953485035131437453, 0.8621029689291523912),
 ( 1.000000000000000000, 1.000000000000000000) ) ) 
 REPRESENTATION_ITEM ( '' )  SURFACE ( )  );
#58000=VERTEX_POINT ( 'NONE', #42696 ) ;
#58002=CARTESIAN_POINT ( 'NONE',  ( -6.078726893082806448, 19.09835798914749816, 2.459016752095430025 ) ) ;
#58004=CARTESIAN_POINT ( 'NONE',  ( 0.3676999524040323597, -44.10520818713899871, -0.8253448321555690859 ) ) ;
#58006=B_SPLINE_CURVE_WITH_KNOTS ( 'NONE', 3,
 ( #6822, #49456, #26575, #54441 ),
 .UNSPECIFIED., .F., .F.,
 ( 4, 4 ),
 ( 0.000000000000000000, 0.004442905043737213969 ),
 .UNSPECIFIED. ) ;
#58009=LINE ( 'NONE', #29212, #37715 ) ;
#58013=EDGE_LOOP ( 'NONE', ( #6372, #39201, #11733, #43031 ) ) ;
#58017=CARTESIAN_POINT ( 'NONE',  ( 4.975610109902397937, 45.55079628452109830, 17.82061629079735354 ) ) ;
#58018=CARTESIAN_POINT ( 'NONE',  ( 4.553261556744873317, 27.56395660609696563, 34.20186927699770507 ) ) ;
#58020=EDGE_CURVE ( 'NONE', #58000, #9797, #5041, .T. ) ;
#58022=CARTESIAN_POINT ( 'NONE',  ( -6.078726893082806448, 7.791390017580090088, 17.60932374802262146 ) ) ;
#58023=CARTESIAN_POINT ( 'NONE',  ( 4.975610109902397937, -36.86873347511098586, -32.14258700041121131 ) ) ;
#58029=CARTESIAN_POINT ( 'NONE',  ( 1.296416391601052487, -42.89856844656344492, -10.10050490379914656 ) ) ;
#58030=CARTESIAN_POINT ( 'NONE',  ( 0.1140933569871964703, 37.18555914042932642, -23.75256073558256986 ) ) ;
#58034=ORIENTED_EDGE ( 'NONE', *, *, #24398, .T. ) ;
#58040=CARTESIAN_POINT ( 'NONE',  ( 0.1149546198390367230, -31.88653494661792465, 30.49910579215944040 ) ) ;
#58041=CARTESIAN_POINT ( 'NONE',  ( 4.335381028904201628, 38.64381571559615480, -30.10668288940825832 ) ) ;
#58048=ORIENTED_EDGE ( 'NONE', *, *, #5545, .T. ) ;
#58053=B_SPLINE_CURVE_WITH_KNOTS ( 'NONE', 3,
 ( #13936, #51803, #52416, #9510, #61499, #8902, #28012, #37750, #47133, #4177, #42438, #28614, #47741, #36816, #29851, #43364, #719, #30153, #29539, #5409, #48649, #44296, #39590, #48966, #49262 ),
 .UNSPECIFIED., .F., .F.,
 ( 4, 3, 3, 3, 3, 3, 3, 3, 4 ),
 ( 5.818439421673296370E-18, 0.0005656085177311394232, 0.001131215744874499622, 0.001696821861372765916, 0.002262427090022498151, 0.002828031679238745925, 0.003393635864401604862, 0.003977030878808132490, 0.004561030005651159000 ),
 .UNSPECIFIED. ) ;
#58056=DIRECTION ( 'NONE',  ( 0.000000000000000000, 0.000000000000000000, -1.000000000000000000 ) ) ;
#58062=CARTESIAN_POINT ( 'NONE',  ( 0.6027444965799114707, 22.82978205664869265, -43.47803545623195021 ) ) ;
#58068=ORIENTED_EDGE ( 'NONE', *, *, #43236, .T. ) ;
#58072=ADVANCED_FACE ( 'NONE', ( #22656 ), #43600, .F. ) ;
#58073=ORIENTED_EDGE ( 'NONE', *, *, #17002, .F. ) ;
#58079=EDGE_LOOP ( 'NONE', ( #13435, #57469, #45927, #2153 ) ) ;
#58084=CARTESIAN_POINT ( 'NONE',  ( 0.2285344041767093937, -44.11262685805537132, 0.7598170683974434514 ) ) ;
#58090=CARTESIAN_POINT ( 'NONE',  ( 0.6000166863083090663, -19.40010892967683986, 45.11606427011477649 ) ) ;
#58091=CARTESIAN_POINT ( 'NONE',  ( 1.112077966505211624, 44.04403987788247576, 1.775634073803769697 ) ) ;
#58096=DIRECTION ( 'NONE',  ( -0.1011922191286467321, -0.9935638751191113727, 0.05090148176737956109 ) ) ;
#58101=EDGE_CURVE ( 'NONE', #23682, #27212, #5762, .T. ) ;
#58106=CARTESIAN_POINT ( 'NONE',  ( 0.5997462898726536595, 4.195097405483644515, -48.92803682862019343 ) ) ;
#58111=EDGE_CURVE ( 'NONE', #13041, #55332, #20026, .T. ) ;
#58117=CARTESIAN_POINT ( 'NONE',  ( 5.901764892641307547, 48.96927204603444039, 0.04315925332823173505 ) ) ;
#58118=CARTESIAN_POINT ( 'NONE',  ( 0.1152809850208375703, 33.74116055389966107, -28.43377159234631435 ) ) ;
#58119=CARTESIAN_POINT ( 'NONE',  ( 4.553261556744875094, 22.57774691820428714, 37.68003330573307608 ) ) ;
#58121=CARTESIAN_POINT ( 'NONE',  ( -6.057079549204054558, 13.82732400278065832, -13.40284828019269625 ) ) ;
#58127=B_SPLINE_CURVE_WITH_KNOTS ( 'NONE', 3,
 ( #5858, #25007, #44147, #15614, #45987, #7728, #12457, #26222, #12775, #31870, #17155, #3329, #55960, #3029, #36268, #40670 ),
 .UNSPECIFIED., .F., .F.,
 ( 4, 3, 3, 3, 3, 4 ),
 ( 2.081781105835003463E-17, 0.0002612764279487748975, 0.0003919131003184784861, 0.0005225497727000651474, 0.0007837925190632454627, 0.001045051706266716084 ),
 .UNSPECIFIED. ) ;
#58131=CARTESIAN_POINT ( 'NONE',  ( 0.8744876279028306332, 10.05549467470575209, -48.05452192277493850 ) ) ;
#58137=CARTESIAN_POINT ( 'NONE',  ( 0.3676999524040366896, -13.34038000160327364, -42.04741186726791113 ) ) ;
#58142=CARTESIAN_POINT ( 'NONE',  ( -6.077587904424778920, 18.62472241188256206, -4.890371813497390363 ) ) ;
#58146=CARTESIAN_POINT ( 'NONE',  ( 0.1145239942831223490, -23.15231174846270079, 37.56216103216998903 ) ) ;
#58147=CARTESIAN_POINT ( 'NONE',  ( 0.5987334308729315158, -35.69483792408773581, -33.72597592572879677 ) ) ;
#58148=B_SPLINE_CURVE_WITH_KNOTS ( 'NONE', 3,
 ( #49117, #16224, #6473, #6169, #25305, #54098 ),
 .UNSPECIFIED., .F., .F.,
 ( 4, 2, 4 ),
 ( 4.878909776184769953E-19, 0.0002293801035737079354, 0.0004587602071474153830 ),
 .UNSPECIFIED. ) ;
#58149=CARTESIAN_POINT ( 'NONE',  ( 0.1149546198390367369, 10.08539897964233134, -42.95615546629666426 ) ) ;
#58165=CARTESIAN_POINT ( 'NONE',  ( 0.8744876279028306332, 43.84003649649945089, -22.09980204357244560 ) ) ;
#58166=B_SPLINE_CURVE_WITH_KNOTS ( 'NONE', 3,
 ( #41763, #22020, #50815, #31101, #3809, #8508 ),
 .UNSPECIFIED., .F., .F.,
 ( 4, 2, 4 ),
 ( 0.000000000000000000, 0.0002293801035737120554, 0.0004587602071474241108 ),
 .UNSPECIFIED. ) ;
#58180=EDGE_CURVE ( 'NONE', #33349, #54794, #8470, .T. ) ;
#58181=CARTESIAN_POINT ( 'NONE',  ( -6.077587904424778920, 18.62472241188249811, 4.890371813497665698 ) ) ;
#58188=CARTESIAN_POINT ( 'NONE',  ( 3.678834586032787346, -48.94070755074899637, -1.849192813206288255 ) ) ;
#58191=CARTESIAN_POINT ( 'NONE',  ( 0.1158403557922069033, -38.46476121139301085, 21.61949241157930857 ) ) ;
#58204=FACE_OUTER_BOUND ( 'NONE', #24683, .T. ) ;
#58207=CARTESIAN_POINT ( 'NONE',  ( 0.6000166863083106206, -47.63401213562570291, 11.95091500980227650 ) ) ;
#58211=CARTESIAN_POINT ( 'NONE',  ( -6.072942160501519915, -11.02874586101335908, -15.78514893886658399 ) ) ;
#58212=CARTESIAN_POINT ( 'NONE',  ( 5.901764892641288895, -4.745137497649592362, -48.73884628884928816 ) ) ;
#58213=DIRECTION ( 'NONE',  ( -1.000000000000000000, -0.000000000000000000, -0.000000000000000000 ) ) ;
#58221=CARTESIAN_POINT ( 'NONE',  ( -6.063463321072278589, -12.93474753578249015, -14.26578980165622035 ) ) ;
#58222=CARTESIAN_POINT ( 'NONE',  ( 0.9268187852002115479, 40.14212586201818311, 18.23085473000422496 ) ) ;
#58224=CARTESIAN_POINT ( 'NONE',  ( 0.5987334363312690755, 32.56457253214104242, 36.75746893178311581 ) ) ;
#58238=DIRECTION ( 'NONE',  ( 0.000000000000000000, 0.000000000000000000, -1.000000000000000000 ) ) ;
#58245=CARTESIAN_POINT ( 'NONE',  ( -6.079354080745853928, 17.84913307564929141, -7.225053888790356815 ) ) ;
#58246=FACE_OUTER_BOUND ( 'NONE', #25140, .T. ) ;
#58250=CARTESIAN_POINT ( 'NONE',  ( 1.296416391601053153, -35.97301573625679083, -25.46074454754181460 ) ) ;
#58252=CARTESIAN_POINT ( 'NONE',  ( -6.078726893082806448, 17.85000270430361269, -7.222980321520601876 ) ) ;
#58254=EDGE_CURVE ( 'NONE', #19623, #21737, #61797, .T. ) ;
#58255=CARTESIAN_POINT ( 'NONE',  ( -6.077587904424778920, -18.27312872431374657, -6.073614082125261326 ) ) ;
#58256=CARTESIAN_POINT ( 'NONE',  ( 0.1145239942831223490, -18.15888904951765781, 40.21442812215511964 ) ) ;
#58261=( BOUNDED_SURFACE ( )  B_SPLINE_SURFACE ( 3, 1, ( 
 ( #27329, #3499 ),
 ( #2033, #21163 ),
 ( #40305, #17946 ),
 ( #37062, #59668 ) ),
 .UNSPECIFIED., .F., .F., .F. ) 
 B_SPLINE_SURFACE_WITH_KNOTS ( ( 4, 4 ),
 ( 2, 2 ),
 ( 0.000000000000000000, 1.000000000000000000 ),
 ( 0.000000000000000000, 1.000000000000000000 ),
 .UNSPECIFIED. ) 
 GEOMETRIC_REPRESENTATION_ITEM ( )  RATIONAL_B_SPLINE_SURFACE ( (
 ( 1.000000000000000000, 1.000000000000000000),
 ( 0.7211978278499968642, 0.9934217856018975334),
 ( 0.7211978278499968642, 0.9934217856018975334),
 ( 1.000000000000000000, 1.000000000000000000) ) ) 
 REPRESENTATION_ITEM ( '' )  SURFACE ( )  );
#58262=LINE ( 'NONE', #34495, #45530 ) ;
#58269=ORIENTED_EDGE ( 'NONE', *, *, #60209, .F. ) ;
#58270=CARTESIAN_POINT ( 'NONE',  ( 0.1155031312995260795, -40.96235978927564503, 16.40203380760271301 ) ) ;
#58282=CARTESIAN_POINT ( 'NONE',  ( 0.1158816050234198619, 39.75696437711800257, 19.13964014347531162 ) ) ;
#58285=EDGE_CURVE ( 'NONE', #54562, #32638, #31998, .T. ) ;
#58291=CARTESIAN_POINT ( 'NONE',  ( 0.8744876279028263033, 37.95405449045444612, -31.14225101233220627 ) ) ;
#58292=VERTEX_POINT ( 'NONE', #61380 ) ;
#58293=CARTESIAN_POINT ( 'NONE',  ( 0.3676999524040323597, 41.59822836379060362, 14.68121181363330408 ) ) ;
#58294=CARTESIAN_POINT ( 'NONE',  ( 0.7413678028165012757, 25.98796241446775923, 35.62459685827271016 ) ) ;
#58296=ORIENTED_EDGE ( 'NONE', *, *, #16060, .T. ) ;
#58299=ORIENTED_EDGE ( 'NONE', *, *, #40700, .F. ) ;
#58300=LINE ( 'NONE', #14209, #6932 ) ;
#58308=CARTESIAN_POINT ( 'NONE',  ( 0.8744876279028263033, 46.86690837902584406, -14.62336997314537790 ) ) ;
#58315=CARTESIAN_POINT ( 'NONE',  ( 0.3676999524040366896, 43.44964275340416293, 7.620966337964807380 ) ) ;
#58320=VECTOR ( 'NONE', #49293, 1000.000000000000000 ) ;
#58323=CARTESIAN_POINT ( 'NONE',  ( 0.1157506346131639274, -1.506969930895584620, -44.09840928457862930 ) ) ;
#58325=EDGE_CURVE ( 'NONE', #47731, #60938, #49181, .T. ) ;
#58330=DIRECTION ( 'NONE',  ( 0.000000000000000000, 0.000000000000000000, 1.000000000000000000 ) ) ;
#58332=CARTESIAN_POINT ( 'NONE',  ( 0.5997462898726536595, -34.91088276334701135, -34.53667463477266608 ) ) ;
#58339=CARTESIAN_POINT ( 'NONE',  ( 0.6039202388192953519, 33.14386950699218204, 36.23599904725224263 ) ) ;
#58342=CARTESIAN_POINT ( 'NONE',  ( 0.1157991065609915715, -31.75315110184360279, 30.63788113824431747 ) ) ;
#58345=CARTESIAN_POINT ( 'NONE',  ( 4.975610109902397937, -23.13264022976583334, 43.09675583078141869 ) ) ;
#58352=CARTESIAN_POINT ( 'NONE',  ( 0.8753041380234465318, 23.49739456791673220, -43.11624724384784457 ) ) ;
#58354=B_SPLINE_CURVE_WITH_KNOTS ( 'NONE', 3,
 ( #35846, #17649, #46172, #59618, #3218, #41169 ),
 .UNSPECIFIED., .F., .F.,
 ( 4, 2, 4 ),
 ( 0.000000000000000000, 0.0002447195606305743124, 0.0004894391212611486248 ),
 .UNSPECIFIED. ) ;
#58361=( BOUNDED_SURFACE ( )  B_SPLINE_SURFACE ( 3, 1, ( 
 ( #26199, #55003 ),
 ( #2382, #21507 ),
 ( #35938, #49391 ),
 ( #40645, #11500 ) ),
 .UNSPECIFIED., .F., .F., .F. ) 
 B_SPLINE_SURFACE_WITH_KNOTS ( ( 4, 4 ),
 ( 2, 2 ),
 ( 0.000000000000000000, 1.000000000000000000 ),
 ( 0.000000000000000000, 1.000000000000000000 ),
 .UNSPECIFIED. ) 
 GEOMETRIC_REPRESENTATION_ITEM ( )  RATIONAL_B_SPLINE_SURFACE ( (
 ( 1.000000000000000000, 1.000000000000000000),
 ( 0.9953485035131437453, 0.8621029689291523912),
 ( 0.9953485035131437453, 0.8621029689291523912),
 ( 1.000000000000000000, 1.000000000000000000) ) ) 
 REPRESENTATION_ITEM ( '' )  SURFACE ( )  );
#58370=CARTESIAN_POINT ( 'NONE',  ( 0.1156495703730067992, 41.91905829288828045, 13.77445117122657159 ) ) ;
#58379=B_SPLINE_CURVE_WITH_KNOTS ( 'NONE', 3,
 ( #10494, #49014, #6065, #25200, #30820, #39957 ),
 .UNSPECIFIED., .F., .F.,
 ( 4, 2, 4 ),
 ( 0.000000000000000000, 0.0002447195606305751256, 0.0004894391212611502512 ),
 .UNSPECIFIED. ) ;
#58383=ADVANCED_FACE ( 'NONE', ( #52607 ), #49975, .F. ) ;
#58388=FACE_OUTER_BOUND ( 'NONE', #7139, .T. ) ;
#58389=CARTESIAN_POINT ( 'NONE',  ( 0.1147471544378677044, 14.94721517719480985, -41.51545431426571042 ) ) ;
#58390=ORIENTED_EDGE ( 'NONE', *, *, #14524, .T. ) ;
#58391=EDGE_CURVE ( 'NONE', #55418, #5254, #28986, .T. ) ;
#58395=ORIENTED_EDGE ( 'NONE', *, *, #40273, .T. ) ;
#58398=CARTESIAN_POINT ( 'NONE',  ( 0.7242486021783819394, -39.83546762662268748, 28.70796024349811049 ) ) ;
#58399=DIRECTION ( 'NONE',  ( 0.000000000000000000, 0.000000000000000000, -1.000000000000000000 ) ) ;
#58400=EDGE_CURVE ( 'NONE', #14042, #55289, #26768, .T. ) ;
#58402=ORIENTED_EDGE ( 'NONE', *, *, #2892, .T. ) ;
#58409=CARTESIAN_POINT ( 'NONE',  ( 0.2279481005628787582, 42.10464047700960322, -13.17963343096747053 ) ) ;
#58414=ORIENTED_EDGE ( 'NONE', *, *, #58254, .F. ) ;
#58415=LINE ( 'NONE', #5789, #35919 ) ;
#58422=CARTESIAN_POINT ( 'NONE',  ( 0.9268187852002115479, 21.26638028268818204, 38.61988351329813440 ) ) ;
#58432=CARTESIAN_POINT ( 'NONE',  ( 0.6008123274975393224, 22.32719666008250314, 43.73843664856413938 ) ) ;
#58445=CARTESIAN_POINT ( 'NONE',  ( 0.8744876279028306332, -31.30103973185180521, -37.82320666052162039 ) ) ;
#58447=CARTESIAN_POINT ( 'NONE',  ( 0.1158516988532803382, -22.83153063445172037, 37.75795767412332538 ) ) ;
#58450=EDGE_CURVE ( 'NONE', #3215, #30048, #17796, .T. ) ;
#58455=EDGE_CURVE ( 'NONE', #2779, #22153, #55160, .T. ) ;
#58456=CARTESIAN_POINT ( 'NONE',  ( 0.5980271706414711508, 28.66946741852874325, -39.87619441194936343 ) ) ;
#58459=ORIENTED_EDGE ( 'NONE', *, *, #49230, .T. ) ;
#58462=DIRECTION ( 'NONE',  ( 0.000000000000000000, 0.000000000000000000, -1.000000000000000000 ) ) ;
#58469=FACE_OUTER_BOUND ( 'NONE', #25763, .T. ) ;
#58474=B_SPLINE_CURVE_WITH_KNOTS ( 'NONE', 3,
 ( #12958, #23261, #61441, #27339, #46466, #4421, #46781, #47373, #18564, #3824, #22961, #18263, #56447, #13561, #8850, #27961, #6503, #35379, #16254, #54438, #30643, #33597, #28877, #35070, #50079 ),
 .UNSPECIFIED., .F., .F.,
 ( 4, 3, 3, 3, 3, 3, 3, 3, 4 ),
 ( 4.906538933386797396E-18, 0.0005656085177311406158, 0.001131215744874499622, 0.001696821861372768084, 0.002262427090022498151, 0.002828031679238745925, 0.003393635864401604862, 0.003977030878808133357, 0.004561030005651159000 ),
 .UNSPECIFIED. ) ;
#58476=CARTESIAN_POINT ( 'NONE',  ( -6.072942160501519915, 9.969886825816056231, -16.47438979050330943 ) ) ;
#58485=CARTESIAN_POINT ( 'NONE',  ( 0.6029442701453591180, -30.68607053265919404, -38.33940923414107971 ) ) ;
#58488=DIRECTION ( 'NONE',  ( -1.000000000000000000, -0.000000000000000000, -0.000000000000000000 ) ) ;
#58498=CARTESIAN_POINT ( 'NONE',  ( 0.8753041380234530822, 32.34805756193409110, -36.94240787824717387 ) ) ;
#58504=ORIENTED_EDGE ( 'NONE', *, *, #10630, .F. ) ;
#58506=CARTESIAN_POINT ( 'NONE',  ( 0.2940135542859015905, -38.82777379878567814, -20.94384230559791860 ) ) ;
#58518=CARTESIAN_POINT ( 'NONE',  ( 3.678748215320118753, -29.06831582091647093, 39.41631425735973693 ) ) ;
#58520=CARTESIAN_POINT ( 'NONE',  ( 0.3676999524040366896, -18.60775935196311082, -39.99627326667158655 ) ) ;
#58523=EDGE_CURVE ( 'NONE', #14826, #21415, #570, .T. ) ;
#58526=ADVANCED_FACE ( 'NONE', ( #10492 ), #60752, .F. ) ;
#58531=CARTESIAN_POINT ( 'NONE',  ( 1.657374760986086271, 40.21406714598089138, 17.99219972184566885 ) ) ;
#58535=( BOUNDED_SURFACE ( )  B_SPLINE_SURFACE ( 3, 1, ( 
 ( #53941, #49561 ),
 ( #39899, #10752 ),
 ( #40829, #59577 ),
 ( #48959, #30143 ) ),
 .UNSPECIFIED., .F., .F., .F. ) 
 B_SPLINE_SURFACE_WITH_KNOTS ( ( 4, 4 ),
 ( 2, 2 ),
 ( 0.000000000000000000, 1.000000000000000000 ),
 ( 0.000000000000000000, 1.000000000000000000 ),
 .UNSPECIFIED. ) 
 GEOMETRIC_REPRESENTATION_ITEM ( )  RATIONAL_B_SPLINE_SURFACE ( (
 ( 1.000000000000000000, 1.000000000000000000),
 ( 0.9953485035131437453, 0.8621029689291523912),
 ( 0.9953485035131437453, 0.8621029689291523912),
 ( 1.000000000000000000, 1.000000000000000000) ) ) 
 REPRESENTATION_ITEM ( '' )  SURFACE ( )  );
#58544=ORIENTED_EDGE ( 'NONE', *, *, #57696, .T. ) ;
#58560=CARTESIAN_POINT ( 'NONE',  ( 3.390910168358336918, -36.38779999262840192, -24.69868717624702725 ) ) ;
#58561=CARTESIAN_POINT ( 'NONE',  ( 0.2285344041767079504, -32.21686831072238277, -30.14257066915542183 ) ) ;
#58564=CARTESIAN_POINT ( 'NONE',  ( -6.077587904424778920, -1.842868750311850601, 19.16767738050321412 ) ) ;
#58565=B_SPLINE_CURVE_WITH_KNOTS ( 'NONE', 3,
 ( #43103, #4225, #39029, #19918, #29283, #14594 ),
 .UNSPECIFIED., .F., .F.,
 ( 4, 2, 4 ),
 ( 1.870900726506760797E-17, 0.0002293755540694306951, 0.0004587511081388426877 ),
 .UNSPECIFIED. ) ;
#58571=CARTESIAN_POINT ( 'NONE',  ( -2.601141883200665639, -12.77988133643086677, -7.711683376289167668 ) ) ;
#58578=CARTESIAN_POINT ( 'NONE',  ( 0.1152809850208375703, -40.98195743264318480, 16.35311736271641436 ) ) ;
#58584=VECTOR ( 'NONE', #24984, 1000.000000000000114 ) ;
#58588=CIRCLE ( 'NONE', #55604, 43.92652462719577500 ) ;
#58596=CARTESIAN_POINT ( 'NONE',  ( 0.8744876279028263033, 16.11801507201566253, 46.37412684372363714 ) ) ;
#58600=CARTESIAN_POINT ( 'NONE',  ( 4.060580049360325461, -3.719146386383672009, -43.79081689710593395 ) ) ;
#58601=CARTESIAN_POINT ( 'NONE',  ( 3.559346040607745287, 18.49490347406712232, -39.89196444181369117 ) ) ;
#58606=CARTESIAN_POINT ( 'NONE',  ( 0.1158816050234198619, 4.242590116464622696, 43.91972757666921012 ) ) ;
#58610=CARTESIAN_POINT ( 'NONE',  ( 4.975610109902397937, -46.23629923292363486, -15.95788333023269878 ) ) ;
#58613=CARTESIAN_POINT ( 'NONE',  ( 0.6029443449137434907, 10.88499636270525350, 47.88586839733853395 ) ) ;
#58614=VERTEX_POINT ( 'NONE', #45879 ) ;
#58617=EDGE_CURVE ( 'NONE', #16048, #22119, #37225, .T. ) ;
#58619=DIRECTION ( 'NONE',  ( 1.000000000000000000, -0.000000000000000000, -0.000000000000000000 ) ) ;
#58646=B_SPLINE_CURVE_WITH_KNOTS ( 'NONE', 3,
 ( #21244, #49129, #39142, #59437 ),
 .UNSPECIFIED., .F., .F.,
 ( 4, 4 ),
 ( 0.000000000000000000, 0.005013413432710145910 ),
 .UNSPECIFIED. ) ;
#58647=ORIENTED_EDGE ( 'NONE', *, *, #29421, .T. ) ;
#58657=CARTESIAN_POINT ( 'NONE',  ( 3.050102900204245682, -14.24207504814269498, -41.62437443975742468 ) ) ;
#58665=CARTESIAN_POINT ( 'NONE',  ( 0.6024113833632039894, 33.17582052207590237, -36.20644696442712274 ) ) ;
#58667=CARTESIAN_POINT ( 'NONE',  ( 0.2940135542859015350, 44.06980801370445278, 2.023010214173724730 ) ) ;
#58672=CARTESIAN_POINT ( 'NONE',  ( 0.6028777368367060907, 49.01203641660475796, -3.059430602004723276 ) ) ;
#58673=CARTESIAN_POINT ( 'NONE',  ( 4.553261556744875094, 12.28162544311214432, 42.17465165592641796 ) ) ;
#58677=CARTESIAN_POINT ( 'NONE',  ( 2.879087469061463178, 43.76579968909067020, -4.544937222643484098 ) ) ;
#58679=CARTESIAN_POINT ( 'NONE',  ( 0.1129192098497455998, 41.72114954716776936, 14.36305915353748297 ) ) ;
#58683=CARTESIAN_POINT ( 'NONE',  ( -6.078075953587585900, 0.6118799989801743111, 19.24631853404655502 ) ) ;
#58687=ORIENTED_EDGE ( 'NONE', *, *, #7058, .T. ) ;
#58690=CARTESIAN_POINT ( 'NONE',  ( 0.3676999524040366896, -40.57213187173863389, 17.31625533148228513 ) ) ;
#58692=CARTESIAN_POINT ( 'NONE',  ( 0.8744876279028263033, 36.80052600666216023, 32.49725120702480297 ) ) ;
#58697=CARTESIAN_POINT ( 'NONE',  ( -6.079354080745853928, -16.13884862108089280, 10.50383360654563170 ) ) ;
#58701=CARTESIAN_POINT ( 'NONE',  ( 0.1119899015040008994, 43.41448048127011816, -7.883158804306861889 ) ) ;
#58718=ORIENTED_EDGE ( 'NONE', *, *, #59252, .T. ) ;
#58729=PLANE ( 'NONE',  #49305 ) ;
#58733=EDGE_CURVE ( 'NONE', #3780, #1834, #37896, .T. ) ;
#58735=CARTESIAN_POINT ( 'NONE',  ( 4.975610109902397937, 0.000000000000000000, 0.000000000000000000 ) ) ;
#58736=CARTESIAN_POINT ( 'NONE',  ( 0.8744876279028263033, 33.66006955981258386, -35.74003032466635688 ) ) ;
#58737=ORIENTED_EDGE ( 'NONE', *, *, #56692, .F. ) ;
#58741=CARTESIAN_POINT ( 'NONE',  ( 0.1152339509894530906, 44.01863748844489521, -3.049958051533963932 ) ) ;
#58756=CARTESIAN_POINT ( 'NONE',  ( 0.1154773475650540532, -22.71965045366799529, 37.82540301582078968 ) ) ;
#58758=CARTESIAN_POINT ( 'NONE',  ( 0.1152339509894530906, 9.600619954257439304, -43.06704989837540154 ) ) ;
#58766=CARTESIAN_POINT ( 'NONE',  ( 1.830465331921976579, -34.54963717569211923, -27.32578684880679276 ) ) ;
#58778=ORIENTED_EDGE ( 'NONE', *, *, #18831, .T. ) ;
#58788=( BOUNDED_SURFACE ( )  B_SPLINE_SURFACE ( 3, 1, ( 
 ( #19242, #1027 ),
 ( #10761, #28927 ),
 ( #398, #14544 ),
 ( #38357, #10136 ) ),
 .UNSPECIFIED., .F., .F., .F. ) 
 B_SPLINE_SURFACE_WITH_KNOTS ( ( 4, 4 ),
 ( 2, 2 ),
 ( 0.000000000000000000, 1.000000000000000000 ),
 ( 0.000000000000000000, 1.000000000000000000 ),
 .UNSPECIFIED. ) 
 GEOMETRIC_REPRESENTATION_ITEM ( )  RATIONAL_B_SPLINE_SURFACE ( (
 ( 1.000000000000000000, 1.000000000000000000),
 ( 0.7211978278499968642, 0.9934217856018975334),
 ( 0.7211978278499968642, 0.9934217856018975334),
 ( 1.000000000000000000, 1.000000000000000000) ) ) 
 REPRESENTATION_ITEM ( '' )  SURFACE ( )  );
#58791=ORIENTED_EDGE ( 'NONE', *, *, #8312, .F. ) ;
#58793=VECTOR ( 'NONE', #60143, 1000.000000000000114 ) ;
#58796=CARTESIAN_POINT ( 'NONE',  ( 0.3676999524040366896, -2.238562284875889041, -44.05609404179596567 ) ) ;
#58797=EDGE_CURVE ( 'NONE', #22171, #33475, #25874, .T. ) ;
#58806=EDGE_CURVE ( 'NONE', #61591, #13969, #28865, .T. ) ;
#58811=CARTESIAN_POINT ( 'NONE',  ( 0.6000166863083106206, 28.52380356231423519, -39.97769518177558723 ) ) ;
#58812=CARTESIAN_POINT ( 'NONE',  ( 0.8753041380234465318, -19.05925361776887073, -45.25354328012939220 ) ) ;
#58817=ADVANCED_FACE ( 'NONE', ( #48314 ), #34807, .F. ) ;
#58824=CARTESIAN_POINT ( 'NONE',  ( 0.7044674535453004927, 41.61193891978847148, 26.08158856639488477 ) ) ;
#58828=CARTESIAN_POINT ( 'NONE',  ( 0.6021447746440204973, 37.22277672027512097, -32.03132891906035695 ) ) ;
#58833=B_SPLINE_CURVE_WITH_KNOTS ( 'NONE', 3,
 ( #12105, #2352, #54344, #16470 ),
 .UNSPECIFIED., .F., .F.,
 ( 4, 4 ),
 ( 0.000000000000000000, 0.005013413432710155451 ),
 .UNSPECIFIED. ) ;
#58834=CIRCLE ( 'NONE', #52855, 10.00000000000000000 ) ;
#58835=EDGE_CURVE ( 'NONE', #12174, #1980, #11039, .T. ) ;
#58842=ORIENTED_EDGE ( 'NONE', *, *, #8312, .T. ) ;
#58852=EDGE_CURVE ( 'NONE', #50931, #1298, #15739, .T. ) ;
#58859=CARTESIAN_POINT ( 'NONE',  ( 0.1365634738349423838, -0.7775954032165560692, -44.11641378231173860 ) ) ;
#58860=VERTEX_POINT ( 'NONE', #10416 ) ;
#58864=ORIENTED_EDGE ( 'NONE', *, *, #56470, .T. ) ;
#58867=CARTESIAN_POINT ( 'NONE',  ( 0.1129192098497455998, 30.02178898772931603, -32.33641869102712718 ) ) ;
#58871=ORIENTED_EDGE ( 'NONE', *, *, #23994, .F. ) ;
#58877=CARTESIAN_POINT ( 'NONE',  ( 4.694002226626921015, -34.93533603653879993, 29.28834354244447624 ) ) ;
#58883=CARTESIAN_POINT ( 'NONE',  ( 0.8753041380234524160, -42.34096624980190171, 24.86726573039578980 ) ) ;
#58885=CARTESIAN_POINT ( 'NONE',  ( -2.601141883200662974, -14.85441002404436439, -1.463533500456662306 ) ) ;
#58893=CARTESIAN_POINT ( 'NONE',  ( -6.078075953587585900, -14.66587681220008577, 12.47827037599793876 ) ) ;
#58897=( BOUNDED_SURFACE ( )  B_SPLINE_SURFACE ( 3, 1, ( 
 ( #16029, #49523 ),
 ( #39538, #16644 ),
 ( #54833, #30103 ),
 ( #11966, #2521 ) ),
 .UNSPECIFIED., .F., .F., .F. ) 
 B_SPLINE_SURFACE_WITH_KNOTS ( ( 4, 4 ),
 ( 2, 2 ),
 ( 0.000000000000000000, 1.000000000000000000 ),
 ( 0.000000000000000000, 1.000000000000000000 ),
 .UNSPECIFIED. ) 
 GEOMETRIC_REPRESENTATION_ITEM ( )  RATIONAL_B_SPLINE_SURFACE ( (
 ( 1.000000000000000000, 1.000000000000000000),
 ( 0.7211978278499968642, 0.9934217856018975334),
 ( 0.7211978278499968642, 0.9934217856018975334),
 ( 1.000000000000000000, 1.000000000000000000) ) ) 
 REPRESENTATION_ITEM ( '' )  SURFACE ( )  );
#58898=ADVANCED_FACE ( 'NONE', ( #17281 ), #9559, .F. ) ;
#58902=CARTESIAN_POINT ( 'NONE',  ( 0.3676999524040323597, 39.37931578712994707, 19.88014264185084912 ) ) ;
#58914=CARTESIAN_POINT ( 'NONE',  ( 0.2285344041767086998, -26.90972407420791868, 34.96237864541611629 ) ) ;
#58920=CARTESIAN_POINT ( 'NONE',  ( 0.6027444965799114707, -45.56734243241186988, 18.30726138816941173 ) ) ;
#58923=CARTESIAN_POINT ( 'NONE',  ( 1.657374760986086271, -2.648674067819503986, -43.97584533507803428 ) ) ;
#58928=CARTESIAN_POINT ( 'NONE',  ( 0.1158516988532803521, 4.285932436189670014, 43.91552051365456322 ) ) ;
#58930=B_SPLINE_CURVE_WITH_KNOTS ( 'NONE', 3,
 ( #46570, #22749, #41882, #56248 ),
 .UNSPECIFIED., .F., .F.,
 ( 4, 4 ),
 ( 0.000000000000000000, 0.005013413432710143308 ),
 .UNSPECIFIED. ) ;
#58933=ORIENTED_EDGE ( 'NONE', *, *, #17062, .T. ) ;
#58939=ORIENTED_EDGE ( 'NONE', *, *, #991, .T. ) ;
#58944=B_SPLINE_CURVE_WITH_KNOTS ( 'NONE', 3,
 ( #7293, #17346, #54915, #59622 ),
 .UNSPECIFIED., .F., .F.,
 ( 4, 4 ),
 ( 0.000000000000000000, 0.005013413432710151114 ),
 .UNSPECIFIED. ) ;
#58947=CARTESIAN_POINT ( 'NONE',  ( 0.3676999524040323597, 37.41430475689418245, -23.36921870497780418 ) ) ;
#58950=EDGE_LOOP ( 'NONE', ( #44887, #9829, #60128, #5360 ) ) ;
#58951=CARTESIAN_POINT ( 'NONE',  ( 0.5997462898726536595, 27.66511329191589397, 40.57330571557817223 ) ) ;
#58957=ORIENTED_EDGE ( 'NONE', *, *, #38018, .T. ) ;
#58961=CARTESIAN_POINT ( 'NONE',  ( 4.975610109902397937, 30.04451009524474969, 38.59762713269442713 ) ) ;
#58964=CARTESIAN_POINT ( 'NONE',  ( 0.6000166863083106206, -25.01014854877471549, 42.26483113981026207 ) ) ;
#58968=EDGE_CURVE ( 'NONE', #17224, #17545, #28204, .T. ) ;
#58972=CARTESIAN_POINT ( 'NONE',  ( 4.834790513006555379, 7.085748555637797708, -46.71596631057371241 ) ) ;
#58983=EDGE_CURVE ( 'NONE', #45131, #5101, #14546, .T. ) ;
#58986=EDGE_CURVE ( 'NONE', #1638, #54620, #43884, .T. ) ;
#58995=CARTESIAN_POINT ( 'NONE',  ( 0.6029443199889047422, 49.00651123133899034, -3.146346895535882648 ) ) ;
#58999=AXIS2_PLACEMENT_3D ( 'NONE', #32475, #13069, #42207 ) ;
#59001=CARTESIAN_POINT ( 'NONE',  ( 4.390527457369402420, 43.61304121279572854, -5.299808751228768600 ) ) ;
#59009=ORIENTED_EDGE ( 'NONE', *, *, #19937, .F. ) ;
#59012=CARTESIAN_POINT ( 'NONE',  ( 0.9268187852002115479, -40.48348757851531587, 17.45971266627324425 ) ) ;
#59014=CARTESIAN_POINT ( 'NONE',  ( 0.5980271706414734822, 49.05158475245161043, 2.447708339390032517 ) ) ;
#59016=CARTESIAN_POINT ( 'NONE',  ( 0.1368894036331282649, 4.870979158004423937, 43.85356186178748317 ) ) ;
#59019=ORIENTED_EDGE ( 'NONE', *, *, #9656, .T. ) ;
#59021=CARTESIAN_POINT ( 'NONE',  ( 0.3676999524040366896, 34.11874447324979087, 27.96179284115963171 ) ) ;
#59022=CARTESIAN_POINT ( 'NONE',  ( 0.1119899015040009271, -40.68569793094620479, -17.07733269759378203 ) ) ;
#59023=ORIENTED_EDGE ( 'NONE', *, *, #3108, .F. ) ;
#59027=CARTESIAN_POINT ( 'NONE',  ( 0.6253024248130485407, -8.514605087301925224, 48.36264806257963755 ) ) ;
#59050=CARTESIAN_POINT ( 'NONE',  ( 1.834102595619085285, -32.53417647307985305, -29.69385636922530125 ) ) ;
#59051=CARTESIAN_POINT ( 'NONE',  ( 4.335381028904216727, -15.96267600302249612, -46.31360299617030307 ) ) ;
#59057=CARTESIAN_POINT ( 'NONE',  ( -6.079354080745853928, -14.66314846858170462, 12.48138743235270454 ) ) ;
#59059=EDGE_CURVE ( 'NONE', #38660, #31310, #59542, .T. ) ;
#59060=CARTESIAN_POINT ( 'NONE',  ( 0.1156867017252034280, 44.04134645836630568, -2.702334066937902346 ) ) ;
#59071=B_SPLINE_CURVE_WITH_KNOTS ( 'NONE', 3,
 ( #41367, #41671, #3413, #40760 ),
 .UNSPECIFIED., .F., .F.,
 ( 4, 4 ),
 ( 0.000000000000000000, 0.004442905043737215703 ),
 .UNSPECIFIED. ) ;
#59073=CARTESIAN_POINT ( 'NONE',  ( 0.2940135542859014794, -42.87040774429959100, -10.41002826744088772 ) ) ;
#59081=ADVANCED_FACE ( 'NONE', ( #43882 ), #22352, .F. ) ;
#59082=CARTESIAN_POINT ( 'NONE',  ( 0.3676999524040366896, -0.5887207181726206162, 44.10900124961835900 ) ) ;
#59084=CARTESIAN_POINT ( 'NONE',  ( 0.6029443199889047422, 37.39265412695906576, 31.83279848200615803 ) ) ;
#59091=CARTESIAN_POINT ( 'NONE',  ( -6.079354080745853928, 5.477739963081766916, 18.46042578449963756 ) ) ;
#59092=CARTESIAN_POINT ( 'NONE',  ( 0.6000166863083090663, 23.17738933882476360, 43.29702189695021275 ) ) ;
#59098=CARTESIAN_POINT ( 'NONE',  ( 0.6000166863083106206, -8.353387137038087218, -48.39467331274403961 ) ) ;
#59099=CARTESIAN_POINT ( 'NONE',  ( 4.553261556744875094, -3.993093339916522488, -43.74465420371214464 ) ) ;
#59110=EDGE_LOOP ( 'NONE', ( #21123, #135, #55114, #3176 ) ) ;
#59112=CARTESIAN_POINT ( 'NONE',  ( 0.6008122571543325074, -30.95730573212618353, -38.12085744409461796 ) ) ;
#59118=ORIENTED_EDGE ( 'NONE', *, *, #329, .F. ) ;
#59123=CARTESIAN_POINT ( 'NONE',  ( 2.879087469061462734, 30.84090478284358383, 31.38375804391427337 ) ) ;
#59124=CARTESIAN_POINT ( 'NONE',  ( 4.553261556744875094, 22.96401893593780841, -37.44587293859667199 ) ) ;
#59131=ORIENTED_EDGE ( 'NONE', *, *, #4629, .T. ) ;
#59132=CARTESIAN_POINT ( 'NONE',  ( 0.7948878604505664747, -34.66113263096703179, 34.77505617589897469 ) ) ;
#59133=CARTESIAN_POINT ( 'NONE',  ( 0.6026777506516367566, -20.03705103671176602, -44.83372588118711377 ) ) ;
#59137=CARTESIAN_POINT ( 'NONE',  ( -6.079354080745853928, 18.62591919961139197, -4.885497847477741296 ) ) ;
#59141=CARTESIAN_POINT ( 'NONE',  ( 0.5997462898726536595, 37.72933316222010802, -31.43324751403371664 ) ) ;
#59145=B_SPLINE_CURVE_WITH_KNOTS ( 'NONE', 3,
 ( #38086, #8372, #15183, #39005, #10165, #38692 ),
 .UNSPECIFIED., .F., .F.,
 ( 4, 2, 4 ),
 ( 2.693102327163510278E-18, 0.0002447193893791690575, 0.0004894387787583354046 ),
 .UNSPECIFIED. ) ;
#59150=CARTESIAN_POINT ( 'NONE',  ( 4.975610109902397937, -33.30777373088848492, -35.81957029655308133 ) ) ;
#59157=ORIENTED_EDGE ( 'NONE', *, *, #21194, .F. ) ;
#59166=LINE ( 'NONE', #20669, #9023 ) ;
#59176=VERTEX_POINT ( 'NONE', #49467 ) ;
#59177=CIRCLE ( 'NONE', #18200, 43.92652462719577500 ) ;
#59180=DIRECTION ( 'NONE',  ( 0.000000000000000000, 0.000000000000000000, 1.000000000000000000 ) ) ;
#59186=CARTESIAN_POINT ( 'NONE',  ( 5.901764892641288895, 13.89173340561033676, -46.95754689533012538 ) ) ;
#59193=CARTESIAN_POINT ( 'NONE',  ( 0.8753041380234471980, -38.81339214172277963, -30.07754840950027386 ) ) ;
#59194=ORIENTED_EDGE ( 'NONE', *, *, #16479, .T. ) ;
#59197=ORIENTED_EDGE ( 'NONE', *, *, #58523, .T. ) ;
#59202=CARTESIAN_POINT ( 'NONE',  ( 0.7044674535453004927, -14.77841640690436620, -46.83376059334811004 ) ) ;
#59210=EDGE_CURVE ( 'NONE', #35184, #33035, #12467, .T. ) ;
#59211=( NAMED_UNIT ( * ) SI_UNIT ( $, .STERADIAN. ) SOLID_ANGLE_UNIT ( ) );
#59213=CARTESIAN_POINT ( 'NONE',  ( -6.063463321072276813, 0.6327935495816255917, 19.24629898975586428 ) ) ;
#59215=CARTESIAN_POINT ( 'NONE',  ( 4.553261556744873317, -43.85016385001095074, -2.588956575693968976 ) ) ;
#59222=CARTESIAN_POINT ( 'NONE',  ( 0.1135584504625008068, 36.74260402655860958, 24.43221442036662694 ) ) ;
#59225=CARTESIAN_POINT ( 'NONE',  ( 4.975610109902397937, 48.90928568712962488, -0.5754830253892166958 ) ) ;
#59226=CARTESIAN_POINT ( 'NONE',  ( 0.9268187852002115479, -42.38381720469895697, 12.13945518000253543 ) ) ;
#59229=CARTESIAN_POINT ( 'NONE',  ( -6.078075953587585900, -18.89992925442658844, -3.686169885505280686 ) ) ;
#59237=EDGE_CURVE ( 'NONE', #4300, #52623, #20668, .T. ) ;
#59242=ORIENTED_EDGE ( 'NONE', *, *, #17789, .F. ) ;
#59243=ORIENTED_EDGE ( 'NONE', *, *, #4570, .T. ) ;
#59244=CARTESIAN_POINT ( 'NONE',  ( 2.648799415243708655, -21.10807549816135875, -44.26021477640521340 ) ) ;
#59245=VERTEX_POINT ( 'NONE', #40410 ) ;
#59246=CARTESIAN_POINT ( 'NONE',  ( 0.2940133293163015860, -13.32164038229105252, 42.05680024803307759 ) ) ;
#59252=EDGE_CURVE ( 'NONE', #450, #47731, #49068, .T. ) ;
#59264=VECTOR ( 'NONE', #880, 1000.000000000000000 ) ;
#59268=CARTESIAN_POINT ( 'NONE',  ( 0.9268187852002115479, -42.88685641119342762, -10.22114866706790615 ) ) ;
#59269=CARTESIAN_POINT ( 'NONE',  ( -6.079354080745853928, 9.983157571107183159, -16.46601105789156705 ) ) ;
#59282=EDGE_CURVE ( 'NONE', #34106, #8248, #16583, .T. ) ;
#59288=DIRECTION ( 'NONE',  ( -0.1011922191286467460, 0.5266864627877126948, -0.8440151092865501026 ) ) ;
#59290=CARTESIAN_POINT ( 'NONE',  ( 0.7948878604505672518, -42.34838794577630949, 24.84577802550052894 ) ) ;
#59291=DIRECTION ( 'NONE',  ( -1.000000000000000000, -0.000000000000000000, -0.000000000000000000 ) ) ;
#59299=CARTESIAN_POINT ( 'NONE',  ( 0.5987334308729320709, -38.99056144767197907, 29.85463154294563992 ) ) ;
#59301=CARTESIAN_POINT ( 'NONE',  ( 0.6029443449137434907, 48.19350774417130623, 9.430023822654650445 ) ) ;
#59310=CARTESIAN_POINT ( 'NONE',  ( 4.553261556744875094, -20.51767157960516741, 38.84024612145369559 ) ) ;
#59311=CARTESIAN_POINT ( 'NONE',  ( -6.063463321072278589, -4.300220425535210111, 18.77041706439363367 ) ) ;
#59325=B_SPLINE_CURVE_WITH_KNOTS ( 'NONE', 3,
 ( #49433, #50358, #25944, #15092 ),
 .UNSPECIFIED., .F., .F.,
 ( 4, 4 ),
 ( 0.000000000000000000, 0.005013413432710138971 ),
 .UNSPECIFIED. ) ;
#59326=CARTESIAN_POINT ( 'NONE',  ( 0.1129192098497447394, 43.99990943031675528, -3.310552508128703497 ) ) ;
#59329=CARTESIAN_POINT ( 'NONE',  ( 0.2279481005628776480, 43.44433607591050617, -7.687206904737967861 ) ) ;
#59330=CARTESIAN_POINT ( 'NONE',  ( 0.7242003506640002364, -19.12400634200194460, 45.22481681065273307 ) ) ;
#59331=ORIENTED_EDGE ( 'NONE', *, *, #54642, .T. ) ;
#59338=CARTESIAN_POINT ( 'NONE',  ( 0.6029443449137436017, -35.30655258969704136, 34.13190416918297387 ) ) ;
#59340=ORIENTED_EDGE ( 'NONE', *, *, #44313, .F. ) ;
#59341=CARTESIAN_POINT ( 'NONE',  ( 0.1129192098497455998, -35.06977877439224045, -26.77802092202373174 ) ) ;
#59343=ORIENTED_EDGE ( 'NONE', *, *, #53900, .T. ) ;
#59352=CARTESIAN_POINT ( 'NONE',  ( 0.6252788684277222897, -14.62912771694895397, -46.87678480244634471 ) ) ;
#59355=CARTESIAN_POINT ( 'NONE',  ( 0.3676999524040366896, -41.19158123804976412, -15.78620342045500280 ) ) ;
#59357=CARTESIAN_POINT ( 'NONE',  ( 4.553261556744873317, 35.33793455049254106, 26.09156851415302825 ) ) ;
#59358=CARTESIAN_POINT ( 'NONE',  ( 1.112077966505211180, -32.38613972894711424, -29.90264668195222697 ) ) ;
#59360=CARTESIAN_POINT ( 'NONE',  ( 0.5997462898726536595, 41.43917033312134635, -26.35046094941917971 ) ) ;
#59361=CARTESIAN_POINT ( 'NONE',  ( 0.7242486021783809402, 33.61309370897174631, -35.79345462072436845 ) ) ;
#59366=CARTESIAN_POINT ( 'NONE',  ( 0.8753041380234530822, 5.600023814135296263, 48.78296896616787848 ) ) ;
#59368=CARTESIAN_POINT ( 'NONE',  ( -6.079354080745853928, 18.62651132414721289, 4.883239819994285469 ) ) ;
#59371=CARTESIAN_POINT ( 'NONE',  ( 0.7948878604505663636, -2.440498608811802583, -49.03817506635828494 ) ) ;
#59372=CARTESIAN_POINT ( 'NONE',  ( 4.390527457369402420, 35.40014937592107458, -26.01950731261247185 ) ) ;
#59381=ORIENTED_EDGE ( 'NONE', *, *, #56639, .T. ) ;
#59382=CARTESIAN_POINT ( 'NONE',  ( 0.3676999524040323597, 44.06746933160595603, -2.002181318164867552 ) ) ;
#59386=VERTEX_POINT ( 'NONE', #22819 ) ;
#59402=VERTEX_POINT ( 'NONE', #31917 ) ;
#59406=ORIENTED_EDGE ( 'NONE', *, *, #28358, .T. ) ;
#59407=CARTESIAN_POINT ( 'NONE',  ( -6.063463321072278589, -11.02986456480193489, 15.78488327994846152 ) ) ;
#59410=CARTESIAN_POINT ( 'NONE',  ( -6.072942160501519915, 16.78547611690376584, 9.436734277167797558 ) ) ;
#59415=CARTESIAN_POINT ( 'NONE',  ( 0.5997462898726536595, 4.195097405483644515, -48.92803682862019343 ) ) ;
#59425=CARTESIAN_POINT ( 'NONE',  ( 0.1156495703730067437, 43.33634112329940535, 8.300872922536509435 ) ) ;
#59432=CARTESIAN_POINT ( 'NONE',  ( 0.3676999524040366896, 30.26295534861856495, 32.09523511193457068 ) ) ;
#59437=CARTESIAN_POINT ( 'NONE',  ( 4.553261556744875094, 42.43205150231973732, 11.36048287389764688 ) ) ;
#59442=CARTESIAN_POINT ( 'NONE',  ( 3.678834586032788234, 42.02542406194491775, -25.14907755847229609 ) ) ;
#59448=CARTESIAN_POINT ( 'NONE',  ( 0.6027444965799114707, 4.585416998493479390, 48.89286723886592512 ) ) ;
#59456=DIRECTION ( 'NONE',  ( 0.09722883295013594329, 0.9754357953229615408, -0.1976652808305395526 ) ) ;
#59472=CARTESIAN_POINT ( 'NONE',  ( 4.553261556744875094, 22.96401893593780841, -37.44587293859667199 ) ) ;
#59478=VERTEX_POINT ( 'NONE', #48466 ) ;
#59480=CARTESIAN_POINT ( 'NONE',  ( 4.553261556744873317, -43.85016385001095074, -2.588956575693968976 ) ) ;
#59482=CARTESIAN_POINT ( 'NONE',  ( -6.063463321072278589, 9.969191071288406647, 16.47530521306399010 ) ) ;
#59485=CARTESIAN_POINT ( 'NONE',  ( 0.1152809850208375425, 20.21276301475716153, 39.22230862403461060 ) ) ;
#59488=VERTEX_POINT ( 'NONE', #38479 ) ;
#59489=CARTESIAN_POINT ( 'NONE',  ( 4.553261556744875094, 1.633632119647590697, -43.89613664004262716 ) ) ;
#59495=CARTESIAN_POINT ( 'NONE',  ( 0.6008122571543325074, -25.82835962906537830, -41.76661812185638922 ) ) ;
#59497=B_SPLINE_CURVE_WITH_KNOTS ( 'NONE', 3,
 ( #32737, #61212, #23330, #42760, #23029, #38074 ),
 .UNSPECIFIED., .F., .F.,
 ( 4, 2, 4 ),
 ( 0.000000000000000000, 0.0002293801035737088299, 0.0004587602071474176598 ),
 .UNSPECIFIED. ) ;
#59505=VERTEX_POINT ( 'NONE', #43180 ) ;
#59509=ORIENTED_EDGE ( 'NONE', *, *, #11399, .T. ) ;
#59510=CARTESIAN_POINT ( 'NONE',  ( -6.078457390727109555, -16.14063570603395803, -10.50116136637322484 ) ) ;
#59520=B_SPLINE_CURVE_WITH_KNOTS ( 'NONE', 3,
 ( #15177, #23951, #10468, #14567 ),
 .UNSPECIFIED., .F., .F.,
 ( 4, 4 ),
 ( 0.000000000000000000, 0.004442905043737213969 ),
 .UNSPECIFIED. ) ;
#59523=CARTESIAN_POINT ( 'NONE',  ( -6.078075953587585900, -18.27673012847640166, -6.062698248962985481 ) ) ;
#59524=CIRCLE ( 'NONE', #494, 10.00000000000000000 ) ;
#59525=ORIENTED_EDGE ( 'NONE', *, *, #39159, .F. ) ;
#59539=CARTESIAN_POINT ( 'NONE',  ( 0.1155031312995260795, 36.88774152132017292, 24.21231418076512298 ) ) ;
#59541=CARTESIAN_POINT ( 'NONE',  ( 0.5987334363312691865, -19.32301417642171515, -45.14625155657866173 ) ) ;
#59542=CIRCLE ( 'NONE', #48547, 48.91267123290010943 ) ;
#59549=ADVANCED_FACE ( 'NONE', ( #35631 ), #58361, .F. ) ;
#59552=ORIENTED_EDGE ( 'NONE', *, *, #43591, .T. ) ;
#59568=ORIENTED_EDGE ( 'NONE', *, *, #25244, .T. ) ;
#59569=CARTESIAN_POINT ( 'NONE',  ( 4.553261556744875094, 0.000000000000000000, 0.000000000000000000 ) ) ;
#59576=EDGE_LOOP ( 'NONE', ( #33248, #61033, #21839, #56799 ) ) ;
#59577=CARTESIAN_POINT ( 'NONE',  ( 0.7044674535452954967, -45.83030039157709012, 17.64614090470532659 ) ) ;
#59579=CARTESIAN_POINT ( 'NONE',  ( 0.08486401232817714080, 0.000000000000000000, 0.000000000000000000 ) ) ;
#59583=CARTESIAN_POINT ( 'NONE',  ( 4.390527457369401532, 7.328357084871000460, -43.31836237746345120 ) ) ;
#59589=CARTESIAN_POINT ( 'NONE',  ( 2.533389852662419894, 42.24569141318911392, 12.35929159601054295 ) ) ;
#59592=VECTOR ( 'NONE', #13102, 1000.000000000000114 ) ;
#59593=CARTESIAN_POINT ( 'NONE',  ( -6.078726893082806448, -12.94330610022628214, -14.25709887966570832 ) ) ;
#59594=EDGE_CURVE ( 'NONE', #46515, #55636, #25901, .T. ) ;
#59600=DIRECTION ( 'NONE',  ( 0.000000000000000000, 0.000000000000000000, -1.000000000000000000 ) ) ;
#59601=CARTESIAN_POINT ( 'NONE',  ( 0.5987334363312690755, 43.97851324882841340, 21.85070431118181844 ) ) ;
#59606=CARTESIAN_POINT ( 'NONE',  ( 2.114184763561894886, 5.677447754278171364E-15, -44.03514965515262247 ) ) ;
#59611=CARTESIAN_POINT ( 'NONE',  ( 0.6021447746440204973, 48.25112305616622876, 9.130731783772414900 ) ) ;
#59618=CARTESIAN_POINT ( 'NONE',  ( 0.7242003506640009025, 44.58862645969713867, 20.56370746153588058 ) ) ;
#59622=CARTESIAN_POINT ( 'NONE',  ( 4.975610109902397937, -17.43163075979644816, -45.70106843599929647 ) ) ;
#59636=CARTESIAN_POINT ( 'NONE',  ( 0.1129192098497447394, 14.78321943369649283, -41.57412910645673776 ) ) ;
#59645=CARTESIAN_POINT ( 'NONE',  ( 2.879087469061463178, -43.82752541487803200, -3.905085503749960552 ) ) ;
#59650=( BOUNDED_SURFACE ( )  B_SPLINE_SURFACE ( 3, 1, ( 
 ( #32468, #42499 ),
 ( #36877, #56565 ),
 ( #31855, #18064 ),
 ( #46575, #26836 ) ),
 .UNSPECIFIED., .F., .F., .F. ) 
 B_SPLINE_SURFACE_WITH_KNOTS ( ( 4, 4 ),
 ( 2, 2 ),
 ( 0.000000000000000000, 1.000000000000000000 ),
 ( 0.000000000000000000, 1.000000000000000000 ),
 .UNSPECIFIED. ) 
 GEOMETRIC_REPRESENTATION_ITEM ( )  RATIONAL_B_SPLINE_SURFACE ( (
 ( 1.000000000000000000, 1.000000000000000000),
 ( 0.9953485035131437453, 0.8621029689291523912),
 ( 0.9953485035131437453, 0.8621029689291523912),
 ( 1.000000000000000000, 1.000000000000000000) ) ) 
 REPRESENTATION_ITEM ( '' )  SURFACE ( )  );
#59657=ORIENTED_EDGE ( 'NONE', *, *, #21671, .F. ) ;
#59660=EDGE_CURVE ( 'NONE', #34351, #450, #45980, .T. ) ;
#59662=EDGE_CURVE ( 'NONE', #6071, #52266, #19910, .T. ) ;
#59664=CARTESIAN_POINT ( 'NONE',  ( 0.2285344041767113366, 10.55674979585326234, 42.83755599988411689 ) ) ;
#59666=CARTESIAN_POINT ( 'NONE',  ( -6.063463321072278589, -18.27076090991269552, -6.082741836727592499 ) ) ;
#59668=CARTESIAN_POINT ( 'NONE',  ( 0.8753041380234524160, 48.93739466471257060, -4.033575498629233813 ) ) ;
#59670=EDGE_CURVE ( 'NONE', #43965, #4156, #49721, .T. ) ;
#59671=CARTESIAN_POINT ( 'NONE',  ( 0.6026777506516367566, 41.06112623026730546, -26.93566972138011195 ) ) ;
#59672=EDGE_CURVE ( 'NONE', #3477, #6245, #37779, .T. ) ;
#59675=AXIS2_PLACEMENT_3D ( 'NONE', #36194, #29929, #11445 ) ;
#59682=CARTESIAN_POINT ( 'NONE',  ( -6.078726893082806448, 18.62710865126528859, 4.881072071039118221 ) ) ;
#59687=CARTESIAN_POINT ( 'NONE',  ( 3.727782113643637096, 35.63527235512886904, -25.74694428629857867 ) ) ;
#59689=CARTESIAN_POINT ( 'NONE',  ( 0.7242003506639960175, -45.19983343645225915, 19.18298025445989907 ) ) ;
#59700=ORIENTED_EDGE ( 'NONE', *, *, #52128, .T. ) ;
#59702=CARTESIAN_POINT ( 'NONE',  ( 4.975610109902397937, 0.000000000000000000, 0.000000000000000000 ) ) ;
#59709=DIRECTION ( 'NONE',  ( 0.000000000000000000, 0.000000000000000000, 1.000000000000000000 ) ) ;
#59714=AXIS2_PLACEMENT_3D ( 'NONE', #6293, #43646, #25429 ) ;
#59716=CARTESIAN_POINT ( 'NONE',  ( 4.975610109902397937, -44.31543648230385202, -20.70245146161840211 ) ) ;
#59721=CARTESIAN_POINT ( 'NONE',  ( 0.8753041380234524160, 27.35839019124417248, -40.77568900725792389 ) ) ;
#59726=EDGE_LOOP ( 'NONE', ( #61346, #7879, #48548, #14325 ) ) ;
#59729=ORIENTED_EDGE ( 'NONE', *, *, #22912, .T. ) ;
#59730=FACE_OUTER_BOUND ( 'NONE', #17344, .T. ) ;
#59738=CARTESIAN_POINT ( 'NONE',  ( 0.1135584504625006819, -43.81516248351064036, 5.213788323169063155 ) ) ;
#59740=CARTESIAN_POINT ( 'NONE',  ( 0.1157991065609915854, -27.44727329912610259, -34.54836543138876692 ) ) ;
#59745=EDGE_CURVE ( 'NONE', #48631, #59245, #54919, .T. ) ;
#59747=LINE ( 'NONE', #36278, #33542 ) ;
#59748=CARTESIAN_POINT ( 'NONE',  ( 5.901764892641307547, 47.37867283933467633, -12.37953260115135734 ) ) ;
#59750=CARTESIAN_POINT ( 'NONE',  ( 2.299746137290198611, -15.18165008456612597, -46.62401568286382769 ) ) ;
#59758=PLANE ( 'NONE',  #10840 ) ;
#59762=CARTESIAN_POINT ( 'NONE',  ( 0.8744876279028306332, -34.64280934553560343, 34.78829991575276637 ) ) ;
#59763=CARTESIAN_POINT ( 'NONE',  ( 0.6027444965799114707, 44.18742767652119596, 21.42451285839772623 ) ) ;
#59764=CARTESIAN_POINT ( 'NONE',  ( 4.553261556744873317, -9.994631851593151595, -42.77437199977056537 ) ) ;
#59768=CARTESIAN_POINT ( 'NONE',  ( 0.1152809850208375703, -12.34233989415304755, -42.36286024841751185 ) ) ;
#59769=CARTESIAN_POINT ( 'NONE',  ( 0.6000166863083106206, 27.66667954482573322, 40.57558779207487021 ) ) ;
#59772=CARTESIAN_POINT ( 'NONE',  ( 0.8744876279028306332, 17.78802839418675674, 45.75954650373076049 ) ) ;
#59776=AXIS2_PLACEMENT_3D ( 'NONE', #19934, #14614, #15223 ) ;
#59790=CARTESIAN_POINT ( 'NONE',  ( 0.8744876279028306332, -6.955970791788286256, 48.60004650947653460 ) ) ;
#59795=CARTESIAN_POINT ( 'NONE',  ( 0.5997462898726536595, -13.47075269803155351, 47.22383351542719510 ) ) ;
#59799=ORIENTED_EDGE ( 'NONE', *, *, #52354, .F. ) ;
#59803=FACE_OUTER_BOUND ( 'NONE', #54616, .T. ) ;
#59812=ORIENTED_EDGE ( 'NONE', *, *, #22213, .T. ) ;
#59816=DIRECTION ( 'NONE',  ( 0.09722883295013594329, -0.5223840607312690842, -0.8471490111763481101 ) ) ;
#59819=CARTESIAN_POINT ( 'NONE',  ( 3.390910168358336918, 6.179655656472472280, 43.54203707339684826 ) ) ;
#59827=ORIENTED_EDGE ( 'NONE', *, *, #10609, .F. ) ;
#59829=CARTESIAN_POINT ( 'NONE',  ( 3.050102900204245682, -34.14444597521366376, 27.74134204078410448 ) ) ;
#59836=ADVANCED_FACE ( 'NONE', ( #49944 ), #39210, .F. ) ;
#59837=CARTESIAN_POINT ( 'NONE',  ( -2.739355103387247858, -11.80442426703883640, -9.138004961410429061 ) ) ;
#59858=CARTESIAN_POINT ( 'NONE',  ( 0.8744876279028306332, 16.11801507201633399, -46.37412684372340266 ) ) ;
#59862=ORIENTED_EDGE ( 'NONE', *, *, #42954, .T. ) ;
#59863=CARTESIAN_POINT ( 'NONE',  ( 0.1129192098497447394, 3.754263797494919341, -43.96427289429421137 ) ) ;
#59880=EDGE_CURVE ( 'NONE', #25604, #14082, #49316, .T. ) ;
#59893=CARTESIAN_POINT ( 'NONE',  ( 4.553261556744875094, 12.71466023209559104, -42.04612920360213479 ) ) ;
#59894=ORIENTED_EDGE ( 'NONE', *, *, #12329, .T. ) ;
#59895=CARTESIAN_POINT ( 'NONE',  ( 0.1129192098497447394, 42.02659449688918869, 13.44310763102032702 ) ) ;
#59896=CARTESIAN_POINT ( 'NONE',  ( 0.7948884756798503259, 46.31693274517635217, 16.29234131974172683 ) ) ;
#59901=EDGE_LOOP ( 'NONE', ( #50837, #26323, #53328, #39036 ) ) ;
#59906=CARTESIAN_POINT ( 'NONE',  ( 0.5997462898726536595, 41.43917033312096265, 26.35046094941977302 ) ) ;
#59911=CARTESIAN_POINT ( 'NONE',  ( 1.657374760986086271, -13.71672357020459643, -41.86576097183517930 ) ) ;
#59915=VECTOR ( 'NONE', #28332, 1000.000000000000114 ) ;
#59917=DIRECTION ( 'NONE',  ( 0.000000000000000000, 0.000000000000000000, 1.000000000000000000 ) ) ;
#59919=CARTESIAN_POINT ( 'NONE',  ( 3.050102900204245682, 41.14650753732696131, -15.56888456694172973 ) ) ;
#59924=( BOUNDED_SURFACE ( )  B_SPLINE_SURFACE ( 3, 1, ( 
 ( #1974, #35526 ),
 ( #54904, #50219 ),
 ( #2594, #4731 ),
 ( #47083, #14188 ) ),
 .UNSPECIFIED., .F., .F., .F. ) 
 B_SPLINE_SURFACE_WITH_KNOTS ( ( 4, 4 ),
 ( 2, 2 ),
 ( 0.000000000000000000, 1.000000000000000000 ),
 ( 0.000000000000000000, 1.000000000000000000 ),
 .UNSPECIFIED. ) 
 GEOMETRIC_REPRESENTATION_ITEM ( )  RATIONAL_B_SPLINE_SURFACE ( (
 ( 1.000000000000000000, 1.000000000000000000),
 ( 0.7211978278499968642, 0.9934217856018975334),
 ( 0.7211978278499968642, 0.9934217856018975334),
 ( 1.000000000000000000, 1.000000000000000000) ) ) 
 REPRESENTATION_ITEM ( '' )  SURFACE ( )  );
#59927=CARTESIAN_POINT ( 'NONE',  ( 4.553261556744875094, -36.69060082144763868, -24.15241969627107110 ) ) ;
#59932=CARTESIAN_POINT ( 'NONE',  ( 4.226256110419179812, 1.821314936738874568, -43.90341742835515504 ) ) ;
#59936=CARTESIAN_POINT ( 'NONE',  ( -6.079354080745853928, 12.00499765711184708, -15.05566293794136179 ) ) ;
#59937=CARTESIAN_POINT ( 'NONE',  ( -6.057079549204054558, -18.90023728169072470, -3.689479881436749764 ) ) ;
#59946=EDGE_CURVE ( 'NONE', #31616, #43286, #7890, .T. ) ;
#59949=ADVANCED_FACE ( 'NONE', ( #58388 ), #15592, .F. ) ;
#59956=CARTESIAN_POINT ( 'NONE',  ( -2.601141883200662974, 12.25953444924679658, -8.514648704269580648 ) ) ;
#59959=VERTEX_POINT ( 'NONE', #36479 ) ;
#59963=CARTESIAN_POINT ( 'NONE',  ( -2.739355103387247858, 11.53562761125311553, -9.475065306662095566 ) ) ;
#59965=CARTESIAN_POINT ( 'NONE',  ( 2.648799415243696664, -48.79107182468962378, 4.893748408692157881 ) ) ;
#59969=ORIENTED_EDGE ( 'NONE', *, *, #8729, .F. ) ;
#59976=CARTESIAN_POINT ( 'NONE',  ( 4.335381028904201628, -40.49335964728638970, 27.56890770668767132 ) ) ;
#59992=CARTESIAN_POINT ( 'NONE',  ( 0.1135584504625007790, 44.05918809782512824, -2.395828937073182008 ) ) ;
#59993=EDGE_CURVE ( 'NONE', #17686, #19345, #13797, .T. ) ;
#59996=CARTESIAN_POINT ( 'NONE',  ( 0.8744876279028306332, -2.462621419132613454, -49.03351451941336592 ) ) ;
#60001=VERTEX_POINT ( 'NONE', #60866 ) ;
#60004=CARTESIAN_POINT ( 'NONE',  ( 1.479689385636123067, -18.90469049123688805, -39.80196631698275667 ) ) ;
#60006=CARTESIAN_POINT ( 'NONE',  ( -4.915099999999998914, 0.000000000000000000, 10.00000000000000000 ) ) ;
#60009=FACE_OUTER_BOUND ( 'NONE', #34642, .T. ) ;
#60012=ORIENTED_EDGE ( 'NONE', *, *, #26903, .F. ) ;
#60018=EDGE_CURVE ( 'NONE', #12019, #855, #25755, .T. ) ;
#60019=CARTESIAN_POINT ( 'NONE',  ( 0.1155031312995260795, -42.63802226078201585, -11.35520542398358579 ) ) ;
#60020=CARTESIAN_POINT ( 'NONE',  ( 0.08486401232817714080, 0.000000000000000000, 0.000000000000000000 ) ) ;
#60023=( BOUNDED_SURFACE ( )  B_SPLINE_SURFACE ( 3, 1, ( 
 ( #38334, #57085 ),
 ( #56783, #9486 ),
 ( #33322, #48024 ),
 ( #28593, #23293 ) ),
 .UNSPECIFIED., .F., .F., .F. ) 
 B_SPLINE_SURFACE_WITH_KNOTS ( ( 4, 4 ),
 ( 2, 2 ),
 ( 0.000000000000000000, 1.000000000000000000 ),
 ( 0.000000000000000000, 1.000000000000000000 ),
 .UNSPECIFIED. ) 
 GEOMETRIC_REPRESENTATION_ITEM ( )  RATIONAL_B_SPLINE_SURFACE ( (
 ( 1.000000000000000000, 1.000000000000000000),
 ( 0.9754377213608244057, 0.9999580625633939235),
 ( 0.9754377213608244057, 0.9999580625633939235),
 ( 1.000000000000000000, 1.000000000000000000) ) ) 
 REPRESENTATION_ITEM ( '' )  SURFACE ( )  );
#60024=DIRECTION ( 'NONE',  ( -1.000000000000000000, -0.000000000000000000, -0.000000000000000000 ) ) ;
#60030=CARTESIAN_POINT ( 'NONE',  ( 4.553261556744875094, 0.000000000000000000, 0.000000000000000000 ) ) ;
#60034=FACE_OUTER_BOUND ( 'NONE', #18075, .T. ) ;
#60039=CARTESIAN_POINT ( 'NONE',  ( 0.1149546198390368479, 39.87261812082539336, -18.89764242475886391 ) ) ;
#60040=ORIENTED_EDGE ( 'NONE', *, *, #12201, .F. ) ;
#60043=EDGE_CURVE ( 'NONE', #14283, #29362, #21593, .T. ) ;
#60049=ADVANCED_FACE ( 'NONE', ( #32389 ), #23629, .F. ) ;
#60057=APPLICATION_CONTEXT ( 'automotive_design' ) ;
#60058=ORIENTED_EDGE ( 'NONE', *, *, #24201, .T. ) ;
#60071=CARTESIAN_POINT ( 'NONE',  ( 0.1145239942831223490, -42.76278809080708498, 10.87609467618780457 ) ) ;
#60073=CARTESIAN_POINT ( 'NONE',  ( -2.739355103387247858, 7.136887160706410604, -13.11153723277179139 ) ) ;
#60078=FACE_OUTER_BOUND ( 'NONE', #24033, .T. ) ;
#60079=CARTESIAN_POINT ( 'NONE',  ( 0.6000166863083106206, -35.63988196839337519, -33.78790160675033860 ) ) ;
#60081=CARTESIAN_POINT ( 'NONE',  ( 0.3676999524040323597, -0.5887207181719652516, -44.10900124961835900 ) ) ;
#60082=LINE ( 'NONE', #9005, #33860 ) ;
#60087=CARTESIAN_POINT ( 'NONE',  ( 0.5997462898726536595, 28.52220283460625438, 39.97543715340569292 ) ) ;
#60096=EDGE_CURVE ( 'NONE', #7798, #1309, #7769, .T. ) ;
#60100=ADVANCED_FACE ( 'NONE', ( #14216 ), #60023, .F. ) ;
#60112=EDGE_LOOP ( 'NONE', ( #13263, #35144, #50233, #56091 ) ) ;
#60113=CARTESIAN_POINT ( 'NONE',  ( -6.057079549204054558, 13.83914966176556582, -13.39063731638611898 ) ) ;
#60114=ORIENTED_EDGE ( 'NONE', *, *, #2112, .F. ) ;
#60127=EDGE_LOOP ( 'NONE', ( #20538, #56196, #43443, #21758 ) ) ;
#60128=ORIENTED_EDGE ( 'NONE', *, *, #35991, .F. ) ;
#60130=CARTESIAN_POINT ( 'NONE',  ( -6.078457390727109555, -17.34717774342088248, 8.358823803363188532 ) ) ;
#60131=CARTESIAN_POINT ( 'NONE',  ( 5.901764892641307547, 25.34839938110013335, 41.89809203598559861 ) ) ;
#60135=CARTESIAN_POINT ( 'NONE',  ( 0.7413678028165011646, -34.77333832429343374, 27.11643475006381721 ) ) ;
#60137=CARTESIAN_POINT ( 'NONE',  ( 0.3676999524040323597, 25.91024933382809436, -35.70167450949183774 ) ) ;
#60143=DIRECTION ( 'NONE',  ( -0.1011922191286467737, -0.7658109114536917339, 0.6350541572860427531 ) ) ;
#60145=ORIENTED_EDGE ( 'NONE', *, *, #20960, .T. ) ;
#60154=CARTESIAN_POINT ( 'NONE',  ( 4.975610109902397937, 0.000000000000000000, 0.000000000000000000 ) ) ;
#60157=ORIENTED_EDGE ( 'NONE', *, *, #11796, .T. ) ;
#60158=CARTESIAN_POINT ( 'NONE',  ( 2.706805983486679779, -3.064257645287458587, -43.90200950301765204 ) ) ;
#60161=ORIENTED_EDGE ( 'NONE', *, *, #6711, .T. ) ;
#60163=CARTESIAN_POINT ( 'NONE',  ( 4.975610109902397937, -33.30777373088848492, -35.81957029655308133 ) ) ;
#60164=CARTESIAN_POINT ( 'NONE',  ( 0.6008123274975393224, 44.43158642411502512, -20.91383941305027605 ) ) ;
#60166=CARTESIAN_POINT ( 'NONE',  ( 4.553261556744875094, 0.000000000000000000, 0.000000000000000000 ) ) ;
#60167=AXIS2_PLACEMENT_3D ( 'NONE', #23195, #22893, #13190 ) ;
#60172=CARTESIAN_POINT ( 'NONE',  ( -6.078075953587585900, -19.21613803895143491, -1.239037172606074488 ) ) ;
#60173=( BOUNDED_SURFACE ( )  B_SPLINE_SURFACE ( 3, 1, ( 
 ( #19439, #57611 ),
 ( #15364, #57301 ),
 ( #297, #52622 ),
 ( #14745, #38256 ) ),
 .UNSPECIFIED., .F., .F., .F. ) 
 B_SPLINE_SURFACE_WITH_KNOTS ( ( 4, 4 ),
 ( 2, 2 ),
 ( 0.000000000000000000, 1.000000000000000000 ),
 ( 0.000000000000000000, 1.000000000000000000 ),
 .UNSPECIFIED. ) 
 GEOMETRIC_REPRESENTATION_ITEM ( )  RATIONAL_B_SPLINE_SURFACE ( (
 ( 1.000000000000000000, 1.000000000000000000),
 ( 0.9953485035131437453, 0.8621029689291515030),
 ( 0.9953485035131437453, 0.8621029689291515030),
 ( 1.000000000000000000, 1.000000000000000000) ) ) 
 REPRESENTATION_ITEM ( '' )  SURFACE ( )  );
#60174=ORIENTED_EDGE ( 'NONE', *, *, #34770, .T. ) ;
#60181=CARTESIAN_POINT ( 'NONE',  ( 0.5980271706414711508, -49.10762822256506865, -0.7000665654016452466 ) ) ;
#60184=CARTESIAN_POINT ( 'NONE',  ( 2.044598208318018973, -0.02734949455884180813, 44.03824229377359245 ) ) ;
#60185=ORIENTED_EDGE ( 'NONE', *, *, #9195, .T. ) ;
#60189=CARTESIAN_POINT ( 'NONE',  ( 4.975610109902397937, -43.81605102859442979, -21.73943604138302987 ) ) ;
#60190=LINE ( 'NONE', #31391, #61626 ) ;
#60197=CARTESIAN_POINT ( 'NONE',  ( 4.553261556744873317, -24.94552653848474222, 36.15605442441679429 ) ) ;
#60200=CARTESIAN_POINT ( 'NONE',  ( 0.7413678028165010536, 8.900374941533167217, -43.18876494726807636 ) ) ;
#60205=CARTESIAN_POINT ( 'NONE',  ( 0.3676999524040366896, 42.11837424242170158, 13.11461530118771179 ) ) ;
#60207=CARTESIAN_POINT ( 'NONE',  ( -6.077587904424778920, -18.27702681447052768, 6.061873655649367088 ) ) ;
#60208=STYLED_ITEM ( 'NONE', ( #50078 ), #30206 ) ;
#60209=EDGE_CURVE ( 'NONE', #16660, #38361, #38423, .T. ) ;
#60216=CARTESIAN_POINT ( 'NONE',  ( 3.221118495291108719, 41.11142598507491641, -15.64007906423297101 ) ) ;
#60221=CARTESIAN_POINT ( 'NONE',  ( 0.6008122571543325074, 17.36801345829917054, 45.93372028235526727 ) ) ;
#60228=CARTESIAN_POINT ( 'NONE',  ( 1.657374760986086271, 2.996577793790630384, -43.95350917478609176 ) ) ;
#60234=ORIENTED_EDGE ( 'NONE', *, *, #3537, .F. ) ;
#60245=EDGE_CURVE ( 'NONE', #39259, #40034, #57793, .T. ) ;
#60250=VERTEX_POINT ( 'NONE', #697 ) ;
#60255=FACE_OUTER_BOUND ( 'NONE', #30372, .T. ) ;
#60263=VERTEX_POINT ( 'NONE', #25130 ) ;
#60275=CARTESIAN_POINT ( 'NONE',  ( 0.6021448801613057400, -42.91582863034458484, 23.86991394198654959 ) ) ;
#60278=CARTESIAN_POINT ( 'NONE',  ( -6.057079549204054558, -18.27326637954045196, -6.076098001357041589 ) ) ;
#60283=ADVANCED_FACE ( 'NONE', ( #1303 ), #36095, .F. ) ;
#60298=ORIENTED_EDGE ( 'NONE', *, *, #53158, .T. ) ;
#60299=DIRECTION ( 'NONE',  ( -0.1011922191286467460, 0.7235494112461693383, -0.6828150439710168884 ) ) ;
#60302=ORIENTED_EDGE ( 'NONE', *, *, #18296, .F. ) ;
#60316=CARTESIAN_POINT ( 'NONE',  ( 0.1129192098497455998, -42.55567333040708888, -11.66046547873770756 ) ) ;
#60321=CARTESIAN_POINT ( 'NONE',  ( 0.7948878604505666967, 21.93744113805909635, -43.92547465438033072 ) ) ;
#60323=EDGE_LOOP ( 'NONE', ( #34084, #48867, #22243, #8956 ) ) ;
#60325=CARTESIAN_POINT ( 'NONE',  ( -6.078457390727109555, -17.34717774342076169, -8.358823803363440774 ) ) ;
#60326=CARTESIAN_POINT ( 'NONE',  ( 0.3676999524040366896, 39.37931578713023839, -19.88014264185028068 ) ) ;
#60330=VERTEX_POINT ( 'NONE', #22827 ) ;
#60336=ORIENTED_EDGE ( 'NONE', *, *, #10998, .F. ) ;
#60345=ORIENTED_EDGE ( 'NONE', *, *, #9911, .T. ) ;
#60350=CARTESIAN_POINT ( 'NONE',  ( 0.6028777368367060907, 32.95046403715527106, 36.41162931052673457 ) ) ;
#60363=CARTESIAN_POINT ( 'NONE',  ( -6.063463321072278589, 9.995861580988218975, -16.45913739335064463 ) ) ;
#60364=LINE ( 'NONE', #50976, #59592 ) ;
#60368=EDGE_CURVE ( 'NONE', #58292, #48331, #36995, .T. ) ;
#60369=CARTESIAN_POINT ( 'NONE',  ( 0.8744876279028263033, -35.88078294188978390, 33.50999053799454686 ) ) ;
#60370=CARTESIAN_POINT ( 'NONE',  ( 3.240649175237395596, 43.74621574345733421, 4.640422989829291467 ) ) ;
#60372=CARTESIAN_POINT ( 'NONE',  ( 0.6024113833632039894, -1.356364261510525138, -49.08871708540531387 ) ) ;
#60394=ORIENTED_EDGE ( 'NONE', *, *, #34044, .T. ) ;
#60405=CARTESIAN_POINT ( 'NONE',  ( 0.1158403557922069033, -1.452093878213947642, 44.10024637745998888 ) ) ;
#60408=ORIENTED_EDGE ( 'NONE', *, *, #8085, .T. ) ;
#60410=B_SPLINE_CURVE_WITH_KNOTS ( 'NONE', 3,
 ( #7278, #36145, #50521, #37071, #27337, #42087 ),
 .UNSPECIFIED., .F., .F.,
 ( 4, 2, 4 ),
 ( 1.951563910473907981E-18, 0.0002447193893791697081, 0.0004894387787583374646 ),
 .UNSPECIFIED. ) ;
#60412=CARTESIAN_POINT ( 'NONE',  ( 0.6028777368367060907, -25.38243257499183869, -42.03893369112811484 ) ) ;
#60416=CARTESIAN_POINT ( 'NONE',  ( 0.9268187852002115479, 5.219396237290944818, 43.77798802853757820 ) ) ;
#60418=CARTESIAN_POINT ( 'NONE',  ( 3.894904216938897878, 0.8163068198993449487, 43.94835577870902910 ) ) ;
#60423=CARTESIAN_POINT ( 'NONE',  ( 3.240649175237397372, 32.28332734583069907, 29.88397050058092219 ) ) ;
#60427=CARTESIAN_POINT ( 'NONE',  ( 4.975610109902397937, -33.30777373088901072, 35.81957029655259817 ) ) ;
#60430=ORIENTED_EDGE ( 'NONE', *, *, #61384, .T. ) ;
#60433=CARTESIAN_POINT ( 'NONE',  ( 0.3676999524040323597, -41.19158123804999860, 15.78620342045440239 ) ) ;
#60435=CARTESIAN_POINT ( 'NONE',  ( 2.706805983486679779, -43.40490398453981413, 7.265701852721114129 ) ) ;
#60439=ORIENTED_EDGE ( 'NONE', *, *, #59993, .T. ) ;
#60440=DIRECTION ( 'NONE',  ( -1.000000000000000000, -0.000000000000000000, -0.000000000000000000 ) ) ;
#60442=EDGE_CURVE ( 'NONE', #36056, #2992, #33988, .T. ) ;
#60446=EDGE_CURVE ( 'NONE', #37050, #38361, #34100, .T. ) ;
#60455=CARTESIAN_POINT ( 'NONE',  ( 0.8753041380234465318, 10.05717963662801573, 48.06237057854693973 ) ) ;
#60458=CARTESIAN_POINT ( 'NONE',  ( 0.8744876279028306332, 46.30617036199629410, -16.31222353896820110 ) ) ;
#60461=CARTESIAN_POINT ( 'NONE',  ( 0.2940133293163018635, -18.59037414415147182, 40.00798093828915825 ) ) ;
#60464=CARTESIAN_POINT ( 'NONE',  ( 0.6021447746440204973, 44.13029411860373585, -21.54201197878266427 ) ) ;
#60471=CARTESIAN_POINT ( 'NONE',  ( 0.7242486021783847150, 36.85241720405513632, 32.44858715864577903 ) ) ;
#60472=VERTEX_POINT ( 'NONE', #59099 ) ;
#60477=CARTESIAN_POINT ( 'NONE',  ( 0.1147471544378676211, 44.05242651652063302, 2.517122658869559881 ) ) ;
#60486=CARTESIAN_POINT ( 'NONE',  ( 0.1156867017252034419, 15.12161881791919882, 41.45213446374913246 ) ) ;
#60495=CARTESIAN_POINT ( 'NONE',  ( 0.1155031312995260795, -12.71598718139274098, 42.25216328822068590 ) ) ;
#60497=ORIENTED_EDGE ( 'NONE', *, *, #7861, .T. ) ;
#60499=CARTESIAN_POINT ( 'NONE',  ( -6.057079549204054558, 7.802675369763813151, -17.60538236374943111 ) ) ;
#60500=CARTESIAN_POINT ( 'NONE',  ( 0.6029443199889047422, 28.09518699877417092, 40.27652057164711152 ) ) ;
#60501=CARTESIAN_POINT ( 'NONE',  ( 4.975610109902397937, -4.123593823332411645, 48.73854102369035957 ) ) ;
#60502=ORIENTED_EDGE ( 'NONE', *, *, #38134, .T. ) ;
#60503=B_SPLINE_CURVE_WITH_KNOTS ( 'NONE', 3,
 ( #36583, #51810, #31560, #11864, #40682, #40075, #32729, #60350, #26862, #55042, #35978, #21241, #8909, #7108, #50351, #55347 ),
 .UNSPECIFIED., .F., .F.,
 ( 4, 3, 3, 3, 3, 4 ),
 ( 1.962735358247463844E-17, 0.0002612764279487754396, 0.0003919131003184795703, 0.0005225497727000676411, 0.0007837925190632380901, 0.001045051706266724757 ),
 .UNSPECIFIED. ) ;
#60508=B_SPLINE_CURVE_WITH_KNOTS ( 'NONE', 3,
 ( #8406, #47882, #56328, #37890 ),
 .UNSPECIFIED., .F., .F.,
 ( 4, 4 ),
 ( 0.000000000000000000, 0.004444103432399268763 ),
 .UNSPECIFIED. ) ;
#60515=EDGE_CURVE ( 'NONE', #13905, #51708, #27974, .T. ) ;
#60516=CARTESIAN_POINT ( 'NONE',  ( -6.078457390727109555, -19.21674198601421324, -1.229365072086556987 ) ) ;
#60519=ADVANCED_FACE ( 'NONE', ( #60034 ), #38845, .F. ) ;
#60520=CARTESIAN_POINT ( 'NONE',  ( 4.335381028904216727, -36.63547605605806012, -32.52074325427298618 ) ) ;
#60528=B_SPLINE_CURVE_WITH_KNOTS ( 'NONE', 3,
 ( #976, #20408, #30099, #6261 ),
 .UNSPECIFIED., .F., .F.,
 ( 4, 4 ),
 ( 0.000000000000000000, 0.004442905043737217438 ),
 .UNSPECIFIED. ) ;
#60529=CARTESIAN_POINT ( 'NONE',  ( 0.6029442701453592290, 17.04172866834603184, 46.05566967434899794 ) ) ;
#60530=( BOUNDED_SURFACE ( )  B_SPLINE_SURFACE ( 3, 1, ( 
 ( #47877, #29366 ),
 ( #10581, #29068 ),
 ( #29672, #43498 ),
 ( #57229, #48787 ) ),
 .UNSPECIFIED., .F., .F., .F. ) 
 B_SPLINE_SURFACE_WITH_KNOTS ( ( 4, 4 ),
 ( 2, 2 ),
 ( 0.000000000000000000, 1.000000000000000000 ),
 ( 0.000000000000000000, 1.000000000000000000 ),
 .UNSPECIFIED. ) 
 GEOMETRIC_REPRESENTATION_ITEM ( )  RATIONAL_B_SPLINE_SURFACE ( (
 ( 1.000000000000000000, 1.000000000000000000),
 ( 0.7211978278499970862, 0.9934217856018976445),
 ( 0.7211978278499970862, 0.9934217856018976445),
 ( 1.000000000000000000, 1.000000000000000000) ) ) 
 REPRESENTATION_ITEM ( '' )  SURFACE ( )  );
#60533=ORIENTED_EDGE ( 'NONE', *, *, #47864, .F. ) ;
#60536=CARTESIAN_POINT ( 'NONE',  ( -6.078075953587585900, 13.83625866741016353, -13.39227838478774935 ) ) ;
#60541=ORIENTED_EDGE ( 'NONE', *, *, #28623, .T. ) ;
#60543=CARTESIAN_POINT ( 'NONE',  ( -6.077587904424778920, 15.42837212129410673, 11.52221137980054699 ) ) ;
#60544=ORIENTED_EDGE ( 'NONE', *, *, #25249, .F. ) ;
#60546=CARTESIAN_POINT ( 'NONE',  ( 4.694002226626920127, -26.36364849202824701, -37.19197238161631702 ) ) ;
#60547=( BOUNDED_SURFACE ( )  B_SPLINE_SURFACE ( 3, 1, ( 
 ( #60207, #17319 ),
 ( #31724, #7908 ),
 ( #27023, #51116 ),
 ( #22631, #27634 ) ),
 .UNSPECIFIED., .F., .F., .F. ) 
 B_SPLINE_SURFACE_WITH_KNOTS ( ( 4, 4 ),
 ( 2, 2 ),
 ( 0.000000000000000000, 1.000000000000000000 ),
 ( 0.000000000000000000, 1.000000000000000000 ),
 .UNSPECIFIED. ) 
 GEOMETRIC_REPRESENTATION_ITEM ( )  RATIONAL_B_SPLINE_SURFACE ( (
 ( 1.000000000000000000, 1.000000000000000000),
 ( 0.9953485035131437453, 0.8621029689291515030),
 ( 0.9953485035131437453, 0.8621029689291515030),
 ( 1.000000000000000000, 1.000000000000000000) ) ) 
 REPRESENTATION_ITEM ( '' )  SURFACE ( )  );
#60554=CARTESIAN_POINT ( 'NONE',  ( 3.678834586032787346, -48.77537454663707450, 4.424387806648834243 ) ) ;
#60557=VERTEX_POINT ( 'NONE', #50937 ) ;
#60566=CARTESIAN_POINT ( 'NONE',  ( 1.296416391601052487, -43.83799569129288898, -4.531832724885665797 ) ) ;
#60573=ORIENTED_EDGE ( 'NONE', *, *, #7457, .F. ) ;
#60575=CARTESIAN_POINT ( 'NONE',  ( 4.553261556744875094, 0.000000000000000000, 0.000000000000000000 ) ) ;
#60582=B_SPLINE_CURVE_WITH_KNOTS ( 'NONE', 3,
 ( #1668, #24582, #39017, #38703, #16112, #34603 ),
 .UNSPECIFIED., .F., .F.,
 ( 4, 2, 4 ),
 ( 7.589415207398531038E-19, 0.0002447193893791721475, 0.0004894387787583435361 ),
 .UNSPECIFIED. ) ;
#60588=ADVANCED_FACE ( 'NONE', ( #3014 ), #59650, .F. ) ;
#60593=CARTESIAN_POINT ( 'NONE',  ( -6.072942160501519027, 15.42355008158960672, 11.52901839575762111 ) ) ;
#60597=CARTESIAN_POINT ( 'NONE',  ( 0.6039202388192953519, -19.71856863334384613, 44.97490148850911140 ) ) ;
#60598=CARTESIAN_POINT ( 'NONE',  ( 2.299746137290199055, 46.11346518359594882, -16.66822325406706184 ) ) ;
#60601=CARTESIAN_POINT ( 'NONE',  ( 0.3676999524040366896, 36.51379593394493384, -24.75264207750488055 ) ) ;
#60603=DIRECTION ( 'NONE',  ( 0.000000000000000000, 0.000000000000000000, 1.000000000000000000 ) ) ;
#60604=ORIENTED_EDGE ( 'NONE', *, *, #58450, .T. ) ;
#60608=CARTESIAN_POINT ( 'NONE',  ( 4.975610109902397937, -10.32228546579766260, 47.81108480154320972 ) ) ;
#60612=CARTESIAN_POINT ( 'NONE',  ( 0.1129192098497455998, -13.01845098534629486, 42.16007260106758281 ) ) ;
#60613=CARTESIAN_POINT ( 'NONE',  ( -6.063463321072278589, -6.665223333113649673, 18.06641221712787626 ) ) ;
#60621=CARTESIAN_POINT ( 'NONE',  ( 0.5997462898726536595, 44.01516392039513903, -21.77652348757843015 ) ) ;
#60624=EDGE_CURVE ( 'NONE', #15275, #41417, #37488, .T. ) ;
#60625=CARTESIAN_POINT ( 'NONE',  ( -6.078457390727109555, -11.02028633642652444, -15.79075046033844210 ) ) ;
#60627=EDGE_LOOP ( 'NONE', ( #28530, #36544, #59340, #39763 ) ) ;
#60631=CARTESIAN_POINT ( 'NONE',  ( 4.553261556744875094, 0.000000000000000000, 0.000000000000000000 ) ) ;
#60635=ORIENTED_EDGE ( 'NONE', *, *, #56080, .T. ) ;
#60643=VERTEX_POINT ( 'NONE', #8638 ) ;
#60654=CARTESIAN_POINT ( 'NONE',  ( 0.1156867017252034557, 43.28642761383349580, 8.557335549546971620 ) ) ;
#60662=ORIENTED_EDGE ( 'NONE', *, *, #56160, .F. ) ;
#60663=ADVANCED_FACE ( 'NONE', ( #3314 ), #2013, .F. ) ;
#60664=AXIS2_PLACEMENT_3D ( 'NONE', #41098, #16968, #45175 ) ;
#60667=ORIENTED_EDGE ( 'NONE', *, *, #43872, .T. ) ;
#60694=CARTESIAN_POINT ( 'NONE',  ( 4.553261556744875094, -33.30082861731464305, -28.64601855797546648 ) ) ;
#60714=VERTEX_POINT ( 'NONE', #53097 ) ;
#60716=ADVANCED_FACE ( 'NONE', ( #61863 ), #30028, .F. ) ;
#60726=CARTESIAN_POINT ( 'NONE',  ( -2.739355103387248747, -7.962282735394911271, -12.62733624295516854 ) ) ;
#60729=CARTESIAN_POINT ( 'NONE',  ( 2.879087469061463178, 5.945365031249853160, 43.59764112229663624 ) ) ;
#60731=CARTESIAN_POINT ( 'NONE',  ( 3.221118495291109163, 0.4792704474710423601, 43.98331182960114916 ) ) ;
#60734=CARTESIAN_POINT ( 'NONE',  ( -6.078726893082806448, -17.34758611460008382, 8.357948149232223400 ) ) ;
#60735=CARTESIAN_POINT ( 'NONE',  ( 4.553261556744873317, 31.71129487083125653, 30.39627186743183174 ) ) ;
#60739=AXIS2_PLACEMENT_3D ( 'NONE', #45737, #3396, #50410 ) ;
#60741=VERTEX_POINT ( 'NONE', #19002 ) ;
#60746=CARTESIAN_POINT ( 'NONE',  ( -6.072942160501519915, 7.781335985898532037, -17.61405610765392993 ) ) ;
#60748=CARTESIAN_POINT ( 'NONE',  ( 2.359973842542475886, -41.34914904924381318, -15.11237134059111220 ) ) ;
#60749=EDGE_CURVE ( 'NONE', #46130, #15298, #34023, .T. ) ;
#60751=DIRECTION ( 'NONE',  ( -1.000000000000000000, -0.000000000000000000, -0.000000000000000000 ) ) ;
#60752=( BOUNDED_SURFACE ( )  B_SPLINE_SURFACE ( 3, 1, ( 
 ( #25815, #49613 ),
 ( #34306, #6673 ),
 ( #34612, #53992 ),
 ( #11418, #773 ) ),
 .UNSPECIFIED., .F., .F., .F. ) 
 B_SPLINE_SURFACE_WITH_KNOTS ( ( 4, 4 ),
 ( 2, 2 ),
 ( 0.000000000000000000, 1.000000000000000000 ),
 ( 0.000000000000000000, 1.000000000000000000 ),
 .UNSPECIFIED. ) 
 GEOMETRIC_REPRESENTATION_ITEM ( )  RATIONAL_B_SPLINE_SURFACE ( (
 ( 1.000000000000000000, 1.000000000000000000),
 ( 0.7211978278499970862, 0.9934217856018976445),
 ( 0.7211978278499970862, 0.9934217856018976445),
 ( 1.000000000000000000, 1.000000000000000000) ) ) 
 REPRESENTATION_ITEM ( '' )  SURFACE ( )  );
#60754=CARTESIAN_POINT ( 'NONE',  ( 4.975610109902397937, -32.45573888811652807, 36.59336579715199633 ) ) ;
#60757=CARTESIAN_POINT ( 'NONE',  ( 0.2279481005628818391, 9.075716850154307735, 43.17562797144632469 ) ) ;
#60764=B_SPLINE_CURVE_WITH_KNOTS ( 'NONE', 3,
 ( #58736, #1417, #59361, #16790, #35281, #25550 ),
 .UNSPECIFIED., .F., .F.,
 ( 4, 2, 4 ),
 ( 2.710505431213761085E-18, 0.0002447193893791735028, 0.0004894387787583442950 ),
 .UNSPECIFIED. ) ;
#60773=DIRECTION ( 'NONE',  ( 1.000000000000000000, 0.000000000000000000, 0.000000000000000000 ) ) ;
#60775=CARTESIAN_POINT ( 'NONE',  ( -6.077587904424778920, 5.484810954822468609, -18.45840919970596516 ) ) ;
#60776=CARTESIAN_POINT ( 'NONE',  ( 4.553261556744873317, 38.16266689001211887, -21.75202109381124771 ) ) ;
#60780=CARTESIAN_POINT ( 'NONE',  ( 4.975610109902397937, 0.000000000000000000, 0.000000000000000000 ) ) ;
#60781=CARTESIAN_POINT ( 'NONE',  ( 0.5549461598389365813, -11.70502281787141463, 42.52305417417608169 ) ) ;
#60785=ORIENTED_EDGE ( 'NONE', *, *, #33268, .T. ) ;
#60789=ORIENTED_EDGE ( 'NONE', *, *, #40629, .T. ) ;
#60793=FACE_OUTER_BOUND ( 'NONE', #57032, .T. ) ;
#60794=CARTESIAN_POINT ( 'NONE',  ( 0.7413678028165009426, -0.4803394418903486063, 44.09371118187726069 ) ) ;
#60795=EDGE_CURVE ( 'NONE', #57613, #23682, #44306, .T. ) ;
#60798=CARTESIAN_POINT ( 'NONE',  ( 4.553261556744875094, 31.71129487083167220, -30.39627186743139831 ) ) ;
#60800=CARTESIAN_POINT ( 'NONE',  ( 0.3676999524040323597, -31.10876963919482563, -31.27610965031216139 ) ) ;
#60803=EDGE_CURVE ( 'NONE', #45637, #21937, #29409, .T. ) ;
#60808=LINE ( 'NONE', #17928, #53710 ) ;
#60810=ORIENTED_EDGE ( 'NONE', *, *, #58455, .F. ) ;
#60811=CARTESIAN_POINT ( 'NONE',  ( 0.1156495703730067853, -12.42380213276527279, 42.33901385007647633 ) ) ;
#60820=FACE_OUTER_BOUND ( 'NONE', #32323, .T. ) ;
#60829=AXIS2_PLACEMENT_3D ( 'NONE', #5008, #48560, #52946 ) ;
#60830=CARTESIAN_POINT ( 'NONE',  ( 3.678834586032788678, -23.78917523055212513, -42.80989969012353669 ) ) ;
#60836=CARTESIAN_POINT ( 'NONE',  ( 0.7242486021783860473, 16.18710914557469138, 46.35718886950788686 ) ) ;
#60839=B_SPLINE_CURVE_WITH_KNOTS ( 'NONE', 3,
 ( #53783, #15310, #24380, #10597, #10915, #39432 ),
 .UNSPECIFIED., .F., .F.,
 ( 4, 2, 4 ),
 ( 0.000000000000000000, 0.0002293801035737099683, 0.0004587602071474199367 ),
 .UNSPECIFIED. ) ;
#60844=CARTESIAN_POINT ( 'NONE',  ( 0.6016117650947691020, -47.41192139277011108, 12.79299668139902835 ) ) ;
#60855=CARTESIAN_POINT ( 'NONE',  ( 0.6000166863083090663, -39.66797998683833271, -28.95297645272843567 ) ) ;
#60861=DIRECTION ( 'NONE',  ( 0.000000000000000000, 0.000000000000000000, 1.000000000000000000 ) ) ;
#60862=CONICAL_SURFACE ( 'NONE', #35768, 43.92652462719577500, 1.486293639869522343 ) ;
#60866=CARTESIAN_POINT ( 'NONE',  ( 0.1129192098497447394, -13.01845098534572820, -42.16007260106777466 ) ) ;
#60870=ORIENTED_EDGE ( 'NONE', *, *, #51828, .T. ) ;
#60876=EDGE_LOOP ( 'NONE', ( #48848, #51806, #58390, #53922 ) ) ;
#60880=EDGE_CURVE ( 'NONE', #7194, #49527, #16638, .T. ) ;
#60882=CARTESIAN_POINT ( 'NONE',  ( 0.5987334363312690755, -2.178790225517574619, 49.05930879685593027 ) ) ;
#60883=VERTEX_POINT ( 'NONE', #46822 ) ;
#60885=CARTESIAN_POINT ( 'NONE',  ( -6.072942160501519915, 18.62280723096624868, -4.898490903052839407 ) ) ;
#60888=B_SPLINE_CURVE_WITH_KNOTS ( 'NONE', 3,
 ( #25566, #5514, #44703, #30564, #1743, #49071 ),
 .UNSPECIFIED., .F., .F.,
 ( 4, 2, 4 ),
 ( 0.000000000000000000, 0.0002447195606305748003, 0.0004894391212611496006 ),
 .UNSPECIFIED. ) ;
#60890=CARTESIAN_POINT ( 'NONE',  ( 0.2940133293163012529, 15.98885808696028832, -41.11686961154860143 ) ) ;
#60891=CARTESIAN_POINT ( 'NONE',  ( 0.3676999524040366896, 30.26295534861856495, 32.09523511193457068 ) ) ;
#60898=CARTESIAN_POINT ( 'NONE',  ( 0.1119899015040013435, 19.90994828224765101, 39.37709064406269022 ) ) ;
#60899=CARTESIAN_POINT ( 'NONE',  ( 4.975610109902397937, 8.374023221152469887, -48.19050883970174226 ) ) ;
#60900=CARTESIAN_POINT ( 'NONE',  ( 4.975610109902397937, -40.67634447773578898, -27.16402781375298403 ) ) ;
#60902=CARTESIAN_POINT ( 'NONE',  ( 0.1152339509894530906, -18.06478845168980385, -40.25675233611048753 ) ) ;
#60905=CARTESIAN_POINT ( 'NONE',  ( 0.3676999524040323597, -7.853951980432424484, 43.40813312746703190 ) ) ;
#60909=CARTESIAN_POINT ( 'NONE',  ( 3.678748215320120973, -12.15226684749034014, 47.44402201296672672 ) ) ;
#60913=CARTESIAN_POINT ( 'NONE',  ( 0.5997462898726536595, -13.47075269803089803, -47.22383351542737984 ) ) ;
#60914=CARTESIAN_POINT ( 'NONE',  ( 4.975610109902397937, 8.374023221152469887, -48.19050883970174226 ) ) ;
#60924=CARTESIAN_POINT ( 'NONE',  ( 0.6026112563231247332, -1.748029877735236770, 49.07632205504760492 ) ) ;
#60933=B_SPLINE_CURVE_WITH_KNOTS ( 'NONE', 3,
 ( #61660, #24091, #23170, #33817 ),
 .UNSPECIFIED., .F., .F.,
 ( 4, 4 ),
 ( 2.385053804394773788E-17, 0.004559932413162187670 ),
 .UNSPECIFIED. ) ;
#60934=ORIENTED_EDGE ( 'NONE', *, *, #23981, .T. ) ;
#60938=VERTEX_POINT ( 'NONE', #3861 ) ;
#60944=CARTESIAN_POINT ( 'NONE',  ( 2.359973842542475886, -43.99839348535093109, 1.509061079190917587 ) ) ;
#60946=CARTESIAN_POINT ( 'NONE',  ( 0.6253024248130480967, 37.83345337727645585, -31.30613411085905895 ) ) ;
#60949=ORIENTED_EDGE ( 'NONE', *, *, #20893, .T. ) ;
#60950=FACE_OUTER_BOUND ( 'NONE', #44959, .T. ) ;
#60951=CARTESIAN_POINT ( 'NONE',  ( 2.648799415243696664, 18.22894499609882502, -45.52167645879051605 ) ) ;
#60956=CARTESIAN_POINT ( 'NONE',  ( 2.533389852662419894, 38.94530847225836823, -20.51130126867280268 ) ) ;
#60959=EDGE_LOOP ( 'NONE', ( #30954, #40869, #44486, #10109 ) ) ;
#60962=CARTESIAN_POINT ( 'NONE',  ( 4.975610109902397937, 0.000000000000000000, 0.000000000000000000 ) ) ;
#60964=ORIENTED_EDGE ( 'NONE', *, *, #53361, .F. ) ;
#60967=CARTESIAN_POINT ( 'NONE',  ( 1.657374760986086271, 43.46266450627546618, 7.203279896490761836 ) ) ;
#60969=ADVANCED_FACE ( 'NONE', ( #60255 ), #46647, .F. ) ;
#60970=AXIS2_PLACEMENT_3D ( 'NONE', #15209, #33395, #52165 ) ;
#60972=VERTEX_POINT ( 'NONE', #56183 ) ;
#60974=CARTESIAN_POINT ( 'NONE',  ( 0.1156867017252034280, -27.60855798176574183, 34.41962134368514370 ) ) ;
#60976=ORIENTED_EDGE ( 'NONE', *, *, #48542, .T. ) ;
#60982=VERTEX_POINT ( 'NONE', #36489 ) ;
#60988=CARTESIAN_POINT ( 'NONE',  ( -6.063463321072278589, -17.35644658106392058, 8.341115906049047624 ) ) ;
#61004=CARTESIAN_POINT ( 'NONE',  ( 2.299652685299201860, 29.09982397834946255, -39.46494608240623592 ) ) ;
#61011=AXIS2_PLACEMENT_3D ( 'NONE', #35647, #49718, #30922 ) ;
#61013=CARTESIAN_POINT ( 'NONE',  ( 2.359973842542475886, 28.46303439710156624, -33.58558571086580713 ) ) ;
#61020=CARTESIAN_POINT ( 'NONE',  ( 0.7044674535453004927, 17.74870190915572010, 45.79067921914718653 ) ) ;
#61022=ORIENTED_EDGE ( 'NONE', *, *, #22831, .T. ) ;
#61033=ORIENTED_EDGE ( 'NONE', *, *, #40269, .F. ) ;
#61034=CARTESIAN_POINT ( 'NONE',  ( 0.6021447746440204973, -8.095348290905777233, -48.43559099605801777 ) ) ;
#61035=B_SPLINE_CURVE_WITH_KNOTS ( 'NONE', 3,
 ( #33095, #29600, #23983, #61858, #52168, #38115, #19926, #48405, #33399, #5467, #43424, #14915, #14604, #5160, #48106, #43113, #52476, #28993, #39038, #24291, #58091, #464, #9567, #24605, #28679 ),
 .UNSPECIFIED., .F., .F.,
 ( 4, 3, 3, 3, 3, 3, 3, 3, 4 ),
 ( 5.057544569639794935E-18, 0.0005656085177311393148, 0.001131215744874499406, 0.001696821861372765699, 0.002262427090022497717, 0.002828031679238745492, 0.003393635864401604429, 0.003977030878808131623, 0.004561030005651158133 ),
 .UNSPECIFIED. ) ;
#61037=ORIENTED_EDGE ( 'NONE', *, *, #28548, .T. ) ;
#61039=VERTEX_POINT ( 'NONE', #33335 ) ;
#61045=CARTESIAN_POINT ( 'NONE',  ( 2.009741617377216460, -28.51672276494278080, -33.56040226770888069 ) ) ;
#61050=CARTESIAN_POINT ( 'NONE',  ( -6.078726893082806448, -18.90026279491059924, 3.684305572565647946 ) ) ;
#61056=CARTESIAN_POINT ( 'NONE',  ( 0.8753041380234471980, 43.84722337925211377, 22.10337824412700414 ) ) ;
#61060=CARTESIAN_POINT ( 'NONE',  ( 5.901764892641288895, -22.61189840244751181, 43.43608543684697310 ) ) ;
#61062=DIRECTION ( 'NONE',  ( -1.000000000000000000, -0.000000000000000000, -0.000000000000000000 ) ) ;
#61063=CARTESIAN_POINT ( 'NONE',  ( 0.7413678028165007206, -43.60517056639338307, 6.563169329369992866 ) ) ;
#61066=FACE_OUTER_BOUND ( 'NONE', #35296, .T. ) ;
#61076=EDGE_CURVE ( 'NONE', #41057, #36974, #36868, .T. ) ;
#61081=CARTESIAN_POINT ( 'NONE',  ( 4.553261556744873317, -41.75933753256789771, -13.62707946203816967 ) ) ;
#61086=ORIENTED_EDGE ( 'NONE', *, *, #23981, .F. ) ;
#61087=CARTESIAN_POINT ( 'NONE',  ( 0.1157991065609915715, 4.317964046107984011, -43.91238495042393453 ) ) ;
#61089=CARTESIAN_POINT ( 'NONE',  ( 4.335381028904201628, 48.97680438974857253, -1.014632658970608059 ) ) ;
#61094=ORIENTED_EDGE ( 'NONE', *, *, #56, .F. ) ;
#61098=ORIENTED_EDGE ( 'NONE', *, *, #60442, .F. ) ;
#61102=CARTESIAN_POINT ( 'NONE',  ( 0.6000166863083106206, 4.195342255947409171, -48.93079383234974244 ) ) ;
#61104=ORIENTED_EDGE ( 'NONE', *, *, #31397, .T. ) ;
#61107=CARTESIAN_POINT ( 'NONE',  ( 3.390910168358337362, -37.31396665576448868, 23.27584647109819116 ) ) ;
#61115=ORIENTED_EDGE ( 'NONE', *, *, #51126, .T. ) ;
#61116=CARTESIAN_POINT ( 'NONE',  ( 0.1158403557922069033, -12.59083259422814294, 42.28961151119671769 ) ) ;
#61118=CARTESIAN_POINT ( 'NONE',  ( 0.6008123274975392114, 46.74120613782822176, -15.06035191951060526 ) ) ;
#61122=CARTESIAN_POINT ( 'NONE',  ( 0.6021447746440204973, 28.30907211267130563, 40.12651959998603957 ) ) ;
#61124=EDGE_LOOP ( 'NONE', ( #38139, #14171, #18505, #5301 ) ) ;
#61131=CARTESIAN_POINT ( 'NONE',  ( 3.678834586032787346, -48.30243548991658287, -8.092409738192980484 ) ) ;
#61133=CARTESIAN_POINT ( 'NONE',  ( 0.8744876279028263033, -24.68559978112701714, -42.43785119236734715 ) ) ;
#61157=ORIENTED_EDGE ( 'NONE', *, *, #15784, .F. ) ;
#61158=CARTESIAN_POINT ( 'NONE',  ( 2.185380717157383579, -30.61275100921421455, 31.64931719192459880 ) ) ;
#61159=CARTESIAN_POINT ( 'NONE',  ( 0.5980271706414734822, -39.77423938000247006, -28.81074668563666208 ) ) ;
#61165=CARTESIAN_POINT ( 'NONE',  ( 0.7948884756798505480, -31.28609784800016769, 37.84017344100726632 ) ) ;
#61169=ORIENTED_EDGE ( 'NONE', *, *, #49786, .F. ) ;
#61175=CARTESIAN_POINT ( 'NONE',  ( 4.834790513006555379, 37.58952546674482420, -28.62895241026682314 ) ) ;
#61177=ORIENTED_EDGE ( 'NONE', *, *, #23967, .T. ) ;
#61181=ORIENTED_EDGE ( 'NONE', *, *, #49077, .T. ) ;
#61182=LINE ( 'NONE', #50863, #23549 ) ;
#61194=CARTESIAN_POINT ( 'NONE',  ( -6.077587904424778920, -1.842868750311850601, 19.16767738050321412 ) ) ;
#61199=VERTEX_POINT ( 'NONE', #48637 ) ;
#61202=CARTESIAN_POINT ( 'NONE',  ( 0.7948884756798505480, -24.70668297336682073, -42.42968843927206279 ) ) ;
#61206=DIRECTION ( 'NONE',  ( -0.1011922191286467321, 0.1714634860903305191, -0.9799797996517943810 ) ) ;
#61212=CARTESIAN_POINT ( 'NONE',  ( 0.2940135542859013684, -22.17757310257280778, 38.13654153133788327 ) ) ;
#61216=CARTESIAN_POINT ( 'NONE',  ( 0.5987334308729317378, 32.56457219905072975, -36.75746922820641771 ) ) ;
#61220=CARTESIAN_POINT ( 'NONE',  ( 4.060580049360325461, -24.72948427782955250, -36.33070742102043482 ) ) ;
#61227=CARTESIAN_POINT ( 'NONE',  ( -6.079354080745853928, 16.77867255551505110, -9.448232772480160691 ) ) ;
#61231=ORIENTED_EDGE ( 'NONE', *, *, #3725, .F. ) ;
#61237=CARTESIAN_POINT ( 'NONE',  ( 0.6029443199889047422, 10.92740274660737221, -47.87618939585563993 ) ) ;
#61239=DIRECTION ( 'NONE',  ( -0.1011922191286467460, 0.9947837607124679904, 0.01286095682984216872 ) ) ;
#61244=CARTESIAN_POINT ( 'NONE',  ( 1.112077966505211624, -40.45272749787142175, 17.51020168677428046 ) ) ;
#61245=CARTESIAN_POINT ( 'NONE',  ( 0.5549461598389369144, 37.43508315588892543, 23.32021107491279110 ) ) ;
#61254=CARTESIAN_POINT ( 'NONE',  ( 0.1147471544378676628, 41.77752542102519584, -14.19825898372188178 ) ) ;
#61256=CARTESIAN_POINT ( 'NONE',  ( 2.009741617377216460, 39.06454069786799721, -20.33385693093319446 ) ) ;
#61257=FACE_OUTER_BOUND ( 'NONE', #13835, .T. ) ;
#61259=ORIENTED_EDGE ( 'NONE', *, *, #30179, .F. ) ;
#61261=CARTESIAN_POINT ( 'NONE',  ( 0.6000166863083090663, -47.36892948402865500, -12.96179004788981182 ) ) ;
#61265=CARTESIAN_POINT ( 'NONE',  ( 4.975610109902397937, -40.67634447773618689, 27.16402781375239073 ) ) ;
#61270=CARTESIAN_POINT ( 'NONE',  ( 0.1139756605157203756, 36.76166588342440633, -24.40358869450336599 ) ) ;
#61273=CARTESIAN_POINT ( 'NONE',  ( 0.8753041380234530822, -49.09527960836077654, 0.8898584437169362316 ) ) ;
#61282=CARTESIAN_POINT ( 'NONE',  ( 0.2940133293163017525, -38.82777377762746340, 20.94384236598979143 ) ) ;
#61283=ORIENTED_EDGE ( 'NONE', *, *, #40269, .T. ) ;
#61287=( BOUNDED_SURFACE ( )  B_SPLINE_SURFACE ( 3, 1, ( 
 ( #27454, #61261 ),
 ( #8645, #22760 ),
 ( #14001, #41894 ),
 ( #33104, #9270 ) ),
 .UNSPECIFIED., .F., .F., .F. ) 
 B_SPLINE_SURFACE_WITH_KNOTS ( ( 4, 4 ),
 ( 2, 2 ),
 ( 0.000000000000000000, 1.000000000000000000 ),
 ( 0.000000000000000000, 1.000000000000000000 ),
 .UNSPECIFIED. ) 
 GEOMETRIC_REPRESENTATION_ITEM ( )  RATIONAL_B_SPLINE_SURFACE ( (
 ( 1.000000000000000000, 1.000000000000000000),
 ( 0.9953485035131437453, 0.8621029689291523912),
 ( 0.9953485035131437453, 0.8621029689291523912),
 ( 1.000000000000000000, 1.000000000000000000) ) ) 
 REPRESENTATION_ITEM ( '' )  SURFACE ( )  );
#61298=EDGE_CURVE ( 'NONE', #49156, #52762, #60190, .T. ) ;
#61300=CARTESIAN_POINT ( 'NONE',  ( -6.078457390727109555, 12.00936083188108583, -15.05223450013945019 ) ) ;
#61304=ORIENTED_EDGE ( 'NONE', *, *, #47827, .T. ) ;
#61310=CARTESIAN_POINT ( 'NONE',  ( 3.559346040607745287, 32.11337397044390940, -30.03600329232243027 ) ) ;
#61324=CARTESIAN_POINT ( 'NONE',  ( 2.648799415243696664, -29.47778256948665998, -39.18644916390953625 ) ) ;
#61333=EDGE_LOOP ( 'NONE', ( #60949, #51090, #56568, #36497 ) ) ;
#61336=ADVANCED_FACE ( 'NONE', ( #22304 ), #57996, .F. ) ;
#61338=ORIENTED_EDGE ( 'NONE', *, *, #49706, .T. ) ;
#61339=DIRECTION ( 'NONE',  ( -1.000000000000000000, -0.000000000000000000, -0.000000000000000000 ) ) ;
#61342=CARTESIAN_POINT ( 'NONE',  ( 3.221118495291108275, -28.87617019281731245, -33.18023831525626832 ) ) ;
#61345=CARTESIAN_POINT ( 'NONE',  ( -6.077587904424778920, -18.89978312007036720, 3.687033958106935128 ) ) ;
#61346=ORIENTED_EDGE ( 'NONE', *, *, #27598, .T. ) ;
#61349=CARTESIAN_POINT ( 'NONE',  ( 0.8744876279028263033, -49.08725279547490317, -0.8897546699139439186 ) ) ;
#61350=CARTESIAN_POINT ( 'NONE',  ( 2.648799415243696664, 15.62808678998912448, 46.47881632070856739 ) ) ;
#61353=CARTESIAN_POINT ( 'NONE',  ( -2.601141883200665639, -9.652501068366241554, 11.38528219213635317 ) ) ;
#61354=B_SPLINE_CURVE_WITH_KNOTS ( 'NONE', 3,
 ( #588, #16251, #34140, #25642, #6500, #5583, #20339, #44479, #20641, #48228, #24723, #19723, #35376, #1823, #11244, #39778, #20952, #5281, #34750 ),
 .UNSPECIFIED., .F., .F.,
 ( 4, 3, 3, 3, 3, 3, 4 ),
 ( 0.000000000000000000, 0.0002612768053151720343, 0.0003919133833142896244, 0.0005225499612322636808, 0.0006531865391693353080, 0.0008112755173415234352, 0.0009693688056799755004 ),
 .UNSPECIFIED. ) ;
#61356=CARTESIAN_POINT ( 'NONE',  ( 4.975610109902397937, -46.59897809419055648, 14.86555238512586463 ) ) ;
#61361=CARTESIAN_POINT ( 'NONE',  ( 1.112077966505211402, -41.24073227881319781, -15.56381464281200877 ) ) ;
#61367=CARTESIAN_POINT ( 'NONE',  ( -6.063463321072276813, -18.27076090991278434, 6.082741836727326934 ) ) ;
#61368=ADVANCED_FACE ( 'NONE', ( #18528 ), #14862, .F. ) ;
#61374=CARTESIAN_POINT ( 'NONE',  ( 0.5997462898726536595, -49.10477184366966696, 0.5225058138009974762 ) ) ;
#61375=VECTOR ( 'NONE', #18001, 1000.000000000000227 ) ;
#61378=VERTEX_POINT ( 'NONE', #51718 ) ;
#61379=CARTESIAN_POINT ( 'NONE',  ( -6.072942160501519915, 19.25627044167811874, -0.01452466776898916206 ) ) ;
#61380=CARTESIAN_POINT ( 'NONE',  ( 4.975610109902397937, -48.11736577406863802, 8.784561349450592971 ) ) ;
#61384=EDGE_CURVE ( 'NONE', #9740, #1744, #27079, .T. ) ;
#61387=DIRECTION ( 'NONE',  ( 0.000000000000000000, 0.000000000000000000, 1.000000000000000000 ) ) ;
#61388=ORIENTED_EDGE ( 'NONE', *, *, #59210, .T. ) ;
#61397=LINE ( 'NONE', #42041, #30475 ) ;
#61398=EDGE_LOOP ( 'NONE', ( #43399, #46668, #12455, #34845 ) ) ;
#61400=VECTOR ( 'NONE', #44551, 1000.000000000000114 ) ;
#61405=CARTESIAN_POINT ( 'NONE',  ( 0.5997462898726536595, 37.05192695178169515, -32.22896739432000146 ) ) ;
#61406=CARTESIAN_POINT ( 'NONE',  ( 0.6039202388192953519, 37.50551550546074253, 31.70015803617760852 ) ) ;
#61408=CARTESIAN_POINT ( 'NONE',  ( 0.7948878604505662526, 27.37440007400915576, -40.75954940730458276 ) ) ;
#61411=CARTESIAN_POINT ( 'NONE',  ( 0.1158516988532803382, -31.73079332305263378, -30.66103249928995922 ) ) ;
#61412=VECTOR ( 'NONE', #27941, 1000.000000000000114 ) ;
#61415=EDGE_CURVE ( 'NONE', #57030, #34351, #15888, .T. ) ;
#61418=CARTESIAN_POINT ( 'NONE',  ( 0.6026112563231247332, 46.66028695286041739, -15.30877579628533702 ) ) ;
#61421=FACE_OUTER_BOUND ( 'NONE', #60127, .T. ) ;
#61434=CARTESIAN_POINT ( 'NONE',  ( 0.8744876279028306332, 21.91587810745098963, -43.93226988397984911 ) ) ;
#61437=CARTESIAN_POINT ( 'NONE',  ( 0.8753041380234524160, -13.11588273819849526, 47.31925557181565267 ) ) ;
#61441=CARTESIAN_POINT ( 'NONE',  ( 4.226256110419179812, -20.68992697050140350, 38.76537336260938815 ) ) ;
#61450=CARTESIAN_POINT ( 'NONE',  ( 4.553261556744875094, 0.000000000000000000, 0.000000000000000000 ) ) ;
#61455=ORIENTED_EDGE ( 'NONE', *, *, #30779, .T. ) ;
#61457=AXIS2_PLACEMENT_3D ( 'NONE', #33166, #52552, #9648 ) ;
#61458=CARTESIAN_POINT ( 'NONE',  ( 0.3676999524040323597, 43.13409918076290950, 9.241215893319909114 ) ) ;
#61464=DIRECTION ( 'NONE',  ( 0.09722883295013594329, 0.5755877901554883325, 0.8119391909909733362 ) ) ;
#61470=CARTESIAN_POINT ( 'NONE',  ( 4.834790513006553603, 24.09885983197524340, 40.64276437108075868 ) ) ;
#61476=( BOUNDED_SURFACE ( )  B_SPLINE_SURFACE ( 3, 1, ( 
 ( #36633, #45728 ),
 ( #7790, #46343 ),
 ( #56019, #31925 ),
 ( #8719, #42269 ) ),
 .UNSPECIFIED., .F., .F., .F. ) 
 B_SPLINE_SURFACE_WITH_KNOTS ( ( 4, 4 ),
 ( 2, 2 ),
 ( 0.000000000000000000, 1.000000000000000000 ),
 ( 0.000000000000000000, 1.000000000000000000 ),
 .UNSPECIFIED. ) 
 GEOMETRIC_REPRESENTATION_ITEM ( )  RATIONAL_B_SPLINE_SURFACE ( (
 ( 1.000000000000000000, 1.000000000000000000),
 ( 0.7211978278499968642, 0.9934217856018975334),
 ( 0.7211978278499968642, 0.9934217856018975334),
 ( 1.000000000000000000, 1.000000000000000000) ) ) 
 REPRESENTATION_ITEM ( '' )  SURFACE ( )  );
#61482=ORIENTED_EDGE ( 'NONE', *, *, #39328, .T. ) ;
#61484=CARTESIAN_POINT ( 'NONE',  ( -6.078726893082806448, -14.66462719274100479, -12.47969352855434444 ) ) ;
#61487=LINE ( 'NONE', #7963, #4349 ) ;
#61495=VERTEX_POINT ( 'NONE', #5622 ) ;
#61497=EDGE_CURVE ( 'NONE', #46812, #2175, #21087, .T. ) ;
#61498=CARTESIAN_POINT ( 'NONE',  ( -6.077587904424778920, 12.01079512011154193, -15.05114022181160927 ) ) ;
#61499=CARTESIAN_POINT ( 'NONE',  ( 3.894904216938897878, -4.810386045490164797, 43.69192738446720625 ) ) ;
#61501=ORIENTED_EDGE ( 'NONE', *, *, #61497, .T. ) ;
#61503=DIRECTION ( 'NONE',  ( 1.000000000000000000, 0.000000000000000000, 0.000000000000000000 ) ) ;
#61505=DIRECTION ( 'NONE',  ( 0.1011922191286467876, 0.1083236746283898905, 0.9889520293233755588 ) ) ;
#61507=LINE ( 'NONE', #37757, #57782 ) ;
#61509=CARTESIAN_POINT ( 'NONE',  ( 0.1135584504625008206, -17.46491369724040865, -40.52072113972302958 ) ) ;
#61512=CARTESIAN_POINT ( 'NONE',  ( -6.078726893082806448, -17.34758611459996303, -8.357948149232475643 ) ) ;
#61514=ADVANCED_FACE ( 'NONE', ( #44831 ), #6027, .F. ) ;
#61517=ORIENTED_EDGE ( 'NONE', *, *, #59660, .F. ) ;
#61521=CARTESIAN_POINT ( 'NONE',  ( 0.1152339509894530906, -35.49488302199451795, -26.21175251123374750 ) ) ;
#61522=CARTESIAN_POINT ( 'NONE',  ( 0.6021448801613057400, -39.19856320471260602, -29.58063186128886457 ) ) ;
#61527=DIRECTION ( 'NONE',  ( 0.000000000000000000, 0.000000000000000000, 1.000000000000000000 ) ) ;
#61529=CARTESIAN_POINT ( 'NONE',  ( 0.3676999524040366896, -35.84016207189403502, -25.71834687500748373 ) ) ;
#61531=VERTEX_POINT ( 'NONE', #36973 ) ;
#61537=CARTESIAN_POINT ( 'NONE',  ( 0.6028777368367060907, 11.01229867075015001, -47.85675613011466112 ) ) ;
#61542=EDGE_LOOP ( 'NONE', ( #9129, #3976, #32146, #52843 ) ) ;
#61548=CARTESIAN_POINT ( 'NONE',  ( 0.5997462898726536595, -7.321308210775074876, -48.55872811583048332 ) ) ;
#61550=VECTOR ( 'NONE', #44764, 1000.000000000000114 ) ;
#61555=ORIENTED_EDGE ( 'NONE', *, *, #38218, .T. ) ;
#61557=CARTESIAN_POINT ( 'NONE',  ( 2.648799415243696664, -48.43667485455532784, -7.642381325456497621 ) ) ;
#61559=CARTESIAN_POINT ( 'NONE',  ( 0.1152339509894530906, 41.80536608004668153, -14.11573793212829386 ) ) ;
#61562=CARTESIAN_POINT ( 'NONE',  ( 0.7242486021783822725, 23.43459903703420366, -43.14894008370782075 ) ) ;
#61566=CARTESIAN_POINT ( 'NONE',  ( 0.1139756605157203340, -44.12252424054494782, 0.3975856354873956722 ) ) ;
#61569=CARTESIAN_POINT ( 'NONE',  ( -6.079354080745853928, -6.651439635596356759, -18.07073064439232368 ) ) ;
#61574=CARTESIAN_POINT ( 'NONE',  ( 4.553261556744875094, 43.53643125131386427, 5.841123155974254466 ) ) ;
#61582=CARTESIAN_POINT ( 'NONE',  ( 0.3676999524040366896, -43.63756228305280160, 6.458617600967457406 ) ) ;
#61591=VERTEX_POINT ( 'NONE', #50716 ) ;
#61596=CIRCLE ( 'NONE', #40631, 43.92652462719577500 ) ;
#61602=CARTESIAN_POINT ( 'NONE',  ( 4.553261556744875094, 0.000000000000000000, 0.000000000000000000 ) ) ;
#61603=CARTESIAN_POINT ( 'NONE',  ( 4.553261556744875094, 12.71466023209559104, -42.04612920360213479 ) ) ;
#61608=LINE ( 'NONE', #38463, #4477 ) ;
#61612=CARTESIAN_POINT ( 'NONE',  ( 4.060580049360325461, 31.91818944962045279, -30.21087348319056431 ) ) ;
#61613=EDGE_CURVE ( 'NONE', #51265, #31834, #51887, .T. ) ;
#61614=ORIENTED_EDGE ( 'NONE', *, *, #48521, .T. ) ;
#61616=CARTESIAN_POINT ( 'NONE',  ( 0.5997462898726536595, -45.71211507932765983, -17.94308126043611296 ) ) ;
#61623=VERTEX_POINT ( 'NONE', #33494 ) ;
#61625=CARTESIAN_POINT ( 'NONE',  ( 0.8744876279028306332, 17.78802839418675674, 45.75954650373076049 ) ) ;
#61626=VECTOR ( 'NONE', #45823, 1000.000000000000114 ) ;
#61633=B_SPLINE_CURVE_WITH_KNOTS ( 'NONE', 3,
 ( #47584, #10836, #24078, #4017, #18776, #43206 ),
 .UNSPECIFIED., .F., .F.,
 ( 4, 2, 4 ),
 ( 1.910758783386232924E-17, 0.0002293755540694310746, 0.0004587511081388430129 ),
 .UNSPECIFIED. ) ;
#61640=ORIENTED_EDGE ( 'NONE', *, *, #50248, .T. ) ;
#61641=CARTESIAN_POINT ( 'NONE',  ( 0.2279481005628816725, 25.86035487905268226, -35.74556661464986007 ) ) ;
#61644=EDGE_CURVE ( 'NONE', #2228, #34059, #61633, .T. ) ;
#61650=EDGE_CURVE ( 'NONE', #41374, #57370, #7845, .T. ) ;
#61653=ORIENTED_EDGE ( 'NONE', *, *, #48591, .T. ) ;
#61655=CARTESIAN_POINT ( 'NONE',  ( 0.7242486021783834937, -49.09521972001481060, -0.8190622793412020153 ) ) ;
#61659=FACE_OUTER_BOUND ( 'NONE', #14272, .T. ) ;
#61660=CARTESIAN_POINT ( 'NONE',  ( 0.3676999524040323597, -38.02468164711575582, -22.36233818182566324 ) ) ;
#61666=CARTESIAN_POINT ( 'NONE',  ( 1.834102595619085507, 42.96742150962945317, -9.695278937272329145 ) ) ;
#61668=CARTESIAN_POINT ( 'NONE',  ( 0.1129192098497455998, -32.03190746135001632, 30.34647742609778831 ) ) ;
#61675=CONICAL_SURFACE ( 'NONE', #19726, 43.92652462719577500, 1.486293639869522343 ) ;
#61684=CARTESIAN_POINT ( 'NONE',  ( 3.050102900204245682, 23.66345782521629459, -37.08727562024838420 ) ) ;
#61692=DIRECTION ( 'NONE',  ( -1.000000000000000000, -0.000000000000000000, -0.000000000000000000 ) ) ;
#61693=CARTESIAN_POINT ( 'NONE',  ( 2.648799415243696664, 49.00436887187491664, -1.757638972831356616 ) ) ;
#61694=ORIENTED_EDGE ( 'NONE', *, *, #56, .T. ) ;
#61701=CARTESIAN_POINT ( 'NONE',  ( 0.6000166863083090663, -48.63754814943186489, 6.797969676318824206 ) ) ;
#61711=( GEOMETRIC_REPRESENTATION_CONTEXT ( 3 ) GLOBAL_UNCERTAINTY_ASSIGNED_CONTEXT ( ( #55535 ) ) GLOBAL_UNIT_ASSIGNED_CONTEXT ( ( #45164, #36067, #59211 ) ) REPRESENTATION_CONTEXT ( 'NONE', 'WORKASPACE' ) );
#61720=CARTESIAN_POINT ( 'NONE',  ( 0.1155031312995260795, -31.57910769448971067, -30.81722878118065623 ) ) ;
#61721=ORIENTED_EDGE ( 'NONE', *, *, #52746, .T. ) ;
#61723=( BOUNDED_SURFACE ( )  B_SPLINE_SURFACE ( 3, 1, ( 
 ( #55355, #27795 ),
 ( #32195, #2428 ),
 ( #26871, #41603 ),
 ( #21869, #41920 ) ),
 .UNSPECIFIED., .F., .F., .F. ) 
 B_SPLINE_SURFACE_WITH_KNOTS ( ( 4, 4 ),
 ( 2, 2 ),
 ( 0.000000000000000000, 1.000000000000000000 ),
 ( 0.000000000000000000, 1.000000000000000000 ),
 .UNSPECIFIED. ) 
 GEOMETRIC_REPRESENTATION_ITEM ( )  RATIONAL_B_SPLINE_SURFACE ( (
 ( 1.000000000000000000, 1.000000000000000000),
 ( 0.9953485035131437453, 0.8621029689291515030),
 ( 0.9953485035131437453, 0.8621029689291515030),
 ( 1.000000000000000000, 1.000000000000000000) ) ) 
 REPRESENTATION_ITEM ( '' )  SURFACE ( )  );
#61727=VERTEX_POINT ( 'NONE', #2017 ) ;
#61731=CARTESIAN_POINT ( 'NONE',  ( -2.601141883200665639, -5.629531953699136615, -13.82402971103827660 ) ) ;
#61737=ADVANCED_FACE ( 'NONE', ( #20537 ), #28026, .F. ) ;
#61740=DIRECTION ( 'NONE',  ( 0.09722883295013594329, 0.8999532196066740708, 0.4250067723727894986 ) ) ;
#61743=FACE_OUTER_BOUND ( 'NONE', #40185, .T. ) ;
#61748=DIRECTION ( 'NONE',  ( -1.000000000000000000, -0.000000000000000000, -0.000000000000000000 ) ) ;
#61750=CARTESIAN_POINT ( 'NONE',  ( 0.1119899015040011075, -31.30369570375773947, -31.09726585214597705 ) ) ;
#61756=CIRCLE ( 'NONE', #27809, 48.91267123290010943 ) ;
#61757=CARTESIAN_POINT ( 'NONE',  ( -6.078457390727109555, 13.83560117034712889, -13.39293288613801280 ) ) ;
#61758=CARTESIAN_POINT ( 'NONE',  ( 0.6253024248130490959, 5.398505417741914947, -48.80881443624968341 ) ) ;
#61774=ORIENTED_EDGE ( 'NONE', *, *, #35461, .T. ) ;
#61775=CARTESIAN_POINT ( 'NONE',  ( 0.1129192098497455998, -23.28677643606931014, 37.47903188453085477 ) ) ;
#61783=EDGE_LOOP ( 'NONE', ( #45195, #16016, #10827, #39494 ) ) ;
#61784=EDGE_CURVE ( 'NONE', #55636, #46169, #39728, .T. ) ;
#61786=FACE_OUTER_BOUND ( 'NONE', #27250, .T. ) ;
#61795=CARTESIAN_POINT ( 'NONE',  ( 0.8744876279028263033, -47.70753782033983725, 11.59055156152357213 ) ) ;
#61797=B_SPLINE_CURVE_WITH_KNOTS ( 'NONE', 3,
 ( #59225, #16333, #35458, #26046 ),
 .UNSPECIFIED., .F., .F.,
 ( 4, 4 ),
 ( 0.000000000000000000, 0.004444103432399266161 ),
 .UNSPECIFIED. ) ;
#61801=CARTESIAN_POINT ( 'NONE',  ( 0.7044674535453004927, -24.73445998053471229, 42.42651543884123555 ) ) ;
#61816=CARTESIAN_POINT ( 'NONE',  ( 0.6000166863083106206, 23.17738933882476005, 43.29702189695021275 ) ) ;
#61819=CARTESIAN_POINT ( 'NONE',  ( 0.1368894036331267383, 40.02613545401979422, 18.56797798737903804 ) ) ;
#61820=ORIENTED_EDGE ( 'NONE', *, *, #24201, .F. ) ;
#61822=CARTESIAN_POINT ( 'NONE',  ( 3.240649175237396484, 18.70948899608092120, 39.81482059363294468 ) ) ;
#61823=CARTESIAN_POINT ( 'NONE',  ( 0.1139756605157204172, -35.59819211292886365, -26.07151583598530209 ) ) ;
#61825=CARTESIAN_POINT ( 'NONE',  ( 4.975610109902397937, 25.84633036597824329, 41.52609557555928177 ) ) ;
#61827=CARTESIAN_POINT ( 'NONE',  ( 4.553261556744875094, 0.000000000000000000, 0.000000000000000000 ) ) ;
#61836=CARTESIAN_POINT ( 'NONE',  ( 0.2285344041767109480, 14.52189545027388284, -41.66072158312635310 ) ) ;
#61837=CARTESIAN_POINT ( 'NONE',  ( 4.975610109902397937, -48.11736577406863802, 8.784561349450592971 ) ) ;
#61840=DIRECTION ( 'NONE',  ( -1.000000000000000000, -0.000000000000000000, -0.000000000000000000 ) ) ;
#61842=CARTESIAN_POINT ( 'NONE',  ( 3.240649175237395596, -43.35902152968361634, -7.433718409119623338 ) ) ;
#61852=CARTESIAN_POINT ( 'NONE',  ( 0.5987334308729321819, -47.65150826912793036, -11.86999015361692678 ) ) ;
#61858=CARTESIAN_POINT ( 'NONE',  ( 4.060580049360325461, 43.94558816817623637, 0.5029661144227123293 ) ) ;
#61860=ORIENTED_EDGE ( 'NONE', *, *, #44068, .F. ) ;
#61861=CARTESIAN_POINT ( 'NONE',  ( 0.1140933569871964287, 41.99434624594081811, -13.54344245234356059 ) ) ;
#61863=FACE_OUTER_BOUND ( 'NONE', #23998, .T. ) ;
#61868=CARTESIAN_POINT ( 'NONE',  ( 0.1155031312995260795, -44.12383981002575695, -0.1685020800892448045 ) ) ;
#61870=ADVANCED_FACE ( 'NONE', ( #41205 ), #7663, .F. ) ;
#61876=CARTESIAN_POINT ( 'NONE',  ( 3.050102900204245682, 43.49164654874852687, 6.625853126714405406 ) ) ;
#61877=CARTESIAN_POINT ( 'NONE',  ( 0.6026112563231247332, -25.60570374804708749, 41.90332839371419738 ) ) ;
#61878=VERTEX_POINT ( 'NONE', #13010 ) ;
#61883=B_SPLINE_CURVE_WITH_KNOTS ( 'NONE', 3,
 ( #55161, #36094, #11653, #12591 ),
 .UNSPECIFIED., .F., .F.,
 ( 4, 4 ),
 ( 2.194270917860438266E-17, 0.004559932413162189405 ),
 .UNSPECIFIED. ) ;
#61886=DIRECTION ( 'NONE',  ( -1.000000000000000000, 0.000000000000000000, 0.000000000000000000 ) ) ;
#61891=CARTESIAN_POINT ( 'NONE',  ( 0.6039202388192952409, -14.13938383033910817, 47.02809306943389345 ) ) ;
#61892=CARTESIAN_POINT ( 'NONE',  ( 4.226256110419178924, -15.56285703882488214, 41.09287931961308971 ) ) ;
#61893=ORIENTED_EDGE ( 'NONE', *, *, #25917, .F. ) ;
#61897=CARTESIAN_POINT ( 'NONE',  ( 2.299746137290199943, 40.37734675500032466, -27.81997855341737491 ) ) ;
#61900=CARTESIAN_POINT ( 'NONE',  ( -6.078726893082806448, -4.281536037413855134, -18.77398440473003305 ) ) ;
#61906=CIRCLE ( 'NONE', #56914, 43.92652462719577500 ) ;
#61909=ORIENTED_EDGE ( 'NONE', *, *, #38632, .T. ) ;
#61914=CARTESIAN_POINT ( 'NONE',  ( -6.057079549204054558, 3.081801865089040415, -19.00878029659116208 ) ) ;
#61917=EDGE_CURVE ( 'NONE', #47787, #45831, #10865, .T. ) ;
#61919=VERTEX_POINT ( 'NONE', #55567 ) ;
#61921=ADVANCED_FACE ( 'NONE', ( #6914 ), #33685, .F. ) ;
#61923=CARTESIAN_POINT ( 'NONE',  ( -6.078075953587585900, -11.01234782890449182, 15.79630873154732917 ) ) ;
#61926=ORIENTED_EDGE ( 'NONE', *, *, #50368, .T. ) ;
#61932=CARTESIAN_POINT ( 'NONE',  ( 0.8753041380234530822, 23.49739456791611047, 43.11624724384818563 ) ) ;
#61933=EDGE_LOOP ( 'NONE', ( #42585, #29198, #33092, #9959 ) ) ;
#61934=EDGE_CURVE ( 'NONE', #27020, #32624, #3634, .T. ) ;
#61937=CARTESIAN_POINT ( 'NONE',  ( 4.975610109902397937, -16.35148546628954236, 46.09857188876348744 ) ) ;
#61949=CARTESIAN_POINT ( 'NONE',  ( 0.6021448801613057400, -42.65943078590919413, -24.32517427787867703 ) ) ;
#61956=CARTESIAN_POINT ( 'NONE',  ( 0.1129192098497455998, -27.88830454350494392, 34.19348267541455044 ) ) ;
#61958=ORIENTED_EDGE ( 'NONE', *, *, #36670, .F. ) ;
#61963=FACE_OUTER_BOUND ( 'NONE', #16906, .T. ) ;
#61969=CARTESIAN_POINT ( 'NONE',  ( 5.901764892641307547, -46.48816889762547078, 15.38965951493164575 ) ) ;
#61971=CARTESIAN_POINT ( 'NONE',  ( 1.296416391601052265, -38.93352552143989698, -20.65158503717203686 ) ) ;
ENDSEC;
END-ISO-10303-21;
